ISO-10303-21;
HEADER;
FILE_DESCRIPTION (('STEP AP214'),
    '1' );
FILE_NAME ('bevel straight.step',
    '2026-10-27T17:59:55',
    ( '' ),
    ( '' ),
    'SwSTEP 2.0',
    'SolidWorks 2025',
    '' );
FILE_SCHEMA (( 'AUTOMOTIVE_DESIGN' ));
ENDSEC;

DATA;
#2=CARTESIAN_POINT ( 'NONE',  ( 1.833838850855486591, 72.47782099564645364, 125.7132320915350618 ) ) ;
#4=ORIENTED_EDGE ( 'NONE', *, *, #19841, .F. ) ;
#5=CARTESIAN_POINT ( 'NONE',  ( 26.11404676487259024, 103.8885755249575453, -45.01677474591305383 ) ) ;
#7=CARTESIAN_POINT ( 'NONE',  ( 1.833838850855486813, -44.75675607098831676, -138.0350826608191994 ) ) ;
#10=CARTESIAN_POINT ( 'NONE',  ( 1.833485406944043827, 96.69979900902318093, -108.1939177044916107 ) ) ;
#12=DIRECTION ( 'NONE',  ( -1.000000000000000000, -0.000000000000000000, -0.000000000000000000 ) ) ;
#13=CARTESIAN_POINT ( 'NONE',  ( 1.834118845439484335, 107.9567937753806035, -96.96525081349894037 ) ) ;
#15=CARTESIAN_POINT ( 'NONE',  ( 2.433796855181219243, -43.58222566461740399, 138.8296532063086772 ) ) ;
#16=CARTESIAN_POINT ( 'NONE',  ( 109.1721716018069657, 0.01157047143379281995, 0.01254847260354831351 ) ) ;
#17=ORIENTED_EDGE ( 'NONE', *, *, #19645, .F. ) ;
#19=VERTEX_POINT ( 'NONE', #7434 ) ;
#20=CARTESIAN_POINT ( 'NONE',  ( 1.833206308920067640, -126.0392061186627330, 71.90885838897354176 ) ) ;
#22=CARTESIAN_POINT ( 'NONE',  ( 32.73300124599738581, -32.68291970228155918, -113.0038235389605461 ) ) ;
#24=EDGE_LOOP ( 'NONE', ( #16873, #10935, #10142, #25938 ) ) ;
#26=VERTEX_POINT ( 'NONE', #9734 ) ;
#27=EDGE_CURVE ( 'NONE', #15045, #24750, #18584, .T. ) ;
#28=ORIENTED_EDGE ( 'NONE', *, *, #4351, .F. ) ;
#30=AXIS2_PLACEMENT_3D ( 'NONE', #2388, #25118, #7714 ) ;
#32=PRODUCT ( 'bevel straight', 'bevel straight', '', ( #7748 ) ) ;
#33=CARTESIAN_POINT ( 'NONE',  ( 1.833838848569445235, 138.0625820091624689, 44.67212175381883554 ) ) ;
#38=CARTESIAN_POINT ( 'NONE',  ( 1.832998868059858122, 117.7096351258399238, -84.86110816369483700 ) ) ;
#39=VECTOR ( 'NONE', #10071, 1000.000000000000000 ) ;
#42=VECTOR ( 'NONE', #28114, 1000.000000000000000 ) ;
#43=CARTESIAN_POINT ( 'NONE',  ( 25.64692872815576408, -110.5102270591924309, 23.16082795281220186 ) ) ;
#46=CARTESIAN_POINT ( 'NONE',  ( 28.43349137099831836, 89.57679848841924297, -86.10800331998703427 ) ) ;
#49=ORIENTED_EDGE ( 'NONE', *, *, #17339, .T. ) ;
#51=CARTESIAN_POINT ( 'NONE',  ( 5.340103556456315737, 133.7487107983443195, 62.06990747183722590 ) ) ;
#52=CARTESIAN_POINT ( 'NONE',  ( 2.433796855181233454, 109.1007109081226076, 96.28145139437721411 ) ) ;
#53=CARTESIAN_POINT ( 'NONE',  ( 55.49584447822657296, -36.04376091928499903, -62.96491934286030556 ) ) ;
#54=CARTESIAN_POINT ( 'NONE',  ( 32.73300124599741423, -75.82012867748416340, -89.94078864464141532 ) ) ;
#57=FACE_OUTER_BOUND ( 'NONE', #2614, .T. ) ;
#59=EDGE_LOOP ( 'NONE', ( #16364, #16288, #13278, #22767 ) ) ;
#60=CARTESIAN_POINT ( 'NONE',  ( 2.108393763691174261, -144.3574619851891327, -16.46048390411948148 ) ) ;
#63=ORIENTED_EDGE ( 'NONE', *, *, #20098, .F. ) ;
#65=CARTESIAN_POINT ( 'NONE',  ( 1.834118845439484335, 0.1779704863070283027, 145.1099497418795750 ) ) ;
#66=B_SPLINE_CURVE_WITH_KNOTS ( 'NONE', 3,
 ( #19256, #1821, #17232, #21839, #4133, #8326, #19665, #8599, #6307, #27897 ),
 .UNSPECIFIED., .F., .F.,
 ( 4, 3, 3, 4 ),
 ( 3.925231146709437917E-17, 0.0002669559177086131842, 0.0005339118354151096806, 0.001067817517169159696 ),
 .UNSPECIFIED. ) ;
#67=ORIENTED_EDGE ( 'NONE', *, *, #11570, .T. ) ;
#68=CARTESIAN_POINT ( 'NONE',  ( 6.224689322667647851, -43.30635742325475945, 141.5842213414011894 ) ) ;
#70=EDGE_CURVE ( 'NONE', #24626, #27978, #23754, .T. ) ;
#71=VECTOR ( 'NONE', #18224, 1000.000000000000114 ) ;
#72=( GEOMETRIC_REPRESENTATION_CONTEXT ( 3 ) GLOBAL_UNCERTAINTY_ASSIGNED_CONTEXT ( ( #16000 ) ) GLOBAL_UNIT_ASSIGNED_CONTEXT ( ( #25277, #3392, #1644 ) ) REPRESENTATION_CONTEXT ( 'NONE', 'WORKASPACE' ) );
#73=CARTESIAN_POINT ( 'NONE',  ( 1.833485406944057594, 97.49333871408690300, 107.4794113447412940 ) ) ;
#74=EDGE_CURVE ( 'NONE', #7427, #22997, #15851, .T. ) ;
#75=VECTOR ( 'NONE', #20368, 1000.000000000000000 ) ;
#78=CARTESIAN_POINT ( 'NONE',  ( 32.73300124599738581, -55.46353551261936587, -103.7392577722181812 ) ) ;
#79=CARTESIAN_POINT ( 'NONE',  ( 2.430230287190589422, 13.76600171652836302, -144.8619874886005334 ) ) ;
#80=CARTESIAN_POINT ( 'NONE',  ( 25.86096068574580897, 55.66087367585407009, 98.40249579084530751 ) ) ;
#81=CARTESIAN_POINT ( 'NONE',  ( 10.93730112725972070, -4.928439153521261495, 151.0983828010090804 ) ) ;
#86=CARTESIAN_POINT ( 'NONE',  ( 25.64681081121879203, -56.81519825470687834, -97.57530875170664331 ) ) ;
#88=CARTESIAN_POINT ( 'NONE',  ( 1.833206310202335487, 125.2945016693821572, -73.19872434058655131 ) ) ;
#89=CARTESIAN_POINT ( 'NONE',  ( 28.37644542392839853, 115.1790646972555550, -46.84227702240664826 ) ) ;
#90=DIRECTION ( 'NONE',  ( -0.5946245182733607137, 0.2512550613902174712, 0.7637359336799413034 ) ) ;
#91=ORIENTED_EDGE ( 'NONE', *, *, #18115, .F. ) ;
#92=CONICAL_SURFACE ( 'NONE', #10236, 117.6351876552689504, 0.9945805576725580410 ) ;
#94=CARTESIAN_POINT ( 'NONE',  ( 55.79472521941428198, -54.55111121764050353, -48.13855120843939517 ) ) ;
#95=CARTESIAN_POINT ( 'NONE',  ( 30.58324630866339433, 67.85993782330898227, -100.1119227962713580 ) ) ;
#96=EDGE_CURVE ( 'NONE', #11003, #17556, #6371, .T. ) ;
#100=CARTESIAN_POINT ( 'NONE',  ( 25.64681081121879203, 84.18689316040048709, 75.24277141833519522 ) ) ;
#101=ORIENTED_EDGE ( 'NONE', *, *, #24597, .T. ) ;
#102=CARTESIAN_POINT ( 'NONE',  ( 25.64708228042119131, -112.9112740241347410, -0.03938584558111280637 ) ) ;
#103=CARTESIAN_POINT ( 'NONE',  ( 55.49584447822657296, 29.75369869231044007, -66.16986612640745591 ) ) ;
#104=AXIS2_PLACEMENT_3D ( 'NONE', #10529, #19295, #19436 ) ;
#105=CARTESIAN_POINT ( 'NONE',  ( 10.93730112725932813, 150.7858122213658305, 10.89264110825069132 ) ) ;
#106=VERTEX_POINT ( 'NONE', #1511 ) ;
#110=AXIS2_PLACEMENT_3D ( 'NONE', #20120, #552, #11348 ) ;
#111=CARTESIAN_POINT ( 'NONE',  ( 28.37599760073042532, -10.20682761621855050, -114.2774414139536105 ) ) ;
#112=DIRECTION ( 'NONE',  ( 0.5914120900931443270, 0.7870418015781034393, 0.1754905759872925630 ) ) ;
#114=CARTESIAN_POINT ( 'NONE',  ( 2.433796855181219243, -126.7346379669260443, 71.49415740225030902 ) ) ;
#116=CARTESIAN_POINT ( 'NONE',  ( 26.11404676487259024, -92.25884714080363835, -65.63269960453335727 ) ) ;
#118=CARTESIAN_POINT ( 'NONE',  ( -40.00000000000000000, 4.592425496802575944E-15, 37.50000000000002132 ) ) ;
#119=VERTEX_POINT ( 'NONE', #8423 ) ;
#121=ORIENTED_EDGE ( 'NONE', *, *, #10704, .F. ) ;
#125=CARTESIAN_POINT ( 'NONE',  ( 25.64704443564079028, 75.45310550990150489, 83.99864088993793132 ) ) ;
#126=CARTESIAN_POINT ( 'NONE',  ( 2.430230287190589422, 60.50928654924753403, 132.3371620660953170 ) ) ;
#127=CARTESIAN_POINT ( 'NONE',  ( 25.64681081121879203, -103.3177883989782657, 45.54494737132187510 ) ) ;
#128=CARTESIAN_POINT ( 'NONE',  ( 25.98552792386802324, 47.00040718953771801, 102.9121737515621930 ) ) ;
#133=CARTESIAN_POINT ( 'NONE',  ( 25.70243777736188306, -112.9457924277214431, -0.7331659071607105060 ) ) ;
#135=EDGE_CURVE ( 'NONE', #16438, #8336, #27522, .T. ) ;
#137=VECTOR ( 'NONE', #20030, 1000.000000000000114 ) ;
#139=CARTESIAN_POINT ( 'NONE',  ( 1.833485406944043827, -107.4794113447415924, 97.49333871408656194 ) ) ;
#141=CARTESIAN_POINT ( 'NONE',  ( 25.64704443564077252, -56.33997466860336090, -97.85065179540814029 ) ) ;
#142=VERTEX_POINT ( 'NONE', #25977 ) ;
#144=EDGE_CURVE ( 'NONE', #16046, #25406, #13445, .T. ) ;
#146=ORIENTED_EDGE ( 'NONE', *, *, #20602, .T. ) ;
#148=CARTESIAN_POINT ( 'NONE',  ( 2.430230287190592531, 125.2872625092172569, -74.01081053030968349 ) ) ;
#149=DIRECTION ( 'NONE',  ( 0.000000000000000000, 0.000000000000000000, 1.000000000000000000 ) ) ;
#152=CONICAL_SURFACE ( 'NONE', #15759, 111.9614997405030152, 0.5880026024245678107 ) ;
#154=AXIS2_PLACEMENT_3D ( 'NONE', #16528, #25317, #5594 ) ;
#156=ORIENTED_EDGE ( 'NONE', *, *, #10565, .F. ) ;
#157=CARTESIAN_POINT ( 'NONE',  ( 26.04756280548352265, 92.21166514879097065, 65.62256188141753910 ) ) ;
#158=ORIENTED_EDGE ( 'NONE', *, *, #12725, .F. ) ;
#162=CARTESIAN_POINT ( 'NONE',  ( 1.894214914920957282, 73.39939580274932496, 125.2241265685472769 ) ) ;
#163=LINE ( 'NONE', #11103, #42 ) ;
#166=EDGE_CURVE ( 'NONE', #18597, #20724, #3825, .T. ) ;
#171=ADVANCED_FACE ( 'NONE', ( #3953 ), #26753, .F. ) ;
#172=CARTESIAN_POINT ( 'NONE',  ( 109.1778270068192853, 0.008960903982066559248, 0.002542344697966475615 ) ) ;
#173=ORIENTED_EDGE ( 'NONE', *, *, #8292, .T. ) ;
#174=VERTEX_POINT ( 'NONE', #332 ) ;
#175=CARTESIAN_POINT ( 'NONE',  ( 2.433796855181219243, -126.7346379669260443, 71.49415740225030902 ) ) ;
#177=ORIENTED_EDGE ( 'NONE', *, *, #10269, .T. ) ;
#178=EDGE_LOOP ( 'NONE', ( #3906, #2305, #10108, #5522 ) ) ;
#180=CARTESIAN_POINT ( 'NONE',  ( 30.59141879584279877, 84.53180090073671238, 79.74795589902048221 ) ) ;
#181=CARTESIAN_POINT ( 'NONE',  ( 109.1587776205901577, 0.005880209827416989048, 0.004375189885414189697 ) ) ;
#182=VERTEX_POINT ( 'NONE', #2340 ) ;
#184=CARTESIAN_POINT ( 'NONE',  ( 109.1589550718174877, 0.006826119083824074701, 0.003284595046925682486 ) ) ;
#185=CARTESIAN_POINT ( 'NONE',  ( 1.831572820252008738, -142.1425225354581983, 29.20415387690522024 ) ) ;
#187=CARTESIAN_POINT ( 'NONE',  ( 30.59138290137883232, -92.40465044710784071, 70.47507990428522362 ) ) ;
#188=CARTESIAN_POINT ( 'NONE',  ( 109.1592201516379674, 0.007051465909551715011, 0.003476928926125415296 ) ) ;
#189=EDGE_CURVE ( 'NONE', #8031, #1001, #28395, .T. ) ;
#190=CARTESIAN_POINT ( 'NONE',  ( 16.05277956358205316, -121.7045645913023293, 75.66118899150477262 ) ) ;
#192=CARTESIAN_POINT ( 'NONE',  ( 1.833485406944057594, -117.0814567582550154, 85.72460230293657446 ) ) ;
#193=EDGE_CURVE ( 'NONE', #16027, #27728, #13099, .T. ) ;
#195=VERTEX_POINT ( 'NONE', #19915 ) ;
#196=CARTESIAN_POINT ( 'NONE',  ( 2.433796855181219243, -145.5024947199069913, 1.451562450949123395 ) ) ;
#198=CARTESIAN_POINT ( 'NONE',  ( 2.433796855181205476, 137.9325382748285165, 46.34326152018790168 ) ) ;
#200=CARTESIAN_POINT ( 'NONE',  ( 25.64681081121879203, 0.4157506337743640534, -112.9102952884414464 ) ) ;
#201=CARTESIAN_POINT ( 'NONE',  ( 32.73300124599733607, 103.7392577722176270, 55.46353551262048853 ) ) ;
#207=VERTEX_POINT ( 'NONE', #201 ) ;
#208=ORIENTED_EDGE ( 'NONE', *, *, #15962, .F. ) ;
#212=CARTESIAN_POINT ( 'NONE',  ( 32.73300124599732186, 0.000000000000000000, 0.000000000000000000 ) ) ;
#213=VERTEX_POINT ( 'NONE', #26527 ) ;
#215=ORIENTED_EDGE ( 'NONE', *, *, #19681, .F. ) ;
#216=CARTESIAN_POINT ( 'NONE',  ( 19.66333377628698997, 133.7337774475000458, 33.01772659807154753 ) ) ;
#218=CARTESIAN_POINT ( 'NONE',  ( 109.1778270068192853, -0.008743876326162617132, 0.003210287141653769046 ) ) ;
#219=EDGE_CURVE ( 'NONE', #10856, #1807, #18227, .T. ) ;
#222=CARTESIAN_POINT ( 'NONE',  ( 10.93730112725969938, 79.81734490845904872, 128.3908183996593948 ) ) ;
#223=EDGE_CURVE ( 'NONE', #27632, #18732, #6944, .T. ) ;
#226=EDGE_CURVE ( 'NONE', #4538, #24427, #4523, .T. ) ;
#227=ORIENTED_EDGE ( 'NONE', *, *, #10953, .F. ) ;
#228=CARTESIAN_POINT ( 'NONE',  ( 109.1587776205901861, -0.006661366261223573317, 0.003057017121600521300 ) ) ;
#229=CARTESIAN_POINT ( 'NONE',  ( 32.73300124599732186, 0.000000000000000000, 0.000000000000000000 ) ) ;
#232=EDGE_CURVE ( 'NONE', #4316, #25484, #25242, .T. ) ;
#233=ORIENTED_EDGE ( 'NONE', *, *, #28355, .F. ) ;
#235=CARTESIAN_POINT ( 'NONE',  ( 32.73300124599738581, -44.31599526637883457, -108.9684813982493097 ) ) ;
#236=CARTESIAN_POINT ( 'NONE',  ( 26.11404676487256893, -92.25884714080449100, 65.63269960453210672 ) ) ;
#237=DIRECTION ( 'NONE',  ( -0.5914120900931443270, -0.7333565075147377987, 0.3352908775637131744 ) ) ;
#238=VERTEX_POINT ( 'NONE', #2060 ) ;
#240=CARTESIAN_POINT ( 'NONE',  ( 13.36082413113063083, -70.90215303572219341, 135.4964217943305016 ) ) ;
#242=( BOUNDED_SURFACE ( )  B_SPLINE_SURFACE ( 3, 1, ( 
 ( #18082, #26857 ),
 ( #7167, #25021 ),
 ( #5274, #14047 ),
 ( #19092, #12595 ) ),
 .UNSPECIFIED., .F., .F., .F. ) 
 B_SPLINE_SURFACE_WITH_KNOTS ( ( 4, 4 ),
 ( 2, 2 ),
 ( 0.000000000000000000, 1.000000000000000000 ),
 ( 0.000000000000000000, 1.000000000000000000 ),
 .UNSPECIFIED. ) 
 GEOMETRIC_REPRESENTATION_ITEM ( )  RATIONAL_B_SPLINE_SURFACE ( (
 ( 1.000000000000000000, 1.000000000000000000),
 ( 0.6386103224230316178, 0.9954351624131538845),
 ( 0.6386103224230316178, 0.9954351624131538845),
 ( 1.000000000000000000, 1.000000000000000000) ) ) 
 REPRESENTATION_ITEM ( '' )  SURFACE ( )  );
#245=B_SPLINE_CURVE_WITH_KNOTS ( 'NONE', 3,
 ( #3724, #1420, #27900, #10365, #12769, #28028 ),
 .UNSPECIFIED., .F., .F.,
 ( 4, 2, 4 ),
 ( 0.000000000000000000, 0.0006311571484585922365, 0.001262314296917184473 ),
 .UNSPECIFIED. ) ;
#246=VERTEX_POINT ( 'NONE', #20051 ) ;
#247=CARTESIAN_POINT ( 'NONE',  ( 25.64692872815577829, 103.2799065540890524, -45.63107645358226705 ) ) ;
#248=CARTESIAN_POINT ( 'NONE',  ( 13.84597867724968090, -129.3717503931856641, 69.17016226639006504 ) ) ;
#252=CARTESIAN_POINT ( 'NONE',  ( 32.73300124599732897, 117.3295799645430151, 8.473903470906510194 ) ) ;
#256=CARTESIAN_POINT ( 'NONE',  ( 109.1721716018069515, -0.01392660302850065417, 0.009868622090669508864 ) ) ;
#257=CARTESIAN_POINT ( 'NONE',  ( 25.64681081121879203, 34.49579773461926635, -107.5125461021399218 ) ) ;
#259=CARTESIAN_POINT ( 'NONE',  ( 32.73300124599741423, 114.2056417606551406, -28.19767303745493336 ) ) ;
#260=ORIENTED_EDGE ( 'NONE', *, *, #18337, .F. ) ;
#262=ORIENTED_EDGE ( 'NONE', *, *, #7996, .F. ) ;
#263=ORIENTED_EDGE ( 'NONE', *, *, #15518, .T. ) ;
#268=CARTESIAN_POINT ( 'NONE',  ( 1.833838848569428581, 72.40075357737826778, -125.7577269771224735 ) ) ;
#269=FACE_OUTER_BOUND ( 'NONE', #11940, .T. ) ;
#272=CARTESIAN_POINT ( 'NONE',  ( 1.893872463202044054, -58.16604752596636274, -132.9857054814986554 ) ) ;
#273=CARTESIAN_POINT ( 'NONE',  ( 2.430230287190572103, 144.8619874886008745, -13.76600171652493998 ) ) ;
#274=FACE_OUTER_BOUND ( 'NONE', #23362, .T. ) ;
#275=CARTESIAN_POINT ( 'NONE',  ( 1.832998868059890096, 73.01698022778356290, 125.4013017422233247 ) ) ;
#276=ORIENTED_EDGE ( 'NONE', *, *, #7410, .F. ) ;
#277=CARTESIAN_POINT ( 'NONE',  ( 1.832998868059890096, 44.33343224355239443, 138.1720401012268553 ) ) ;
#278=CARTESIAN_POINT ( 'NONE',  ( 25.64699802086726521, -56.66140964017665738, -97.66487797954063410 ) ) ;
#279=ORIENTED_EDGE ( 'NONE', *, *, #27399, .T. ) ;
#281=ORIENTED_EDGE ( 'NONE', *, *, #16616, .F. ) ;
#282=( BOUNDED_SURFACE ( )  B_SPLINE_SURFACE ( 3, 1, ( 
 ( #7883, #14041 ),
 ( #12179, #23143 ),
 ( #27133, #12311 ),
 ( #3114, #25284 ) ),
 .UNSPECIFIED., .F., .F., .F. ) 
 B_SPLINE_SURFACE_WITH_KNOTS ( ( 4, 4 ),
 ( 2, 2 ),
 ( 0.000000000000000000, 1.000000000000000000 ),
 ( 0.000000000000000000, 1.000000000000000000 ),
 .UNSPECIFIED. ) 
 GEOMETRIC_REPRESENTATION_ITEM ( )  RATIONAL_B_SPLINE_SURFACE ( (
 ( 1.000000000000000000, 1.000000000000000000),
 ( 0.6386103224230302855, 0.9954351624131538845),
 ( 0.6386103224230302855, 0.9954351624131538845),
 ( 1.000000000000000000, 1.000000000000000000) ) ) 
 REPRESENTATION_ITEM ( '' )  SURFACE ( )  );
#285=EDGE_LOOP ( 'NONE', ( #12898, #28285, #1711, #7886 ) ) ;
#290=EDGE_CURVE ( 'NONE', #23510, #9049, #9297, .T. ) ;
#292=CARTESIAN_POINT ( 'NONE',  ( 2.433796855181233454, 126.7346379669255754, 71.49415740225120430 ) ) ;
#293=CARTESIAN_POINT ( 'NONE',  ( 28.37644542392844826, -58.62516076109965724, -109.6517504963494929 ) ) ;
#295=EDGE_CURVE ( 'NONE', #5458, #2573, #27496, .T. ) ;
#296=CARTESIAN_POINT ( 'NONE',  ( 1.833206308920041883, -0.7447049373421851248, 145.1075835660718383 ) ) ;
#299=CARTESIAN_POINT ( 'NONE',  ( 2.433796855181205476, -57.85512797797802165, -133.5135467655523769 ) ) ;
#301=PLANE ( 'NONE',  #25895 ) ;
#302=CARTESIAN_POINT ( 'NONE',  ( 25.98107933586721430, -65.61242423298374149, -92.16448350435784675 ) ) ;
#303=CARTESIAN_POINT ( 'NONE',  ( 1.833206310202331712, 141.7818020564282619, -30.89799345102821349 ) ) ;
#304=CARTESIAN_POINT ( 'NONE',  ( 55.79472521941428198, -23.17337251492715922, -68.96476385670688103 ) ) ;
#305=ORIENTED_EDGE ( 'NONE', *, *, #26640, .T. ) ;
#307=CARTESIAN_POINT ( 'NONE',  ( 25.64681081121879203, 0.4157506337743640534, -112.9102952884414464 ) ) ;
#308=CARTESIAN_POINT ( 'NONE',  ( 25.87036335909425944, 107.2165474610300322, -35.87755773825609396 ) ) ;
#309=VERTEX_POINT ( 'NONE', #27238 ) ;
#310=ORIENTED_EDGE ( 'NONE', *, *, #10304, .F. ) ;
#313=EDGE_CURVE ( 'NONE', #17905, #7760, #18301, .T. ) ;
#314=CARTESIAN_POINT ( 'NONE',  ( 1.833603222531974719, 137.8693250773477814, 45.26427810762952930 ) ) ;
#315=ORIENTED_EDGE ( 'NONE', *, *, #23818, .T. ) ;
#317=ADVANCED_FACE ( 'NONE', ( #25104 ), #23847, .F. ) ;
#318=CARTESIAN_POINT ( 'NONE',  ( 10.93730112725978110, -119.3442956573278479, 92.80059208661636205 ) ) ;
#320=CARTESIAN_POINT ( 'NONE',  ( 1.894214914920949955, -144.4515288797482526, -14.22353624692145324 ) ) ;
#321=LINE ( 'NONE', #25093, #2849 ) ;
#322=CARTESIAN_POINT ( 'NONE',  ( 8.186469829614352989, -127.5731248499971997, -77.65916164626476359 ) ) ;
#323=CARTESIAN_POINT ( 'NONE',  ( 25.81918753295379787, -65.67738364544791807, 91.98563552013010280 ) ) ;
#324=CARTESIAN_POINT ( 'NONE',  ( 109.1587776205901861, 0.002904816147411970386, -0.006729130500864220592 ) ) ;
#327=CARTESIAN_POINT ( 'NONE',  ( 25.64692232868534560, 91.53874134430799359, 66.10288322707224040 ) ) ;
#330=CARTESIAN_POINT ( 'NONE',  ( 25.64703792032467433, 46.06101937225606235, 103.0889146124066968 ) ) ;
#332=CARTESIAN_POINT ( 'NONE',  ( 32.73300124599734318, 99.90245962373836619, 62.10906484417276374 ) ) ;
#334=CARTESIAN_POINT ( 'NONE',  ( 109.1624594426973260, -0.004489871836309199289, -0.01531968460305922070 ) ) ;
#335=VERTEX_POINT ( 'NONE', #11997 ) ;
#337=CARTESIAN_POINT ( 'NONE',  ( 1.833485406944043827, 141.8265699653867387, 30.69200235378984232 ) ) ;
#339=B_SPLINE_CURVE_WITH_KNOTS ( 'NONE', 3,
 ( #7794, #16848, #3453, #21294, #25631, #12237, #12504, #1706 ),
 .UNSPECIFIED., .F., .F.,
 ( 4, 2, 2, 4 ),
 ( 6.938893903907228378E-18, 0.0002429592666046687642, 0.0004859185332093305895, 0.0009718370664186714789 ),
 .UNSPECIFIED. ) ;
#340=ORIENTED_EDGE ( 'NONE', *, *, #22680, .F. ) ;
#342=VERTEX_POINT ( 'NONE', #20623 ) ;
#343=CARTESIAN_POINT ( 'NONE',  ( 2.063896406836605024, -96.20114399516322123, -108.8509294491474861 ) ) ;
#344=B_SPLINE_CURVE_WITH_KNOTS ( 'NONE', 3,
 ( #15021, #2939, #13866, #20192 ),
 .UNSPECIFIED., .F., .F.,
 ( 4, 4 ),
 ( 2.281672496420497865E-17, 0.008383560773332699931 ),
 .UNSPECIFIED. ) ;
#347=EDGE_CURVE ( 'NONE', #22931, #27450, #12814, .T. ) ;
#348=EDGE_CURVE ( 'NONE', #19892, #25954, #10374, .T. ) ;
#349=CARTESIAN_POINT ( 'NONE',  ( 32.73300124599732186, 0.000000000000000000, 0.000000000000000000 ) ) ;
#352=CARTESIAN_POINT ( 'NONE',  ( 25.64703792032472407, -66.24710921678119746, 91.43447020678409842 ) ) ;
#353=AXIS2_PLACEMENT_3D ( 'NONE', #16721, #21587, #19154 ) ;
#354=CARTESIAN_POINT ( 'NONE',  ( 1.832998868059890096, 138.1720401012272816, -44.33343224355093781 ) ) ;
#355=CARTESIAN_POINT ( 'NONE',  ( 2.433796855181205476, -60.50726454507993424, 132.3327394885229182 ) ) ;
#356=FACE_OUTER_BOUND ( 'NONE', #18685, .T. ) ;
#359=DIRECTION ( 'NONE',  ( 0.000000000000000000, 0.000000000000000000, 1.000000000000000000 ) ) ;
#360=CARTESIAN_POINT ( 'NONE',  ( 25.64660436782549269, -112.2303901742708376, 12.37913844083004733 ) ) ;
#362=CARTESIAN_POINT ( 'NONE',  ( 2.433796855181219243, -31.67151202412867761, -142.0211193075559493 ) ) ;
#364=CARTESIAN_POINT ( 'NONE',  ( 25.64681081121879203, -107.2555980796243773, 35.28660243342513070 ) ) ;
#365=CARTESIAN_POINT ( 'NONE',  ( 1.894214914920953952, -125.2241265685475895, 73.39939580274894126 ) ) ;
#368=CARTESIAN_POINT ( 'NONE',  ( 25.65782528836479770, 110.5695798068306317, -22.91156770660693454 ) ) ;
#369=FACE_OUTER_BOUND ( 'NONE', #18098, .T. ) ;
#370=DIRECTION ( 'NONE',  ( -1.000000000000000000, -0.000000000000000000, -0.000000000000000000 ) ) ;
#371=AXIS2_PLACEMENT_3D ( 'NONE', #18675, #18230, #11912 ) ;
#372=ORIENTED_EDGE ( 'NONE', *, *, #18657, .T. ) ;
#373=CARTESIAN_POINT ( 'NONE',  ( 109.1592201516379674, -0.005485778713202971689, -0.005631912476303796086 ) ) ;
#378=VERTEX_POINT ( 'NONE', #8125 ) ;
#379=CARTESIAN_POINT ( 'NONE',  ( 6.224689322667630975, 84.93872395422975785, 121.2721959030541115 ) ) ;
#382=LINE ( 'NONE', #15620, #6481 ) ;
#385=EDGE_CURVE ( 'NONE', #12613, #15221, #10008, .T. ) ;
#387=CARTESIAN_POINT ( 'NONE',  ( 25.64708010899963142, -34.83947233573751134, 107.4019003251855366 ) ) ;
#390=CARTESIAN_POINT ( 'NONE',  ( 25.64681081121879203, 110.3564950173081769, 23.88203588908119457 ) ) ;
#391=VERTEX_POINT ( 'NONE', #27957 ) ;
#393=AXIS2_PLACEMENT_3D ( 'NONE', #9843, #3208, #902 ) ;
#398=FACE_OUTER_BOUND ( 'NONE', #13442, .T. ) ;
#400=ORIENTED_EDGE ( 'NONE', *, *, #20280, .T. ) ;
#402=CARTESIAN_POINT ( 'NONE',  ( -90.83090735639699176, 2.449293598294706119E-15, 20.00000000000000000 ) ) ;
#403=LINE ( 'NONE', #691, #28171 ) ;
#404=CARTESIAN_POINT ( 'NONE',  ( 25.98107933586746654, -24.58827779736852648, 110.4296102877912205 ) ) ;
#407=CARTESIAN_POINT ( 'NONE',  ( 25.65782528836481191, -103.3897864210299105, 45.39960327191575118 ) ) ;
#408=ORIENTED_EDGE ( 'NONE', *, *, #26281, .F. ) ;
#410=CARTESIAN_POINT ( 'NONE',  ( 109.1586900883932856, -0.006960773163852201732, 0.001582822706032804708 ) ) ;
#411=CARTESIAN_POINT ( 'NONE',  ( 25.64706233108855216, -0.08898442853967061805, 112.9112020921832453 ) ) ;
#412=CARTESIAN_POINT ( 'NONE',  ( 25.64681081121880624, 12.21581276189807497, 112.2483031020013868 ) ) ;
#417=EDGE_CURVE ( 'NONE', #342, #6343, #26799, .T. ) ;
#418=ORIENTED_EDGE ( 'NONE', *, *, #11574, .F. ) ;
#419=LINE ( 'NONE', #6915, #25368 ) ;
#420=B_SPLINE_CURVE_WITH_KNOTS ( 'NONE', 3,
 ( #20470, #3346, #12134, #20901, #1191, #9985, #22944 ),
 .UNSPECIFIED., .F., .F.,
 ( 4, 3, 4 ),
 ( 1.734723475976807094E-18, 0.02816610861753245793, 0.04000277880656208374 ),
 .UNSPECIFIED. ) ;
#421=CARTESIAN_POINT ( 'NONE',  ( 1.833838850855462166, -117.3439621615258233, -85.36536653357470072 ) ) ;
#422=VERTEX_POINT ( 'NONE', #16758 ) ;
#424=ORIENTED_EDGE ( 'NONE', *, *, #2283, .T. ) ;
#425=ORIENTED_EDGE ( 'NONE', *, *, #11302, .F. ) ;
#426=EDGE_CURVE ( 'NONE', #2712, #13659, #1071, .T. ) ;
#427=CARTESIAN_POINT ( 'NONE',  ( 9.884929003653608603, 109.0134320167733364, 103.8128997986861322 ) ) ;
#428=EDGE_CURVE ( 'NONE', #3933, #17753, #6233, .T. ) ;
#429=LINE ( 'NONE', #11507, #25331 ) ;
#430=CARTESIAN_POINT ( 'NONE',  ( 2.430230287190589422, -109.1043569252007615, -96.28466919684210268 ) ) ;
#431=VERTEX_POINT ( 'NONE', #21481 ) ;
#432=CARTESIAN_POINT ( 'NONE',  ( 32.73300124599738581, 99.90245962373917621, -62.10906484417127871 ) ) ;
#434=CARTESIAN_POINT ( 'NONE',  ( 55.79472521941428198, -43.35047097963410323, -58.42842213658372685 ) ) ;
#435=ORIENTED_EDGE ( 'NONE', *, *, #9896, .F. ) ;
#436=LINE ( 'NONE', #22029, #7013 ) ;
#437=VERTEX_POINT ( 'NONE', #1752 ) ;
#438=CARTESIAN_POINT ( 'NONE',  ( 2.433796855181233454, 142.6247129145648387, 28.83182736670586266 ) ) ;
#439=CARTESIAN_POINT ( 'NONE',  ( 16.75465622695653423, -67.05928661304268701, -125.4242432475199962 ) ) ;
#441=CARTESIAN_POINT ( 'NONE',  ( 32.73300124599732186, 0.000000000000000000, 0.000000000000000000 ) ) ;
#442=CARTESIAN_POINT ( 'NONE',  ( 2.430230287190589422, -46.34481016236729545, -137.9371479820467243 ) ) ;
#443=CARTESIAN_POINT ( 'NONE',  ( 32.73300124599735739, 32.68291970228236920, 113.0038235389603472 ) ) ;
#447=CARTESIAN_POINT ( 'NONE',  ( 1.832998868059890096, 97.49378069860796359, 107.4798986104863303 ) ) ;
#448=CARTESIAN_POINT ( 'NONE',  ( 25.69398547355840989, -107.6418378907641511, -34.19446713634692259 ) ) ;
#449=VERTEX_POINT ( 'NONE', #25543 ) ;
#450=( BOUNDED_SURFACE ( )  B_SPLINE_SURFACE ( 3, 1, ( 
 ( #22540, #11583 ),
 ( #13591, #17896 ),
 ( #15756, #11163 ),
 ( #11441, #9010 ) ),
 .UNSPECIFIED., .F., .F., .F. ) 
 B_SPLINE_SURFACE_WITH_KNOTS ( ( 4, 4 ),
 ( 2, 2 ),
 ( 0.000000000000000000, 1.000000000000000000 ),
 ( 0.000000000000000000, 1.000000000000000000 ),
 .UNSPECIFIED. ) 
 GEOMETRIC_REPRESENTATION_ITEM ( )  RATIONAL_B_SPLINE_SURFACE ( (
 ( 1.000000000000000000, 1.000000000000000000),
 ( 0.9960225298536222738, 0.9999952330161893110),
 ( 0.9960225298536222738, 0.9999952330161893110),
 ( 1.000000000000000000, 1.000000000000000000) ) ) 
 REPRESENTATION_ITEM ( '' )  SURFACE ( )  );
#452=CARTESIAN_POINT ( 'NONE',  ( 25.64681081121879203, 23.88203588908081443, 110.3564950173082480 ) ) ;
#454=ORIENTED_EDGE ( 'NONE', *, *, #2186, .F. ) ;
#455=EDGE_CURVE ( 'NONE', #26384, #7211, #18757, .T. ) ;
#459=EDGE_CURVE ( 'NONE', #23588, #27642, #11361, .T. ) ;
#462=CARTESIAN_POINT ( 'NONE',  ( 28.37603512858456156, 58.91311972676539455, 98.45183098817996381 ) ) ;
#468=CARTESIAN_POINT ( 'NONE',  ( 8.186469777910550860, 143.0750864738774624, 42.84118569629400497 ) ) ;
#469=CARTESIAN_POINT ( 'NONE',  ( 25.64670758986457599, 34.41755235608744101, 107.5375791514044579 ) ) ;
#470=CARTESIAN_POINT ( 'NONE',  ( 25.87036335909428075, -65.65170964736196879, 92.04585932622757127 ) ) ;
#474=CARTESIAN_POINT ( 'NONE',  ( 32.73300124599740002, 62.10906484417377271, -99.90245962373766986 ) ) ;
#475=VECTOR ( 'NONE', #9261, 1000.000000000000227 ) ;
#476=CARTESIAN_POINT ( 'NONE',  ( 32.73300124599739291, 81.52272205837319063, -84.80615050150287004 ) ) ;
#477=CARTESIAN_POINT ( 'NONE',  ( 109.1586900883932856, 0.005371970278528643075, 0.004701023939945730111 ) ) ;
#478=CARTESIAN_POINT ( 'NONE',  ( 109.1624594426973118, 0.002863932759303090912, -0.01570508117120619079 ) ) ;
#482=ORIENTED_EDGE ( 'NONE', *, *, #25056, .F. ) ;
#484=CARTESIAN_POINT ( 'NONE',  ( 28.37599760073040045, -100.2461467136614175, 55.80522390574083857 ) ) ;
#485=ORIENTED_EDGE ( 'NONE', *, *, #70, .T. ) ;
#486=ADVANCED_FACE ( 'NONE', ( #274 ), #4144, .F. ) ;
#488=ORIENTED_EDGE ( 'NONE', *, *, #17893, .F. ) ;
#489=DIRECTION ( 'NONE',  ( 0.000000000000000000, 0.000000000000000000, 1.000000000000000000 ) ) ;
#490=ORIENTED_EDGE ( 'NONE', *, *, #6319, .F. ) ;
#492=EDGE_CURVE ( 'NONE', #14205, #24138, #20617, .T. ) ;
#493=ORIENTED_EDGE ( 'NONE', *, *, #16429, .F. ) ;
#494=CARTESIAN_POINT ( 'NONE',  ( 10.93730112725996406, 10.89264110825190457, -150.7858122213661716 ) ) ;
#495=CIRCLE ( 'NONE', #5559, 151.1787379149930359 ) ;
#496=B_SPLINE_CURVE_WITH_KNOTS ( 'NONE', 3,
 ( #10138, #14280, #27678, #12557, #8124, #3925, #6368 ),
 .UNSPECIFIED., .F., .F.,
 ( 4, 3, 4 ),
 ( 5.442941977417787173E-16, 0.02816610861753245793, 0.04000277880656272211 ),
 .UNSPECIFIED. ) ;
#497=CARTESIAN_POINT ( 'NONE',  ( 109.1586059443104944, -0.001014167950280833253, 0.007001002073871743885 ) ) ;
#501=CARTESIAN_POINT ( 'NONE',  ( 109.1586900883932856, -0.006231977675082131345, 0.003481399864227353348 ) ) ;
#505=CARTESIAN_POINT ( 'NONE',  ( 25.65782528836480836, -0.5778133093785753349, 112.9169519833626509 ) ) ;
#507=ORIENTED_EDGE ( 'NONE', *, *, #17028, .F. ) ;
#511=CARTESIAN_POINT ( 'NONE',  ( 2.430230287190589422, -43.58368230469487514, 138.8342928068218498 ) ) ;
#512=CARTESIAN_POINT ( 'NONE',  ( 2.433796855181233454, 126.7346379669255754, 71.49415740225120430 ) ) ;
#513=EDGE_CURVE ( 'NONE', #28027, #12090, #11490, .T. ) ;
#516=VECTOR ( 'NONE', #25527, 1000.000000000000114 ) ;
#517=CARTESIAN_POINT ( 'NONE',  ( 25.70243777736189017, 110.6300896395620157, -22.76560620136952906 ) ) ;
#518=CARTESIAN_POINT ( 'NONE',  ( 1.832998868059858122, 45.34898734666231235, -137.8420662456165644 ) ) ;
#519=ORIENTED_EDGE ( 'NONE', *, *, #17768, .F. ) ;
#520=CARTESIAN_POINT ( 'NONE',  ( 25.64700659047692710, 110.4909389345862536, -23.25292178500255247 ) ) ;
#521=VECTOR ( 'NONE', #13115, 1000.000000000000000 ) ;
#522=EDGE_CURVE ( 'NONE', #14145, #16310, #19942, .T. ) ;
#523=EDGE_LOOP ( 'NONE', ( #9442, #25220, #8557, #9955 ) ) ;
#525=EDGE_CURVE ( 'NONE', #18738, #20839, #8007, .T. ) ;
#526=CIRCLE ( 'NONE', #16645, 117.6351876552689504 ) ;
#527=CARTESIAN_POINT ( 'NONE',  ( 10.93730112725990011, -151.0983828010092225, 4.928439153519769356 ) ) ;
#528=CARTESIAN_POINT ( 'NONE',  ( 26.11404676487257603, 112.4785329405483765, -12.95861723607337979 ) ) ;
#531=VERTEX_POINT ( 'NONE', #9493 ) ;
#534=CARTESIAN_POINT ( 'NONE',  ( 10.93730112725991077, -79.81734490845832397, -128.3908183996600201 ) ) ;
#538=B_SPLINE_CURVE_WITH_KNOTS ( 'NONE', 3,
 ( #22328, #10958, #3277, #25461, #1248, #12470, #17073, #12058, #12199, #19232 ),
 .UNSPECIFIED., .F., .F.,
 ( 4, 3, 3, 4 ),
 ( 5.003707553108401214E-17, 0.0002669559177086153526, 0.0005339118354151005733, 0.001067817517169148637 ),
 .UNSPECIFIED. ) ;
#539=ORIENTED_EDGE ( 'NONE', *, *, #25407, .T. ) ;
#540=CARTESIAN_POINT ( 'NONE',  ( 32.73300124599735739, -51.32617430724984331, 105.8473486001049224 ) ) ;
#542=CARTESIAN_POINT ( 'NONE',  ( 1.834118845439484335, 141.9759513273468485, -29.99597360112932520 ) ) ;
#543=EDGE_LOOP ( 'NONE', ( #12436, #24728, #15919, #11277 ) ) ;
#544=VECTOR ( 'NONE', #20502, 1000.000000000000000 ) ;
#545=ADVANCED_FACE ( 'NONE', ( #26604 ), #27863, .F. ) ;
#546=VERTEX_POINT ( 'NONE', #17962 ) ;
#547=ORIENTED_EDGE ( 'NONE', *, *, #14124, .T. ) ;
#552=DIRECTION ( 'NONE',  ( 0.000000000000000000, -1.000000000000000000, 0.000000000000000000 ) ) ;
#553=CARTESIAN_POINT ( 'NONE',  ( 21.16825799904901828, -46.02882515936396857, -127.3716170292828167 ) ) ;
#554=CARTESIAN_POINT ( 'NONE',  ( 10.93730112725993919, -42.00474393596157086, -145.2260730187406352 ) ) ;
#555=EDGE_CURVE ( 'NONE', #27960, #13900, #7200, .T. ) ;
#556=ORIENTED_EDGE ( 'NONE', *, *, #4783, .T. ) ;
#557=CARTESIAN_POINT ( 'NONE',  ( 1.894214914920960835, 145.1469726764544532, -0.9536781033365084870 ) ) ;
#561=EDGE_CURVE ( 'NONE', #945, #6378, #2452, .T. ) ;
#562=CARTESIAN_POINT ( 'NONE',  ( 13.36082413113061307, 81.89226687792266546, -129.1512766091112780 ) ) ;
#563=ORIENTED_EDGE ( 'NONE', *, *, #1401, .F. ) ;
#564=CARTESIAN_POINT ( 'NONE',  ( 25.64681081121879203, -12.21581276189731469, -112.2483031020014579 ) ) ;
#568=ORIENTED_EDGE ( 'NONE', *, *, #226, .T. ) ;
#569=VECTOR ( 'NONE', #11846, 1000.000000000000114 ) ;
#571=ORIENTED_EDGE ( 'NONE', *, *, #1469, .T. ) ;
#573=CARTESIAN_POINT ( 'NONE',  ( 109.1586900883932856, -0.005715190711488748326, -0.004277182003220934836 ) ) ;
#574=DIRECTION ( 'NONE',  ( 0.000000000000000000, 0.000000000000000000, 1.000000000000000000 ) ) ;
#575=CARTESIAN_POINT ( 'NONE',  ( 28.37644542392841274, 17.02293047611527399, -123.1691345231580783 ) ) ;
#576=EDGE_LOOP ( 'NONE', ( #8508, #7598, #22350, #4722 ) ) ;
#577=CARTESIAN_POINT ( 'NONE',  ( 1.894214914920941517, 14.22353624692188667, -144.4515288797482242 ) ) ;
#579=CARTESIAN_POINT ( 'NONE',  ( 25.64660436782565256, -45.39454672041182448, 103.3839381879729444 ) ) ;
#582=ORIENTED_EDGE ( 'NONE', *, *, #6651, .F. ) ;
#584=ADVANCED_FACE ( 'NONE', ( #995 ), #20713, .F. ) ;
#585=CARTESIAN_POINT ( 'NONE',  ( 19.66333377628711432, -64.94841092372091396, -121.4767361208140670 ) ) ;
#587=CARTESIAN_POINT ( 'NONE',  ( 24.01988960052062438, 23.05141021591281714, 129.0012934948647683 ) ) ;
#588=CARTESIAN_POINT ( 'NONE',  ( 30.58324630866345473, -63.85566901681546881, -102.7123253644122087 ) ) ;
#590=( BOUNDED_SURFACE ( )  B_SPLINE_SURFACE ( 3, 1, ( 
 ( #23272, #3523 ),
 ( #12305, #12797 ),
 ( #23778, #4027 ),
 ( #10517, #28197 ) ),
 .UNSPECIFIED., .F., .F., .F. ) 
 B_SPLINE_SURFACE_WITH_KNOTS ( ( 4, 4 ),
 ( 2, 2 ),
 ( 0.000000000000000000, 1.000000000000000000 ),
 ( 0.000000000000000000, 1.000000000000000000 ),
 .UNSPECIFIED. ) 
 GEOMETRIC_REPRESENTATION_ITEM ( )  RATIONAL_B_SPLINE_SURFACE ( (
 ( 1.000000000000000000, 1.000000000000000000),
 ( 0.9956975270656954757, 0.8568959468854893125),
 ( 0.9956975270656954757, 0.8568959468854893125),
 ( 1.000000000000000000, 1.000000000000000000) ) ) 
 REPRESENTATION_ITEM ( '' )  SURFACE ( )  );
#591=CARTESIAN_POINT ( 'NONE',  ( 9.884929003653626367, -50.49804566712026599, -141.8132360130362883 ) ) ;
#592=CARTESIAN_POINT ( 'NONE',  ( 5.340103579038268045, 43.36842539899559767, -140.9275371836307613 ) ) ;
#593=FACE_OUTER_BOUND ( 'NONE', #4583, .T. ) ;
#594=VECTOR ( 'NONE', #26291, 1000.000000000000000 ) ;
#595=ADVANCED_FACE ( 'NONE', ( #18838 ), #19043, .F. ) ;
#598=CARTESIAN_POINT ( 'NONE',  ( 13.36082413113063083, 109.3026516754246558, -106.9547846563624773 ) ) ;
#599=EDGE_CURVE ( 'NONE', #14659, #15269, #12220, .T. ) ;
#601=DIRECTION ( 'NONE',  ( 0.000000000000000000, 0.000000000000000000, 1.000000000000000000 ) ) ;
#603=B_SPLINE_CURVE_WITH_KNOTS ( 'NONE', 3,
 ( #15031, #8290, #3829, #25855, #6149, #12737 ),
 .UNSPECIFIED., .F., .F.,
 ( 4, 2, 4 ),
 ( 5.898697549827395015E-18, 0.0006311636237756845487, 0.001262327247551363243 ),
 .UNSPECIFIED. ) ;
#604=VERTEX_POINT ( 'NONE', #5604 ) ;
#605=CONICAL_SURFACE ( 'NONE', #20816, 151.1787379149930359, 0.5880026024245678107 ) ;
#606=ORIENTED_EDGE ( 'NONE', *, *, #15154, .F. ) ;
#610=AXIS2_PLACEMENT_3D ( 'NONE', #8684, #19070, #1914 ) ;
#612=CARTESIAN_POINT ( 'NONE',  ( 10.93730112725972781, -71.28103789255033007, 133.3192575531796251 ) ) ;
#613=CIRCLE ( 'NONE', #154, 20.00000000000000000 ) ;
#614=FACE_BOUND ( 'NONE', #9901, .T. ) ;
#615=CARTESIAN_POINT ( 'NONE',  ( 26.11404676487257603, -107.3263591096427945, -36.06104232266560672 ) ) ;
#616=DIRECTION ( 'NONE',  ( -1.000000000000000000, -0.000000000000000000, -0.000000000000000000 ) ) ;
#617=CARTESIAN_POINT ( 'NONE',  ( 25.64699802086724389, 112.2675771984165891, -12.03888878460358391 ) ) ;
#618=CARTESIAN_POINT ( 'NONE',  ( 1.833485406944057594, 132.7804117027888253, 58.53321471326925263 ) ) ;
#619=EDGE_CURVE ( 'NONE', #10772, #4669, #18254, .T. ) ;
#621=CARTESIAN_POINT ( 'NONE',  ( 2.433796855181205476, -31.67151202413066713, 142.0211193075554945 ) ) ;
#622=CARTESIAN_POINT ( 'NONE',  ( 1.833485406944057594, 59.50871042846225834, 132.3460930279893262 ) ) ;
#623=CARTESIAN_POINT ( 'NONE',  ( 109.1592201516379674, 0.001331853079201392653, -0.007748443302134886378 ) ) ;
#624=CARTESIAN_POINT ( 'NONE',  ( 25.64681081121880624, -23.88203588908156760, 110.3564950173080916 ) ) ;
#626=EDGE_CURVE ( 'NONE', #21463, #9601, #19292, .T. ) ;
#627=ORIENTED_EDGE ( 'NONE', *, *, #8785, .T. ) ;
#628=FACE_OUTER_BOUND ( 'NONE', #11290, .T. ) ;
#630=CARTESIAN_POINT ( 'NONE',  ( 16.75465622695655199, 87.30527857298585559, -112.2763423369171107 ) ) ;
#631=CARTESIAN_POINT ( 'NONE',  ( 30.59141879584321799, 101.9665761624300728, -55.75104644134783172 ) ) ;
#633=ORIENTED_EDGE ( 'NONE', *, *, #20499, .F. ) ;
#634=ORIENTED_EDGE ( 'NONE', *, *, #20397, .T. ) ;
#636=CARTESIAN_POINT ( 'NONE',  ( 25.65782528836479770, -12.37768345530052905, 112.2379831684172302 ) ) ;
#639=ORIENTED_EDGE ( 'NONE', *, *, #20990, .T. ) ;
#640=CARTESIAN_POINT ( 'NONE',  ( 30.59141879584291956, -99.26511058698852707, -60.43012207291066318 ) ) ;
#642=EDGE_LOOP ( 'NONE', ( #20424, #21101, #20237, #10246 ) ) ;
#648=EDGE_CURVE ( 'NONE', #3159, #8671, #4487, .T. ) ;
#649=B_SPLINE_CURVE_WITH_KNOTS ( 'NONE', 3,
 ( #20292, #9647, #11812, #722, #22472, #5322, #13667, #27341, #11664, #7351 ),
 .UNSPECIFIED., .F., .F.,
 ( 4, 3, 3, 4 ),
 ( 2.501853776554200607E-17, 0.0002669560319015759414, 0.0005492286108966312622, 0.0008315040496093394767 ),
 .UNSPECIFIED. ) ;
#652=CARTESIAN_POINT ( 'NONE',  ( 25.86096068574580542, 83.34468010038291652, 76.38617895399373481 ) ) ;
#653=EDGE_CURVE ( 'NONE', #28198, #2053, #6600, .T. ) ;
#656=CARTESIAN_POINT ( 'NONE',  ( 55.49584447822657296, 72.12568090333353155, -7.849835876627591524 ) ) ;
#660=CARTESIAN_POINT ( 'NONE',  ( 1.833485406944043827, 138.1714136985314383, -44.33323125129781772 ) ) ;
#663=CARTESIAN_POINT ( 'NONE',  ( 109.1586900883932856, -0.005371970278523999220, 0.004701023939953835606 ) ) ;
#664=CARTESIAN_POINT ( 'NONE',  ( 109.1586900883932856, -0.007002774699553650055, 0.001385221016536926190 ) ) ;
#665=CARTESIAN_POINT ( 'NONE',  ( 109.1721716018069515, 0.01254847260354035460, 0.01157047143378742843 ) ) ;
#666=CARTESIAN_POINT ( 'NONE',  ( 25.64681081121879203, 110.3564950173084895, -23.88203588907973085 ) ) ;
#668=( BOUNDED_SURFACE ( )  B_SPLINE_SURFACE ( 3, 1, ( 
 ( #9433, #12157 ),
 ( #16468, #784 ),
 ( #1213, #25259 ),
 ( #27255, #3373 ) ),
 .UNSPECIFIED., .F., .F., .F. ) 
 B_SPLINE_SURFACE_WITH_KNOTS ( ( 4, 4 ),
 ( 2, 2 ),
 ( 0.000000000000000000, 1.000000000000000000 ),
 ( 0.000000000000000000, 1.000000000000000000 ),
 .UNSPECIFIED. ) 
 GEOMETRIC_REPRESENTATION_ITEM ( )  RATIONAL_B_SPLINE_SURFACE ( (
 ( 1.000000000000000000, 1.000000000000000000),
 ( 0.9956975270656955868, 0.8568959468854907557),
 ( 0.9956975270656955868, 0.8568959468854907557),
 ( 1.000000000000000000, 1.000000000000000000) ) ) 
 REPRESENTATION_ITEM ( '' )  SURFACE ( )  );
#670=EDGE_LOOP ( 'NONE', ( #19059, #14520, #8651, #23980 ) ) ;
#671=CARTESIAN_POINT ( 'NONE',  ( 8.186469829614464899, 143.0750865143074577, -42.84118568057052556 ) ) ;
#672=EDGE_CURVE ( 'NONE', #14178, #9075, #27322, .T. ) ;
#674=CARTESIAN_POINT ( 'NONE',  ( 109.1586059443104944, -0.006856640434645994327, -0.001740416220250450095 ) ) ;
#675=VERTEX_POINT ( 'NONE', #1688 ) ;
#677=CARTESIAN_POINT ( 'NONE',  ( 16.75465622695643475, -125.4242432475199394, 67.05928661304321281 ) ) ;
#678=DIRECTION ( 'NONE',  ( -1.000000000000000000, -0.000000000000000000, -0.000000000000000000 ) ) ;
#680=CARTESIAN_POINT ( 'NONE',  ( 10.93730112725985926, -150.7858122213662853, 10.89264110824944609 ) ) ;
#682=ORIENTED_EDGE ( 'NONE', *, *, #14733, .T. ) ;
#685=CARTESIAN_POINT ( 'NONE',  ( 32.73300124599735739, 51.32617430724909013, 105.8473486001052777 ) ) ;
#686=CARTESIAN_POINT ( 'NONE',  ( 24.01988960052036148, -111.2910478357999295, -69.18817751538435346 ) ) ;
#688=EDGE_LOOP ( 'NONE', ( #23009, #27097, #24333, #18034 ) ) ;
#689=ORIENTED_EDGE ( 'NONE', *, *, #24280, .T. ) ;
#691=CARTESIAN_POINT ( 'NONE',  ( 55.79472521941428198, 58.42842213658386896, -43.35047097963390428 ) ) ;
#692=CARTESIAN_POINT ( 'NONE',  ( 109.1589550718174877, 0.002553077953671612117, -0.007132058561965959158 ) ) ;
#694=LINE ( 'NONE', #7473, #6923 ) ;
#695=CARTESIAN_POINT ( 'NONE',  ( 32.73300124599738581, 8.473903470907664826, -117.3295799645428588 ) ) ;
#697=ORIENTED_EDGE ( 'NONE', *, *, #27504, .F. ) ;
#698=CARTESIAN_POINT ( 'NONE',  ( 1.832998868059858122, -142.0492247521720799, -29.64765804470217958 ) ) ;
#700=CARTESIAN_POINT ( 'NONE',  ( 25.64681081121879203, -0.4157506337735756285, 112.9102952884414464 ) ) ;
#701=CARTESIAN_POINT ( 'NONE',  ( 2.430230287190581429, -74.01081053031187196, 125.2872625092160064 ) ) ;
#702=CARTESIAN_POINT ( 'NONE',  ( 109.1586059443104944, 0.003930911098385077469, -0.005881369279880109546 ) ) ;
#703=CARTESIAN_POINT ( 'NONE',  ( 25.73574536432417048, 102.8730547980549659, 46.68445899255523557 ) ) ;
#704=VERTEX_POINT ( 'NONE', #10621 ) ;
#705=LINE ( 'NONE', #26893, #20384 ) ;
#706=EDGE_LOOP ( 'NONE', ( #2799, #7129, #15020, #177, #14414, #23981 ) ) ;
#707=CARTESIAN_POINT ( 'NONE',  ( 1.833838850093465034, -30.17001957361884124, -141.9387658801234124 ) ) ;
#708=FACE_OUTER_BOUND ( 'NONE', #2088, .T. ) ;
#709=VERTEX_POINT ( 'NONE', #26019 ) ;
#712=CARTESIAN_POINT ( 'NONE',  ( 10.93730112725996051, -4.928439153519255989, -151.0983828010092793 ) ) ;
#713=EDGE_CURVE ( 'NONE', #12372, #246, #28206, .T. ) ;
#714=VECTOR ( 'NONE', #2936, 1000.000000000000000 ) ;
#715=CARTESIAN_POINT ( 'NONE',  ( 2.430230287190592531, 138.8342928068220203, 43.58368230469437776 ) ) ;
#716=EDGE_CURVE ( 'NONE', #21261, #24227, #66, .T. ) ;
#717=LINE ( 'NONE', #26759, #22695 ) ;
#718=LINE ( 'NONE', #9508, #7650 ) ;
#719=ORIENTED_EDGE ( 'NONE', *, *, #1749, .T. ) ;
#721=EDGE_CURVE ( 'NONE', #1061, #823, #15129, .T. ) ;
#722=CARTESIAN_POINT ( 'NONE',  ( 25.64703792032470631, -103.0889146124068532, 46.06101937225569287 ) ) ;
#724=ORIENTED_EDGE ( 'NONE', *, *, #20732, .F. ) ;
#727=CARTESIAN_POINT ( 'NONE',  ( 25.64708010899964208, -45.97512510001836006, -103.1273237223354187 ) ) ;
#729=CARTESIAN_POINT ( 'NONE',  ( 1.833206308920081407, 96.54250175814114243, 108.3342547309368484 ) ) ;
#730=B_SPLINE_CURVE_WITH_KNOTS ( 'NONE', 3,
 ( #20327, #11407, #25094, #11985, #18163, #20756 ),
 .UNSPECIFIED., .F., .F.,
 ( 4, 2, 4 ),
 ( 1.389302603484999005E-17, 0.0006311571484586055722, 0.001262314296917197484 ),
 .UNSPECIFIED. ) ;
#731=FACE_OUTER_BOUND ( 'NONE', #16382, .T. ) ;
#732=B_SPLINE_CURVE_WITH_KNOTS ( 'NONE', 3,
 ( #22479, #26914, #2448, #11240, #9083, #4764 ),
 .UNSPECIFIED., .F., .F.,
 ( 4, 2, 4 ),
 ( 1.852685484479510670E-17, 0.0006311636237756926802, 0.001262327247551366495 ),
 .UNSPECIFIED. ) ;
#734=CARTESIAN_POINT ( 'NONE',  ( 25.64681081121879203, 46.30456157731328659, 102.9795863647030103 ) ) ;
#735=CARTESIAN_POINT ( 'NONE',  ( 5.340103579038250281, -32.90561047415497598, -143.7310399932981397 ) ) ;
#737=CARTESIAN_POINT ( 'NONE',  ( 25.64681081121879203, -75.86069728269045243, 83.63051021305875565 ) ) ;
#738=CARTESIAN_POINT ( 'NONE',  ( 25.69398547355839924, -0.7422864227357194311, -112.9401428107247369 ) ) ;
#740=ORIENTED_EDGE ( 'NONE', *, *, #14373, .T. ) ;
#741=CARTESIAN_POINT ( 'NONE',  ( 26.04756280548352976, -57.54844730865598734, -97.45505646068890826 ) ) ;
#743=ORIENTED_EDGE ( 'NONE', *, *, #24981, .F. ) ;
#746=EDGE_CURVE ( 'NONE', #14753, #8031, #12746, .T. ) ;
#748=EDGE_CURVE ( 'NONE', #11307, #9768, #22724, .T. ) ;
#751=ADVANCED_FACE ( 'NONE', ( #24729 ), #17387, .T. ) ;
#752=FACE_OUTER_BOUND ( 'NONE', #21378, .T. ) ;
#754=( BOUNDED_SURFACE ( )  B_SPLINE_SURFACE ( 3, 1, ( 
 ( #5912, #7944 ),
 ( #27908, #14668 ),
 ( #28042, #8347 ),
 ( #23761, #21145 ) ),
 .UNSPECIFIED., .F., .F., .F. ) 
 B_SPLINE_SURFACE_WITH_KNOTS ( ( 4, 4 ),
 ( 2, 2 ),
 ( 0.000000000000000000, 1.000000000000000000 ),
 ( 0.000000000000000000, 1.000000000000000000 ),
 .UNSPECIFIED. ) 
 GEOMETRIC_REPRESENTATION_ITEM ( )  RATIONAL_B_SPLINE_SURFACE ( (
 ( 1.000000000000000000, 1.000000000000000000),
 ( 0.9960225298536222738, 0.9999952330161893110),
 ( 0.9960225298536222738, 0.9999952330161893110),
 ( 1.000000000000000000, 1.000000000000000000) ) ) 
 REPRESENTATION_ITEM ( '' )  SURFACE ( )  );
#755=EDGE_CURVE ( 'NONE', #14003, #2917, #5214, .T. ) ;
#757=CARTESIAN_POINT ( 'NONE',  ( 25.73574536432414561, -35.67555431182906744, 107.1893601970593863 ) ) ;
#759=FACE_OUTER_BOUND ( 'NONE', #1679, .T. ) ;
#761=CARTESIAN_POINT ( 'NONE',  ( 1.833485406944043827, 117.0814567582556407, -85.72460230293573602 ) ) ;
#762=CARTESIAN_POINT ( 'NONE',  ( 25.70243777736190438, -55.83795591307065109, -98.18050844655130049 ) ) ;
#767=CARTESIAN_POINT ( 'NONE',  ( 26.11404676487257603, 65.63269960453241936, 92.25884714080432047 ) ) ;
#769=ORIENTED_EDGE ( 'NONE', *, *, #5904, .T. ) ;
#771=VERTEX_POINT ( 'NONE', #9316 ) ;
#772=CARTESIAN_POINT ( 'NONE',  ( 109.1587776205901861, -0.005978137617721869003, -0.004240403845331854223 ) ) ;
#773=B_SPLINE_CURVE_WITH_KNOTS ( 'NONE', 3,
 ( #27875, #7903, #16664, #25460, #5733, #19103, #8173 ),
 .UNSPECIFIED., .F., .F.,
 ( 4, 3, 4 ),
 ( 4.967492064660139599E-16, 0.02816610861753249262, 0.04000277880656270824 ),
 .UNSPECIFIED. ) ;
#774=DIRECTION ( 'NONE',  ( -1.000000000000000000, -0.000000000000000000, -0.000000000000000000 ) ) ;
#775=ORIENTED_EDGE ( 'NONE', *, *, #11570, .F. ) ;
#776=ORIENTED_EDGE ( 'NONE', *, *, #21780, .F. ) ;
#777=EDGE_LOOP ( 'NONE', ( #11721, #1209, #5595, #9182 ) ) ;
#778=EDGE_CURVE ( 'NONE', #20282, #13345, #21328, .T. ) ;
#779=B_SPLINE_CURVE_WITH_KNOTS ( 'NONE', 3,
 ( #26938, #7250, #16003, #22359 ),
 .UNSPECIFIED., .F., .F.,
 ( 4, 4 ),
 ( 2.248458606249288556E-16, 0.008383748772659682658 ),
 .UNSPECIFIED. ) ;
#780=EDGE_CURVE ( 'NONE', #9272, #4028, #15485, .T. ) ;
#781=ORIENTED_EDGE ( 'NONE', *, *, #28040, .F. ) ;
#782=CARTESIAN_POINT ( 'NONE',  ( 109.1778270068192853, 0.009307953841262543021, 0.0003511581237570110558 ) ) ;
#783=ADVANCED_FACE ( 'NONE', ( #6867 ), #2280, .F. ) ;
#784=CARTESIAN_POINT ( 'NONE',  ( 1.831572820252008738, -16.14965423926307153, 144.2101521542829801 ) ) ;
#787=( BOUNDED_SURFACE ( )  B_SPLINE_SURFACE ( 3, 1, ( 
 ( #2630, #26655 ),
 ( #16010, #2481 ),
 ( #8981, #16158 ),
 ( #17741, #18022 ) ),
 .UNSPECIFIED., .F., .F., .F. ) 
 B_SPLINE_SURFACE_WITH_KNOTS ( ( 4, 4 ),
 ( 2, 2 ),
 ( 0.000000000000000000, 1.000000000000000000 ),
 ( 0.000000000000000000, 1.000000000000000000 ),
 .UNSPECIFIED. ) 
 GEOMETRIC_REPRESENTATION_ITEM ( )  RATIONAL_B_SPLINE_SURFACE ( (
 ( 1.000000000000000000, 1.000000000000000000),
 ( 0.9960225298536222738, 0.9999952330161893110),
 ( 0.9960225298536222738, 0.9999952330161893110),
 ( 1.000000000000000000, 1.000000000000000000) ) ) 
 REPRESENTATION_ITEM ( '' )  SURFACE ( )  );
#788=CARTESIAN_POINT ( 'NONE',  ( 109.1624594426973260, 0.01216903288310108508, -0.01033277910988601375 ) ) ;
#790=CARTESIAN_POINT ( 'NONE',  ( 1.832998868059890096, 107.4798986104860319, 97.49378069860830465 ) ) ;
#791=DIRECTION ( 'NONE',  ( 0.5946245182733607137, -0.5357871896547450330, -0.5994612328333200901 ) ) ;
#792=CARTESIAN_POINT ( 'NONE',  ( 25.64681081121879203, -34.49579773461859133, 107.5125461021401492 ) ) ;
#793=CARTESIAN_POINT ( 'NONE',  ( 109.1586900883932856, 0.003656351050331851926, 0.006130969560687375870 ) ) ;
#794=EDGE_LOOP ( 'NONE', ( #6516, #11457 ) ) ;
#796=CARTESIAN_POINT ( 'NONE',  ( 119.2224693531408803, 90.00000000000005684, -40.00000000000000711 ) ) ;
#803=CARTESIAN_POINT ( 'NONE',  ( 24.22246935314087324, 69.99999999999998579, -40.00000000000000711 ) ) ;
#805=CARTESIAN_POINT ( 'NONE',  ( 109.1589550718174877, 0.007553890059312246691, -0.0005685167901298649948 ) ) ;
#806=CARTESIAN_POINT ( 'NONE',  ( 9.884929003653626367, -85.04731144912598495, 124.2095058357574544 ) ) ;
#807=ORIENTED_EDGE ( 'NONE', *, *, #23491, .F. ) ;
#809=EDGE_LOOP ( 'NONE', ( #28304, #26897 ) ) ;
#810=CARTESIAN_POINT ( 'NONE',  ( 32.73300124599737160, -84.80615050150427692, 81.52272205837169849 ) ) ;
#812=ADVANCED_FACE ( 'NONE', ( #26429 ), #24939, .F. ) ;
#813=VERTEX_POINT ( 'NONE', #24432 ) ;
#814=ORIENTED_EDGE ( 'NONE', *, *, #21780, .T. ) ;
#815=EDGE_CURVE ( 'NONE', #20966, #16465, #11181, .T. ) ;
#818=EDGE_CURVE ( 'NONE', #2385, #24314, #8998, .T. ) ;
#819=CARTESIAN_POINT ( 'NONE',  ( 32.73300124599735739, -103.7392577722179823, 55.46353551261974957 ) ) ;
#821=CARTESIAN_POINT ( 'NONE',  ( 25.64703792032469920, 107.3388703233126904, -35.03296646432450245 ) ) ;
#822=CARTESIAN_POINT ( 'NONE',  ( 1.833838850093440165, -125.6687394363102896, 72.55488452980823411 ) ) ;
#823=VERTEX_POINT ( 'NONE', #26563 ) ;
#824=CARTESIAN_POINT ( 'NONE',  ( 5.340103556456459621, -32.90561046456809180, 143.7310399800116727 ) ) ;
#825=CARTESIAN_POINT ( 'NONE',  ( 25.69398547355838858, 34.19446713634726365, -107.6418378907640943 ) ) ;
#826=CARTESIAN_POINT ( 'NONE',  ( 10.93730112725971715, -20.69552240458431314, 149.7554878793147282 ) ) ;
#827=ORIENTED_EDGE ( 'NONE', *, *, #2766, .F. ) ;
#828=ORIENTED_EDGE ( 'NONE', *, *, #20094, .T. ) ;
#830=LINE ( 'NONE', #20840, #2333 ) ;
#831=FACE_OUTER_BOUND ( 'NONE', #22609, .T. ) ;
#832=CARTESIAN_POINT ( 'NONE',  ( 30.59141879584283075, 9.457572341076559752, 115.8270959620728320 ) ) ;
#833=CARTESIAN_POINT ( 'NONE',  ( 25.64704443564074765, 11.93517308299288082, -112.2786464378872751 ) ) ;
#835=CARTESIAN_POINT ( 'NONE',  ( 1.833691583653549229, 144.2771263798446455, 15.52203496788964365 ) ) ;
#837=( BOUNDED_SURFACE ( )  B_SPLINE_SURFACE ( 3, 1, ( 
 ( #9543, #18295 ),
 ( #16154, #23664 ),
 ( #14702, #21473 ),
 ( #10543, #25672 ) ),
 .UNSPECIFIED., .F., .F., .F. ) 
 B_SPLINE_SURFACE_WITH_KNOTS ( ( 4, 4 ),
 ( 2, 2 ),
 ( 0.000000000000000000, 1.000000000000000000 ),
 ( 0.000000000000000000, 1.000000000000000000 ),
 .UNSPECIFIED. ) 
 GEOMETRIC_REPRESENTATION_ITEM ( )  RATIONAL_B_SPLINE_SURFACE ( (
 ( 1.000000000000000000, 1.000000000000000000),
 ( 0.9960225298536222738, 0.9999952330161893110),
 ( 0.9960225298536222738, 0.9999952330161893110),
 ( 1.000000000000000000, 1.000000000000000000) ) ) 
 REPRESENTATION_ITEM ( '' )  SURFACE ( )  );
#839=ORIENTED_EDGE ( 'NONE', *, *, #3305, .T. ) ;
#843=CARTESIAN_POINT ( 'NONE',  ( 9.884929003653608603, 103.8128997986872690, -109.0134320167722137 ) ) ;
#844=CARTESIAN_POINT ( 'NONE',  ( 28.37599760073042532, -48.29934869928239749, 104.0705811520812460 ) ) ;
#846=CARTESIAN_POINT ( 'NONE',  ( 16.05277956358235869, 132.7473359121861165, 53.98852998724608909 ) ) ;
#847=LINE ( 'NONE', #11934, #6608 ) ;
#851=ORIENTED_EDGE ( 'NONE', *, *, #15279, .T. ) ;
#852=EDGE_CURVE ( 'NONE', #19554, #24126, #4700, .T. ) ;
#856=CARTESIAN_POINT ( 'NONE',  ( 25.64703792032468854, -23.62108504469166803, -110.4127989088532900 ) ) ;
#857=CARTESIAN_POINT ( 'NONE',  ( 13.36082413113063083, 147.2768864064167929, 41.18148072373664803 ) ) ;
#858=AXIS2_PLACEMENT_3D ( 'NONE', #3079, #23101, #908 ) ;
#861=CARTESIAN_POINT ( 'NONE',  ( 2.108985857320903712, 13.91228467252010148, -144.6256801373125427 ) ) ;
#862=CARTESIAN_POINT ( 'NONE',  ( 25.64681081121879203, 34.49579773461785948, 107.5125461021403765 ) ) ;
#868=CARTESIAN_POINT ( 'NONE',  ( 109.1586900883932856, 0.006819617742893400482, 0.002109621908814826672 ) ) ;
#869=DIRECTION ( 'NONE',  ( 0.000000000000000000, 0.000000000000000000, 1.000000000000000000 ) ) ;
#870=CARTESIAN_POINT ( 'NONE',  ( 1.834118845439484335, -107.9567937753799782, 96.96525081349965092 ) ) ;
#871=DIRECTION ( 'NONE',  ( 0.000000000000000000, 0.000000000000000000, -1.000000000000000000 ) ) ;
#872=CARTESIAN_POINT ( 'NONE',  ( 1.831572820252009626, 142.1425225354579993, 29.20415387690616171 ) ) ;
#873=EDGE_LOOP ( 'NONE', ( #20603, #6803, #23325, #21961 ) ) ;
#875=CARTESIAN_POINT ( 'NONE',  ( 2.433796855181205476, 16.65276281464756636, -144.5536872373190533 ) ) ;
#876=( BOUNDED_SURFACE ( )  B_SPLINE_SURFACE ( 3, 1, ( 
 ( #20704, #2871 ),
 ( #12085, #11649 ),
 ( #7783, #3301 ),
 ( #27177, #14082 ) ),
 .UNSPECIFIED., .F., .F., .F. ) 
 B_SPLINE_SURFACE_WITH_KNOTS ( ( 4, 4 ),
 ( 2, 2 ),
 ( 0.000000000000000000, 1.000000000000000000 ),
 ( 0.000000000000000000, 1.000000000000000000 ),
 .UNSPECIFIED. ) 
 GEOMETRIC_REPRESENTATION_ITEM ( )  RATIONAL_B_SPLINE_SURFACE ( (
 ( 1.000000000000000000, 1.000000000000000000),
 ( 0.9956975270656954757, 0.8568959468854893125),
 ( 0.9956975270656954757, 0.8568959468854893125),
 ( 1.000000000000000000, 1.000000000000000000) ) ) 
 REPRESENTATION_ITEM ( '' )  SURFACE ( )  );
#877=CARTESIAN_POINT ( 'NONE',  ( 26.11404676487257603, -65.63269960453179408, -92.25884714080473259 ) ) ;
#878=DIRECTION ( 'NONE',  ( -0.5914120900931443270, 0.6942916636548193132, -0.4101107478121997496 ) ) ;
#879=CARTESIAN_POINT ( 'NONE',  ( 25.64692872815576408, -107.4838747185723378, 34.58541472378613690 ) ) ;
#883=ORIENTED_EDGE ( 'NONE', *, *, #26063, .T. ) ;
#884=CARTESIAN_POINT ( 'NONE',  ( 26.28373643307407903, -105.5888781856746448, -71.57300207276496451 ) ) ;
#885=ORIENTED_EDGE ( 'NONE', *, *, #27518, .F. ) ;
#886=EDGE_CURVE ( 'NONE', #25087, #20633, #25492, .T. ) ;
#887=B_SPLINE_CURVE_WITH_KNOTS ( 'NONE', 3,
 ( #21127, #14927, #20984, #3717 ),
 .UNSPECIFIED., .F., .F.,
 ( 4, 4 ),
 ( 3.469446951953614189E-18, 0.008383560773332729421 ),
 .UNSPECIFIED. ) ;
#888=ORIENTED_EDGE ( 'NONE', *, *, #16125, .T. ) ;
#889=ORIENTED_EDGE ( 'NONE', *, *, #8584, .F. ) ;
#891=CARTESIAN_POINT ( 'NONE',  ( 28.37644542392842695, 111.8804331835015233, 54.25112470585763447 ) ) ;
#892=CARTESIAN_POINT ( 'NONE',  ( 2.063896406836605024, -144.6078654718903067, 13.84738934186143666 ) ) ;
#893=CARTESIAN_POINT ( 'NONE',  ( 1.833485406944043827, -14.63699153649458040, 144.3694338680884641 ) ) ;
#897=FACE_OUTER_BOUND ( 'NONE', #24368, .T. ) ;
#899=DIRECTION ( 'NONE',  ( -1.000000000000000000, -0.000000000000000000, -0.000000000000000000 ) ) ;
#902=DIRECTION ( 'NONE',  ( 0.000000000000000000, 0.000000000000000000, 1.000000000000000000 ) ) ;
#903=ADVANCED_FACE ( 'NONE', ( #7296 ), #282, .F. ) ;
#906=CARTESIAN_POINT ( 'NONE',  ( 109.1586900883932856, 0.006757191295060846481, 0.002301750759599797969 ) ) ;
#907=CARTESIAN_POINT ( 'NONE',  ( 2.430230287190592531, -96.28466919684171899, 109.1043569252011025 ) ) ;
#908=DIRECTION ( 'NONE',  ( 0.000000000000000000, 0.000000000000000000, 1.000000000000000000 ) ) ;
#910=ORIENTED_EDGE ( 'NONE', *, *, #5742, .F. ) ;
#911=CARTESIAN_POINT ( 'NONE',  ( 109.1721716018069515, 0.001984900887706656826, -0.01695288006056419258 ) ) ;
#915=( BOUNDED_SURFACE ( )  B_SPLINE_SURFACE ( 3, 1, ( 
 ( #18286, #24946 ),
 ( #6379, #20172 ),
 ( #26645, #10844 ),
 ( #24228, #11263 ) ),
 .UNSPECIFIED., .F., .F., .F. ) 
 B_SPLINE_SURFACE_WITH_KNOTS ( ( 4, 4 ),
 ( 2, 2 ),
 ( 0.000000000000000000, 1.000000000000000000 ),
 ( 0.000000000000000000, 1.000000000000000000 ),
 .UNSPECIFIED. ) 
 GEOMETRIC_REPRESENTATION_ITEM ( )  RATIONAL_B_SPLINE_SURFACE ( (
 ( 1.000000000000000000, 1.000000000000000000),
 ( 0.9956975270656954757, 0.8568959468854893125),
 ( 0.9956975270656954757, 0.8568959468854893125),
 ( 1.000000000000000000, 1.000000000000000000) ) ) 
 REPRESENTATION_ITEM ( '' )  SURFACE ( )  );
#917=ORIENTED_EDGE ( 'NONE', *, *, #13125, .T. ) ;
#918=ORIENTED_EDGE ( 'NONE', *, *, #7791, .F. ) ;
#919=ORIENTED_EDGE ( 'NONE', *, *, #18893, .T. ) ;
#921=( BOUNDED_SURFACE ( )  B_SPLINE_SURFACE ( 3, 1, ( 
 ( #9026, #4135 ),
 ( #2238, #1969 ),
 ( #17507, #26294 ),
 ( #15476, #2381 ) ),
 .UNSPECIFIED., .F., .F., .F. ) 
 B_SPLINE_SURFACE_WITH_KNOTS ( ( 4, 4 ),
 ( 2, 2 ),
 ( 0.000000000000000000, 1.000000000000000000 ),
 ( 0.000000000000000000, 1.000000000000000000 ),
 .UNSPECIFIED. ) 
 GEOMETRIC_REPRESENTATION_ITEM ( )  RATIONAL_B_SPLINE_SURFACE ( (
 ( 1.000000000000000000, 1.000000000000000000),
 ( 0.6386103224230302855, 0.9954351624131538845),
 ( 0.6386103224230302855, 0.9954351624131538845),
 ( 1.000000000000000000, 1.000000000000000000) ) ) 
 REPRESENTATION_ITEM ( '' )  SURFACE ( )  );
#922=ORIENTED_EDGE ( 'NONE', *, *, #28349, .T. ) ;
#923=CARTESIAN_POINT ( 'NONE',  ( 109.1721716018069515, 0.01488186354165284969, -0.008358834333178128198 ) ) ;
#924=CARTESIAN_POINT ( 'NONE',  ( 1.832998868059890096, -125.4013017422236089, 73.01698022778312236 ) ) ;
#925=CARTESIAN_POINT ( 'NONE',  ( 2.433796855181205476, 138.8296532063094162, -43.58222566461498815 ) ) ;
#926=CARTESIAN_POINT ( 'NONE',  ( 1.833809397773861649, 29.99591688577088178, 141.9756687985003794 ) ) ;
#927=CARTESIAN_POINT ( 'NONE',  ( 25.64670758986456889, 35.36461833156663914, -107.2298587623391768 ) ) ;
#928=CARTESIAN_POINT ( 'NONE',  ( 109.1586900883932856, -0.005371970278523997486, 0.004701023939953838209 ) ) ;
#930=VECTOR ( 'NONE', #12606, 1000.000000000000114 ) ;
#931=CARTESIAN_POINT ( 'NONE',  ( 109.1587776205901577, -0.0008489206734409406778, 0.007280006032833115891 ) ) ;
#932=CARTESIAN_POINT ( 'NONE',  ( 25.64704443564077252, 56.33997466860400749, 97.85065179540777081 ) ) ;
#933=LINE ( 'NONE', #9724, #23078 ) ;
#935=EDGE_CURVE ( 'NONE', #246, #26070, #25013, .T. ) ;
#938=CARTESIAN_POINT ( 'NONE',  ( 25.64681081121879203, 91.59071981940661544, -66.03065707438841514 ) ) ;
#939=EDGE_CURVE ( 'NONE', #22112, #15531, #951, .T. ) ;
#940=CARTESIAN_POINT ( 'NONE',  ( 25.64704443564077252, 66.47548630737979636, -91.26857357624498945 ) ) ;
#941=CARTESIAN_POINT ( 'NONE',  ( 25.64708010899961366, -91.31497827399779510, 66.41183455464110352 ) ) ;
#943=DIRECTION ( 'NONE',  ( -1.000000000000000000, -0.000000000000000000, -0.000000000000000000 ) ) ;
#945=VERTEX_POINT ( 'NONE', #18510 ) ;
#946=CARTESIAN_POINT ( 'NONE',  ( 10.93730112725972070, -51.37919228020375328, 142.1801301103782293 ) ) ;
#948=CARTESIAN_POINT ( 'NONE',  ( 2.063896406836605024, 144.3268707900447225, 16.52087515463826151 ) ) ;
#949=LINE ( 'NONE', #9739, #14379 ) ;
#951=LINE ( 'NONE', #9741, #11893 ) ;
#952=PLANE ( 'NONE',  #23667 ) ;
#953=ADVANCED_FACE ( 'NONE', ( #1099 ), #25363, .F. ) ;
#954=VECTOR ( 'NONE', #18803, 1000.000000000000114 ) ;
#956=B_SPLINE_CURVE_WITH_KNOTS ( 'NONE', 3,
 ( #4955, #25257, #9287, #13728 ),
 .UNSPECIFIED., .F., .F.,
 ( 4, 4 ),
 ( 0.000000000000000000, 0.008383560773332696461 ),
 .UNSPECIFIED. ) ;
#957=VECTOR ( 'NONE', #13588, 1000.000000000000114 ) ;
#959=ORIENTED_EDGE ( 'NONE', *, *, #1565, .T. ) ;
#960=CARTESIAN_POINT ( 'NONE',  ( 1.833485406944043827, -84.86072343962486286, -117.7091014914958578 ) ) ;
#964=ORIENTED_EDGE ( 'NONE', *, *, #17303, .T. ) ;
#968=CARTESIAN_POINT ( 'NONE',  ( 1.831572820252008738, 141.7320553118906048, 31.13525033585541735 ) ) ;
#969=CARTESIAN_POINT ( 'NONE',  ( 1.833750490713684123, -107.6587173638740467, -97.29556423840249124 ) ) ;
#971=CARTESIAN_POINT ( 'NONE',  ( 32.73300124599741423, -84.80615050150312584, -81.52272205837286378 ) ) ;
#972=CARTESIAN_POINT ( 'NONE',  ( 109.1624594426973260, 0.009004164758061389967, 0.01318243916934106613 ) ) ;
#973=CARTESIAN_POINT ( 'NONE',  ( 2.433796855181219243, 144.5536872373191670, 16.65276281464612396 ) ) ;
#977=EDGE_LOOP ( 'NONE', ( #3699, #10552, #19085, #2167 ) ) ;
#979=CARTESIAN_POINT ( 'NONE',  ( 32.73300124599738581, 51.32617430725051832, -105.8473486001045387 ) ) ;
#981=CARTESIAN_POINT ( 'NONE',  ( 19.66333377628693313, 108.7423656420560008, 84.55762186019606474 ) ) ;
#982=CARTESIAN_POINT ( 'NONE',  ( 109.1586900883932856, 0.007137750914552286330, 0.0001010081143884431274 ) ) ;
#986=CARTESIAN_POINT ( 'NONE',  ( 25.64699802086726876, 45.70780507840577656, -103.2460182674612668 ) ) ;
#988=CARTESIAN_POINT ( 'NONE',  ( 2.263178607246642216, 145.3892423243864584, -1.401567185706980245 ) ) ;
#989=VECTOR ( 'NONE', #21263, 1000.000000000000000 ) ;
#991=CARTESIAN_POINT ( 'NONE',  ( 25.81918753295376590, -67.18811037444370982, -90.88802830332029714 ) ) ;
#994=DIRECTION ( 'NONE',  ( 0.000000000000000000, -0.000000000000000000, 1.000000000000000000 ) ) ;
#995=FACE_OUTER_BOUND ( 'NONE', #19528, .T. ) ;
#997=CARTESIAN_POINT ( 'NONE',  ( 1.833485406944071361, 29.64752363041738548, -142.0485807715643034 ) ) ;
#998=CARTESIAN_POINT ( 'NONE',  ( 26.11404676487257603, -65.63269960453179408, -92.25884714080473259 ) ) ;
#999=CARTESIAN_POINT ( 'NONE',  ( 10.93730112725970294, 65.95960219663110990, 136.0306644680985642 ) ) ;
#1001=VERTEX_POINT ( 'NONE', #4613 ) ;
#1002=FACE_OUTER_BOUND ( 'NONE', #27553, .T. ) ;
#1003=CARTESIAN_POINT ( 'NONE',  ( 2.433796855181205476, 74.00833731765735024, -125.2830755159746445 ) ) ;
#1006=AXIS2_PLACEMENT_3D ( 'NONE', #13827, #3328, #7810 ) ;
#1007=CARTESIAN_POINT ( 'NONE',  ( 25.64681081121879203, 83.63051021305903987, 75.86069728269016821 ) ) ;
#1008=FACE_OUTER_BOUND ( 'NONE', #523, .T. ) ;
#1010=CARTESIAN_POINT ( 'NONE',  ( 2.433796855181233454, 13.76554153471886366, -144.8571464219887730 ) ) ;
#1012=( BOUNDED_SURFACE ( )  B_SPLINE_SURFACE ( 3, 1, ( 
 ( #11858, #9699 ),
 ( #10699, #19466 ),
 ( #15124, #26083 ),
 ( #19602, #27829 ) ),
 .UNSPECIFIED., .F., .F., .F. ) 
 B_SPLINE_SURFACE_WITH_KNOTS ( ( 4, 4 ),
 ( 2, 2 ),
 ( 0.000000000000000000, 1.000000000000000000 ),
 ( 0.000000000000000000, 1.000000000000000000 ),
 .UNSPECIFIED. ) 
 GEOMETRIC_REPRESENTATION_ITEM ( )  RATIONAL_B_SPLINE_SURFACE ( (
 ( 1.000000000000000000, 1.000000000000000000),
 ( 0.9960225298536222738, 0.9999952330161893110),
 ( 0.9960225298536222738, 0.9999952330161893110),
 ( 1.000000000000000000, 1.000000000000000000) ) ) 
 REPRESENTATION_ITEM ( '' )  SURFACE ( )  );
#1014=EDGE_LOOP ( 'NONE', ( #22771, #13153, #16173, #16960 ) ) ;
#1015=ORIENTED_EDGE ( 'NONE', *, *, #21712, .F. ) ;
#1017=CARTESIAN_POINT ( 'NONE',  ( 16.05277956358203895, -80.40847413522624265, 118.6216415718958359 ) ) ;
#1019=CARTESIAN_POINT ( 'NONE',  ( 28.43349137099838941, -17.01091693849658526, -123.0821667346709489 ) ) ;
#1020=CARTESIAN_POINT ( 'NONE',  ( 109.1721716018069515, 0.0002019688922688021263, -0.01706748904931388797 ) ) ;
#1022=CARTESIAN_POINT ( 'NONE',  ( 25.64681081121879203, 107.5125461021402486, 34.49579773461821475 ) ) ;
#1023=B_SPLINE_CURVE_WITH_KNOTS ( 'NONE', 3,
 ( #15716, #187, #8834, #26653 ),
 .UNSPECIFIED., .F., .F.,
 ( 4, 4 ),
 ( 1.745790404657100200E-16, 0.008383748772659646228 ),
 .UNSPECIFIED. ) ;
#1025=VERTEX_POINT ( 'NONE', #22181 ) ;
#1027=CARTESIAN_POINT ( 'NONE',  ( 32.73300124599732186, 0.000000000000000000, 0.000000000000000000 ) ) ;
#1028=CARTESIAN_POINT ( 'NONE',  ( 30.59138290137883942, -75.73279410806787837, 88.14703743378208856 ) ) ;
#1029=ADVANCED_FACE ( 'NONE', ( #9517 ), #15798, .F. ) ;
#1030=EDGE_CURVE ( 'NONE', #24050, #19015, #732, .T. ) ;
#1032=VECTOR ( 'NONE', #13741, 1000.000000000000114 ) ;
#1034=VERTEX_POINT ( 'NONE', #2742 ) ;
#1037=CARTESIAN_POINT ( 'NONE',  ( 25.64692232868535626, -75.30916867847156482, 84.12764974008001673 ) ) ;
#1040=ORIENTED_EDGE ( 'NONE', *, *, #21609, .F. ) ;
#1041=CARTESIAN_POINT ( 'NONE',  ( 10.93730112725939030, 136.0306644680981947, 65.95960219663135149 ) ) ;
#1044=CARTESIAN_POINT ( 'NONE',  ( 109.1586900883932856, 0.004277182003227222341, 0.005715190711481739176 ) ) ;
#1047=AXIS2_PLACEMENT_3D ( 'NONE', #4963, #16042, #359 ) ;
#1049=CARTESIAN_POINT ( 'NONE',  ( 1.833809397773829453, 132.4918864201828228, 59.18399778167182745 ) ) ;
#1051=EDGE_CURVE ( 'NONE', #9366, #14748, #20844, .T. ) ;
#1052=CARTESIAN_POINT ( 'NONE',  ( 5.340103556456507583, -108.0219267027623715, -100.3626145793573698 ) ) ;
#1053=CARTESIAN_POINT ( 'NONE',  ( 1.833603222531957400, -84.93295186324782264, -117.6571262511687195 ) ) ;
#1054=CARTESIAN_POINT ( 'NONE',  ( 1.832998868059890096, 73.01698022778529662, -125.4013017422223299 ) ) ;
#1055=CARTESIAN_POINT ( 'NONE',  ( 26.11404676487256893, -55.62948129436175293, -98.61392875273419634 ) ) ;
#1057=CARTESIAN_POINT ( 'NONE',  ( 26.11404676487259024, -22.43340081644844020, 110.9778746459746372 ) ) ;
#1058=CARTESIAN_POINT ( 'NONE',  ( 16.75465622695657331, 34.09043808962603350, -138.0797984721902196 ) ) ;
#1060=CARTESIAN_POINT ( 'NONE',  ( 2.263178607246672414, -107.1074316126224488, 98.32595927618818621 ) ) ;
#1061=VERTEX_POINT ( 'NONE', #27791 ) ;
#1062=DIRECTION ( 'NONE',  ( 0.000000000000000000, 0.000000000000000000, 1.000000000000000000 ) ) ;
#1063=ORIENTED_EDGE ( 'NONE', *, *, #13566, .F. ) ;
#1065=CARTESIAN_POINT ( 'NONE',  ( 6.224689322667630975, -62.55544044765341027, 134.1951906609236858 ) ) ;
#1067=AXIS2_PLACEMENT_3D ( 'NONE', #14772, #4114, #28146 ) ;
#1068=VERTEX_POINT ( 'NONE', #21157 ) ;
#1071=B_SPLINE_CURVE_WITH_KNOTS ( 'NONE', 3,
 ( #3634, #14439, #4446, #1336, #23673, #24187, #13221 ),
 .UNSPECIFIED., .F., .F.,
 ( 4, 3, 4 ),
 ( 3.404394821604483923E-17, 0.0002669559177086211531, 0.0005339083821118883934 ),
 .UNSPECIFIED. ) ;
#1073=CARTESIAN_POINT ( 'NONE',  ( 2.430230287190592531, 16.65331920325739645, 144.5585181921886715 ) ) ;
#1074=CARTESIAN_POINT ( 'NONE',  ( 109.1586059443104944, 0.005881369279875405844, -0.003930911098393235874 ) ) ;
#1075=CARTESIAN_POINT ( 'NONE',  ( 2.063896406836605024, -84.29612368209072315, -118.3103904147690173 ) ) ;
#1076=EDGE_CURVE ( 'NONE', #813, #11790, #25508, .T. ) ;
#1078=EDGE_CURVE ( 'NONE', #17856, #14908, #16032, .T. ) ;
#1080=CARTESIAN_POINT ( 'NONE',  ( 119.2224693531408803, 90.00000000000005684, -19.99999999999998934 ) ) ;
#1087=VERTEX_POINT ( 'NONE', #18421 ) ;
#1090=CARTESIAN_POINT ( 'NONE',  ( 32.73300124599737160, -108.9684813982492244, 44.31599526637918274 ) ) ;
#1091=CARTESIAN_POINT ( 'NONE',  ( 8.186469777910742707, -27.65107827750183134, 146.7694294853781685 ) ) ;
#1093=CARTESIAN_POINT ( 'NONE',  ( 2.433796855181233454, 144.8571464219889151, 13.76554153471742481 ) ) ;
#1094=VERTEX_POINT ( 'NONE', #5478 ) ;
#1095=CARTESIAN_POINT ( 'NONE',  ( 1.833838850855463720, 44.75675607098931152, 138.0350826608189720 ) ) ;
#1099=FACE_OUTER_BOUND ( 'NONE', #1014, .T. ) ;
#1101=ADVANCED_FACE ( 'NONE', ( #16274 ), #27971, .T. ) ;
#1104=CARTESIAN_POINT ( 'NONE',  ( 32.73300124599732186, 0.000000000000000000, 0.000000000000000000 ) ) ;
#1105=EDGE_CURVE ( 'NONE', #14457, #15269, #6847, .T. ) ;
#1107=CARTESIAN_POINT ( 'NONE',  ( 1.834118845439484335, -144.3336252355298370, 14.99112450600202173 ) ) ;
#1108=CARTESIAN_POINT ( 'NONE',  ( 26.04756280548353331, 112.6689254848259196, 10.72497307632831642 ) ) ;
#1109=EDGE_CURVE ( 'NONE', #16636, #9768, #14101, .T. ) ;
#1110=ORIENTED_EDGE ( 'NONE', *, *, #4327, .T. ) ;
#1112=CARTESIAN_POINT ( 'NONE',  ( 109.1589550718174877, -0.005777059646704624067, 0.004900004919104979095 ) ) ;
#1113=EDGE_CURVE ( 'NONE', #13345, #26365, #18077, .T. ) ;
#1116=VERTEX_POINT ( 'NONE', #12375 ) ;
#1117=ADVANCED_FACE ( 'NONE', ( #27198 ), #5848, .F. ) ;
#1119=CARTESIAN_POINT ( 'NONE',  ( 16.05277956358206737, -142.9335921074871010, -10.32496049470232435 ) ) ;
#1120=CARTESIAN_POINT ( 'NONE',  ( 109.1592201516379674, 0.007620268632968142664, 0.001934867487012853927 ) ) ;
#1121=ORIENTED_EDGE ( 'NONE', *, *, #144, .F. ) ;
#1124=CARTESIAN_POINT ( 'NONE',  ( 55.79472521941426777, 63.36760613016273425, -35.74479459808780746 ) ) ;
#1126=CARTESIAN_POINT ( 'NONE',  ( 2.063896406836609909, 16.52087515463778544, 144.3268707900447794 ) ) ;
#1127=CARTESIAN_POINT ( 'NONE',  ( 28.37644542392838432, -115.1790646972553276, 46.84227702240740143 ) ) ;
#1130=VERTEX_POINT ( 'NONE', #10097 ) ;
#1131=CARTESIAN_POINT ( 'NONE',  ( 1.833485406944043827, 107.4794113447409529, 97.49333871408727248 ) ) ;
#1133=EDGE_LOOP ( 'NONE', ( #14391, #13621, #6892, #12399 ) ) ;
#1137=CARTESIAN_POINT ( 'NONE',  ( 1.834118845439484335, 85.14950727126013419, -117.5010238212690155 ) ) ;
#1139=CARTESIAN_POINT ( 'NONE',  ( 2.108393763691209788, -108.8265195087755188, 96.26428731761947688 ) ) ;
#1141=ORIENTED_EDGE ( 'NONE', *, *, #1465, .F. ) ;
#1144=DIRECTION ( 'NONE',  ( 0.000000000000000000, 0.000000000000000000, -1.000000000000000000 ) ) ;
#1145=B_SPLINE_CURVE_WITH_KNOTS ( 'NONE', 3,
 ( #2477, #20038, #320, #17868, #16151, #24956 ),
 .UNSPECIFIED., .F., .F.,
 ( 4, 2, 4 ),
 ( 8.684452633802430946E-18, 0.0006311571484586112101, 0.001262314296917213747 ),
 .UNSPECIFIED. ) ;
#1148=ORIENTED_EDGE ( 'NONE', *, *, #27023, .T. ) ;
#1150=ADVANCED_FACE ( 'NONE', ( #10249 ), #8779, .F. ) ;
#1151=DIRECTION ( 'NONE',  ( -1.000000000000000000, -0.000000000000000000, -0.000000000000000000 ) ) ;
#1152=CARTESIAN_POINT ( 'NONE',  ( 109.1778270068192853, -0.009031542838317238586, -0.002278716897421720778 ) ) ;
#1156=CARTESIAN_POINT ( 'NONE',  ( 9.884929003653626367, -150.4771565009630763, 4.203795436551833298 ) ) ;
#1158=CARTESIAN_POINT ( 'NONE',  ( 1.833485406944043827, -144.3694338680886062, 14.63699153649312201 ) ) ;
#1159=CARTESIAN_POINT ( 'NONE',  ( 55.49584447822657296, -72.12568090333348891, 7.849835876628097786 ) ) ;
#1160=CARTESIAN_POINT ( 'NONE',  ( 28.37603512858355614, 22.09615328858603789, -112.5845402829046833 ) ) ;
#1161=VERTEX_POINT ( 'NONE', #8626 ) ;
#1163=ORIENTED_EDGE ( 'NONE', *, *, #13205, .T. ) ;
#1165=CARTESIAN_POINT ( 'NONE',  ( 6.224689322667630975, -111.7293398381271459, 97.14981701196286679 ) ) ;
#1166=CARTESIAN_POINT ( 'NONE',  ( 2.430230287190572103, 132.3371620660950896, 60.50928654924799588 ) ) ;
#1169=DIRECTION ( 'NONE',  ( 0.000000000000000000, 3.122502256758243698E-15, -1.000000000000000000 ) ) ;
#1170=ORIENTED_EDGE ( 'NONE', *, *, #15237, .F. ) ;
#1174=CARTESIAN_POINT ( 'NONE',  ( 109.1592201516379674, 0.006536841731953405704, -0.004368284148529032879 ) ) ;
#1175=ORIENTED_EDGE ( 'NONE', *, *, #22436, .F. ) ;
#1176=VERTEX_POINT ( 'NONE', #21727 ) ;
#1177=CARTESIAN_POINT ( 'NONE',  ( 1.834118845439484335, -132.6369225636070155, -58.85894970555047934 ) ) ;
#1179=CARTESIAN_POINT ( 'NONE',  ( 32.73300124599735739, 28.19767303745605602, 114.2056417606549132 ) ) ;
#1180=VERTEX_POINT ( 'NONE', #6066 ) ;
#1181=EDGE_LOOP ( 'NONE', ( #27339, #25625, #20061, #18942 ) ) ;
#1184=( BOUNDED_SURFACE ( )  B_SPLINE_SURFACE ( 3, 1, ( 
 ( #8102, #25655 ),
 ( #16871, #14689 ),
 ( #20131, #11358 ),
 ( #13516, #277 ) ),
 .UNSPECIFIED., .F., .F., .F. ) 
 B_SPLINE_SURFACE_WITH_KNOTS ( ( 4, 4 ),
 ( 2, 2 ),
 ( 0.000000000000000000, 1.000000000000000000 ),
 ( 0.000000000000000000, 1.000000000000000000 ),
 .UNSPECIFIED. ) 
 GEOMETRIC_REPRESENTATION_ITEM ( )  RATIONAL_B_SPLINE_SURFACE ( (
 ( 1.000000000000000000, 1.000000000000000000),
 ( 0.9960225298536222738, 0.9999952330161893110),
 ( 0.9960225298536222738, 0.9999952330161893110),
 ( 1.000000000000000000, 1.000000000000000000) ) ) 
 REPRESENTATION_ITEM ( '' )  SURFACE ( )  );
#1186=DIRECTION ( 'NONE',  ( 0.000000000000000000, 0.000000000000000000, 1.000000000000000000 ) ) ;
#1187=ADVANCED_FACE ( 'NONE', ( #8215 ), #23353, .F. ) ;
#1191=CARTESIAN_POINT ( 'NONE',  ( 28.43349137099849955, 123.9292945876796352, 8.951033805645105090 ) ) ;
#1192=CARTESIAN_POINT ( 'NONE',  ( 25.86096068574580897, 107.8247115223745993, -33.98552076022083668 ) ) ;
#1193=CARTESIAN_POINT ( 'NONE',  ( 25.64692232868534560, 84.12764974008027252, 75.30916867847129481 ) ) ;
#1195=CARTESIAN_POINT ( 'NONE',  ( 32.73300124599735739, -99.90245962373877830, 62.10906484417201767 ) ) ;
#1196=CARTESIAN_POINT ( 'NONE',  ( 1.834118845439484335, 72.40084790867506115, -125.7578880615037491 ) ) ;
#1198=CARTESIAN_POINT ( 'NONE',  ( 32.73300124599735739, -20.69176323058707823, 115.8010721414082980 ) ) ;
#1199=CARTESIAN_POINT ( 'NONE',  ( 25.69398547355841700, -22.75551036952002804, 110.6264597420659612 ) ) ;
#1203=DIRECTION ( 'NONE',  ( 0.000000000000000000, 1.000000000000000000, 0.000000000000000000 ) ) ;
#1204=ORIENTED_EDGE ( 'NONE', *, *, #10395, .T. ) ;
#1206=DIRECTION ( 'NONE',  ( 0.000000000000000000, 0.000000000000000000, 1.000000000000000000 ) ) ;
#1209=ORIENTED_EDGE ( 'NONE', *, *, #11374, .T. ) ;
#1210=EDGE_LOOP ( 'NONE', ( #20866, #21982 ) ) ;
#1211=ADVANCED_FACE ( 'NONE', ( #23632 ), #12805, .F. ) ;
#1213=CARTESIAN_POINT ( 'NONE',  ( 109.1589550718175161, -0.002553077953680983961, -0.007132058561966975706 ) ) ;
#1214=CARTESIAN_POINT ( 'NONE',  ( 26.04756280548352976, 107.9769918539640514, 33.91579348271552874 ) ) ;
#1216=B_SPLINE_CURVE_WITH_KNOTS ( 'NONE', 3,
 ( #5483, #592, #20735, #27055 ),
 .UNSPECIFIED., .F., .F.,
 ( 4, 4 ),
 ( 3.314910864404112914E-16, 0.01077107486149839373 ),
 .UNSPECIFIED. ) ;
#1217=CARTESIAN_POINT ( 'NONE',  ( 1.832998868059890096, 125.4013017422241063, -73.01698022778224129 ) ) ;
#1221=ORIENTED_EDGE ( 'NONE', *, *, #16545, .T. ) ;
#1222=CARTESIAN_POINT ( 'NONE',  ( 32.73300124599732186, 0.000000000000000000, 0.000000000000000000 ) ) ;
#1223=CARTESIAN_POINT ( 'NONE',  ( 25.64703792032471696, 66.24710921678179432, -91.43447020678362946 ) ) ;
#1225=CARTESIAN_POINT ( 'NONE',  ( 1.833838848569455893, -85.14939661881641086, 117.5008734796307976 ) ) ;
#1226=CARTESIAN_POINT ( 'NONE',  ( 25.98552792386799837, 10.75254026142952135, -112.6247604222997438 ) ) ;
#1228=ORIENTED_EDGE ( 'NONE', *, *, #25694, .F. ) ;
#1232=ORIENTED_EDGE ( 'NONE', *, *, #28135, .F. ) ;
#1236=ORIENTED_EDGE ( 'NONE', *, *, #3674, .T. ) ;
#1237=EDGE_CURVE ( 'NONE', #8709, #10429, #1618, .T. ) ;
#1238=ADVANCED_FACE ( 'NONE', ( #12793 ), #12841, .F. ) ;
#1239=FACE_OUTER_BOUND ( 'NONE', #28366, .T. ) ;
#1240=ORIENTED_EDGE ( 'NONE', *, *, #14373, .F. ) ;
#1241=CARTESIAN_POINT ( 'NONE',  ( 25.64681081121879203, -45.54494737132156246, -103.3177883989783936 ) ) ;
#1242=CARTESIAN_POINT ( 'NONE',  ( 10.93730112725972781, -71.28103789255033007, 133.3192575531796251 ) ) ;
#1247=EDGE_LOOP ( 'NONE', ( #20214, #9048, #11519, #1121 ) ) ;
#1248=CARTESIAN_POINT ( 'NONE',  ( 1.833809397773856986, 85.43729755723308017, -117.2915757704548838 ) ) ;
#1249=CARTESIAN_POINT ( 'NONE',  ( 109.1721716018069515, 0.003350975118860970506, 0.01673651515802105152 ) ) ;
#1251=ORIENTED_EDGE ( 'NONE', *, *, #18700, .T. ) ;
#1253=ORIENTED_EDGE ( 'NONE', *, *, #21125, .T. ) ;
#1256=CARTESIAN_POINT ( 'NONE',  ( 1.833838850093452821, 107.8375672471895399, -97.09738632348927467 ) ) ;
#1257=CARTESIAN_POINT ( 'NONE',  ( 10.93730112725978287, -140.0398180619114896, 56.95489579269701608 ) ) ;
#1258=B_SPLINE_CURVE_WITH_KNOTS ( 'NONE', 3,
 ( #14134, #20912, #5818, #7697 ),
 .UNSPECIFIED., .F., .F.,
 ( 4, 4 ),
 ( 7.152448122690996019E-18, 0.008383560773332713809 ),
 .UNSPECIFIED. ) ;
#1260=CARTESIAN_POINT ( 'NONE',  ( 1.833485406944057594, -132.7804117027884274, -58.53321471327013370 ) ) ;
#1261=ORIENTED_EDGE ( 'NONE', *, *, #12602, .F. ) ;
#1263=CARTESIAN_POINT ( 'NONE',  ( 25.64692872815577118, 46.21877827526699889, -103.0182448446669241 ) ) ;
#1264=ORIENTED_EDGE ( 'NONE', *, *, #22425, .F. ) ;
#1266=LINE ( 'NONE', #12347, #27185 ) ;
#1269=CARTESIAN_POINT ( 'NONE',  ( 8.186469829614267724, -137.8131829164339024, 57.56191610809328552 ) ) ;
#1270=CARTESIAN_POINT ( 'NONE',  ( 2.430230287190581429, -71.49654683843421310, -126.7388733285352345 ) ) ;
#1272=CARTESIAN_POINT ( 'NONE',  ( 109.1778270068192853, -0.008236503545664842357, 0.004349865064712375717 ) ) ;
#1273=ORIENTED_EDGE ( 'NONE', *, *, #7597, .T. ) ;
#1276=EDGE_CURVE ( 'NONE', #8760, #14056, #5386, .T. ) ;
#1278=EDGE_CURVE ( 'NONE', #2646, #3538, #13274, .T. ) ;
#1279=ORIENTED_EDGE ( 'NONE', *, *, #11247, .F. ) ;
#1282=B_SPLINE_CURVE_WITH_KNOTS ( 'NONE', 3,
 ( #16754, #23098, #27675, #11850 ),
 .UNSPECIFIED., .F., .F.,
 ( 4, 4 ),
 ( 0.000000000000000000, 0.01077107196513874335 ),
 .UNSPECIFIED. ) ;
#1285=CARTESIAN_POINT ( 'NONE',  ( 25.64708010899966339, -23.42206246795081981, 110.4552579818684563 ) ) ;
#1286=CARTESIAN_POINT ( 'NONE',  ( 1.833838850093452599, 138.0075846865486824, -44.84138612520948897 ) ) ;
#1287=ORIENTED_EDGE ( 'NONE', *, *, #14329, .F. ) ;
#1288=CARTESIAN_POINT ( 'NONE',  ( 28.37644542392838432, 89.64009552702908934, 86.16884085957975969 ) ) ;
#1289=CARTESIAN_POINT ( 'NONE',  ( 1.833691583653537016, -125.4903330494893936, -72.86287859464719929 ) ) ;
#1290=CARTESIAN_POINT ( 'NONE',  ( 25.64681081121879203, -35.28660243342623204, 107.2555980796239936 ) ) ;
#1291=LINE ( 'NONE', #17250, #16391 ) ;
#1292=VERTEX_POINT ( 'NONE', #4868 ) ;
#1294=CARTESIAN_POINT ( 'NONE',  ( 10.93730112725932635, 0.000000000000000000, 0.000000000000000000 ) ) ;
#1296=CARTESIAN_POINT ( 'NONE',  ( 24.22246935314087324, 0.000000000000000000, 0.000000000000000000 ) ) ;
#1297=CARTESIAN_POINT ( 'NONE',  ( 2.433796855181219243, 144.5536872373191670, 16.65276281464612396 ) ) ;
#1298=CARTESIAN_POINT ( 'NONE',  ( 10.93730112726003156, 108.9902118373755684, -104.7670965581001781 ) ) ;
#1302=CARTESIAN_POINT ( 'NONE',  ( 1.833809397773891403, -144.3333383260367668, 14.99109763364097248 ) ) ;
#1307=CARTESIAN_POINT ( 'NONE',  ( 109.1586900883932856, 0.0006456433529069069291, -0.007109207791180753924 ) ) ;
#1308=ORIENTED_EDGE ( 'NONE', *, *, #24787, .F. ) ;
#1309=VERTEX_POINT ( 'NONE', #26592 ) ;
#1310=CARTESIAN_POINT ( 'NONE',  ( 25.86096068574581253, 22.52859312382188861, 110.7864907291859424 ) ) ;
#1312=CARTESIAN_POINT ( 'NONE',  ( 2.063896406836609909, -28.88716984836416657, 142.3682421260906779 ) ) ;
#1313=ORIENTED_EDGE ( 'NONE', *, *, #20571, .F. ) ;
#1314=EDGE_CURVE ( 'NONE', #18428, #3848, #22295, .T. ) ;
#1316=VECTOR ( 'NONE', #10362, 1000.000000000000114 ) ;
#1318=B_SPLINE_CURVE_WITH_KNOTS ( 'NONE', 3,
 ( #28279, #19786, #15460, #15322 ),
 .UNSPECIFIED., .F., .F.,
 ( 4, 4 ),
 ( 0.000000000000000000, 0.008383560773332708604 ),
 .UNSPECIFIED. ) ;
#1322=CARTESIAN_POINT ( 'NONE',  ( 1.833485406944043827, -132.7804117027891948, 58.53321471326832182 ) ) ;
#1323=FACE_OUTER_BOUND ( 'NONE', #15025, .T. ) ;
#1326=CARTESIAN_POINT ( 'NONE',  ( 10.93730112725932635, 0.000000000000000000, 0.000000000000000000 ) ) ;
#1327=CARTESIAN_POINT ( 'NONE',  ( 5.340103579038201431, 47.74933483136881307, 139.5040934216401070 ) ) ;
#1329=CARTESIAN_POINT ( 'NONE',  ( 16.05277956358213487, 48.70400867629093256, 134.7758735858403440 ) ) ;
#1330=CARTESIAN_POINT ( 'NONE',  ( 109.1721716018069515, -0.01254847260354027827, -0.01157047143378750823 ) ) ;
#1331=DIRECTION ( 'NONE',  ( -0.5946245182733607137, -0.6977579871484507201, -0.3994439555666302599 ) ) ;
#1334=CARTESIAN_POINT ( 'NONE',  ( 10.93730112725997294, 36.23586118136742584, -146.7718404940639516 ) ) ;
#1335=CARTESIAN_POINT ( 'NONE',  ( 109.1586900883932856, -0.005833932871491344374, -0.004113747440992306104 ) ) ;
#1336=CARTESIAN_POINT ( 'NONE',  ( 1.833750490713715209, -0.2669522761655517273, 145.1094586213657749 ) ) ;
#1338=CARTESIAN_POINT ( 'NONE',  ( 109.1624594426973260, 0.01405141589343893681, -0.007576898892904924791 ) ) ;
#1340=CARTESIAN_POINT ( 'NONE',  ( 26.11404676487259024, -22.43340081644844020, 110.9778746459746372 ) ) ;
#1341=EDGE_CURVE ( 'NONE', #21070, #7362, #27726, .T. ) ;
#1342=LINE ( 'NONE', #14142, #24030 ) ;
#1343=VERTEX_POINT ( 'NONE', #16675 ) ;
#1345=( BOUNDED_SURFACE ( )  B_SPLINE_SURFACE ( 3, 1, ( 
 ( #793, #25127 ),
 ( #18332, #20364 ),
 ( #9300, #7425 ),
 ( #4964, #13596 ) ),
 .UNSPECIFIED., .F., .F., .F. ) 
 B_SPLINE_SURFACE_WITH_KNOTS ( ( 4, 4 ),
 ( 2, 2 ),
 ( 0.000000000000000000, 1.000000000000000000 ),
 ( 0.000000000000000000, 1.000000000000000000 ),
 .UNSPECIFIED. ) 
 GEOMETRIC_REPRESENTATION_ITEM ( )  RATIONAL_B_SPLINE_SURFACE ( (
 ( 1.000000000000000000, 1.000000000000000000),
 ( 0.9960225298536222738, 0.9999952330161893110),
 ( 0.9960225298536222738, 0.9999952330161893110),
 ( 1.000000000000000000, 1.000000000000000000) ) ) 
 REPRESENTATION_ITEM ( '' )  SURFACE ( )  );
#1349=CARTESIAN_POINT ( 'NONE',  ( 2.433796855181233454, -118.5671979538051062, -84.34988187691051564 ) ) ;
#1352=CARTESIAN_POINT ( 'NONE',  ( 2.430230287190581429, 13.76600171652644278, 144.8619874886007324 ) ) ;
#1354=CARTESIAN_POINT ( 'NONE',  ( 55.79472521941426777, 68.96476385670665366, 23.17337251492787331 ) ) ;
#1355=EDGE_LOOP ( 'NONE', ( #18978, #2999, #769, #14797 ) ) ;
#1356=VERTEX_POINT ( 'NONE', #16376 ) ;
#1357=CARTESIAN_POINT ( 'NONE',  ( 1.833485406944043827, -29.64752363041439764, -142.0485807715649003 ) ) ;
#1358=B_SPLINE_CURVE_WITH_KNOTS ( 'NONE', 3,
 ( #21003, #1288, #1576, #3588, #14230, #14386, #5622 ),
 .UNSPECIFIED., .F., .F.,
 ( 4, 3, 4 ),
 ( 0.000000000000000000, 0.02398743853561353251, 0.04000277880656209761 ),
 .UNSPECIFIED. ) ;
#1359=CARTESIAN_POINT ( 'NONE',  ( 1.893872463202038503, 144.4512189534319759, -14.22435552397860548 ) ) ;
#1360=CARTESIAN_POINT ( 'NONE',  ( 25.64681081121879203, -91.10197563707990298, 66.70335573067838197 ) ) ;
#1369=EDGE_CURVE ( 'NONE', #4903, #16481, #21061, .T. ) ;
#1370=ORIENTED_EDGE ( 'NONE', *, *, #1908, .F. ) ;
#1374=ORIENTED_EDGE ( 'NONE', *, *, #24628, .T. ) ;
#1376=B_SPLINE_CURVE_WITH_KNOTS ( 'NONE', 3,
 ( #2464, #18147, #24801, #20166, #22491, #11117 ),
 .UNSPECIFIED., .F., .F.,
 ( 4, 2, 4 ),
 ( 2.168404344971008868E-18, 0.0006311636237756793446, 0.001262327247551356521 ),
 .UNSPECIFIED. ) ;
#1377=EDGE_CURVE ( 'NONE', #1601, #19236, #20169, .T. ) ;
#1378=CARTESIAN_POINT ( 'NONE',  ( 1.833603222531971610, 96.76619886578326657, 108.1346772638449920 ) ) ;
#1379=ORIENTED_EDGE ( 'NONE', *, *, #19031, .T. ) ;
#1381=CIRCLE ( 'NONE', #12420, 117.6351876552689504 ) ;
#1384=CARTESIAN_POINT ( 'NONE',  ( 109.1592201516379674, 0.0005146241775907373474, -0.007845213074660002325 ) ) ;
#1385=CARTESIAN_POINT ( 'NONE',  ( 2.433796855181233454, 138.8296532063088193, 43.58222566461690661 ) ) ;
#1386=CARTESIAN_POINT ( 'NONE',  ( 1.833603222531971610, 0.4449221977539696282, -145.1089511853978422 ) ) ;
#1387=CARTESIAN_POINT ( 'NONE',  ( 1.894214914920927528, -141.7768822502889066, 31.11059045489088959 ) ) ;
#1388=ORIENTED_EDGE ( 'NONE', *, *, #13947, .T. ) ;
#1390=CARTESIAN_POINT ( 'NONE',  ( 6.224689322667630975, -12.92299475786858842, -147.4941644018829265 ) ) ;
#1391=CARTESIAN_POINT ( 'NONE',  ( 1.833485406944043827, 14.63699153649359452, 144.3694338680885778 ) ) ;
#1392=CARTESIAN_POINT ( 'NONE',  ( 2.430230287190572103, 16.65331920325932202, -144.5585181921884157 ) ) ;
#1394=EDGE_LOOP ( 'NONE', ( #26087, #3282, #16540, #13815 ) ) ;
#1398=CARTESIAN_POINT ( 'NONE',  ( 32.73300124599732186, 0.000000000000000000, 0.000000000000000000 ) ) ;
#1399=CARTESIAN_POINT ( 'NONE',  ( 10.93730112725932635, 0.000000000000000000, 0.000000000000000000 ) ) ;
#1401=EDGE_CURVE ( 'NONE', #28403, #12613, #18443, .T. ) ;
#1402=CARTESIAN_POINT ( 'NONE',  ( 1.833838848569454782, -132.6367525013572788, -58.85887272891319810 ) ) ;
#1403=LINE ( 'NONE', #14504, #20757 ) ;
#1405=VERTEX_POINT ( 'NONE', #3286 ) ;
#1407=CARTESIAN_POINT ( 'NONE',  ( 30.59141879584313628, 14.83090566979595870, -115.2623358717303717 ) ) ;
#1409=FACE_OUTER_BOUND ( 'NONE', #777, .T. ) ;
#1413=VECTOR ( 'NONE', #12119, 1000.000000000000114 ) ;
#1414=CARTESIAN_POINT ( 'NONE',  ( 30.58324630866352578, 112.0331114996534296, 45.56259622822393851 ) ) ;
#1417=CARTESIAN_POINT ( 'NONE',  ( 28.37644542392843405, 54.25112470585876423, -111.8804331835009691 ) ) ;
#1418=CONICAL_SURFACE ( 'NONE', #26670, 117.6351876552689504, 0.9945805576725580410 ) ;
#1419=CARTESIAN_POINT ( 'NONE',  ( 1.834118845439484335, 117.5010238212698823, 85.14950727125895469 ) ) ;
#1420=CARTESIAN_POINT ( 'NONE',  ( 1.833206310202323053, -137.7753867363981044, 45.54896489827107331 ) ) ;
#1421=VERTEX_POINT ( 'NONE', #27309 ) ;
#1424=CARTESIAN_POINT ( 'NONE',  ( 28.37599760073042532, -68.88138253892459772, 91.75439000741670270 ) ) ;
#1425=B_SPLINE_CURVE_WITH_KNOTS ( 'NONE', 3,
 ( #17345, #8305, #6424, #12608, #28418, #8580, #11028, #21678, #26134, #15323 ),
 .UNSPECIFIED., .F., .F.,
 ( 4, 3, 3, 4 ),
 ( 5.003707553108401214E-17, 0.0002669559177086402351, 0.0005339118354150940680, 0.001067817517169129121 ),
 .UNSPECIFIED. ) ;
#1427=B_SPLINE_CURVE_WITH_KNOTS ( 'NONE', 3,
 ( #875, #27056, #7364, #14244, #18274, #23068 ),
 .UNSPECIFIED., .F., .F.,
 ( 4, 2, 4 ),
 ( 3.903127820947815962E-18, 0.0006311636237756693699, 0.001262327247551335054 ),
 .UNSPECIFIED. ) ;
#1429=VECTOR ( 'NONE', #12856, 1000.000000000000000 ) ;
#1430=CARTESIAN_POINT ( 'NONE',  ( 10.93730112725943471, 125.1380233598475229, 84.82621002473483429 ) ) ;
#1431=CARTESIAN_POINT ( 'NONE',  ( 19.66333377628719958, 136.4524620437343003, 18.85786579349995762 ) ) ;
#1432=CIRCLE ( 'NONE', #11088, 117.6351876552689504 ) ;
#1434=EDGE_CURVE ( 'NONE', #24791, #813, #8161, .T. ) ;
#1436=CARTESIAN_POINT ( 'NONE',  ( 1.833485406944043827, -15.69895494453482598, 144.2578170162062463 ) ) ;
#1437=EDGE_LOOP ( 'NONE', ( #9079, #697, #16838, #10518 ) ) ;
#1438=CIRCLE ( 'NONE', #12458, 117.6351876552689504 ) ;
#1439=ADVANCED_FACE ( 'NONE', ( #9618 ), #16507, .F. ) ;
#1442=CARTESIAN_POINT ( 'NONE',  ( 2.430230287190572103, -109.1043569252020831, 96.28466919684061054 ) ) ;
#1443=CARTESIAN_POINT ( 'NONE',  ( 1.832998868059890096, 132.3466930259802439, -59.50898020732379479 ) ) ;
#1444=PLANE ( 'NONE',  #8294 ) ;
#1445=CARTESIAN_POINT ( 'NONE',  ( 25.69398547355839924, -91.80679989327096280, -65.78402800526257010 ) ) ;
#1446=CARTESIAN_POINT ( 'NONE',  ( 1.833809397773874084, -138.0624841332890753, 44.67209459545020422 ) ) ;
#1447=FACE_OUTER_BOUND ( 'NONE', #21884, .T. ) ;
#1448=ORIENTED_EDGE ( 'NONE', *, *, #26567, .F. ) ;
#1449=CARTESIAN_POINT ( 'NONE',  ( 2.433796855181205476, 57.85512797797890272, 133.5135467655520074 ) ) ;
#1451=CARTESIAN_POINT ( 'NONE',  ( 25.73574536432414561, -11.00659994954073184, -112.4329083163019618 ) ) ;
#1454=CARTESIAN_POINT ( 'NONE',  ( 2.430230287190592531, 107.1617224697477297, -98.44218333480665706 ) ) ;
#1455=ORIENTED_EDGE ( 'NONE', *, *, #12599, .T. ) ;
#1457=CARTESIAN_POINT ( 'NONE',  ( 25.64699802086724034, -12.03888878460397649, -112.2675771984165607 ) ) ;
#1458=ORIENTED_EDGE ( 'NONE', *, *, #25670, .F. ) ;
#1460=ORIENTED_EDGE ( 'NONE', *, *, #20738, .T. ) ;
#1461=VERTEX_POINT ( 'NONE', #14069 ) ;
#1462=AXIS2_PLACEMENT_3D ( 'NONE', #2300, #22338, #22187 ) ;
#1463=CARTESIAN_POINT ( 'NONE',  ( 2.263178113027036531, 28.85718369185711651, 142.5035404044874952 ) ) ;
#1464=CARTESIAN_POINT ( 'NONE',  ( 109.1592201516379674, 0.007780772729118878156, 0.001127733110579607657 ) ) ;
#1465=EDGE_CURVE ( 'NONE', #27866, #2646, #5439, .T. ) ;
#1466=EDGE_CURVE ( 'NONE', #20633, #26751, #7143, .T. ) ;
#1467=CARTESIAN_POINT ( 'NONE',  ( 1.893872463202069145, -132.9857054814983712, 58.16604752596676775 ) ) ;
#1468=CARTESIAN_POINT ( 'NONE',  ( 55.49584447822657296, -54.09506550945592807, -48.34726110740042060 ) ) ;
#1469=EDGE_CURVE ( 'NONE', #11691, #24126, #12925, .T. ) ;
#1470=DIRECTION ( 'NONE',  ( -1.000000000000000000, -0.000000000000000000, -0.000000000000000000 ) ) ;
#1471=CARTESIAN_POINT ( 'NONE',  ( 30.59141879584283430, -26.79785525806475377, 113.0806649571965465 ) ) ;
#1473=EDGE_CURVE ( 'NONE', #21210, #26606, #26990, .T. ) ;
#1474=CARTESIAN_POINT ( 'NONE',  ( 1.832998868059890096, 144.2584710144580242, 15.69902610990420122 ) ) ;
#1475=CARTESIAN_POINT ( 'NONE',  ( 25.64708228042118421, -75.52311986517973708, -83.93578330383164143 ) ) ;
#1476=CARTESIAN_POINT ( 'NONE',  ( 2.430230287190592531, 84.35270093935415048, -118.5711603495673074 ) ) ;
#1478=CARTESIAN_POINT ( 'NONE',  ( 25.73574536432415272, -112.9674920590232716, -0.8061344836380949230 ) ) ;
#1481=CARTESIAN_POINT ( 'NONE',  ( 13.36082413113063083, 70.90215303572314554, -135.4964217943299900 ) ) ;
#1482=CARTESIAN_POINT ( 'NONE',  ( 25.64670758986457955, 102.9458331681485532, 46.37945960491909148 ) ) ;
#1483=ORIENTED_EDGE ( 'NONE', *, *, #25373, .T. ) ;
#1488=ORIENTED_EDGE ( 'NONE', *, *, #1237, .F. ) ;
#1489=ORIENTED_EDGE ( 'NONE', *, *, #16081, .F. ) ;
#1490=VERTEX_POINT ( 'NONE', #19523 ) ;
#1491=CONICAL_SURFACE ( 'NONE', #18480, 117.6351876552689504, 0.9945805576725580410 ) ;
#1498=DIRECTION ( 'NONE',  ( -1.000000000000000000, -0.000000000000000000, -0.000000000000000000 ) ) ;
#1499=DIRECTION ( 'NONE',  ( -0.000000000000000000, 1.000000000000000000, -0.000000000000000000 ) ) ;
#1502=ORIENTED_EDGE ( 'NONE', *, *, #19891, .T. ) ;
#1506=CARTESIAN_POINT ( 'NONE',  ( 1.833485406944043827, 132.7804117027896211, -58.53321471326746916 ) ) ;
#1508=B_SPLINE_CURVE_WITH_KNOTS ( 'NONE', 3,
 ( #7576, #3239, #14160, #14735, #12021, #23121 ),
 .UNSPECIFIED., .F., .F.,
 ( 4, 2, 4 ),
 ( 2.602085213965210642E-18, 0.0006311636237756765256, 0.001262327247551350666 ),
 .UNSPECIFIED. ) ;
#1509=CARTESIAN_POINT ( 'NONE',  ( 10.93730112725972070, -26.59437931460858451, 148.8212007290659642 ) ) ;
#1510=CARTESIAN_POINT ( 'NONE',  ( 109.1586900883932856, 0.006479576224403786264, 0.002995460350180832385 ) ) ;
#1511=CARTESIAN_POINT ( 'NONE',  ( 26.11404676487257603, 33.91085499298520034, -108.0249973236464314 ) ) ;
#1514=EDGE_LOOP ( 'NONE', ( #16978, #15733, #24881, #15385, #5827, #11832 ) ) ;
#1520=ORIENTED_EDGE ( 'NONE', *, *, #2351, .T. ) ;
#1521=FACE_OUTER_BOUND ( 'NONE', #17886, .T. ) ;
#1522=ORIENTED_EDGE ( 'NONE', *, *, #2533, .F. ) ;
#1524=VECTOR ( 'NONE', #8411, 1000.000000000000341 ) ;
#1525=CARTESIAN_POINT ( 'NONE',  ( 30.58324630866343696, 95.47492154584260504, -74.24222250960141878 ) ) ;
#1527=CARTESIAN_POINT ( 'NONE',  ( 1.834118845439484335, -144.2964192726483361, 15.34511559672636238 ) ) ;
#1528=DIRECTION ( 'NONE',  ( 0.000000000000000000, 0.000000000000000000, 1.000000000000000000 ) ) ;
#1529=EDGE_CURVE ( 'NONE', #7265, #5626, #3649, .T. ) ;
#1530=AXIS2_PLACEMENT_3D ( 'NONE', #12824, #19308, #6236 ) ;
#1534=CARTESIAN_POINT ( 'NONE',  ( 109.1624594426973260, 0.01263706729758982267, 0.009754804742273323268 ) ) ;
#1535=CARTESIAN_POINT ( 'NONE',  ( 32.73300124599735028, 110.6325518752274206, 39.98094346392350218 ) ) ;
#1537=CARTESIAN_POINT ( 'NONE',  ( 109.1778270068192853, 0.006682187084648908565, -0.006489198140359554549 ) ) ;
#1539=LINE ( 'NONE', #14775, #20543 ) ;
#1541=ORIENTED_EDGE ( 'NONE', *, *, #14828, .T. ) ;
#1544=FACE_OUTER_BOUND ( 'NONE', #24260, .T. ) ;
#1547=CARTESIAN_POINT ( 'NONE',  ( 10.93730112725971892, -10.89264110825104837, 150.7858122213660863 ) ) ;
#1548=ORIENTED_EDGE ( 'NONE', *, *, #348, .T. ) ;
#1549=LINE ( 'NONE', #14785, #11108 ) ;
#1551=ORIENTED_EDGE ( 'NONE', *, *, #5562, .T. ) ;
#1553=CARTESIAN_POINT ( 'NONE',  ( 99.22246935314079508, 90.00000000000005684, 39.99999999999999289 ) ) ;
#1554=( BOUNDED_SURFACE ( )  B_SPLINE_SURFACE ( 3, 1, ( 
 ( #14884, #23547 ),
 ( #5983, #18783 ),
 ( #8276, #27556 ),
 ( #16631, #1641 ) ),
 .UNSPECIFIED., .F., .F., .F. ) 
 B_SPLINE_SURFACE_WITH_KNOTS ( ( 4, 4 ),
 ( 2, 2 ),
 ( 0.000000000000000000, 1.000000000000000000 ),
 ( 0.000000000000000000, 1.000000000000000000 ),
 .UNSPECIFIED. ) 
 GEOMETRIC_REPRESENTATION_ITEM ( )  RATIONAL_B_SPLINE_SURFACE ( (
 ( 1.000000000000000000, 1.000000000000000000),
 ( 0.9960225298536222738, 0.9999952330161893110),
 ( 0.9960225298536222738, 0.9999952330161893110),
 ( 1.000000000000000000, 1.000000000000000000) ) ) 
 REPRESENTATION_ITEM ( '' )  SURFACE ( )  );
#1555=CARTESIAN_POINT ( 'NONE',  ( 109.1586059443104944, -0.004524147648825598347, 0.005438258427231118172 ) ) ;
#1556=CARTESIAN_POINT ( 'NONE',  ( 25.64670758986456889, 75.18147256662052769, 84.24158725144647519 ) ) ;
#1557=CARTESIAN_POINT ( 'NONE',  ( 25.64670758986457955, -110.5460908981863355, 22.98827151089250620 ) ) ;
#1562=EDGE_CURVE ( 'NONE', #10623, #9334, #17413, .T. ) ;
#1563=CARTESIAN_POINT ( 'NONE',  ( 109.1624594426973118, 0.004489871836309348475, -0.01531968460306870790 ) ) ;
#1564=ORIENTED_EDGE ( 'NONE', *, *, #24628, .F. ) ;
#1565=EDGE_CURVE ( 'NONE', #9768, #14537, #9530, .T. ) ;
#1567=B_SPLINE_CURVE_WITH_KNOTS ( 'NONE', 3,
 ( #1677, #15049, #6579, #12755, #4402, #8591, #19656 ),
 .UNSPECIFIED., .F., .F.,
 ( 4, 3, 4 ),
 ( 0.000000000000000000, 0.02398743853561352557, 0.04000277880656212537 ),
 .UNSPECIFIED. ) ;
#1568=B_SPLINE_CURVE_WITH_KNOTS ( 'NONE', 3,
 ( #15627, #5140, #20244, #13629 ),
 .UNSPECIFIED., .F., .F.,
 ( 4, 4 ),
 ( 0.000000000000000000, 0.008383560773332734625 ),
 .UNSPECIFIED. ) ;
#1569=ADVANCED_FACE ( 'NONE', ( #12171 ), #3820, .F. ) ;
#1572=EDGE_CURVE ( 'NONE', #23165, #26, #27367, .T. ) ;
#1575=CARTESIAN_POINT ( 'NONE',  ( 26.11404676487257603, -107.3263591096427945, -36.06104232266560672 ) ) ;
#1576=CARTESIAN_POINT ( 'NONE',  ( 24.01988960052055333, 94.47404045191640876, 90.81495976423825311 ) ) ;
#1577=B_SPLINE_CURVE_WITH_KNOTS ( 'NONE', 3,
 ( #19975, #15364, #8911, #22290, #15496, #4571, #17528, #2550 ),
 .UNSPECIFIED., .F., .F.,
 ( 4, 2, 2, 4 ),
 ( 3.469446951953614189E-18, 0.0002429592666046673818, 0.0004859185332093312942, 0.0009718370664186931629 ),
 .UNSPECIFIED. ) ;
#1579=CARTESIAN_POINT ( 'NONE',  ( 10.93730112725932635, 0.000000000000000000, 0.000000000000000000 ) ) ;
#1583=CARTESIAN_POINT ( 'NONE',  ( 25.64670758986457955, -97.53391148296633162, -56.88615781331589716 ) ) ;
#1585=CARTESIAN_POINT ( 'NONE',  ( 16.05277956358202474, -87.96830019103585130, -113.1291064380272218 ) ) ;
#1588=CARTESIAN_POINT ( 'NONE',  ( 1.833485406944043827, -144.2578170162061895, -15.69895494453532869 ) ) ;
#1589=CARTESIAN_POINT ( 'NONE',  ( 26.28373643307403640, -48.05579805965621176, 118.1623717393434418 ) ) ;
#1591=DIRECTION ( 'NONE',  ( -1.000000000000000000, -0.000000000000000000, -0.000000000000000000 ) ) ;
#1594=CARTESIAN_POINT ( 'NONE',  ( 109.1586059443104944, -0.001198897580748387297, -0.006971743774738781672 ) ) ;
#1595=CARTESIAN_POINT ( 'NONE',  ( 25.64700659047696973, 0.2275682798802720064, -112.9110011064639565 ) ) ;
#1596=ORIENTED_EDGE ( 'NONE', *, *, #11628, .T. ) ;
#1597=CARTESIAN_POINT ( 'NONE',  ( 25.64703792032466012, -45.78915563622635432, 103.2099561461823214 ) ) ;
#1599=ORIENTED_EDGE ( 'NONE', *, *, #21466, .F. ) ;
#1601=VERTEX_POINT ( 'NONE', #1090 ) ;
#1603=ORIENTED_EDGE ( 'NONE', *, *, #15318, .F. ) ;
#1605=CARTESIAN_POINT ( 'NONE',  ( 1.833206308920109606, 29.44113170198547635, 142.0914675761164006 ) ) ;
#1607=CARTESIAN_POINT ( 'NONE',  ( 10.93730112725932635, 0.000000000000000000, 0.000000000000000000 ) ) ;
#1609=VERTEX_POINT ( 'NONE', #3105 ) ;
#1610=CARTESIAN_POINT ( 'NONE',  ( 1.833603222531972277, -58.61467103263656497, -132.7445893798463601 ) ) ;
#1611=DIRECTION ( 'NONE',  ( -1.000000000000000000, -0.000000000000000000, -0.000000000000000000 ) ) ;
#1614=CARTESIAN_POINT ( 'NONE',  ( 1.833485406944043827, -141.8265699653865113, -30.69200235379080510 ) ) ;
#1615=B_SPLINE_CURVE_WITH_KNOTS ( 'NONE', 3,
 ( #3684, #1108, #8036, #21095, #18951, #10336, #3269, #27435 ),
 .UNSPECIFIED., .F., .F.,
 ( 4, 2, 2, 4 ),
 ( 0.000000000000000000, 0.0002429592666046676800, 0.0004859185332093353600, 0.0009718370664186789598 ),
 .UNSPECIFIED. ) ;
#1616=CARTESIAN_POINT ( 'NONE',  ( 1.832998868059858122, 73.01698022778532504, -125.4013017422223299 ) ) ;
#1618=B_SPLINE_CURVE_WITH_KNOTS ( 'NONE', 3,
 ( #14954, #6472, #4306, #19282 ),
 .UNSPECIFIED., .F., .F.,
 ( 4, 4 ),
 ( 1.734723475976807094E-17, 0.008383560773332727686 ),
 .UNSPECIFIED. ) ;
#1620=CARTESIAN_POINT ( 'NONE',  ( 109.1589550718174877, -0.0005685167901298913409, -0.007553890059312244956 ) ) ;
#1621=CARTESIAN_POINT ( 'NONE',  ( 28.43349137099835744, -122.3147591366315510, -21.85613782299105878 ) ) ;
#1622=VECTOR ( 'NONE', #7177, 1000.000000000000114 ) ;
#1623=ORIENTED_EDGE ( 'NONE', *, *, #10544, .F. ) ;
#1624=EDGE_CURVE ( 'NONE', #20099, #11885, #2254, .T. ) ;
#1630=ORIENTED_EDGE ( 'NONE', *, *, #16544, .T. ) ;
#1631=ORIENTED_EDGE ( 'NONE', *, *, #28355, .T. ) ;
#1633=EDGE_CURVE ( 'NONE', #21599, #9317, #25567, .T. ) ;
#1634=FACE_OUTER_BOUND ( 'NONE', #4278, .T. ) ;
#1635=LINE ( 'NONE', #26097, #10715 ) ;
#1636=CARTESIAN_POINT ( 'NONE',  ( 32.73300124599737160, -117.5726003567929610, 3.836798148478423265 ) ) ;
#1637=CARTESIAN_POINT ( 'NONE',  ( 28.37599760073042532, 55.80522390574119385, 100.2461467136612328 ) ) ;
#1638=CARTESIAN_POINT ( 'NONE',  ( 25.69398547355839924, 102.8740393624600955, -46.61500694509545184 ) ) ;
#1640=EDGE_LOOP ( 'NONE', ( #17197, #15813, #14446, #14411 ) ) ;
#1641=CARTESIAN_POINT ( 'NONE',  ( 1.832998868059890096, -29.64765804469973531, -142.0492247521725631 ) ) ;
#1642=CARTESIAN_POINT ( 'NONE',  ( 32.73300124599735739, 32.68291970228236920, 113.0038235389603472 ) ) ;
#1644=( NAMED_UNIT ( * ) SI_UNIT ( $, .STERADIAN. ) SOLID_ANGLE_UNIT ( ) );
#1645=CARTESIAN_POINT ( 'NONE',  ( 25.86096068574580897, 112.5344699600050404, -10.82483750674488832 ) ) ;
#1646=VERTEX_POINT ( 'NONE', #17185 ) ;
#1647=CARTESIAN_POINT ( 'NONE',  ( 25.64708010899962787, 91.31497827399827827, -66.41183455464044982 ) ) ;
#1648=EDGE_CURVE ( 'NONE', #10148, #21175, #1778, .T. ) ;
#1655=ORIENTED_EDGE ( 'NONE', *, *, #22704, .F. ) ;
#1656=ORIENTED_EDGE ( 'NONE', *, *, #19589, .F. ) ;
#1657=ADVANCED_FACE ( 'NONE', ( #14603 ), #1783, .F. ) ;
#1658=CARTESIAN_POINT ( 'NONE',  ( 55.49584447822657296, -42.86099773636581034, 58.53775398922241635 ) ) ;
#1659=ORIENTED_EDGE ( 'NONE', *, *, #13520, .T. ) ;
#1660=( BOUNDED_SURFACE ( )  B_SPLINE_SURFACE ( 3, 1, ( 
 ( #1910, #10566 ),
 ( #15135, #8412 ),
 ( #4216, #14728 ),
 ( #21361, #12998 ) ),
 .UNSPECIFIED., .F., .F., .F. ) 
 B_SPLINE_SURFACE_WITH_KNOTS ( ( 4, 4 ),
 ( 2, 2 ),
 ( 0.000000000000000000, 1.000000000000000000 ),
 ( 0.000000000000000000, 1.000000000000000000 ),
 .UNSPECIFIED. ) 
 GEOMETRIC_REPRESENTATION_ITEM ( )  RATIONAL_B_SPLINE_SURFACE ( (
 ( 1.000000000000000000, 1.000000000000000000),
 ( 0.9956975270656955868, 0.8568959468854907557),
 ( 0.9956975270656955868, 0.8568959468854907557),
 ( 1.000000000000000000, 1.000000000000000000) ) ) 
 REPRESENTATION_ITEM ( '' )  SURFACE ( )  );
#1662=CARTESIAN_POINT ( 'NONE',  ( 25.64681081121879203, 0.4157506337727869816, 112.9102952884414464 ) ) ;
#1663=CARTESIAN_POINT ( 'NONE',  ( 1.833206310202337930, 138.2356391007182879, 44.13245377365679190 ) ) ;
#1664=CARTESIAN_POINT ( 'NONE',  ( 109.1587776205901577, 0.006995903587858427232, -0.002185517590245281139 ) ) ;
#1665=LINE ( 'NONE', #10752, #19759 ) ;
#1667=LINE ( 'NONE', #19231, #10299 ) ;
#1668=FACE_OUTER_BOUND ( 'NONE', #27616, .T. ) ;
#1669=CARTESIAN_POINT ( 'NONE',  ( 32.73300124599732186, 0.000000000000000000, 0.000000000000000000 ) ) ;
#1671=ORIENTED_EDGE ( 'NONE', *, *, #23458, .F. ) ;
#1673=CARTESIAN_POINT ( 'NONE',  ( 2.433796855181233454, -46.34326152018648060, -137.9325382748289996 ) ) ;
#1674=B_SPLINE_CURVE_WITH_KNOTS ( 'NONE', 3,
 ( #17267, #10528, #2009, #17404, #26057, #15099, #3761, #25929, #19160, #23917 ),
 .UNSPECIFIED., .F., .F.,
 ( 4, 3, 3, 4 ),
 ( 1.040834085586084257E-17, 0.0002669560319015720925, 0.0005492286108966365748, 0.0008315040496093422957 ),
 .UNSPECIFIED. ) ;
#1675=CARTESIAN_POINT ( 'NONE',  ( 1.834118845439484335, -15.34511559672778347, 144.2964192726481372 ) ) ;
#1676=DIRECTION ( 'NONE',  ( 1.000000000000000000, 0.000000000000000000, 0.000000000000000000 ) ) ;
#1677=CARTESIAN_POINT ( 'NONE',  ( 32.73300124599735739, 55.46353551262010484, 103.7392577722178260 ) ) ;
#1679=EDGE_LOOP ( 'NONE', ( #25564, #11319, #22717, #13689 ) ) ;
#1681=CARTESIAN_POINT ( 'NONE',  ( 25.64681081121880624, -75.86069728268932977, -83.63051021305977883 ) ) ;
#1682=ORIENTED_EDGE ( 'NONE', *, *, #26728, .F. ) ;
#1684=CARTESIAN_POINT ( 'NONE',  ( 109.1586059443104944, -0.007001002073871752558, -0.001014167950280760828 ) ) ;
#1686=CARTESIAN_POINT ( 'NONE',  ( 25.64681081121879203, 107.2555980796241215, 35.28660243342585545 ) ) ;
#1687=CARTESIAN_POINT ( 'NONE',  ( 2.433796855181233454, -107.1581411821792216, 98.43889364293823974 ) ) ;
#1688=CARTESIAN_POINT ( 'NONE',  ( 25.64681081121879203, -91.59071981940525120, -66.03065707439029097 ) ) ;
#1691=B_SPLINE_CURVE_WITH_KNOTS ( 'NONE', 3,
 ( #26699, #8593, #19952, #6581, #17356, #15188, #9020, #24010 ),
 .UNSPECIFIED., .F., .F.,
 ( 4, 2, 2, 4 ),
 ( 0.000000000000000000, 0.0002429592666046731823, 0.0004859185332093463646, 0.0009718370664186793935 ),
 .UNSPECIFIED. ) ;
#1693=CARTESIAN_POINT ( 'NONE',  ( 13.36082413113061307, 25.56125765253451831, 150.7747251079862849 ) ) ;
#1695=CARTESIAN_POINT ( 'NONE',  ( 10.93730112725996229, -10.89264110824889364, -150.7858122213663989 ) ) ;
#1696=EDGE_CURVE ( 'NONE', #6748, #24062, #22902, .T. ) ;
#1699=ORIENTED_EDGE ( 'NONE', *, *, #12262, .F. ) ;
#1702=CARTESIAN_POINT ( 'NONE',  ( 1.832998868059890096, 30.69214149074206688, -141.8272129421605712 ) ) ;
#1704=CARTESIAN_POINT ( 'NONE',  ( 2.433796855181219243, 28.83182736670734059, -142.6247129145645829 ) ) ;
#1706=CARTESIAN_POINT ( 'NONE',  ( 25.64681081121879203, 75.24277141833607629, -84.18689316039970549 ) ) ;
#1707=CARTESIAN_POINT ( 'NONE',  ( 10.93730112725991077, -79.81734490845832397, -128.3908183996600201 ) ) ;
#1708=CARTESIAN_POINT ( 'NONE',  ( 109.1592201516379674, -0.007566779963325582538, -0.002134489919768117836 ) ) ;
#1709=CARTESIAN_POINT ( 'NONE',  ( 109.1624594426973118, -0.01531968460306872698, -0.004489871836309295566 ) ) ;
#1711=ORIENTED_EDGE ( 'NONE', *, *, #10237, .F. ) ;
#1713=ORIENTED_EDGE ( 'NONE', *, *, #16291, .F. ) ;
#1714=ORIENTED_EDGE ( 'NONE', *, *, #16181, .T. ) ;
#1715=DIRECTION ( 'NONE',  ( 0.5946245182733608248, -0.5994612328333251972, 0.5357871896547391488 ) ) ;
#1716=CARTESIAN_POINT ( 'NONE',  ( 2.063896406836609909, 144.6078654718901646, 13.84738934186238524 ) ) ;
#1717=CARTESIAN_POINT ( 'NONE',  ( 1.894214914920977266, -97.83100278581332532, -107.2270864706600122 ) ) ;
#1719=CARTESIAN_POINT ( 'NONE',  ( 28.37603512858447630, -84.05169593519779880, 78.09501335733563110 ) ) ;
#1720=DIRECTION ( 'NONE',  ( 0.5914120900931444380, -0.7333565075147354673, -0.3352908775637181149 ) ) ;
#1722=CARTESIAN_POINT ( 'NONE',  ( 32.73300124599739291, 89.94078864464164269, -75.82012867748392182 ) ) ;
#1724=CARTESIAN_POINT ( 'NONE',  ( 1.833838850093452599, 117.3962623502786187, -85.29338149487099940 ) ) ;
#1726=EDGE_CURVE ( 'NONE', #15408, #20144, #16349, .T. ) ;
#1727=DIRECTION ( 'NONE',  ( -0.5946245182733607137, -0.1700465163848142724, -0.7858154137795737570 ) ) ;
#1728=B_SPLINE_CURVE_WITH_KNOTS ( 'NONE', 3,
 ( #11036, #4406, #9021, #15472, #26287, #21834, #2231, #19798, #22264, #17911 ),
 .UNSPECIFIED., .F., .F.,
 ( 4, 3, 3, 4 ),
 ( 6.938893903907228378E-18, 0.0002669560319015785977, 0.0005492286108966380927, 0.0008315040496093435967 ),
 .UNSPECIFIED. ) ;
#1732=CARTESIAN_POINT ( 'NONE',  ( 25.64660436782539676, -97.49251393956821232, 56.95711784271951217 ) ) ;
#1733=ORIENTED_EDGE ( 'NONE', *, *, #7695, .T. ) ;
#1734=EDGE_LOOP ( 'NONE', ( #20934, #15080, #4778, #23923 ) ) ;
#1736=CARTESIAN_POINT ( 'NONE',  ( 25.64708010899964918, -110.4552579818683853, -23.42206246795119995 ) ) ;
#1737=CARTESIAN_POINT ( 'NONE',  ( 24.01988960052042898, -103.4492499592080463, -80.44223964539959582 ) ) ;
#1738=CARTESIAN_POINT ( 'NONE',  ( 1.833838848569416591, 29.99593366454950782, -141.9757689770218860 ) ) ;
#1740=CARTESIAN_POINT ( 'NONE',  ( 32.73300124599734318, 99.90245962373836619, 62.10906484417276374 ) ) ;
#1741=ORIENTED_EDGE ( 'NONE', *, *, #23367, .T. ) ;
#1744=CARTESIAN_POINT ( 'NONE',  ( 1.833485406944043827, 84.86072343962726450, -117.7091014914941809 ) ) ;
#1747=CARTESIAN_POINT ( 'NONE',  ( 1.833691583653536572, 97.36155720551622039, -107.5990239011816527 ) ) ;
#1748=CARTESIAN_POINT ( 'NONE',  ( 6.224689322667647851, 84.93872395423136368, -121.2721959030529462 ) ) ;
#1749=EDGE_CURVE ( 'NONE', #14867, #6575, #24262, .T. ) ;
#1752=CARTESIAN_POINT ( 'NONE',  ( -40.00000000000000000, 0.000000000000000000, -37.50000000000002132 ) ) ;
#1753=( BOUNDED_SURFACE ( )  B_SPLINE_SURFACE ( 3, 1, ( 
 ( #11437, #14806 ),
 ( #26030, #6321 ),
 ( #497, #12644 ),
 ( #12915, #1702 ) ),
 .UNSPECIFIED., .F., .F., .F. ) 
 B_SPLINE_SURFACE_WITH_KNOTS ( ( 4, 4 ),
 ( 2, 2 ),
 ( 0.000000000000000000, 1.000000000000000000 ),
 ( 0.000000000000000000, 1.000000000000000000 ),
 .UNSPECIFIED. ) 
 GEOMETRIC_REPRESENTATION_ITEM ( )  RATIONAL_B_SPLINE_SURFACE ( (
 ( 1.000000000000000000, 1.000000000000000000),
 ( 0.9960225298536222738, 0.9999952330161893110),
 ( 0.9960225298536222738, 0.9999952330161893110),
 ( 1.000000000000000000, 1.000000000000000000) ) ) 
 REPRESENTATION_ITEM ( '' )  SURFACE ( )  );
#1755=VECTOR ( 'NONE', #27643, 1000.000000000000114 ) ;
#1757=CARTESIAN_POINT ( 'NONE',  ( 25.81918753295377300, -24.41190151229177729, -110.3582118788979756 ) ) ;
#1758=ORIENTED_EDGE ( 'NONE', *, *, #17002, .T. ) ;
#1760=ORIENTED_EDGE ( 'NONE', *, *, #24696, .F. ) ;
#1761=ORIENTED_EDGE ( 'NONE', *, *, #25590, .T. ) ;
#1764=CARTESIAN_POINT ( 'NONE',  ( 1.833206308920072081, -73.19872517709806914, 125.2945011813203848 ) ) ;
#1766=CARTESIAN_POINT ( 'NONE',  ( 10.93730112726003156, 108.9902118373755684, -104.7670965581001781 ) ) ;
#1767=EDGE_CURVE ( 'NONE', #9334, #7451, #20526, .T. ) ;
#1768=CARTESIAN_POINT ( 'NONE',  ( 32.73300124599738581, 75.82012867748602503, -89.94078864463983791 ) ) ;
#1769=CARTESIAN_POINT ( 'NONE',  ( 30.59138290137884653, -66.10404757334126202, 95.58039132682505112 ) ) ;
#1771=CARTESIAN_POINT ( 'NONE',  ( 26.04756280548354042, 102.9366382251199497, -47.04636360340725076 ) ) ;
#1772=FACE_OUTER_BOUND ( 'NONE', #15985, .T. ) ;
#1773=CARTESIAN_POINT ( 'NONE',  ( 1.833485406944085350, 132.3460930279899515, -59.50871042846091541 ) ) ;
#1774=EDGE_CURVE ( 'NONE', #20441, #17039, #8864, .T. ) ;
#1778=LINE ( 'NONE', #18934, #2677 ) ;
#1780=CARTESIAN_POINT ( 'NONE',  ( 25.64681081121880624, -112.2483031020014295, 12.21581276189770904 ) ) ;
#1783=( BOUNDED_SURFACE ( )  B_SPLINE_SURFACE ( 3, 1, ( 
 ( #27852, #14743 ),
 ( #21229, #23406 ),
 ( #23699, #8277 ),
 ( #6263, #10444 ) ),
 .UNSPECIFIED., .F., .F., .F. ) 
 B_SPLINE_SURFACE_WITH_KNOTS ( ( 4, 4 ),
 ( 2, 2 ),
 ( 0.000000000000000000, 1.000000000000000000 ),
 ( 0.000000000000000000, 1.000000000000000000 ),
 .UNSPECIFIED. ) 
 GEOMETRIC_REPRESENTATION_ITEM ( )  RATIONAL_B_SPLINE_SURFACE ( (
 ( 1.000000000000000000, 1.000000000000000000),
 ( 0.6386103224230316178, 0.9954351624131538845),
 ( 0.6386103224230316178, 0.9954351624131538845),
 ( 1.000000000000000000, 1.000000000000000000) ) ) 
 REPRESENTATION_ITEM ( '' )  SURFACE ( )  );
#1789=CARTESIAN_POINT ( 'NONE',  ( 8.186469777910904355, -131.0413692044507172, -71.65198614410340383 ) ) ;
#1791=ORIENTED_EDGE ( 'NONE', *, *, #18888, .F. ) ;
#1792=CARTESIAN_POINT ( 'NONE',  ( 32.73300124599739291, 92.86301839380121237, -72.21147546950456331 ) ) ;
#1793=ORIENTED_EDGE ( 'NONE', *, *, #5865, .T. ) ;
#1794=CARTESIAN_POINT ( 'NONE',  ( 32.73300124599734318, 114.2056417606548706, 28.19767303745648945 ) ) ;
#1795=CARTESIAN_POINT ( 'NONE',  ( 13.84597867724971287, -90.05293531772709059, 115.8103190066270258 ) ) ;
#1796=ADVANCED_FACE ( 'NONE', ( #13144 ), #20366, .F. ) ;
#1797=FACE_OUTER_BOUND ( 'NONE', #5905, .T. ) ;
#1799=CARTESIAN_POINT ( 'NONE',  ( 109.1624594426973118, -0.004489871836309242657, 0.01531968460306874259 ) ) ;
#1800=CARTESIAN_POINT ( 'NONE',  ( 28.37599760073042532, -111.8383885143453256, -25.60640155549280550 ) ) ;
#1805=CARTESIAN_POINT ( 'NONE',  ( 25.65782528836479770, -102.9197507294672818, -46.45532072021288172 ) ) ;
#1806=EDGE_CURVE ( 'NONE', #4100, #22982, #26685, .T. ) ;
#1807=VERTEX_POINT ( 'NONE', #2779 ) ;
#1808=ORIENTED_EDGE ( 'NONE', *, *, #2764, .F. ) ;
#1809=CARTESIAN_POINT ( 'NONE',  ( 2.433796855181219243, -137.9325382748288291, 46.34326152018696376 ) ) ;
#1811=LINE ( 'NONE', #23439, #11618 ) ;
#1812=CARTESIAN_POINT ( 'NONE',  ( 1.833485406944043827, 45.34878176254236593, 137.8414413349087511 ) ) ;
#1814=CARTESIAN_POINT ( 'NONE',  ( 9.884929003653626367, 78.87917189084909353, 128.2151425008044328 ) ) ;
#1815=CARTESIAN_POINT ( 'NONE',  ( 55.79472521941428198, -37.00555938668216527, -62.63970324008300139 ) ) ;
#1817=ORIENTED_EDGE ( 'NONE', *, *, #25192, .F. ) ;
#1818=CARTESIAN_POINT ( 'NONE',  ( 25.64692232868535982, -112.2580042965358160, 12.12735788170774320 ) ) ;
#1820=DIRECTION ( 'NONE',  ( 0.000000000000000000, 0.000000000000000000, 1.000000000000000000 ) ) ;
#1821=CARTESIAN_POINT ( 'NONE',  ( 1.833603222531973387, 117.1340888386549750, 85.65285110156177950 ) ) ;
#1822=ORIENTED_EDGE ( 'NONE', *, *, #19278, .T. ) ;
#1823=CARTESIAN_POINT ( 'NONE',  ( 32.73300124599735739, -28.19767303745682341, 114.2056417606547285 ) ) ;
#1824=( BOUNDED_SURFACE ( )  B_SPLINE_SURFACE ( 3, 1, ( 
 ( #19112, #23304 ),
 ( #27750, #12754 ),
 ( #28013, #21686 ),
 ( #3702, #14500 ) ),
 .UNSPECIFIED., .F., .F., .F. ) 
 B_SPLINE_SURFACE_WITH_KNOTS ( ( 4, 4 ),
 ( 2, 2 ),
 ( 0.000000000000000000, 1.000000000000000000 ),
 ( 0.000000000000000000, 1.000000000000000000 ),
 .UNSPECIFIED. ) 
 GEOMETRIC_REPRESENTATION_ITEM ( )  RATIONAL_B_SPLINE_SURFACE ( (
 ( 1.000000000000000000, 1.000000000000000000),
 ( 0.9956975270656954757, 0.8568959468854893125),
 ( 0.9956975270656954757, 0.8568959468854893125),
 ( 1.000000000000000000, 1.000000000000000000) ) ) 
 REPRESENTATION_ITEM ( '' )  SURFACE ( )  );
#1825=CARTESIAN_POINT ( 'NONE',  ( 6.224689322667630975, -148.0369967195762513, -2.565137105445306709 ) ) ;
#1827=ORIENTED_EDGE ( 'NONE', *, *, #3412, .F. ) ;
#1828=DIRECTION ( 'NONE',  ( 0.000000000000000000, -1.000000000000000000, 0.000000000000000000 ) ) ;
#1829=ORIENTED_EDGE ( 'NONE', *, *, #16621, .F. ) ;
#1831=CARTESIAN_POINT ( 'NONE',  ( 26.11404676487257603, 92.25884714080409310, 65.63269960453273200 ) ) ;
#1832=DIRECTION ( 'NONE',  ( -1.000000000000000000, -0.000000000000000000, -0.000000000000000000 ) ) ;
#1833=CARTESIAN_POINT ( 'NONE',  ( 2.433796855181219243, -116.8607839509062671, 86.69855925933937613 ) ) ;
#1834=( BOUNDED_SURFACE ( )  B_SPLINE_SURFACE ( 3, 1, ( 
 ( #4226, #10724 ),
 ( #1920, #22071 ),
 ( #13009, #11282 ),
 ( #15017, #24392 ) ),
 .UNSPECIFIED., .F., .F., .F. ) 
 B_SPLINE_SURFACE_WITH_KNOTS ( ( 4, 4 ),
 ( 2, 2 ),
 ( 0.000000000000000000, 1.000000000000000000 ),
 ( 0.000000000000000000, 1.000000000000000000 ),
 .UNSPECIFIED. ) 
 GEOMETRIC_REPRESENTATION_ITEM ( )  RATIONAL_B_SPLINE_SURFACE ( (
 ( 1.000000000000000000, 1.000000000000000000),
 ( 0.6386103224230302855, 0.9954351624131538845),
 ( 0.6386103224230302855, 0.9954351624131538845),
 ( 1.000000000000000000, 1.000000000000000000) ) ) 
 REPRESENTATION_ITEM ( '' )  SURFACE ( )  );
#1839=DIRECTION ( 'NONE',  ( 0.000000000000000000, 0.000000000000000000, 1.000000000000000000 ) ) ;
#1841=CARTESIAN_POINT ( 'NONE',  ( 1.831572820252009626, 45.77972211429817406, 137.7011124121618764 ) ) ;
#1843=CARTESIAN_POINT ( 'NONE',  ( 25.81918753295378011, -46.82320532096449739, -102.8711004511197729 ) ) ;
#1848=ORIENTED_EDGE ( 'NONE', *, *, #16071, .T. ) ;
#1849=AXIS2_PLACEMENT_3D ( 'NONE', #14685, #5485, #12524 ) ;
#1851=CARTESIAN_POINT ( 'NONE',  ( 16.05277956358205316, -128.9466020665978760, 62.52511797226075174 ) ) ;
#1852=CARTESIAN_POINT ( 'NONE',  ( 109.1592201516379674, 0.003476928926134712113, 0.007051465909552774060 ) ) ;
#1856=CARTESIAN_POINT ( 'NONE',  ( 28.37644542392831681, 65.64862111872214712, -105.5967537682337394 ) ) ;
#1859=CARTESIAN_POINT ( 'NONE',  ( 10.93730112725969938, 56.95489579269752767, 140.0398180619111770 ) ) ;
#1864=CARTESIAN_POINT ( 'NONE',  ( 119.2224693531408803, -90.00000000000005684, -20.00000000000001066 ) ) ;
#1867=CARTESIAN_POINT ( 'NONE',  ( 25.64681081121879203, 112.2483031020015147, -12.21581276189692211 ) ) ;
#1868=VERTEX_POINT ( 'NONE', #9991 ) ;
#1870=ORIENTED_EDGE ( 'NONE', *, *, #23849, .T. ) ;
#1871=ORIENTED_EDGE ( 'NONE', *, *, #18220, .F. ) ;
#1873=B_SPLINE_CURVE_WITH_KNOTS ( 'NONE', 3,
 ( #1722, #14401, #23212, #8095, #16864, #3752, #4029 ),
 .UNSPECIFIED., .F., .F.,
 ( 4, 3, 4 ),
 ( 0.000000000000000000, 0.02398743853561338332, 0.04000277880656218782 ),
 .UNSPECIFIED. ) ;
#1874=CIRCLE ( 'NONE', #17479, 151.1787379149930359 ) ;
#1875=CARTESIAN_POINT ( 'NONE',  ( 55.49584447822657296, -22.67407039687288872, 68.91748907713581218 ) ) ;
#1877=( BOUNDED_SURFACE ( )  B_SPLINE_SURFACE ( 3, 1, ( 
 ( #28336, #26187 ),
 ( #6480, #4312 ),
 ( #24184, #21875 ),
 ( #2269, #2131 ) ),
 .UNSPECIFIED., .F., .F., .F. ) 
 B_SPLINE_SURFACE_WITH_KNOTS ( ( 4, 4 ),
 ( 2, 2 ),
 ( 0.000000000000000000, 1.000000000000000000 ),
 ( 0.000000000000000000, 1.000000000000000000 ),
 .UNSPECIFIED. ) 
 GEOMETRIC_REPRESENTATION_ITEM ( )  RATIONAL_B_SPLINE_SURFACE ( (
 ( 1.000000000000000000, 1.000000000000000000),
 ( 0.6386103224230302855, 0.9954351624131538845),
 ( 0.6386103224230302855, 0.9954351624131538845),
 ( 1.000000000000000000, 1.000000000000000000) ) ) 
 REPRESENTATION_ITEM ( '' )  SURFACE ( )  );
#1880=ADVANCED_FACE ( 'NONE', ( #3209 ), #15745, .F. ) ;
#1881=CARTESIAN_POINT ( 'NONE',  ( 32.73300124599738581, 75.82012867748602503, -89.94078864463983791 ) ) ;
#1882=ORIENTED_EDGE ( 'NONE', *, *, #17781, .F. ) ;
#1884=CARTESIAN_POINT ( 'NONE',  ( 1.833750490713743853, 59.26520711750040249, -132.4555075118561547 ) ) ;
#1885=EDGE_CURVE ( 'NONE', #10927, #1116, #8216, .T. ) ;
#1886=CARTESIAN_POINT ( 'NONE',  ( 25.64692872815573921, 56.17679456083801881, 97.94438212068848770 ) ) ;
#1887=CARTESIAN_POINT ( 'NONE',  ( 1.893872463202044054, -138.3372034345894690, 43.94661640105973532 ) ) ;
#1889=VECTOR ( 'NONE', #17665, 1000.000000000000000 ) ;
#1890=CIRCLE ( 'NONE', #9712, 151.1787379149930359 ) ;
#1892=CARTESIAN_POINT ( 'NONE',  ( 55.49584447822657296, -22.67407039687194015, -68.91748907713612482 ) ) ;
#1893=B_SPLINE_CURVE_WITH_KNOTS ( 'NONE', 3,
 ( #6727, #21551, #10902, #6866, #4409, #26562, #6588, #19389, #8735, #15473 ),
 .UNSPECIFIED., .F., .F.,
 ( 4, 3, 3, 4 ),
 ( 1.040834085586084257E-17, 0.0002669560319015743151, 0.0005492286108966349485, 0.0008315040496093406694 ),
 .UNSPECIFIED. ) ;
#1894=CARTESIAN_POINT ( 'NONE',  ( 2.063896406836609909, 73.79559738457753326, 125.1295119249441683 ) ) ;
#1895=CARTESIAN_POINT ( 'NONE',  ( 109.1592201516379674, -0.002913740842103232798, 0.007302213399787543455 ) ) ;
#1896=VERTEX_POINT ( 'NONE', #18613 ) ;
#1897=AXIS2_PLACEMENT_3D ( 'NONE', #14466, #3955, #10029 ) ;
#1902=ADVANCED_FACE ( 'NONE', ( #628 ), #21467, .F. ) ;
#1905=EDGE_CURVE ( 'NONE', #20917, #20493, #3359, .T. ) ;
#1906=CARTESIAN_POINT ( 'NONE',  ( 1.894214914920991921, -145.1469726764544532, 0.9536781033354796433 ) ) ;
#1908=EDGE_CURVE ( 'NONE', #25971, #27431, #21556, .T. ) ;
#1910=CARTESIAN_POINT ( 'NONE',  ( 109.1586900883932856, -0.006479576224403807948, -0.002995460350180787282 ) ) ;
#1913=( BOUNDED_SURFACE ( )  B_SPLINE_SURFACE ( 3, 1, ( 
 ( #2922, #11838 ),
 ( #11699, #18157 ),
 ( #16147, #892 ),
 ( #5212, #24951 ) ),
 .UNSPECIFIED., .F., .F., .F. ) 
 B_SPLINE_SURFACE_WITH_KNOTS ( ( 4, 4 ),
 ( 2, 2 ),
 ( 0.000000000000000000, 1.000000000000000000 ),
 ( 0.000000000000000000, 1.000000000000000000 ),
 .UNSPECIFIED. ) 
 GEOMETRIC_REPRESENTATION_ITEM ( )  RATIONAL_B_SPLINE_SURFACE ( (
 ( 1.000000000000000000, 1.000000000000000000),
 ( 0.9956975270656955868, 0.8568959468854907557),
 ( 0.9956975270656955868, 0.8568959468854907557),
 ( 1.000000000000000000, 1.000000000000000000) ) ) 
 REPRESENTATION_ITEM ( '' )  SURFACE ( )  );
#1914=DIRECTION ( 'NONE',  ( 0.000000000000000000, 0.000000000000000000, 1.000000000000000000 ) ) ;
#1917=CARTESIAN_POINT ( 'NONE',  ( 32.73300124599741423, 117.3295799645430435, -8.473903470904879498 ) ) ;
#1918=CARTESIAN_POINT ( 'NONE',  ( 10.93730112725970827, 42.00474393596263667, 145.2260730187401236 ) ) ;
#1919=CARTESIAN_POINT ( 'NONE',  ( 26.04756280548354397, 22.44333019059152079, -110.9306483680200301 ) ) ;
#1920=CARTESIAN_POINT ( 'NONE',  ( 109.1624594426973118, 0.01405141589344814472, 0.007576898892907140901 ) ) ;
#1922=ORIENTED_EDGE ( 'NONE', *, *, #22807, .F. ) ;
#1923=CARTESIAN_POINT ( 'NONE',  ( 25.64681081121879203, 97.99105938548001404, -56.09509703373240797 ) ) ;
#1926=VECTOR ( 'NONE', #17137, 1000.000000000000341 ) ;
#1928=ORIENTED_EDGE ( 'NONE', *, *, #23656, .T. ) ;
#1932=EDGE_CURVE ( 'NONE', #27476, #19810, #14132, .T. ) ;
#1933=CARTESIAN_POINT ( 'NONE',  ( 25.86096068574579832, 107.2082119295153149, 35.88291140783953637 ) ) ;
#1937=EDGE_CURVE ( 'NONE', #21184, #14114, #9893, .T. ) ;
#1939=EDGE_LOOP ( 'NONE', ( #21151, #2756, #7592, #26841 ) ) ;
#1941=CARTESIAN_POINT ( 'NONE',  ( 109.1624594426973118, -0.01476644236456993789, -0.006066618937910856803 ) ) ;
#1942=CARTESIAN_POINT ( 'NONE',  ( 6.224689322667630975, -129.4863684118292326, 71.79702446228257884 ) ) ;
#1944=CARTESIAN_POINT ( 'NONE',  ( 109.1721716018069515, 0.008358834333178081361, 0.01488186354165287398 ) ) ;
#1945=CARTESIAN_POINT ( 'NONE',  ( 25.70243777736188306, 55.83795591307134742, 98.18050844655094522 ) ) ;
#1946=CARTESIAN_POINT ( 'NONE',  ( 24.01988960052066346, -9.440825210282529412, -130.7041393974934635 ) ) ;
#1947=CIRCLE ( 'NONE', #3344, 117.6351876552689504 ) ;
#1948=CARTESIAN_POINT ( 'NONE',  ( 2.433796855181205476, -98.43889364293931976, 107.1581411821782268 ) ) ;
#1949=CARTESIAN_POINT ( 'NONE',  ( 2.430230287190581429, -31.67257033707599589, 142.0258656395020864 ) ) ;
#1950=CARTESIAN_POINT ( 'NONE',  ( 25.64681081121880624, -112.2483031020014295, 12.21581276189770904 ) ) ;
#1951=VECTOR ( 'NONE', #21579, 1000.000000000000227 ) ;
#1953=ORIENTED_EDGE ( 'NONE', *, *, #9934, .T. ) ;
#1954=CARTESIAN_POINT ( 'NONE',  ( 2.433796855181205476, -13.76554153471595043, -144.8571464219890572 ) ) ;
#1955=CARTESIAN_POINT ( 'NONE',  ( 1.833838848569429469, -72.40075357737740092, 125.7577269771229851 ) ) ;
#1957=CARTESIAN_POINT ( 'NONE',  ( 16.05277956358223435, 19.61822947416006357, 141.9568301782832975 ) ) ;
#1959=CARTESIAN_POINT ( 'NONE',  ( 2.108393763691202683, 84.36147263237569405, 118.2927144690661692 ) ) ;
#1960=EDGE_CURVE ( 'NONE', #13141, #17999, #5816, .T. ) ;
#1964=FACE_OUTER_BOUND ( 'NONE', #20797, .T. ) ;
#1965=FACE_OUTER_BOUND ( 'NONE', #24649, .T. ) ;
#1967=EDGE_LOOP ( 'NONE', ( #3766, #28122, #10032, #6877 ) ) ;
#1969=CARTESIAN_POINT ( 'NONE',  ( 6.224689322667630975, -136.2818611715194663, 57.86870174583380333 ) ) ;
#1971=EDGE_CURVE ( 'NONE', #26248, #15804, #14000, .T. ) ;
#1974=CARTESIAN_POINT ( 'NONE',  ( 24.01988960052063504, -84.46375358746846018, -100.1926921796492280 ) ) ;
#1975=AXIS2_PLACEMENT_3D ( 'NONE', #8904, #21713, #1984 ) ;
#1979=CARTESIAN_POINT ( 'NONE',  ( 1.833206310202332379, 108.3342540861879257, 96.54250248081029895 ) ) ;
#1980=CARTESIAN_POINT ( 'NONE',  ( 1.894214914920994586, -71.74757687370546932, 126.1778046718833082 ) ) ;
#1981=CARTESIAN_POINT ( 'NONE',  ( 32.73300124599732186, 0.000000000000000000, 0.000000000000000000 ) ) ;
#1983=CARTESIAN_POINT ( 'NONE',  ( 55.79472521941428198, 0.7279028900793619306, 72.75035398477136539 ) ) ;
#1984=DIRECTION ( 'NONE',  ( 0.000000000000000000, 0.000000000000000000, 1.000000000000000000 ) ) ;
#1985=CARTESIAN_POINT ( 'NONE',  ( 25.64692232868534560, 23.79507962493625328, 110.3753891203787134 ) ) ;
#1986=FACE_BOUND ( 'NONE', #22565, .T. ) ;
#1988=FACE_OUTER_BOUND ( 'NONE', #11900, .T. ) ;
#1989=AXIS2_PLACEMENT_3D ( 'NONE', #20453, #15990, #3186 ) ;
#1991=DIRECTION ( 'NONE',  ( 0.000000000000000000, -6.938893903907228378E-16, -1.000000000000000000 ) ) ;
#1992=CARTESIAN_POINT ( 'NONE',  ( 30.59138290137868665, 115.8270707793589054, 9.457588828075607523 ) ) ;
#1993=VERTEX_POINT ( 'NONE', #21338 ) ;
#2000=CARTESIAN_POINT ( 'NONE',  ( 13.84597867724958853, 77.45414123936396322, -124.5889929031781520 ) ) ;
#2001=CARTESIAN_POINT ( 'NONE',  ( 32.73300124599736449, -117.3295799645430435, 8.473903470905730373 ) ) ;
#2002=ORIENTED_EDGE ( 'NONE', *, *, #26446, .T. ) ;
#2004=CARTESIAN_POINT ( 'NONE',  ( 28.37599760073043242, 91.75439000741693008, 68.88138253892428509 ) ) ;
#2005=CARTESIAN_POINT ( 'NONE',  ( 109.1592201516379674, 0.006044422199831473233, 0.005027640251764405217 ) ) ;
#2007=ADVANCED_FACE ( 'NONE', ( #12553 ), #21629, .F. ) ;
#2009=CARTESIAN_POINT ( 'NONE',  ( 25.64699802086725455, -112.3172869996024588, -11.56593161917429846 ) ) ;
#2011=ORIENTED_EDGE ( 'NONE', *, *, #8618, .F. ) ;
#2012=ADVANCED_FACE ( 'NONE', ( #6626 ), #15558, .F. ) ;
#2014=ORIENTED_EDGE ( 'NONE', *, *, #11773, .T. ) ;
#2016=ADVANCED_FACE ( 'NONE', ( #18245 ), #24600, .F. ) ;
#2017=CARTESIAN_POINT ( 'NONE',  ( 1.832998868059858122, 96.70023740551269498, -108.1944082009147508 ) ) ;
#2018=CARTESIAN_POINT ( 'NONE',  ( 26.11404676487257603, 57.58742681967449784, 97.48350837663630841 ) ) ;
#2019=CARTESIAN_POINT ( 'NONE',  ( 1.833750490713712322, 72.32354185792559065, 125.8019536335922339 ) ) ;
#2023=EDGE_LOOP ( 'NONE', ( #1520, #20808, #18081, #14758 ) ) ;
#2025=DIRECTION ( 'NONE',  ( 0.000000000000000000, 0.000000000000000000, 1.000000000000000000 ) ) ;
#2032=CARTESIAN_POINT ( 'NONE',  ( 25.81918753295377300, -0.9336804662319195813, -113.0221398901142180 ) ) ;
#2033=ORIENTED_EDGE ( 'NONE', *, *, #26992, .T. ) ;
#2034=ORIENTED_EDGE ( 'NONE', *, *, #24362, .T. ) ;
#2035=CARTESIAN_POINT ( 'NONE',  ( 1.832998868059890096, -142.0492247521724494, 29.64765804470029664 ) ) ;
#2039=VERTEX_POINT ( 'NONE', #412 ) ;
#2040=ORIENTED_EDGE ( 'NONE', *, *, #20635, .F. ) ;
#2041=( BOUNDED_SURFACE ( )  B_SPLINE_SURFACE ( 3, 1, ( 
 ( #12791, #27916 ),
 ( #19420, #8087 ),
 ( #12243, #21301 ),
 ( #12373, #23343 ) ),
 .UNSPECIFIED., .F., .F., .F. ) 
 B_SPLINE_SURFACE_WITH_KNOTS ( ( 4, 4 ),
 ( 2, 2 ),
 ( 0.000000000000000000, 1.000000000000000000 ),
 ( 0.000000000000000000, 1.000000000000000000 ),
 .UNSPECIFIED. ) 
 GEOMETRIC_REPRESENTATION_ITEM ( )  RATIONAL_B_SPLINE_SURFACE ( (
 ( 1.000000000000000000, 1.000000000000000000),
 ( 0.9960225298536222738, 0.9999952330161893110),
 ( 0.9960225298536222738, 0.9999952330161893110),
 ( 1.000000000000000000, 1.000000000000000000) ) ) 
 REPRESENTATION_ITEM ( '' )  SURFACE ( )  );
#2043=ADVANCED_FACE ( 'NONE', ( #26602 ), #27516, .F. ) ;
#2044=CARTESIAN_POINT ( 'NONE',  ( 1.833838850855486369, 137.9800888515323152, 44.92600961247709535 ) ) ;
#2045=CARTESIAN_POINT ( 'NONE',  ( 109.1586900883932856, -0.0008465529156546283815, 0.007088091345232576390 ) ) ;
#2046=B_SPLINE_CURVE_WITH_KNOTS ( 'NONE', 3,
 ( #25557, #23398, #27975, #5975 ),
 .UNSPECIFIED., .F., .F.,
 ( 4, 4 ),
 ( 0.000000000000000000, 0.01077107196513895325 ),
 .UNSPECIFIED. ) ;
#2048=DIRECTION ( 'NONE',  ( -0.7071067811865485719, 0.000000000000000000, -0.7071067811865465735 ) ) ;
#2049=LINE ( 'NONE', #16905, #26727 ) ;
#2051=CARTESIAN_POINT ( 'NONE',  ( 13.36082413113061307, 148.1362653801002978, 37.97423473099346580 ) ) ;
#2052=CARTESIAN_POINT ( 'NONE',  ( 1.832998868059858122, -59.50898020732424953, -132.3466930259799597 ) ) ;
#2053=VERTEX_POINT ( 'NONE', #15656 ) ;
#2058=DIRECTION ( 'NONE',  ( 0.000000000000000000, 0.000000000000000000, 1.000000000000000000 ) ) ;
#2059=CARTESIAN_POINT ( 'NONE',  ( 2.430230287190572103, 133.5180086894999363, -57.85706160874012483 ) ) ;
#2060=CARTESIAN_POINT ( 'NONE',  ( 26.11404676487257603, 107.3263591096430218, 36.06104232266487486 ) ) ;
#2065=VERTEX_POINT ( 'NONE', #24762 ) ;
#2068=CARTESIAN_POINT ( 'NONE',  ( 25.70243777736189728, 107.1912711514954850, 35.59945151684112830 ) ) ;
#2069=ORIENTED_EDGE ( 'NONE', *, *, #12705, .F. ) ;
#2070=CARTESIAN_POINT ( 'NONE',  ( 2.108393763691202238, -125.1820217068190857, -73.75286979200589599 ) ) ;
#2071=CIRCLE ( 'NONE', #22344, 151.1787379149930359 ) ;
#2072=ORIENTED_EDGE ( 'NONE', *, *, #22683, .T. ) ;
#2074=CARTESIAN_POINT ( 'NONE',  ( 6.224689322667630975, -18.02516478984242809, 146.9579047224769113 ) ) ;
#2075=CARTESIAN_POINT ( 'NONE',  ( 109.1592201516379674, -0.001934867487021774525, -0.007620268632971101234 ) ) ;
#2076=CARTESIAN_POINT ( 'NONE',  ( 1.832998868059858122, 14.63705790014199692, -144.3700883710215521 ) ) ;
#2077=CARTESIAN_POINT ( 'NONE',  ( 55.79472521941428198, 72.27573336313963637, -8.328398066091017071 ) ) ;
#2078=CARTESIAN_POINT ( 'NONE',  ( 55.49584447822657296, 36.50733923851286278, -62.69727227546362514 ) ) ;
#2079=LINE ( 'NONE', #23725, #3685 ) ;
#2084=CARTESIAN_POINT ( 'NONE',  ( 109.1592201516379674, 0.004867031887019543715, 0.006174480289199423509 ) ) ;
#2086=DIRECTION ( 'NONE',  ( -0.000000000000000000, 1.000000000000000000, -0.000000000000000000 ) ) ;
#2088=EDGE_LOOP ( 'NONE', ( #25991, #17783, #19091, #7467 ) ) ;
#2089=CARTESIAN_POINT ( 'NONE',  ( 5.340103556456540446, -13.12023871801021180, -146.8647350107030718 ) ) ;
#2090=CARTESIAN_POINT ( 'NONE',  ( 109.1592201516379674, 0.0005146241775982810093, 0.007845213074654433863 ) ) ;
#2093=CARTESIAN_POINT ( 'NONE',  ( 26.11404676487257603, 97.48350837663606683, 57.58742681967482469 ) ) ;
#2095=ADVANCED_FACE ( 'NONE', ( #15954 ), #28259, .F. ) ;
#2099=EDGE_CURVE ( 'NONE', #342, #23477, #6369, .T. ) ;
#2100=CARTESIAN_POINT ( 'NONE',  ( 25.86096068574579476, -92.04529103340814800, 65.64181925268293583 ) ) ;
#2102=ORIENTED_EDGE ( 'NONE', *, *, #21324, .F. ) ;
#2103=ADVANCED_FACE ( 'NONE', ( #1409 ), #18552, .F. ) ;
#2106=DIRECTION ( 'NONE',  ( 0.000000000000000000, 0.000000000000000000, 1.000000000000000000 ) ) ;
#2107=CARTESIAN_POINT ( 'NONE',  ( 25.87036335909426299, 65.65170964736253723, -92.04585932622704547 ) ) ;
#2112=CARTESIAN_POINT ( 'NONE',  ( 1.833485406944043827, 142.0485807715649571, -29.64752363041402816 ) ) ;
#2113=CARTESIAN_POINT ( 'NONE',  ( 109.1778270068192853, 0.008236503545664811132, -0.004349865064712430361 ) ) ;
#2116=CARTESIAN_POINT ( 'NONE',  ( 109.1587776205901577, 8.330235397644728467E-05, -0.007328861771496577443 ) ) ;
#2117=FACE_OUTER_BOUND ( 'NONE', #27397, .T. ) ;
#2118=CARTESIAN_POINT ( 'NONE',  ( 10.93730112725978287, -125.1380233598484182, 84.82621002473399585 ) ) ;
#2120=VERTEX_POINT ( 'NONE', #12490 ) ;
#2121=EDGE_CURVE ( 'NONE', #1001, #14400, #21914, .T. ) ;
#2122=ORIENTED_EDGE ( 'NONE', *, *, #2933, .T. ) ;
#2125=CARTESIAN_POINT ( 'NONE',  ( 13.36082413113063083, -147.2768864064165086, -41.18148072373763569 ) ) ;
#2126=CARTESIAN_POINT ( 'NONE',  ( 1.833603222531973165, 72.93978951866159832, -125.4455769441935047 ) ) ;
#2129=ORIENTED_EDGE ( 'NONE', *, *, #3415, .F. ) ;
#2130=CARTESIAN_POINT ( 'NONE',  ( 28.37599760073042887, 113.9023239246302808, 13.77583212279370350 ) ) ;
#2131=CARTESIAN_POINT ( 'NONE',  ( 13.36082413113061307, 56.35051087434963080, 142.1654513177089996 ) ) ;
#2132=CARTESIAN_POINT ( 'NONE',  ( 25.64681081121880624, 23.06870491922473931, -110.5293738517606243 ) ) ;
#2134=EDGE_CURVE ( 'NONE', #21234, #11951, #11610, .T. ) ;
#2135=B_SPLINE_CURVE_WITH_KNOTS ( 'NONE', 3,
 ( #14058, #6163, #28281, #21530 ),
 .UNSPECIFIED., .F., .F.,
 ( 4, 4 ),
 ( 0.000000000000000000, 0.008383560773332719013 ),
 .UNSPECIFIED. ) ;
#2138=ORIENTED_EDGE ( 'NONE', *, *, #2285, .T. ) ;
#2140=ORIENTED_EDGE ( 'NONE', *, *, #27157, .T. ) ;
#2141=ORIENTED_EDGE ( 'NONE', *, *, #20467, .F. ) ;
#2142=EDGE_LOOP ( 'NONE', ( #9932, #6346, #22327, #5320 ) ) ;
#2143=CARTESIAN_POINT ( 'NONE',  ( 26.11404676487259024, 24.64483677385001315, -110.5078194225158654 ) ) ;
#2146=B_SPLINE_CURVE_WITH_KNOTS ( 'NONE', 3,
 ( #12838, #314, #11123, #10982, #15557, #2044, #15130, #33, #24524, #15706 ),
 .UNSPECIFIED., .F., .F.,
 ( 4, 3, 3, 4 ),
 ( 2.775557561562891351E-17, 0.0002669559177086200147, 0.0005339118354151127163, 0.001067817517169171622 ),
 .UNSPECIFIED. ) ;
#2147=ORIENTED_EDGE ( 'NONE', *, *, #6401, .T. ) ;
#2148=CARTESIAN_POINT ( 'NONE',  ( 1.833485406944043827, 73.01664920992966756, 125.4007332306548221 ) ) ;
#2151=EDGE_CURVE ( 'NONE', #19236, #27960, #23321, .T. ) ;
#2152=CARTESIAN_POINT ( 'NONE',  ( 26.11404676487257603, 92.25884714080409310, 65.63269960453273200 ) ) ;
#2153=ORIENTED_EDGE ( 'NONE', *, *, #19990, .F. ) ;
#2154=CARTESIAN_POINT ( 'NONE',  ( 2.108985857320916146, 126.4634971826984469, 71.53406810961526219 ) ) ;
#2156=B_SPLINE_CURVE_WITH_KNOTS ( 'NONE', 3,
 ( #15816, #22448, #13935, #20266, #4877, #15953, #24623, #13789, #27019, #15655 ),
 .UNSPECIFIED., .F., .F.,
 ( 4, 3, 3, 4 ),
 ( 3.393552799879628878E-17, 0.0002669559177086209363, 0.0005339118354151020911, 0.001067817517169162515 ),
 .UNSPECIFIED. ) ;
#2157=CARTESIAN_POINT ( 'NONE',  ( 2.263178113027050742, -1.401567040889206917, 145.3892419963351017 ) ) ;
#2158=DIRECTION ( 'NONE',  ( 0.5914120900931444380, 0.6476200150380150289, 0.4804373588864832567 ) ) ;
#2161=FACE_OUTER_BOUND ( 'NONE', #13939, .T. ) ;
#2163=CARTESIAN_POINT ( 'NONE',  ( 55.49584447822657296, -0.2676470673951589219, -72.55110015779771970 ) ) ;
#2164=FACE_OUTER_BOUND ( 'NONE', #24804, .T. ) ;
#2165=ADVANCED_FACE ( 'NONE', ( #25049 ), #9704, .F. ) ;
#2167=ORIENTED_EDGE ( 'NONE', *, *, #10704, .T. ) ;
#2169=CARTESIAN_POINT ( 'NONE',  ( 30.58324630866341209, 33.60235057864129260, -116.1819705588610105 ) ) ;
#2170=ORIENTED_EDGE ( 'NONE', *, *, #26446, .F. ) ;
#2171=ORIENTED_EDGE ( 'NONE', *, *, #20137, .T. ) ;
#2172=ORIENTED_EDGE ( 'NONE', *, *, #6808, .T. ) ;
#2173=LINE ( 'NONE', #8967, #137 ) ;
#2174=DIRECTION ( 'NONE',  ( 0.000000000000000000, 0.000000000000000000, -1.000000000000000000 ) ) ;
#2175=CARTESIAN_POINT ( 'NONE',  ( 2.108985857320901491, -144.3577886602087119, 16.46110181986639986 ) ) ;
#2176=CARTESIAN_POINT ( 'NONE',  ( 55.49584447822657296, 58.85239198729244947, -42.42793568432897189 ) ) ;
#2178=CARTESIAN_POINT ( 'NONE',  ( 109.1586900883932856, 0.006561743627143330412, -0.002810909342011619870 ) ) ;
#2180=CARTESIAN_POINT ( 'NONE',  ( 2.433796855181219243, -132.3327394885235435, 60.50726454507858421 ) ) ;
#2181=ADVANCED_FACE ( 'NONE', ( #14362 ), #4741, .F. ) ;
#2182=DIRECTION ( 'NONE',  ( 0.5914120900931444380, 0.7333565075147332468, 0.3352908775637229444 ) ) ;
#2183=CARTESIAN_POINT ( 'NONE',  ( 25.64660436782557440, -65.89729635302973065, 91.68669413043116379 ) ) ;
#2186=EDGE_CURVE ( 'NONE', #21439, #4100, #15730, .T. ) ;
#2187=ORIENTED_EDGE ( 'NONE', *, *, #15179, .T. ) ;
#2190=CARTESIAN_POINT ( 'NONE',  ( 109.1624594426973260, 0.002863932759303830771, 0.01570508117119675390 ) ) ;
#2191=CARTESIAN_POINT ( 'NONE',  ( 1.833838850093439943, -144.3148369740567603, -15.16809710532209721 ) ) ;
#2195=DIRECTION ( 'NONE',  ( 0.000000000000000000, 0.000000000000000000, 1.000000000000000000 ) ) ;
#2196=ORIENTED_EDGE ( 'NONE', *, *, #7772, .T. ) ;
#2197=CARTESIAN_POINT ( 'NONE',  ( 25.64699802086724034, 97.66487797954091832, -56.66140964017631632 ) ) ;
#2198=DIRECTION ( 'NONE',  ( 0.000000000000000000, 0.000000000000000000, 1.000000000000000000 ) ) ;
#2202=ORIENTED_EDGE ( 'NONE', *, *, #1466, .T. ) ;
#2203=CARTESIAN_POINT ( 'NONE',  ( 5.340103579038255610, -128.8311297206837480, -71.72120379026158332 ) ) ;
#2206=ORIENTED_EDGE ( 'NONE', *, *, #3536, .F. ) ;
#2207=B_SPLINE_CURVE_WITH_KNOTS ( 'NONE', 3,
 ( #22732, #5432, #13922, #7464, #20401, #20544, #826 ),
 .UNSPECIFIED., .F., .F.,
 ( 4, 3, 4 ),
 ( 0.000000000000000000, 0.02398743853561317169, 0.04000277880656214619 ),
 .UNSPECIFIED. ) ;
#2209=AXIS2_PLACEMENT_3D ( 'NONE', #2489, #21800, #2195 ) ;
#2210=ORIENTED_EDGE ( 'NONE', *, *, #21590, .T. ) ;
#2213=FACE_OUTER_BOUND ( 'NONE', #12790, .T. ) ;
#2216=CARTESIAN_POINT ( 'NONE',  ( 25.65782528836479770, 55.95807498711486971, 98.07785559018897459 ) ) ;
#2217=CARTESIAN_POINT ( 'NONE',  ( 13.84597867724975373, -4.782757490006857459, 146.6243035057531472 ) ) ;
#2218=ADVANCED_FACE ( 'NONE', ( #23601 ), #16949, .T. ) ;
#2219=CARTESIAN_POINT ( 'NONE',  ( 26.11404676487259024, 103.8885755249569485, 45.01677474591446781 ) ) ;
#2220=CARTESIAN_POINT ( 'NONE',  ( 25.64681081121879203, -11.38886654529750331, 112.3352186517030447 ) ) ;
#2222=EDGE_CURVE ( 'NONE', #19171, #20839, #16953, .T. ) ;
#2223=ORIENTED_EDGE ( 'NONE', *, *, #12506, .T. ) ;
#2229=CARTESIAN_POINT ( 'NONE',  ( 13.84597867724972708, 144.4146018799366118, -25.80666409311425369 ) ) ;
#2231=CARTESIAN_POINT ( 'NONE',  ( 25.64704443564076897, -34.76451658509458298, -107.4261196778966365 ) ) ;
#2232=CARTESIAN_POINT ( 'NONE',  ( 109.1586900883932856, 0.001582822706024254473, -0.006960773163856035471 ) ) ;
#2233=DIRECTION ( 'NONE',  ( -1.000000000000000000, -0.000000000000000000, -0.000000000000000000 ) ) ;
#2234=CARTESIAN_POINT ( 'NONE',  ( 8.186469777910911461, -90.56875928602647718, -118.7566730872910767 ) ) ;
#2236=B_SPLINE_CURVE_WITH_KNOTS ( 'NONE', 3,
 ( #1547, #10353, #19115, #27887, #8184, #18545, #16946 ),
 .UNSPECIFIED., .F., .F.,
 ( 4, 3, 4 ),
 ( 4.358266177795834884E-16, 0.02816610861753242670, 0.04000277880656261803 ),
 .UNSPECIFIED. ) ;
#2237=EDGE_CURVE ( 'NONE', #10703, #14908, #23718, .T. ) ;
#2238=CARTESIAN_POINT ( 'NONE',  ( 109.1624594426973118, -0.002129375066974356807, -0.01582142368019175474 ) ) ;
#2240=( BOUNDED_SURFACE ( )  B_SPLINE_SURFACE ( 3, 1, ( 
 ( #12545, #20790 ),
 ( #7574, #5391 ),
 ( #27262, #25799 ),
 ( #14849, #17152 ) ),
 .UNSPECIFIED., .F., .F., .F. ) 
 B_SPLINE_SURFACE_WITH_KNOTS ( ( 4, 4 ),
 ( 2, 2 ),
 ( 0.000000000000000000, 1.000000000000000000 ),
 ( 0.000000000000000000, 1.000000000000000000 ),
 .UNSPECIFIED. ) 
 GEOMETRIC_REPRESENTATION_ITEM ( )  RATIONAL_B_SPLINE_SURFACE ( (
 ( 1.000000000000000000, 1.000000000000000000),
 ( 0.9956975270656955868, 0.8568959468854907557),
 ( 0.9956975270656955868, 0.8568959468854907557),
 ( 1.000000000000000000, 1.000000000000000000) ) ) 
 REPRESENTATION_ITEM ( '' )  SURFACE ( )  );
#2241=ORIENTED_EDGE ( 'NONE', *, *, #144, .T. ) ;
#2242=DIRECTION ( 'NONE',  ( 0.000000000000000000, 0.000000000000000000, 1.000000000000000000 ) ) ;
#2243=CARTESIAN_POINT ( 'NONE',  ( 30.59141879584293378, -92.40465812955496006, -70.47510900703881020 ) ) ;
#2244=CARTESIAN_POINT ( 'NONE',  ( 109.1586900883932856, 0.003656351050331851926, 0.006130969560687375870 ) ) ;
#2245=VERTEX_POINT ( 'NONE', #6009 ) ;
#2247=EDGE_CURVE ( 'NONE', #3848, #23708, #12632, .T. ) ;
#2252=CARTESIAN_POINT ( 'NONE',  ( 109.1778270068192853, -0.004106684808172176952, 0.008360410075186655923 ) ) ;
#2254=B_SPLINE_CURVE_WITH_KNOTS ( 'NONE', 3,
 ( #1360, #10167, #20511, #11881, #941, #9730, #18499, #27273, #4086, #6132 ),
 .UNSPECIFIED., .F., .F.,
 ( 4, 3, 3, 4 ),
 ( 1.387778780781445676E-17, 0.0002669560319015683520, 0.0005492286108966489347, 0.0008315040496093463072 ),
 .UNSPECIFIED. ) ;
#2255=CARTESIAN_POINT ( 'NONE',  ( 25.64660436782558151, 110.5628080555245845, 22.90783756890889578 ) ) ;
#2256=CARTESIAN_POINT ( 'NONE',  ( 32.73300124599734318, 81.52272205837205377, 84.80615050150403533 ) ) ;
#2257=CARTESIAN_POINT ( 'NONE',  ( 2.433796855181205476, 13.76554153471693454, 144.8571464219890004 ) ) ;
#2259=ORIENTED_EDGE ( 'NONE', *, *, #28204, .T. ) ;
#2264=CARTESIAN_POINT ( 'NONE',  ( 2.263178113027036531, -141.9207360579559634, -31.59906256848430672 ) ) ;
#2265=CARTESIAN_POINT ( 'NONE',  ( 2.433796855181205476, 126.7346379669265843, -71.49415740224942795 ) ) ;
#2266=CARTESIAN_POINT ( 'NONE',  ( 25.64708010899965629, -91.37928813995122823, -66.32331961783478391 ) ) ;
#2267=ORIENTED_EDGE ( 'NONE', *, *, #1937, .F. ) ;
#2269=CARTESIAN_POINT ( 'NONE',  ( 109.1778270068192853, -0.004349865064721190715, 0.008236503545668676096 ) ) ;
#2271=CARTESIAN_POINT ( 'NONE',  ( 8.186469777910879486, -149.3111477498017621, 3.468244369821378292 ) ) ;
#2272=CARTESIAN_POINT ( 'NONE',  ( 2.430230287190572103, 74.01081053031275303, -125.2872625092154522 ) ) ;
#2273=CARTESIAN_POINT ( 'NONE',  ( 30.59141879584315404, 49.72305007553607226, -105.0379937202710323 ) ) ;
#2274=CARTESIAN_POINT ( 'NONE',  ( 1.833721034905664737, -107.5990973104329385, 97.36162733017677340 ) ) ;
#2276=ORIENTED_EDGE ( 'NONE', *, *, #12388, .F. ) ;
#2278=ORIENTED_EDGE ( 'NONE', *, *, #13597, .T. ) ;
#2280=( BOUNDED_SURFACE ( )  B_SPLINE_SURFACE ( 3, 1, ( 
 ( #26852, #8889 ),
 ( #17649, #22558 ),
 ( #4549, #15474 ),
 ( #15773, #2827 ) ),
 .UNSPECIFIED., .F., .F., .F. ) 
 B_SPLINE_SURFACE_WITH_KNOTS ( ( 4, 4 ),
 ( 2, 2 ),
 ( 0.000000000000000000, 1.000000000000000000 ),
 ( 0.000000000000000000, 1.000000000000000000 ),
 .UNSPECIFIED. ) 
 GEOMETRIC_REPRESENTATION_ITEM ( )  RATIONAL_B_SPLINE_SURFACE ( (
 ( 1.000000000000000000, 1.000000000000000000),
 ( 0.9960225298536222738, 0.9999952330161893110),
 ( 0.9960225298536222738, 0.9999952330161893110),
 ( 1.000000000000000000, 1.000000000000000000) ) ) 
 REPRESENTATION_ITEM ( '' )  SURFACE ( )  );
#2282=CARTESIAN_POINT ( 'NONE',  ( 9.884929003653626367, 128.2151425008052570, -78.87917189084775771 ) ) ;
#2283=EDGE_CURVE ( 'NONE', #17335, #15244, #2681, .T. ) ;
#2284=CARTESIAN_POINT ( 'NONE',  ( 13.36082413113061307, 143.3553710183989551, 53.25066407421853398 ) ) ;
#2285=EDGE_CURVE ( 'NONE', #18662, #27008, #14480, .T. ) ;
#2286=AXIS2_PLACEMENT_3D ( 'NONE', #25208, #23065, #12110 ) ;
#2289=AXIS2_PLACEMENT_3D ( 'NONE', #22998, #9598, #18215 ) ;
#2295=CARTESIAN_POINT ( 'NONE',  ( 2.433796855181219243, 31.67151202413165478, -142.0211193075552956 ) ) ;
#2297=CARTESIAN_POINT ( 'NONE',  ( 21.16825799904904670, -71.50503315297801521, -115.0183107335396642 ) ) ;
#2298=CARTESIAN_POINT ( 'NONE',  ( 55.79472521941426777, -21.78881894124655716, -69.41463258328535346 ) ) ;
#2299=CARTESIAN_POINT ( 'NONE',  ( 109.1778270068192853, 0.002542344697966444390, -0.008960903982066569656 ) ) ;
#2300=CARTESIAN_POINT ( 'NONE',  ( 32.73300124599732186, 0.000000000000000000, 0.000000000000000000 ) ) ;
#2301=CARTESIAN_POINT ( 'NONE',  ( 8.186469829614226867, -3.468244397268101853, 149.3111477833937784 ) ) ;
#2304=CARTESIAN_POINT ( 'NONE',  ( 6.224689322667630975, -144.2687111683192995, -33.28770499679482953 ) ) ;
#2305=ORIENTED_EDGE ( 'NONE', *, *, #27, .F. ) ;
#2308=AXIS2_PLACEMENT_3D ( 'NONE', #25916, #6209, #24046 ) ;
#2309=CARTESIAN_POINT ( 'NONE',  ( 25.81918753295380142, 107.2019194967340496, -35.81374485821504550 ) ) ;
#2310=B_SPLINE_CURVE_WITH_KNOTS ( 'NONE', 3,
 ( #16928, #25443, #12318, #28136, #10184, #18800 ),
 .UNSPECIFIED., .F., .F.,
 ( 4, 2, 4 ),
 ( 2.168404344971008868E-19, 0.0006311571484586057891, 0.001262314296917211361 ),
 .UNSPECIFIED. ) ;
#2311=ORIENTED_EDGE ( 'NONE', *, *, #7679, .T. ) ;
#2316=DIRECTION ( 'NONE',  ( 0.000000000000000000, 0.000000000000000000, 1.000000000000000000 ) ) ;
#2320=B_SPLINE_CURVE_WITH_KNOTS ( 'NONE', 3,
 ( #3342, #23657, #12541, #1467, #3914, #1322 ),
 .UNSPECIFIED., .F., .F.,
 ( 4, 2, 4 ),
 ( 1.257674520083185143E-17, 0.0006311636237756764172, 0.001262327247551340475 ),
 .UNSPECIFIED. ) ;
#2321=CARTESIAN_POINT ( 'NONE',  ( 25.64681081121880624, 11.38886654529674303, 112.3352186517031157 ) ) ;
#2322=CARTESIAN_POINT ( 'NONE',  ( 2.063896406836609909, -145.2631347824382999, 1.344106060019858884 ) ) ;
#2323=ADVANCED_FACE ( 'NONE', ( #17970 ), #12784, .T. ) ;
#2324=CARTESIAN_POINT ( 'NONE',  ( 2.108985857320889945, 43.67763756616835735, -138.5727354014053390 ) ) ;
#2326=CARTESIAN_POINT ( 'NONE',  ( 32.73300124599739291, -66.00340565729273123, -97.37344512919924000 ) ) ;
#2327=AXIS2_PLACEMENT_3D ( 'NONE', #17394, #14956, #19284 ) ;
#2328=CARTESIAN_POINT ( 'NONE',  ( 25.65782528836479770, 24.04194111109019616, -110.3293115225704781 ) ) ;
#2329=LINE ( 'NONE', #20182, #19916 ) ;
#2330=DIRECTION ( 'NONE',  ( 0.000000000000000000, 0.000000000000000000, 1.000000000000000000 ) ) ;
#2332=CARTESIAN_POINT ( 'NONE',  ( 1.833838850093452599, -117.3962623502780218, 85.29338149487179521 ) ) ;
#2333=VECTOR ( 'NONE', #11479, 1000.000000000000114 ) ;
#2334=ORIENTED_EDGE ( 'NONE', *, *, #2356, .F. ) ;
#2337=CARTESIAN_POINT ( 'NONE',  ( 30.59141879584320023, 79.74795589902169013, -84.53180090073595920 ) ) ;
#2340=CARTESIAN_POINT ( 'NONE',  ( 2.433796855181233454, -109.1007109081219539, -96.28145139437795308 ) ) ;
#2341=ORIENTED_EDGE ( 'NONE', *, *, #15603, .T. ) ;
#2344=DIRECTION ( 'NONE',  ( -0.5914120900931443270, 0.8063295922669343474, -0.008020494142999051376 ) ) ;
#2345=ORIENTED_EDGE ( 'NONE', *, *, #11680, .F. ) ;
#2346=ORIENTED_EDGE ( 'NONE', *, *, #11026, .T. ) ;
#2348=ORIENTED_EDGE ( 'NONE', *, *, #15709, .T. ) ;
#2349=CARTESIAN_POINT ( 'NONE',  ( 109.1586900883932856, -0.004851151255037395443, -0.005236795036860529204 ) ) ;
#2350=ORIENTED_EDGE ( 'NONE', *, *, #11494, .T. ) ;
#2351=EDGE_CURVE ( 'NONE', #3038, #24477, #17696, .T. ) ;
#2352=CIRCLE ( 'NONE', #12041, 12.50000000000000178 ) ;
#2354=AXIS2_PLACEMENT_3D ( 'NONE', #16199, #15916, #18345 ) ;
#2355=ORIENTED_EDGE ( 'NONE', *, *, #27918, .F. ) ;
#2356=EDGE_CURVE ( 'NONE', #26821, #26828, #20000, .T. ) ;
#2359=CARTESIAN_POINT ( 'NONE',  ( 109.1721716018069657, -0.01673651515803011372, -0.003350975118864128570 ) ) ;
#2361=B_SPLINE_CURVE_WITH_KNOTS ( 'NONE', 3,
 ( #13666, #9646, #13956, #27340, #11513, #11369, #20580, #5321 ),
 .UNSPECIFIED., .F., .F.,
 ( 4, 2, 2, 4 ),
 ( 0.000000000000000000, 0.0002429588503611220809, 0.0004859177007222441618, 0.0009718354014444829025 ),
 .UNSPECIFIED. ) ;
#2363=B_SPLINE_CURVE_WITH_KNOTS ( 'NONE', 3,
 ( #20654, #11886, #9883, #22554, #22410, #9737, #16342, #20377 ),
 .UNSPECIFIED., .F., .F.,
 ( 4, 2, 2, 4 ),
 ( 1.993045536433795054E-17, 0.0002429588503611349558, 0.0004859177007222500165, 0.0009718354014444676153 ),
 .UNSPECIFIED. ) ;
#2364=CARTESIAN_POINT ( 'NONE',  ( 109.1592201516379674, 0.005027640251764384401, -0.006044422199831492315 ) ) ;
#2365=FACE_OUTER_BOUND ( 'NONE', #9824, .T. ) ;
#2366=CARTESIAN_POINT ( 'NONE',  ( 26.11404676487259024, -33.91085499298451822, 108.0249973236466445 ) ) ;
#2367=CARTESIAN_POINT ( 'NONE',  ( 119.2224693531408803, -90.00000000000005684, 19.99999999999990052 ) ) ;
#2369=CARTESIAN_POINT ( 'NONE',  ( 109.1586900883932856, -0.006819617742892453323, 0.002109621908824122621 ) ) ;
#2370=CARTESIAN_POINT ( 'NONE',  ( 32.73300124599735739, 62.10906484417237294, 99.90245962373859356 ) ) ;
#2371=FACE_OUTER_BOUND ( 'NONE', #12750, .T. ) ;
#2372=FACE_OUTER_BOUND ( 'NONE', #12315, .T. ) ;
#2373=CARTESIAN_POINT ( 'NONE',  ( 2.108985857320910817, -125.1820688103226757, 73.75356715683039965 ) ) ;
#2376=CARTESIAN_POINT ( 'NONE',  ( 109.1592201516379674, -0.005027640251767255368, -0.006044422199822518590 ) ) ;
#2377=CARTESIAN_POINT ( 'NONE',  ( 26.11404676487259024, 55.62948129436384193, -98.61392875273304526 ) ) ;
#2379=CARTESIAN_POINT ( 'NONE',  ( 2.430230287190581429, -118.5711603495686859, 84.35270093935218938 ) ) ;
#2380=ORIENTED_EDGE ( 'NONE', *, *, #14936, .T. ) ;
#2381=CARTESIAN_POINT ( 'NONE',  ( 13.36082413113061307, -142.1654513177092269, 56.35051087434914763 ) ) ;
#2382=FACE_OUTER_BOUND ( 'NONE', #17560, .T. ) ;
#2384=ADVANCED_FACE ( 'NONE', ( #15389 ), #4912, .F. ) ;
#2385=VERTEX_POINT ( 'NONE', #17829 ) ;
#2386=CARTESIAN_POINT ( 'NONE',  ( 109.1721716018069657, -0.01254847260354819902, 0.01157047143379294832 ) ) ;
#2388=CARTESIAN_POINT ( 'NONE',  ( 94.22246935314088034, -90.00000000000005684, -6.938893903907228378E-15 ) ) ;
#2389=FACE_OUTER_BOUND ( 'NONE', #809, .T. ) ;
#2391=EDGE_CURVE ( 'NONE', #422, #12008, #11260, .T. ) ;
#2392=DIRECTION ( 'NONE',  ( 0.000000000000000000, 0.000000000000000000, 1.000000000000000000 ) ) ;
#2393=CONICAL_SURFACE ( 'NONE', #4710, 117.6351876552689504, 0.9945805576725580410 ) ;
#2395=CONICAL_SURFACE ( 'NONE', #1047, 117.6351876552689504, 0.9945805576725580410 ) ;
#2396=CARTESIAN_POINT ( 'NONE',  ( 1.833206310202350808, 132.2594754479313792, -59.70089235435300878 ) ) ;
#2397=LINE ( 'NONE', #24032, #23245 ) ;
#2399=CARTESIAN_POINT ( 'NONE',  ( 1.833838848569426361, -132.4919773286273426, 59.18404309081314807 ) ) ;
#2400=EDGE_LOOP ( 'NONE', ( #14615, #9558, #4860, #2982 ) ) ;
#2402=CARTESIAN_POINT ( 'NONE',  ( 109.1624594426973260, -0.002863932759303939191, -0.01570508117119672614 ) ) ;
#2404=CARTESIAN_POINT ( 'NONE',  ( 1.833485406944057594, 108.1939177044926055, 96.69979900902202985 ) ) ;
#2405=EDGE_LOOP ( 'NONE', ( #20624, #1599, #14286, #5807 ) ) ;
#2406=ORIENTED_EDGE ( 'NONE', *, *, #26096, .T. ) ;
#2408=CARTESIAN_POINT ( 'NONE',  ( 25.64708010899965629, 103.1718249732474249, 45.87517365398517910 ) ) ;
#2409=CARTESIAN_POINT ( 'NONE',  ( 109.1586900883932856, 0.005833932871487514972, -0.004113747441000934618 ) ) ;
#2410=CARTESIAN_POINT ( 'NONE',  ( 25.64681081121879203, 75.86069728268988399, 83.63051021305928145 ) ) ;
#2414=CARTESIAN_POINT ( 'NONE',  ( 25.64681081121879203, 46.30456157731328659, 102.9795863647030103 ) ) ;
#2415=CIRCLE ( 'NONE', #18517, 80.00000000000000000 ) ;
#2416=VERTEX_POINT ( 'NONE', #2143 ) ;
#2417=CARTESIAN_POINT ( 'NONE',  ( 25.65782528836479059, -34.34372400279175963, -107.5689571161382929 ) ) ;
#2421=CARTESIAN_POINT ( 'NONE',  ( 25.70243777736188306, 102.8829101922930960, 46.60897284577198718 ) ) ;
#2422=CARTESIAN_POINT ( 'NONE',  ( 109.1586900883932856, -0.002301750759607945531, -0.006757191295056121962 ) ) ;
#2423=CIRCLE ( 'NONE', #9360, 143.8872038478949946 ) ;
#2426=VECTOR ( 'NONE', #14860, 1000.000000000000227 ) ;
#2427=VERTEX_POINT ( 'NONE', #14381 ) ;
#2428=CARTESIAN_POINT ( 'NONE',  ( 1.833206308920097172, 142.0914675761166563, -29.44113170198408014 ) ) ;
#2430=ORIENTED_EDGE ( 'NONE', *, *, #3842, .F. ) ;
#2431=EDGE_CURVE ( 'NONE', #9946, #7628, #9797, .T. ) ;
#2434=ORIENTED_EDGE ( 'NONE', *, *, #3842, .T. ) ;
#2435=CARTESIAN_POINT ( 'NONE',  ( 9.884929003653608603, 114.6392083957130836, -97.56484214660510190 ) ) ;
#2436=CARTESIAN_POINT ( 'NONE',  ( 26.04756280548354042, 84.84709444968909509, 74.90181827458373220 ) ) ;
#2438=ORIENTED_EDGE ( 'NONE', *, *, #7235, .F. ) ;
#2440=AXIS2_PLACEMENT_3D ( 'NONE', #25533, #3626, #19456 ) ;
#2441=VECTOR ( 'NONE', #18680, 1000.000000000000000 ) ;
#2442=CARTESIAN_POINT ( 'NONE',  ( 26.11404676487259024, 67.46175819463365997, 90.92995828888226129 ) ) ;
#2443=VERTEX_POINT ( 'NONE', #100 ) ;
#2444=CARTESIAN_POINT ( 'NONE',  ( 25.87036335909427720, 92.04585932622775601, 65.65170964736162773 ) ) ;
#2445=VERTEX_POINT ( 'NONE', #6734 ) ;
#2447=CARTESIAN_POINT ( 'NONE',  ( 24.01988960052062083, -61.78678588189937670, -115.5642432877697416 ) ) ;
#2448=CARTESIAN_POINT ( 'NONE',  ( 2.108393763691190248, -145.2872457912033042, -1.280847988473292398 ) ) ;
#2451=LINE ( 'NONE', #20300, #27627 ) ;
#2452=B_SPLINE_CURVE_WITH_KNOTS ( 'NONE', 3,
 ( #24765, #27022, #7336, #16098 ),
 .UNSPECIFIED., .F., .F.,
 ( 4, 4 ),
 ( 0.000000000000000000, 0.01077107196513877631 ),
 .UNSPECIFIED. ) ;
#2456=DIRECTION ( 'NONE',  ( 0.000000000000000000, 0.000000000000000000, -1.000000000000000000 ) ) ;
#2457=CARTESIAN_POINT ( 'NONE',  ( 2.108985857320919699, -43.67763756616749049, 138.5727354014056516 ) ) ;
#2458=CARTESIAN_POINT ( 'NONE',  ( 13.36082413113061307, -148.1362653801000135, -37.97423473099446767 ) ) ;
#2459=ADVANCED_FACE ( 'NONE', ( #2382 ), #2721, .F. ) ;
#2461=( BOUNDED_SURFACE ( )  B_SPLINE_SURFACE ( 3, 1, ( 
 ( #16845, #3880 ),
 ( #3312, #1156 ),
 ( #21293, #25344 ),
 ( #21000, #3586 ) ),
 .UNSPECIFIED., .F., .F., .F. ) 
 B_SPLINE_SURFACE_WITH_KNOTS ( ( 4, 4 ),
 ( 2, 2 ),
 ( 0.000000000000000000, 1.000000000000000000 ),
 ( 0.000000000000000000, 1.000000000000000000 ),
 .UNSPECIFIED. ) 
 GEOMETRIC_REPRESENTATION_ITEM ( )  RATIONAL_B_SPLINE_SURFACE ( (
 ( 1.000000000000000000, 1.000000000000000000),
 ( 0.6386103224230316178, 0.9954351624131538845),
 ( 0.6386103224230316178, 0.9954351624131538845),
 ( 1.000000000000000000, 1.000000000000000000) ) ) 
 REPRESENTATION_ITEM ( '' )  SURFACE ( )  );
#2463=ORIENTED_EDGE ( 'NONE', *, *, #28164, .F. ) ;
#2464=CARTESIAN_POINT ( 'NONE',  ( 2.433796855181205476, -96.28145139437610567, -109.1007109081235882 ) ) ;
#2465=CARTESIAN_POINT ( 'NONE',  ( 25.98552792386799126, 107.2612904323495542, -35.98568266743403399 ) ) ;
#2469=ORIENTED_EDGE ( 'NONE', *, *, #23569, .F. ) ;
#2474=CARTESIAN_POINT ( 'NONE',  ( 25.73574536432414561, -107.1893601970592300, -35.67555431182938719 ) ) ;
#2476=ORIENTED_EDGE ( 'NONE', *, *, #9411, .T. ) ;
#2477=CARTESIAN_POINT ( 'NONE',  ( 1.833485406944057594, -144.3694338680884073, -14.63699153649508311 ) ) ;
#2480=CARTESIAN_POINT ( 'NONE',  ( 2.433796855181205476, -142.6247129145649808, 28.83182736670489987 ) ) ;
#2481=CARTESIAN_POINT ( 'NONE',  ( 1.834118845439484335, -29.99597360113166289, 141.9759513273463938 ) ) ;
#2482=CARTESIAN_POINT ( 'NONE',  ( 32.73300124599738581, 84.80615050150476009, -81.52272205837115848 ) ) ;
#2483=EDGE_CURVE ( 'NONE', #11098, #16995, #6093, .T. ) ;
#2485=CARTESIAN_POINT ( 'NONE',  ( 25.64692872815575342, 91.15762468787745831, 66.62748454953189992 ) ) ;
#2489=CARTESIAN_POINT ( 'NONE',  ( 32.73300124599732186, 0.000000000000000000, 0.000000000000000000 ) ) ;
#2490=EDGE_LOOP ( 'NONE', ( #12175, #4207, #10346, #10001 ) ) ;
#2491=CARTESIAN_POINT ( 'NONE',  ( 2.430230287190592531, 145.5073573687466819, -1.451610819318251089 ) ) ;
#2492=ADVANCED_FACE ( 'NONE', ( #21844 ), #24417, .F. ) ;
#2495=CARTESIAN_POINT ( 'NONE',  ( 2.263178113027049410, 141.9207360579561055, 31.59906256848331907 ) ) ;
#2498=B_SPLINE_CURVE_WITH_KNOTS ( 'NONE', 3,
 ( #3002, #9346, #6896, #2853 ),
 .UNSPECIFIED., .F., .F.,
 ( 4, 4 ),
 ( 5.845992376248150641E-16, 0.008383748772660029602 ),
 .UNSPECIFIED. ) ;
#2502=CARTESIAN_POINT ( 'NONE',  ( 1.833750490713699444, -96.89879583303773813, -108.0159692407140568 ) ) ;
#2505=CARTESIAN_POINT ( 'NONE',  ( 28.37603512858455446, 68.88140609180194929, 91.75440368549958237 ) ) ;
#2506=CARTESIAN_POINT ( 'NONE',  ( 5.340103556456506695, -84.79482753886469482, -120.6284720803335091 ) ) ;
#2509=CARTESIAN_POINT ( 'NONE',  ( 8.186469829614228644, -63.89871393833106339, 134.9918587494111648 ) ) ;
#2511=CARTESIAN_POINT ( 'NONE',  ( 13.36082413113061307, -147.2768864064170486, 41.18148072373564617 ) ) ;
#2512=CARTESIAN_POINT ( 'NONE',  ( 30.59138290137891047, -79.74792615266090934, -84.53179630244071063 ) ) ;
#2517=CARTESIAN_POINT ( 'NONE',  ( 30.59138290137879679, -33.33271994911419256, 111.3296280985501596 ) ) ;
#2518=EDGE_CURVE ( 'NONE', #24427, #1176, #4328, .T. ) ;
#2521=B_SPLINE_CURVE_WITH_KNOTS ( 'NONE', 3,
 ( #12749, #21533, #1805, #10605, #25304, #14493, #23298, #18964 ),
 .UNSPECIFIED., .F., .F.,
 ( 4, 2, 2, 4 ),
 ( 0.000000000000000000, 0.0002429588503611183675, 0.0004859177007222367350, 0.0009718354014444859383 ),
 .UNSPECIFIED. ) ;
#2523=CARTESIAN_POINT ( 'NONE',  ( 1.832998868059890096, -44.33343224355329681, 138.1720401012265427 ) ) ;
#2526=FACE_OUTER_BOUND ( 'NONE', #25146, .T. ) ;
#2528=CARTESIAN_POINT ( 'NONE',  ( 2.430230287190589422, -125.2872625092167596, 74.01081053031055035 ) ) ;
#2530=CARTESIAN_POINT ( 'NONE',  ( 26.28373643307407548, 71.57300207276523452, -105.5888781856744174 ) ) ;
#2532=CARTESIAN_POINT ( 'NONE',  ( 1.832998868059890096, -138.1720401012269974, 44.33343224355190415 ) ) ;
#2533=EDGE_CURVE ( 'NONE', #6495, #27090, #24587, .T. ) ;
#2534=CARTESIAN_POINT ( 'NONE',  ( 6.224689322667647851, -71.79702446228394308, 129.4863684118285221 ) ) ;
#2536=VERTEX_POINT ( 'NONE', #15428 ) ;
#2538=CARTESIAN_POINT ( 'NONE',  ( 2.433796855181205476, 86.69855925934130880, -116.8607839509047892 ) ) ;
#2539=CARTESIAN_POINT ( 'NONE',  ( 13.36082413113061307, -119.8836995922720092, -94.94363694444177781 ) ) ;
#2540=ORIENTED_EDGE ( 'NONE', *, *, #25433, .T. ) ;
#2543=CARTESIAN_POINT ( 'NONE',  ( 5.340103579038286696, 28.39990973304668032, -144.6887562507421876 ) ) ;
#2544=CARTESIAN_POINT ( 'NONE',  ( 25.64681081121879203, 23.88203588908081443, 110.3564950173082480 ) ) ;
#2545=CARTESIAN_POINT ( 'NONE',  ( 1.833603222531960952, -125.8904991419471884, 72.16916166673696864 ) ) ;
#2546=EDGE_LOOP ( 'NONE', ( #11351, #14635, #21006, #5852 ) ) ;
#2548=CARTESIAN_POINT ( 'NONE',  ( 2.433796855181205476, -132.3327394885227477, -60.50726454508036056 ) ) ;
#2549=CARTESIAN_POINT ( 'NONE',  ( 5.340103579038244952, -62.06990748397762303, -133.7487108093470169 ) ) ;
#2550=CARTESIAN_POINT ( 'NONE',  ( 25.64681081121879203, -97.99105938547884875, -56.09509703373446854 ) ) ;
#2553=ORIENTED_EDGE ( 'NONE', *, *, #13372, .T. ) ;
#2557=ADVANCED_FACE ( 'NONE', ( #6972, #22368 ), #28387, .T. ) ;
#2559=CARTESIAN_POINT ( 'NONE',  ( 1.832998868059858122, -84.86110816369684073, 117.7096351258385027 ) ) ;
#2560=CARTESIAN_POINT ( 'NONE',  ( 1.833838850093478579, 144.3148369740567318, 15.16809710532109712 ) ) ;
#2562=CARTESIAN_POINT ( 'NONE',  ( 1.833485406944057594, 117.7091014914950193, 84.86072343962607079 ) ) ;
#2563=VERTEX_POINT ( 'NONE', #24242 ) ;
#2564=CARTESIAN_POINT ( 'NONE',  ( 26.11404676487257603, -84.89295829319442532, -74.91683232331061504 ) ) ;
#2565=CARTESIAN_POINT ( 'NONE',  ( 109.1589550718174877, -0.007571935245604908930, -0.0002241941239241235554 ) ) ;
#2566=CARTESIAN_POINT ( 'NONE',  ( 26.11404676487259024, -112.4785329405482912, 12.95861723607416671 ) ) ;
#2567=CARTESIAN_POINT ( 'NONE',  ( 109.1587776205901861, 0.001442274044995796702, -0.007186028091168164718 ) ) ;
#2569=CARTESIAN_POINT ( 'NONE',  ( 55.79472521941426777, -66.75682020267549888, 28.92526238350451351 ) ) ;
#2571=ORIENTED_EDGE ( 'NONE', *, *, #24124, .T. ) ;
#2572=CARTESIAN_POINT ( 'NONE',  ( 2.430230287190592531, 142.6294793592097960, 28.83279105684475851 ) ) ;
#2573=VERTEX_POINT ( 'NONE', #22062 ) ;
#2575=B_SPLINE_CURVE_WITH_KNOTS ( 'NONE', 3,
 ( #20845, #10352, #25312, #16524, #19114, #10058 ),
 .UNSPECIFIED., .F., .F.,
 ( 4, 2, 4 ),
 ( 1.389302603484999005E-17, 0.0006311571484586086080, 0.001262314296917203555 ),
 .UNSPECIFIED. ) ;
#2576=CARTESIAN_POINT ( 'NONE',  ( 1.833485406944057594, -142.0485807715644171, -29.64752363041688454 ) ) ;
#2577=VERTEX_POINT ( 'NONE', #4367 ) ;
#2582=FACE_OUTER_BOUND ( 'NONE', #23599, .T. ) ;
#2584=( BOUNDED_SURFACE ( )  B_SPLINE_SURFACE ( 3, 1, ( 
 ( #14917, #21403 ),
 ( #10477, #3981 ),
 ( #18971, #19378 ),
 ( #21111, #10350 ) ),
 .UNSPECIFIED., .F., .F., .F. ) 
 B_SPLINE_SURFACE_WITH_KNOTS ( ( 4, 4 ),
 ( 2, 2 ),
 ( 0.000000000000000000, 1.000000000000000000 ),
 ( 0.000000000000000000, 1.000000000000000000 ),
 .UNSPECIFIED. ) 
 GEOMETRIC_REPRESENTATION_ITEM ( )  RATIONAL_B_SPLINE_SURFACE ( (
 ( 1.000000000000000000, 1.000000000000000000),
 ( 0.6386103224230302855, 0.9954351624131538845),
 ( 0.6386103224230302855, 0.9954351624131538845),
 ( 1.000000000000000000, 1.000000000000000000) ) ) 
 REPRESENTATION_ITEM ( '' )  SURFACE ( )  );
#2586=CARTESIAN_POINT ( 'NONE',  ( 10.93730112726007775, 51.37919228020501805, -142.1801301103781725 ) ) ;
#2588=CARTESIAN_POINT ( 'NONE',  ( 10.93730112725990367, -92.80059208661606363, -119.3442956573281748 ) ) ;
#2589=ORIENTED_EDGE ( 'NONE', *, *, #11086, .F. ) ;
#2590=CARTESIAN_POINT ( 'NONE',  ( 25.69398547355838502, 91.80679989327151702, 65.78402800526194483 ) ) ;
#2591=EDGE_LOOP ( 'NONE', ( #22277, #4233, #1204, #9913 ) ) ;
#2594=EDGE_CURVE ( 'NONE', #19089, #5993, #11871, .T. ) ;
#2596=CARTESIAN_POINT ( 'NONE',  ( 16.75465622695657331, 25.01894884133855612, 140.0080030360327896 ) ) ;
#2597=CARTESIAN_POINT ( 'NONE',  ( 109.1592201516379674, -0.001934867487012880598, 0.007620268632968135725 ) ) ;
#2603=CARTESIAN_POINT ( 'NONE',  ( 10.93730112726002979, 92.80059208661855052, -119.3442956573263558 ) ) ;
#2604=CARTESIAN_POINT ( 'NONE',  ( 25.64681081121879203, -66.03065707438874199, -91.59071981940638807 ) ) ;
#2607=ORIENTED_EDGE ( 'NONE', *, *, #10395, .F. ) ;
#2609=CARTESIAN_POINT ( 'NONE',  ( 26.11404676487259024, 24.64483677384848903, 110.5078194225162207 ) ) ;
#2610=CARTESIAN_POINT ( 'NONE',  ( 1.832998868059890096, -117.7096351258381901, -84.86110816369725285 ) ) ;
#2611=VERTEX_POINT ( 'NONE', #26382 ) ;
#2612=B_SPLINE_CURVE_WITH_KNOTS ( 'NONE', 3,
 ( #6426, #15042, #17490, #19371 ),
 .UNSPECIFIED., .F., .F.,
 ( 4, 4 ),
 ( 0.000000000000000000, 0.01077107196513815181 ),
 .UNSPECIFIED. ) ;
#2613=ORIENTED_EDGE ( 'NONE', *, *, #7561, .T. ) ;
#2614=EDGE_LOOP ( 'NONE', ( #22494, #19497, #25440, #28061 ) ) ;
#2616=B_SPLINE_CURVE_WITH_KNOTS ( 'NONE', 3,
 ( #12303, #18500, #18935, #27711 ),
 .UNSPECIFIED., .F., .F.,
 ( 4, 4 ),
 ( 4.887365971079175436E-16, 0.008383748772659961948 ),
 .UNSPECIFIED. ) ;
#2617=CARTESIAN_POINT ( 'NONE',  ( 9.884929003653626367, 124.2095058357577670, 85.04731144912555862 ) ) ;
#2618=DIRECTION ( 'NONE',  ( 0.7071067811865485719, 4.906538933386790339E-16, 0.7071067811865465735 ) ) ;
#2619=EDGE_CURVE ( 'NONE', #23901, #10557, #24104, .T. ) ;
#2621=ORIENTED_EDGE ( 'NONE', *, *, #14464, .T. ) ;
#2622=CARTESIAN_POINT ( 'NONE',  ( 32.73300124599732186, 0.000000000000000000, 0.000000000000000000 ) ) ;
#2624=B_SPLINE_CURVE_WITH_KNOTS ( 'NONE', 3,
 ( #621, #16007, #7544, #24818, #25096, #16156 ),
 .UNSPECIFIED., .F., .F.,
 ( 4, 2, 4 ),
 ( 2.684971462552800574E-17, 0.0006311636237756952823, 0.001262327247551372567 ),
 .UNSPECIFIED. ) ;
#2626=CARTESIAN_POINT ( 'NONE',  ( 9.884929003653608603, 11.54837932063031047, 150.0922431698405717 ) ) ;
#2627=EDGE_CURVE ( 'NONE', #11607, #19219, #27684, .T. ) ;
#2628=EDGE_CURVE ( 'NONE', #4784, #17963, #21543, .T. ) ;
#2629=CARTESIAN_POINT ( 'NONE',  ( 16.05277956358197144, 134.7758735858410830, -48.70400867628961095 ) ) ;
#2630=CARTESIAN_POINT ( 'NONE',  ( 109.1586900883932856, 0.002810909342002405019, -0.006561743627145274170 ) ) ;
#2633=EDGE_LOOP ( 'NONE', ( #13746, #22279, #11686, #21522 ) ) ;
#2636=CARTESIAN_POINT ( 'NONE',  ( 1.833485406944043827, -144.2578170162061895, -15.69895494453532869 ) ) ;
#2637=CARTESIAN_POINT ( 'NONE',  ( 25.64708228042119487, 45.88917180166276921, 103.1656011680034055 ) ) ;
#2638=CARTESIAN_POINT ( 'NONE',  ( 2.430230287190589422, 84.35270093935415048, -118.5711603495673074 ) ) ;
#2640=ORIENTED_EDGE ( 'NONE', *, *, #25373, .F. ) ;
#2642=ORIENTED_EDGE ( 'NONE', *, *, #13129, .F. ) ;
#2644=B_SPLINE_CURVE_WITH_KNOTS ( 'NONE', 3,
 ( #4743, #24060, #278, #24193, #22313, #20277, #141, #4886, #15382, #8936 ),
 .UNSPECIFIED., .F., .F.,
 ( 4, 3, 3, 4 ),
 ( 0.000000000000000000, 0.0002669560319015610878, 0.0005492286108966271422, 0.0008315040496093543303 ),
 .UNSPECIFIED. ) ;
#2645=CARTESIAN_POINT ( 'NONE',  ( 2.433796855181233454, 137.9325382748291418, -46.34326152018600453 ) ) ;
#2646=VERTEX_POINT ( 'NONE', #624 ) ;
#2647=CARTESIAN_POINT ( 'NONE',  ( 19.66333377628682655, 121.4767361208146639, -64.94841092372071500 ) ) ;
#2649=CARTESIAN_POINT ( 'NONE',  ( 2.430230287190581429, -96.28466919684025527, -109.1043569252024099 ) ) ;
#2651=B_SPLINE_CURVE_WITH_KNOTS ( 'NONE', 3,
 ( #2001, #8365, #10390, #6338, #12941, #15230, #25778 ),
 .UNSPECIFIED., .F., .F.,
 ( 4, 3, 4 ),
 ( 0.000000000000000000, 0.02398743853561338332, 0.04000277880656213231 ),
 .UNSPECIFIED. ) ;
#2656=CARTESIAN_POINT ( 'NONE',  ( 1.833838850855462166, 30.08297881069679391, 141.9572669680996739 ) ) ;
#2657=AXIS2_PLACEMENT_3D ( 'NONE', #5788, #1591, #19428 ) ;
#2658=EDGE_CURVE ( 'NONE', #18577, #2563, #22539, .T. ) ;
#2659=CARTESIAN_POINT ( 'NONE',  ( 1.834118845439484335, 138.0627591860436212, -44.67218053242251585 ) ) ;
#2662=CARTESIAN_POINT ( 'NONE',  ( 94.22246935314088034, -90.00000000000005684, -6.938893903907228378E-15 ) ) ;
#2663=CARTESIAN_POINT ( 'NONE',  ( 109.1778270068192853, 0.005967275455169884606, 0.007152128381194073486 ) ) ;
#2664=DIRECTION ( 'NONE',  ( 0.000000000000000000, 0.000000000000000000, 1.000000000000000000 ) ) ;
#2665=DIRECTION ( 'NONE',  ( -1.000000000000000000, -0.000000000000000000, -0.000000000000000000 ) ) ;
#2667=CARTESIAN_POINT ( 'NONE',  ( 30.59138290137885718, -109.6600423140543228, 38.47117663195916037 ) ) ;
#2669=ORIENTED_EDGE ( 'NONE', *, *, #11224, .F. ) ;
#2670=CARTESIAN_POINT ( 'NONE',  ( 25.64681081121879203, 23.06870491922322230, 110.5293738517609228 ) ) ;
#2671=CARTESIAN_POINT ( 'NONE',  ( 1.834118845439484335, 145.1099497418795750, 0.1779704863075100008 ) ) ;
#2674=CARTESIAN_POINT ( 'NONE',  ( 25.64703792032472052, 75.44170528134999643, -84.00887408968974057 ) ) ;
#2677=VECTOR ( 'NONE', #16786, 1000.000000000000114 ) ;
#2678=( BOUNDED_SURFACE ( )  B_SPLINE_SURFACE ( 3, 1, ( 
 ( #17697, #17143 ),
 ( #26477, #6224 ),
 ( #15105, #14976 ),
 ( #21601, #8516 ) ),
 .UNSPECIFIED., .F., .F., .F. ) 
 B_SPLINE_SURFACE_WITH_KNOTS ( ( 4, 4 ),
 ( 2, 2 ),
 ( 0.000000000000000000, 1.000000000000000000 ),
 ( 0.000000000000000000, 1.000000000000000000 ),
 .UNSPECIFIED. ) 
 GEOMETRIC_REPRESENTATION_ITEM ( )  RATIONAL_B_SPLINE_SURFACE ( (
 ( 1.000000000000000000, 1.000000000000000000),
 ( 0.9960225298536222738, 0.9999952330161893110),
 ( 0.9960225298536222738, 0.9999952330161893110),
 ( 1.000000000000000000, 1.000000000000000000) ) ) 
 REPRESENTATION_ITEM ( '' )  SURFACE ( )  );
#2679=CARTESIAN_POINT ( 'NONE',  ( 32.73300124599735028, 8.473903470906103408, 117.3295799645430151 ) ) ;
#2681=B_SPLINE_CURVE_WITH_KNOTS ( 'NONE', 3,
 ( #10190, #8037, #22092, #13029 ),
 .UNSPECIFIED., .F., .F.,
 ( 4, 4 ),
 ( 8.993834424997155211E-17, 0.008383748772659552553 ),
 .UNSPECIFIED. ) ;
#2682=EDGE_LOOP ( 'NONE', ( #11533, #19060, #3372, #482 ) ) ;
#2683=CARTESIAN_POINT ( 'NONE',  ( 9.884929003653608603, 85.04731144912511809, 124.2095058357580513 ) ) ;
#2684=EDGE_CURVE ( 'NONE', #27364, #10661, #25389, .T. ) ;
#2686=CARTESIAN_POINT ( 'NONE',  ( 109.1586059443104944, -0.006570129623063787269, -0.002622205828279724604 ) ) ;
#2688=ORIENTED_EDGE ( 'NONE', *, *, #24702, .F. ) ;
#2689=FACE_OUTER_BOUND ( 'NONE', #28127, .T. ) ;
#2690=CARTESIAN_POINT ( 'NONE',  ( 26.28373643307398666, -97.52903534490815218, -82.21796085350759142 ) ) ;
#2691=EDGE_CURVE ( 'NONE', #24160, #8435, #7391, .T. ) ;
#2693=CARTESIAN_POINT ( 'NONE',  ( 32.73300124599737160, -113.0038235389604466, 32.68291970228198551 ) ) ;
#2701=CARTESIAN_POINT ( 'NONE',  ( 26.11404676487259024, -1.130420376096339385, -113.2169081140374232 ) ) ;
#2702=EDGE_LOOP ( 'NONE', ( #15664, #5473, #1063, #23629 ) ) ;
#2705=DIRECTION ( 'NONE',  ( 0.5946245182733608248, -0.7332888028688925308, -0.3297108033645242964 ) ) ;
#2708=B_SPLINE_CURVE_WITH_KNOTS ( 'NONE', 3,
 ( #25315, #18384, #7626, #5593, #5155, #3290, #12073, #20848, #24756, #18239 ),
 .UNSPECIFIED., .F., .F.,
 ( 4, 3, 3, 4 ),
 ( 3.925231146709437917E-17, 0.0002669559177086447345, 0.0005339118354151110900, 0.001067817517169167285 ),
 .UNSPECIFIED. ) ;
#2710=CARTESIAN_POINT ( 'NONE',  ( 25.70243777736190438, -103.4793210720851278, 45.26941207740255635 ) ) ;
#2711=DIRECTION ( 'NONE',  ( -0.5914120900931443270, 0.6570486713847245586, 0.4674599267565369143 ) ) ;
#2712=VERTEX_POINT ( 'NONE', #9990 ) ;
#2713=CARTESIAN_POINT ( 'NONE',  ( 13.36082413113063083, 137.0038452127809876, -67.94366799842680393 ) ) ;
#2715=CARTESIAN_POINT ( 'NONE',  ( 2.263178113027053406, -57.85473702513782257, -133.3897502891100260 ) ) ;
#2716=CARTESIAN_POINT ( 'NONE',  ( 2.063896406836605024, -73.79559738457841434, 125.1295119249436851 ) ) ;
#2717=DIRECTION ( 'NONE',  ( -1.000000000000000000, -0.000000000000000000, -0.000000000000000000 ) ) ;
#2718=ORIENTED_EDGE ( 'NONE', *, *, #10921, .F. ) ;
#2719=CARTESIAN_POINT ( 'NONE',  ( 2.430230287190592531, -31.67257033707400993, -142.0258656395025412 ) ) ;
#2720=EDGE_CURVE ( 'NONE', #28456, #14178, #2957, .T. ) ;
#2721=( BOUNDED_SURFACE ( )  B_SPLINE_SURFACE ( 3, 1, ( 
 ( #19960, #240 ),
 ( #19538, #24020 ),
 ( #26568, #2534 ),
 ( #13475, #22272 ) ),
 .UNSPECIFIED., .F., .F., .F. ) 
 B_SPLINE_SURFACE_WITH_KNOTS ( ( 4, 4 ),
 ( 2, 2 ),
 ( 0.000000000000000000, 1.000000000000000000 ),
 ( 0.000000000000000000, 1.000000000000000000 ),
 .UNSPECIFIED. ) 
 GEOMETRIC_REPRESENTATION_ITEM ( )  RATIONAL_B_SPLINE_SURFACE ( (
 ( 1.000000000000000000, 1.000000000000000000),
 ( 0.6386103224230316178, 0.9954351624131538845),
 ( 0.6386103224230316178, 0.9954351624131538845),
 ( 1.000000000000000000, 1.000000000000000000) ) ) 
 REPRESENTATION_ITEM ( '' )  SURFACE ( )  );
#2722=ORIENTED_EDGE ( 'NONE', *, *, #1908, .T. ) ;
#2723=CARTESIAN_POINT ( 'NONE',  ( 1.833485406944043827, 142.0485807715649571, -29.64752363041402816 ) ) ;
#2727=ORIENTED_EDGE ( 'NONE', *, *, #25925, .T. ) ;
#2728=EDGE_CURVE ( 'NONE', #3474, #2611, #22806, .T. ) ;
#2731=EDGE_CURVE ( 'NONE', #15244, #7653, #16011, .T. ) ;
#2732=CARTESIAN_POINT ( 'NONE',  ( 2.108985857320909485, 57.92316197981838144, -133.2480631238187243 ) ) ;
#2735=CARTESIAN_POINT ( 'NONE',  ( 1.833206310202337042, 14.42724831649545081, -144.3905118062892257 ) ) ;
#2738=ORIENTED_EDGE ( 'NONE', *, *, #16014, .F. ) ;
#2739=EDGE_LOOP ( 'NONE', ( #25148, #23733, #13608, #12334 ) ) ;
#2742=CARTESIAN_POINT ( 'NONE',  ( 25.64681081121879203, 112.3352186517030731, 11.38886654529711961 ) ) ;
#2744=CARTESIAN_POINT ( 'NONE',  ( 10.93730112725932635, 0.000000000000000000, 0.000000000000000000 ) ) ;
#2746=B_SPLINE_CURVE_WITH_KNOTS ( 'NONE', 3,
 ( #946, #22991, #18206, #25009 ),
 .UNSPECIFIED., .F., .F.,
 ( 4, 4 ),
 ( 0.000000000000000000, 0.01077107196513849528 ),
 .UNSPECIFIED. ) ;
#2748=DIRECTION ( 'NONE',  ( 0.000000000000000000, 0.000000000000000000, 1.000000000000000000 ) ) ;
#2751=DIRECTION ( 'NONE',  ( 0.5914120900931443270, 0.5335794202785180129, 0.6045864222316765790 ) ) ;
#2752=ORIENTED_EDGE ( 'NONE', *, *, #15285, .T. ) ;
#2755=ORIENTED_EDGE ( 'NONE', *, *, #9123, .T. ) ;
#2756=ORIENTED_EDGE ( 'NONE', *, *, #19898, .F. ) ;
#2757=ORIENTED_EDGE ( 'NONE', *, *, #20662, .F. ) ;
#2759=ADVANCED_FACE ( 'NONE', ( #21041 ), #13556, .F. ) ;
#2760=AXIS2_PLACEMENT_3D ( 'NONE', #1104, #16066, #20387 ) ;
#2762=CARTESIAN_POINT ( 'NONE',  ( 1.832998868059858122, 125.4013017422241063, -73.01698022778225550 ) ) ;
#2764=EDGE_CURVE ( 'NONE', #18334, #12354, #5352, .T. ) ;
#2765=DIRECTION ( 'NONE',  ( -0.7071067811865485719, 0.000000000000000000, 0.7071067811865465735 ) ) ;
#2766=EDGE_CURVE ( 'NONE', #18662, #21864, #15615, .T. ) ;
#2767=CARTESIAN_POINT ( 'NONE',  ( 32.73300124599732186, 0.000000000000000000, 0.000000000000000000 ) ) ;
#2768=( BOUNDED_SURFACE ( )  B_SPLINE_SURFACE ( 3, 1, ( 
 ( #2178, #19748 ),
 ( #6677, #185 ),
 ( #24678, #8973 ),
 ( #18013, #26801 ) ),
 .UNSPECIFIED., .F., .F., .F. ) 
 B_SPLINE_SURFACE_WITH_KNOTS ( ( 4, 4 ),
 ( 2, 2 ),
 ( 0.000000000000000000, 1.000000000000000000 ),
 ( 0.000000000000000000, 1.000000000000000000 ),
 .UNSPECIFIED. ) 
 GEOMETRIC_REPRESENTATION_ITEM ( )  RATIONAL_B_SPLINE_SURFACE ( (
 ( 1.000000000000000000, 1.000000000000000000),
 ( 0.9956975270656955868, 0.8568959468854907557),
 ( 0.9956975270656955868, 0.8568959468854907557),
 ( 1.000000000000000000, 1.000000000000000000) ) ) 
 REPRESENTATION_ITEM ( '' )  SURFACE ( )  );
#2769=CARTESIAN_POINT ( 'NONE',  ( 32.73300124599732186, 0.000000000000000000, 0.000000000000000000 ) ) ;
#2770=CARTESIAN_POINT ( 'NONE',  ( 10.93730112725995873, 4.928439153522441885, -151.0983828010091656 ) ) ;
#2771=CARTESIAN_POINT ( 'NONE',  ( 109.1721716018069657, -0.01665253177026227577, 0.003746085893652734838 ) ) ;
#2774=CARTESIAN_POINT ( 'NONE',  ( 1.832998868059858122, -97.49378069860870255, 107.4798986104856766 ) ) ;
#2776=ORIENTED_EDGE ( 'NONE', *, *, #818, .T. ) ;
#2778=CARTESIAN_POINT ( 'NONE',  ( 32.73300124599738581, -72.21147546950486174, -92.86301839380092815 ) ) ;
#2779=CARTESIAN_POINT ( 'NONE',  ( 32.73300124599737160, -75.82012867748541396, 89.94078864464039214 ) ) ;
#2780=CIRCLE ( 'NONE', #23503, 117.6351876552689504 ) ;
#2781=CARTESIAN_POINT ( 'NONE',  ( 9.884929003653626367, -132.4189379373565316, -71.59798461011472170 ) ) ;
#2784=ADVANCED_FACE ( 'NONE', ( #16888 ), #12640, .F. ) ;
#2785=ORIENTED_EDGE ( 'NONE', *, *, #3535, .T. ) ;
#2786=CARTESIAN_POINT ( 'NONE',  ( 32.73300124599732186, 0.000000000000000000, 0.000000000000000000 ) ) ;
#2787=VECTOR ( 'NONE', #26228, 1000.000000000000114 ) ;
#2791=ORIENTED_EDGE ( 'NONE', *, *, #13176, .F. ) ;
#2792=CARTESIAN_POINT ( 'NONE',  ( 10.93730112726024117, 133.3192575531818136, -71.28103789254788580 ) ) ;
#2796=ADVANCED_FACE ( 'NONE', ( #6238 ), #22399, .F. ) ;
#2797=B_SPLINE_CURVE_WITH_KNOTS ( 'NONE', 3,
 ( #4649, #2629, #11132, #13706, #11410, #15567, #10992 ),
 .UNSPECIFIED., .F., .F.,
 ( 4, 3, 4 ),
 ( 6.745041218394538905E-16, 0.02816610861753245793, 0.04000277880656290252 ),
 .UNSPECIFIED. ) ;
#2799=ORIENTED_EDGE ( 'NONE', *, *, #13654, .F. ) ;
#2800=DIRECTION ( 'NONE',  ( 0.000000000000000000, 0.000000000000000000, 1.000000000000000000 ) ) ;
#2801=AXIS2_PLACEMENT_3D ( 'NONE', #25808, #23379, #3630 ) ;
#2803=CARTESIAN_POINT ( 'NONE',  ( 1.832998868059858122, -84.86110816369524912, -117.7096351258396396 ) ) ;
#2804=CARTESIAN_POINT ( 'NONE',  ( 1.833485406944057594, 15.69895494453384721, 144.2578170162063884 ) ) ;
#2807=CARTESIAN_POINT ( 'NONE',  ( 1.833838850855489255, -72.47782099564557257, -125.7132320915355876 ) ) ;
#2808=CARTESIAN_POINT ( 'NONE',  ( 13.36082413113063083, 106.9547846563635431, 109.3026516754236184 ) ) ;
#2811=FACE_OUTER_BOUND ( 'NONE', #10078, .T. ) ;
#2812=CARTESIAN_POINT ( 'NONE',  ( 16.75465622695647738, -98.56308464785139734, 102.5353941815400418 ) ) ;
#2814=ORIENTED_EDGE ( 'NONE', *, *, #26216, .T. ) ;
#2816=CARTESIAN_POINT ( 'NONE',  ( 94.22246935314088034, 90.00000000000005684, -6.938893903907228378E-15 ) ) ;
#2817=CARTESIAN_POINT ( 'NONE',  ( 25.70243777736191859, 45.26941207740291873, 103.4793210720849004 ) ) ;
#2818=CARTESIAN_POINT ( 'NONE',  ( 25.65782528836477638, -84.30028114518222537, 75.12678957786475564 ) ) ;
#2821=EDGE_LOOP ( 'NONE', ( #19997, #20775, #3010, #19375 ) ) ;
#2822=DIRECTION ( 'NONE',  ( 0.000000000000000000, 0.000000000000000000, 1.000000000000000000 ) ) ;
#2823=VECTOR ( 'NONE', #4638, 1000.000000000000227 ) ;
#2824=CARTESIAN_POINT ( 'NONE',  ( 1.832998868059890096, 145.1092030902949830, 0.5339089137752738301 ) ) ;
#2826=ORIENTED_EDGE ( 'NONE', *, *, #21057, .T. ) ;
#2827=CARTESIAN_POINT ( 'NONE',  ( 1.832998868059890096, 97.49378069860942730, -107.4798986104850087 ) ) ;
#2828=CIRCLE ( 'NONE', #9742, 151.1787379149930359 ) ;
#2829=EDGE_LOOP ( 'NONE', ( #10399, #3790, #8937, #775 ) ) ;
#2830=CARTESIAN_POINT ( 'NONE',  ( 24.22246935314087324, 90.00000000000005684, 39.99999999999999289 ) ) ;
#2831=EDGE_CURVE ( 'NONE', #7680, #22569, #14980, .T. ) ;
#2832=CIRCLE ( 'NONE', #13394, 117.6351876552689504 ) ;
#2835=CARTESIAN_POINT ( 'NONE',  ( 109.1586059443104944, 0.002622205828288684017, 0.006570129623060880740 ) ) ;
#2836=ORIENTED_EDGE ( 'NONE', *, *, #2720, .F. ) ;
#2837=CARTESIAN_POINT ( 'NONE',  ( 32.73300124599735739, -44.31599526638029118, 108.9684813982487412 ) ) ;
#2839=ORIENTED_EDGE ( 'NONE', *, *, #8333, .T. ) ;
#2840=DIRECTION ( 'NONE',  ( -0.5946245182733607137, 0.08110646981860127058, -0.7999021332774015614 ) ) ;
#2841=DIRECTION ( 'NONE',  ( 0.000000000000000000, 0.000000000000000000, 1.000000000000000000 ) ) ;
#2845=CARTESIAN_POINT ( 'NONE',  ( 25.64681081121879203, 0.4157506337727869816, 112.9102952884414464 ) ) ;
#2847=CARTESIAN_POINT ( 'NONE',  ( 25.64681081121880624, 23.06870491922473931, -110.5293738517606243 ) ) ;
#2848=VERTEX_POINT ( 'NONE', #23936 ) ;
#2849=VECTOR ( 'NONE', #25234, 1000.000000000000341 ) ;
#2850=ORIENTED_EDGE ( 'NONE', *, *, #26796, .F. ) ;
#2851=ORIENTED_EDGE ( 'NONE', *, *, #17222, .T. ) ;
#2853=CARTESIAN_POINT ( 'NONE',  ( 26.11404676487259024, 45.01677474591551942, -103.8885755249565079 ) ) ;
#2854=CARTESIAN_POINT ( 'NONE',  ( 1.832998868059858122, 15.69902610990375713, 144.2584710144581095 ) ) ;
#2855=CARTESIAN_POINT ( 'NONE',  ( 25.64708228042121618, 75.52311986518023446, 83.93578330383108721 ) ) ;
#2858=CARTESIAN_POINT ( 'NONE',  ( 25.64692872815575342, -84.12425003484094077, 75.31297890941242201 ) ) ;
#2861=VERTEX_POINT ( 'NONE', #15540 ) ;
#2862=CARTESIAN_POINT ( 'NONE',  ( 2.430230287190592531, 132.3371620660959138, -60.50928654924622663 ) ) ;
#2863=CARTESIAN_POINT ( 'NONE',  ( 26.11404676487257603, 110.9778746459746941, 22.43340081644806006 ) ) ;
#2864=CARTESIAN_POINT ( 'NONE',  ( 25.64681081121880624, 11.38886654529674303, 112.3352186517031157 ) ) ;
#2868=EDGE_CURVE ( 'NONE', #10229, #9016, #15998, .T. ) ;
#2869=CARTESIAN_POINT ( 'NONE',  ( 25.65782528836481191, -75.12678957786447143, -84.30028114518245275 ) ) ;
#2871=CARTESIAN_POINT ( 'NONE',  ( 2.430230287190589422, -137.9371479820465254, 46.34481016236777862 ) ) ;
#2873=CARTESIAN_POINT ( 'NONE',  ( 30.59141879584294443, -44.78722686469137670, -107.2355637993506292 ) ) ;
#2875=CARTESIAN_POINT ( 'NONE',  ( 13.36082413113063083, -56.35051087435060424, 142.1654513177086301 ) ) ;
#2880=VERTEX_POINT ( 'NONE', #8660 ) ;
#2882=CARTESIAN_POINT ( 'NONE',  ( 25.64660436782539676, 56.95711784271983902, 97.49251393956794232 ) ) ;
#2884=CARTESIAN_POINT ( 'NONE',  ( 1.833485406944043827, 125.9346397303445286, -72.09189602597577107 ) ) ;
#2885=VERTEX_POINT ( 'NONE', #9087 ) ;
#2887=CARTESIAN_POINT ( 'NONE',  ( 25.98552792386798060, 45.02923844025622202, -103.7897946223260703 ) ) ;
#2890=ORIENTED_EDGE ( 'NONE', *, *, #9074, .F. ) ;
#2893=CARTESIAN_POINT ( 'NONE',  ( 5.340103579038181003, 2.303180387975235277, 147.4316330314912591 ) ) ;
#2894=CARTESIAN_POINT ( 'NONE',  ( 109.1589550718174877, 0.007359857714023718654, 0.001793588804091254558 ) ) ;
#2895=B_SPLINE_CURVE_WITH_KNOTS ( 'NONE', 3,
 ( #5873, #14632, #23431, #3695, #21257, #14773, #23584, #3844, #12609, #21395 ),
 .UNSPECIFIED., .F., .F.,
 ( 4, 3, 3, 4 ),
 ( 1.387778780781445676E-17, 0.0002669560319015968665, 0.0005492286108966422126, 0.0008315040496093392599 ),
 .UNSPECIFIED. ) ;
#2897=CARTESIAN_POINT ( 'NONE',  ( 2.433796855181205476, 109.1007109081238724, -96.28145139437575040 ) ) ;
#2898=AXIS2_PLACEMENT_3D ( 'NONE', #10997, #15291, #13006 ) ;
#2900=VERTEX_POINT ( 'NONE', #26491 ) ;
#2901=CARTESIAN_POINT ( 'NONE',  ( 25.65782528836479770, 84.30028114518268012, -75.12678957786421563 ) ) ;
#2903=AXIS2_PLACEMENT_3D ( 'NONE', #3556, #18970, #12337 ) ;
#2905=EDGE_CURVE ( 'NONE', #24611, #6748, #19418, .T. ) ;
#2910=ORIENTED_EDGE ( 'NONE', *, *, #166, .T. ) ;
#2912=PLANE ( 'NONE',  #14273 ) ;
#2913=ADVANCED_FACE ( 'NONE', ( #4620 ), #19608, .F. ) ;
#2914=B_SPLINE_CURVE_WITH_KNOTS ( 'NONE', 3,
 ( #24111, #25319, #5596, #18979 ),
 .UNSPECIFIED., .F., .F.,
 ( 4, 4 ),
 ( 2.938411120583618971E-16, 0.01077107486149829312 ),
 .UNSPECIFIED. ) ;
#2916=ORIENTED_EDGE ( 'NONE', *, *, #14570, .F. ) ;
#2917=VERTEX_POINT ( 'NONE', #6939 ) ;
#2918=CARTESIAN_POINT ( 'NONE',  ( 109.1624594426973118, -0.01405141589344819329, -0.007576898892907043756 ) ) ;
#2921=CARTESIAN_POINT ( 'NONE',  ( 28.43349137099833968, 46.80919715693054428, -115.0977416143052068 ) ) ;
#2922=CARTESIAN_POINT ( 'NONE',  ( 109.1586900883932856, 0.006819617742892441180, -0.002109621908824171194 ) ) ;
#2923=CARTESIAN_POINT ( 'NONE',  ( 26.11404676487257603, 22.43340081644767636, 110.9778746459747794 ) ) ;
#2925=DIRECTION ( 'NONE',  ( -1.000000000000000000, -0.000000000000000000, -0.000000000000000000 ) ) ;
#2927=B_SPLINE_CURVE_WITH_KNOTS ( 'NONE', 3,
 ( #7432, #9581, #18341, #27124, #1058, #23099, #1334 ),
 .UNSPECIFIED., .F., .F.,
 ( 4, 3, 4 ),
 ( 0.000000000000000000, 0.02398743853561339720, 0.04000277880656218088 ),
 .UNSPECIFIED. ) ;
#2928=CARTESIAN_POINT ( 'NONE',  ( 1.833838850093465700, -85.29338149487134046, -117.3962623502782918 ) ) ;
#2929=CARTESIAN_POINT ( 'NONE',  ( 8.186469829614351212, -118.7566730983342325, -90.56875932797710504 ) ) ;
#2932=CARTESIAN_POINT ( 'NONE',  ( 25.87036335909426654, -83.35447252092919257, 76.38467849957120848 ) ) ;
#2933=EDGE_CURVE ( 'NONE', #3608, #8194, #4681, .T. ) ;
#2934=CARTESIAN_POINT ( 'NONE',  ( 1.833206310202338374, 15.90849712171739405, 144.2348262833782542 ) ) ;
#2936=DIRECTION ( 'NONE',  ( -0.5946245182733607137, -0.7356888587241614541, -0.3243201896541662577 ) ) ;
#2937=DIRECTION ( 'NONE',  ( -1.000000000000000000, -0.000000000000000000, -0.000000000000000000 ) ) ;
#2939=CARTESIAN_POINT ( 'NONE',  ( 28.37599760073041821, -13.77583212279408720, 113.9023239246302523 ) ) ;
#2940=ORIENTED_EDGE ( 'NONE', *, *, #10678, .T. ) ;
#2941=CARTESIAN_POINT ( 'NONE',  ( 109.1586900883932856, -0.005236795036868191477, -0.004851151255031838257 ) ) ;
#2942=EDGE_CURVE ( 'NONE', #16635, #1896, #1216, .T. ) ;
#2943=CARTESIAN_POINT ( 'NONE',  ( 25.87036335909427720, 12.80197335559962468, 112.3329723497411408 ) ) ;
#2944=EDGE_LOOP ( 'NONE', ( #22047, #2129, #9802, #26217 ) ) ;
#2946=VERTEX_POINT ( 'NONE', #734 ) ;
#2948=B_SPLINE_CURVE_WITH_KNOTS ( 'NONE', 3,
 ( #26181, #2264, #24179, #8362, #23775, #21728 ),
 .UNSPECIFIED., .F., .F.,
 ( 4, 2, 4 ),
 ( 1.908688579121390716E-17, 0.0006311636237756899697, 0.001262327247551360641 ),
 .UNSPECIFIED. ) ;
#2949=B_SPLINE_CURVE_WITH_KNOTS ( 'NONE', 3,
 ( #21219, #18489, #27260, #27840, #7572, #16327 ),
 .UNSPECIFIED., .F., .F.,
 ( 4, 2, 4 ),
 ( 3.930079588515292562E-17, 0.0006311571484586184742, 0.001262314296917197484 ),
 .UNSPECIFIED. ) ;
#2950=( BOUNDED_SURFACE ( )  B_SPLINE_SURFACE ( 3, 1, ( 
 ( #20484, #18470 ),
 ( #18307, #20767 ),
 ( #9694, #24691 ),
 ( #24826, #907 ) ),
 .UNSPECIFIED., .F., .F., .F. ) 
 B_SPLINE_SURFACE_WITH_KNOTS ( ( 4, 4 ),
 ( 2, 2 ),
 ( 0.000000000000000000, 1.000000000000000000 ),
 ( 0.000000000000000000, 1.000000000000000000 ),
 .UNSPECIFIED. ) 
 GEOMETRIC_REPRESENTATION_ITEM ( )  RATIONAL_B_SPLINE_SURFACE ( (
 ( 1.000000000000000000, 1.000000000000000000),
 ( 0.6386103224230316178, 0.9954351624131538845),
 ( 0.6386103224230316178, 0.9954351624131538845),
 ( 1.000000000000000000, 1.000000000000000000) ) ) 
 REPRESENTATION_ITEM ( '' )  SURFACE ( )  );
#2951=CARTESIAN_POINT ( 'NONE',  ( 8.186469777910955870, 12.15801985874169056, -148.8557359139592506 ) ) ;
#2954=CARTESIAN_POINT ( 'NONE',  ( 1.834118845439484335, -132.6369225636078113, 58.85894970554871009 ) ) ;
#2955=CARTESIAN_POINT ( 'NONE',  ( 1.833691583653537238, 29.82175144858098648, 142.0122737882508943 ) ) ;
#2957=B_SPLINE_CURVE_WITH_KNOTS ( 'NONE', 3,
 ( #7837, #26944, #5665, #23239 ),
 .UNSPECIFIED., .F., .F.,
 ( 4, 4 ),
 ( 0.000000000000000000, 0.01077107196513799915 ),
 .UNSPECIFIED. ) ;
#2959=CARTESIAN_POINT ( 'NONE',  ( 109.1587776205901861, -0.002185517590237729887, 0.006995903587863968806 ) ) ;
#2962=CARTESIAN_POINT ( 'NONE',  ( 25.64681081121879203, -110.3564950173080206, -23.88203588908195130 ) ) ;
#2963=CARTESIAN_POINT ( 'NONE',  ( 28.37603512858450117, -78.09501335733530425, -84.05169593519805460 ) ) ;
#2965=ORIENTED_EDGE ( 'NONE', *, *, #23655, .T. ) ;
#2966=CARTESIAN_POINT ( 'NONE',  ( 1.834118845439484335, -145.1099497418795750, -0.1779704863085233013 ) ) ;
#2967=LINE ( 'NONE', #24850, #27207 ) ;
#2971=CARTESIAN_POINT ( 'NONE',  ( 109.1586900883932856, 0.0008465529156545837123, -0.007088091345232582462 ) ) ;
#2972=B_SPLINE_CURVE_WITH_KNOTS ( 'NONE', 3,
 ( #18754, #2934, #7696, #20910, #12277, #7395 ),
 .UNSPECIFIED., .F., .F.,
 ( 4, 2, 4 ),
 ( 1.042864983293993125E-17, 0.0006311571484586064396, 0.001262314296917202688 ),
 .UNSPECIFIED. ) ;
#2973=CARTESIAN_POINT ( 'NONE',  ( 28.37603512858360588, -113.9023475466375572, 13.77584568114256314 ) ) ;
#2974=VERTEX_POINT ( 'NONE', #15848 ) ;
#2975=ORIENTED_EDGE ( 'NONE', *, *, #23914, .T. ) ;
#2976=FACE_OUTER_BOUND ( 'NONE', #28445, .T. ) ;
#2977=CARTESIAN_POINT ( 'NONE',  ( 109.1778270068192853, 0.002542344697958587828, 0.008960903982060992520 ) ) ;
#2978=VERTEX_POINT ( 'NONE', #18273 ) ;
#2979=CARTESIAN_POINT ( 'NONE',  ( 25.64692872815577829, -97.94438212068862981, 56.17679456083764222 ) ) ;
#2980=ORIENTED_EDGE ( 'NONE', *, *, #13125, .F. ) ;
#2981=CARTESIAN_POINT ( 'NONE',  ( 109.1587776205901861, 0.007186028091168156912, 0.001442274044995822289 ) ) ;
#2982=ORIENTED_EDGE ( 'NONE', *, *, #9468, .T. ) ;
#2983=CARTESIAN_POINT ( 'NONE',  ( 10.93730112726006354, 145.2260730187408626, -42.00474393596100953 ) ) ;
#2985=ORIENTED_EDGE ( 'NONE', *, *, #12549, .T. ) ;
#2986=CARTESIAN_POINT ( 'NONE',  ( 32.73300124599737160, -117.3295799645428872, -8.473903470907334423 ) ) ;
#2987=ORIENTED_EDGE ( 'NONE', *, *, #14695, .T. ) ;
#2991=CARTESIAN_POINT ( 'NONE',  ( 1.833809397773861205, -125.7576368866148755, 72.40070666294548118 ) ) ;
#2992=ORIENTED_EDGE ( 'NONE', *, *, #20471, .T. ) ;
#2994=CARTESIAN_POINT ( 'NONE',  ( 10.93730112725990722, -136.0306644680979389, -65.95960219663263047 ) ) ;
#2996=CARTESIAN_POINT ( 'NONE',  ( 25.87036335909427720, 98.40409479825439121, 55.67065048714044195 ) ) ;
#2999=ORIENTED_EDGE ( 'NONE', *, *, #23329, .F. ) ;
#3000=VERTEX_POINT ( 'NONE', #20592 ) ;
#3002=CARTESIAN_POINT ( 'NONE',  ( 32.73300124599738581, 44.31599526638102304, -108.9684813982483860 ) ) ;
#3005=EDGE_CURVE ( 'NONE', #25954, #1001, #20128, .T. ) ;
#3006=CARTESIAN_POINT ( 'NONE',  ( 16.75465622695663725, 48.33695624543491931, -133.7599617830020122 ) ) ;
#3007=CARTESIAN_POINT ( 'NONE',  ( 1.833485406944043827, 144.3694338680884925, 14.63699153649408480 ) ) ;
#3009=CARTESIAN_POINT ( 'NONE',  ( 25.64700659047693065, 46.13293552475933978, -103.0567718204598435 ) ) ;
#3010=ORIENTED_EDGE ( 'NONE', *, *, #27252, .T. ) ;
#3012=CARTESIAN_POINT ( 'NONE',  ( 28.37599760073042532, 98.45181492308118720, 58.91309773266183925 ) ) ;
#3013=CARTESIAN_POINT ( 'NONE',  ( 25.64708228042121618, 11.76327187353814807, 112.2968511928420128 ) ) ;
#3014=CARTESIAN_POINT ( 'NONE',  ( 1.832998868059890096, 84.86110816369760812, -117.7096351258379343 ) ) ;
#3015=CARTESIAN_POINT ( 'NONE',  ( 26.11404676487257603, -47.08215554553588333, 102.9690087468800073 ) ) ;
#3016=CARTESIAN_POINT ( 'NONE',  ( 25.98552792386797705, -84.79516057869827250, -74.89816102339797510 ) ) ;
#3017=ORIENTED_EDGE ( 'NONE', *, *, #232, .T. ) ;
#3019=CARTESIAN_POINT ( 'NONE',  ( 24.01988960052061017, -100.1926921796488728, 84.46375358746880124 ) ) ;
#3020=B_SPLINE_CURVE_WITH_KNOTS ( 'NONE', 3,
 ( #999, #7207, #3304, #18561, #14084, #12088, #5019 ),
 .UNSPECIFIED., .F., .F.,
 ( 4, 3, 4 ),
 ( 3.555125210177727942E-17, 0.02816610861753246139, 0.04000277880656218782 ),
 .UNSPECIFIED. ) ;
#3021=CARTESIAN_POINT ( 'NONE',  ( 2.433796855181205476, -60.50726454507993424, 132.3327394885229182 ) ) ;
#3022=ORIENTED_EDGE ( 'NONE', *, *, #14591, .F. ) ;
#3027=CARTESIAN_POINT ( 'NONE',  ( 25.64681081121880624, -23.88203588908001507, -110.3564950173084185 ) ) ;
#3029=EDGE_CURVE ( 'NONE', #27652, #9673, #16279, .T. ) ;
#3030=CARTESIAN_POINT ( 'NONE',  ( 26.11404676487257603, 112.4785329405482059, 12.95861723607491456 ) ) ;
#3034=CARTESIAN_POINT ( 'NONE',  ( 1.833838850093477912, 44.84137955663405251, -138.0075868208081715 ) ) ;
#3037=CARTESIAN_POINT ( 'NONE',  ( 32.73300124599737870, 20.69176323058787759, -115.8010721414081132 ) ) ;
#3038=VERTEX_POINT ( 'NONE', #25648 ) ;
#3039=EDGE_CURVE ( 'NONE', #1356, #5719, #15940, .T. ) ;
#3042=CARTESIAN_POINT ( 'NONE',  ( 1.833485406944043827, 14.63699153649359452, 144.3694338680885778 ) ) ;
#3044=CARTESIAN_POINT ( 'NONE',  ( 26.11404676487257603, -113.2169081140374232, 1.130420376096734847 ) ) ;
#3045=CARTESIAN_POINT ( 'NONE',  ( 109.1589550718175161, -0.007507020724820348372, 0.001014448720249620404 ) ) ;
#3048=CARTESIAN_POINT ( 'NONE',  ( 1.833838850093465700, 59.02146106675083104, 132.5643635152036097 ) ) ;
#3049=CARTESIAN_POINT ( 'NONE',  ( 109.1587776205901861, 0.007328861771499511728, -8.330235398538848315E-05 ) ) ;
#3051=CARTESIAN_POINT ( 'NONE',  ( 2.430230287190572103, 144.5585181921885862, 16.65331920325788317 ) ) ;
#3052=CARTESIAN_POINT ( 'NONE',  ( 25.64660436782551400, -107.5626123667556442, -34.33930645842109897 ) ) ;
#3054=CARTESIAN_POINT ( 'NONE',  ( 25.87036335909427009, -57.38512068812939759, -97.41424496619579543 ) ) ;
#3056=ORIENTED_EDGE ( 'NONE', *, *, #27807, .T. ) ;
#3057=ORIENTED_EDGE ( 'NONE', *, *, #24283, .F. ) ;
#3060=CARTESIAN_POINT ( 'NONE',  ( 19.66333377628720314, 123.9466021833770526, 60.10102584214407528 ) ) ;
#3061=ADVANCED_FACE ( 'NONE', ( #21309 ), #5683, .F. ) ;
#3062=ADVANCED_FACE ( 'NONE', ( #5927 ), #14139, .T. ) ;
#3064=CARTESIAN_POINT ( 'NONE',  ( 1.894214914920914650, -14.22353624692096474, 144.4515288797483379 ) ) ;
#3066=ADVANCED_FACE ( 'NONE', ( #17126 ), #27959, .T. ) ;
#3067=CARTESIAN_POINT ( 'NONE',  ( 10.93730112725972070, -4.928439153521261495, 151.0983828010090804 ) ) ;
#3070=CARTESIAN_POINT ( 'NONE',  ( 109.1589550718174877, -0.007507020724817397607, -0.001014448720240716502 ) ) ;
#3071=EDGE_CURVE ( 'NONE', #2974, #18117, #17366, .T. ) ;
#3073=CARTESIAN_POINT ( 'NONE',  ( 25.64699802086727587, -75.72889180797064057, -83.75009658924072653 ) ) ;
#3074=CARTESIAN_POINT ( 'NONE',  ( 55.79472521941426777, 66.75682020267569783, -28.92526238350408008 ) ) ;
#3076=CARTESIAN_POINT ( 'NONE',  ( 109.1721716018069657, 0.005466227998629004728, 0.01616973485710952382 ) ) ;
#3077=CARTESIAN_POINT ( 'NONE',  ( 25.64692872815575342, 45.63107645358331155, 103.2799065540885834 ) ) ;
#3078=CARTESIAN_POINT ( 'NONE',  ( 28.37599760073041821, 100.2461467136618012, -55.80522390574013514 ) ) ;
#3079=CARTESIAN_POINT ( 'NONE',  ( 32.73300124599732186, 0.000000000000000000, 0.000000000000000000 ) ) ;
#3081=FACE_OUTER_BOUND ( 'NONE', #27655, .T. ) ;
#3083=CARTESIAN_POINT ( 'NONE',  ( 2.433796855181233454, -16.65276281464466024, -144.5536872373193660 ) ) ;
#3084=CARTESIAN_POINT ( 'NONE',  ( 25.73574536432414916, -12.61003673871966235, 112.2643803187784926 ) ) ;
#3086=ORIENTED_EDGE ( 'NONE', *, *, #17960, .T. ) ;
#3088=CARTESIAN_POINT ( 'NONE',  ( 26.11404676487257603, -97.48350837663569735, -57.58742681967552102 ) ) ;
#3089=CARTESIAN_POINT ( 'NONE',  ( 109.1586900883932856, 0.006757191295056129768, -0.002301750759607921679 ) ) ;
#3090=EDGE_CURVE ( 'NONE', #704, #2885, #27925, .T. ) ;
#3091=CARTESIAN_POINT ( 'NONE',  ( 10.93730112725932635, 0.000000000000000000, 0.000000000000000000 ) ) ;
#3092=DIRECTION ( 'NONE',  ( 0.000000000000000000, 0.000000000000000000, 1.000000000000000000 ) ) ;
#3094=EDGE_CURVE ( 'NONE', #13345, #18731, #9114, .T. ) ;
#3097=CARTESIAN_POINT ( 'NONE',  ( 9.884929003653626367, 103.8128997986857627, 109.0134320167736774 ) ) ;
#3098=CARTESIAN_POINT ( 'NONE',  ( 109.1586059443104944, -0.003294606663363280809, -0.006260042619939223604 ) ) ;
#3099=DIRECTION ( 'NONE',  ( 0.5946245182733607137, -0.2512550613902274632, 0.7637359336799379728 ) ) ;
#3101=ORIENTED_EDGE ( 'NONE', *, *, #2619, .F. ) ;
#3102=ORIENTED_EDGE ( 'NONE', *, *, #15067, .T. ) ;
#3103=CARTESIAN_POINT ( 'NONE',  ( 26.11404676487259024, 12.95861723607453619, 112.4785329405482628 ) ) ;
#3104=CARTESIAN_POINT ( 'NONE',  ( 5.340103556456544887, 62.06990747183869672, -133.7487107983438364 ) ) ;
#3105=CARTESIAN_POINT ( 'NONE',  ( 10.93730112725943293, 128.3908183996590537, 79.81734490845931873 ) ) ;
#3108=CARTESIAN_POINT ( 'NONE',  ( 30.59138290137886784, -111.3296280985501312, -33.33271994911455494 ) ) ;
#3110=CARTESIAN_POINT ( 'NONE',  ( 1.832998868059858122, 125.9352106559994127, -72.09222286250950162 ) ) ;
#3113=ORIENTED_EDGE ( 'NONE', *, *, #19740, .T. ) ;
#3114=CARTESIAN_POINT ( 'NONE',  ( 109.1778270068192853, -0.007152128381195992091, -0.005967275455179304154 ) ) ;
#3115=CARTESIAN_POINT ( 'NONE',  ( 25.73574536432415982, -112.4329083163019476, 11.00659994954114218 ) ) ;
#3116=B_SPLINE_CURVE_WITH_KNOTS ( 'NONE', 3,
 ( #18438, #16434, #25520, #23074, #11969, #1310, #7371, #20743 ),
 .UNSPECIFIED., .F., .F.,
 ( 4, 2, 2, 4 ),
 ( 3.469446951953614189E-18, 0.0002429588503611279356, 0.0004859177007222524017, 0.0009718354014444825772 ),
 .UNSPECIFIED. ) ;
#3117=CARTESIAN_POINT ( 'NONE',  ( 1.833206310202320388, -132.2594754479309245, 59.70089235435385433 ) ) ;
#3118=EDGE_LOOP ( 'NONE', ( #9560, #21723, #11395, #9807 ) ) ;
#3119=CARTESIAN_POINT ( 'NONE',  ( 1.832998868059890096, -45.34898734665952702, -137.8420662456174739 ) ) ;
#3121=CARTESIAN_POINT ( 'NONE',  ( 25.65782528836481191, -45.39960327191544565, -103.3897864210300810 ) ) ;
#3122=CARTESIAN_POINT ( 'NONE',  ( 32.73300124599738581, 3.836798148480494497, -117.5726003567928757 ) ) ;
#3124=ORIENTED_EDGE ( 'NONE', *, *, #26063, .F. ) ;
#3125=B_SPLINE_CURVE_WITH_KNOTS ( 'NONE', 3,
 ( #6709, #7416, #16182, #18324, #9566, #24989, #22828, #27104, #5245, #11869 ),
 .UNSPECIFIED., .F., .F.,
 ( 4, 3, 3, 4 ),
 ( 3.122502256758252770E-17, 0.0002669559177086159489, 0.0005339118354151012238, 0.001067817517169167719 ),
 .UNSPECIFIED. ) ;
#3127=EDGE_CURVE ( 'NONE', #4329, #10668, #6679, .T. ) ;
#3129=DIRECTION ( 'NONE',  ( 0.5946245182733607137, 0.5994612328333218665, -0.5357871896547430346 ) ) ;
#3131=EDGE_CURVE ( 'NONE', #14400, #14753, #1873, .T. ) ;
#3136=CARTESIAN_POINT ( 'NONE',  ( 2.433796855181205476, 107.1581411821785821, 98.43889364293895028 ) ) ;
#3137=ORIENTED_EDGE ( 'NONE', *, *, #4526, .F. ) ;
#3138=ORIENTED_EDGE ( 'NONE', *, *, #19330, .F. ) ;
#3139=VERTEX_POINT ( 'NONE', #3467 ) ;
#3140=CARTESIAN_POINT ( 'NONE',  ( 32.73300124599732186, 0.000000000000000000, 0.000000000000000000 ) ) ;
#3141=CARTESIAN_POINT ( 'NONE',  ( 1.833809397773830563, 107.9565774559024760, -96.96506043213346970 ) ) ;
#3142=CARTESIAN_POINT ( 'NONE',  ( 5.340103556456599954, 47.74933482044561828, -139.5040934094286911 ) ) ;
#3144=EDGE_CURVE ( 'NONE', #15935, #16104, #24222, .T. ) ;
#3147=EDGE_LOOP ( 'NONE', ( #27890, #19517, #27434, #12577 ) ) ;
#3149=CARTESIAN_POINT ( 'NONE',  ( 25.65782528836480125, -66.83837989650129430, 91.01210296572919844 ) ) ;
#3150=CARTESIAN_POINT ( 'NONE',  ( 109.1624594426973260, -0.01438905500501222109, -0.006914244825461785676 ) ) ;
#3153=CARTESIAN_POINT ( 'NONE',  ( 109.1721716018069515, -0.008708654716135843035, 0.01467989464938419288 ) ) ;
#3154=VERTEX_POINT ( 'NONE', #25780 ) ;
#3155=CARTESIAN_POINT ( 'NONE',  ( 25.69398547355842055, -12.54367966927970102, -112.2438548322124205 ) ) ;
#3157=CARTESIAN_POINT ( 'NONE',  ( 19.66333377628710011, -105.3186440504701125, 88.78556591841261536 ) ) ;
#3158=FACE_OUTER_BOUND ( 'NONE', #13040, .T. ) ;
#3159=VERTEX_POINT ( 'NONE', #2564 ) ;
#3161=VERTEX_POINT ( 'NONE', #10803 ) ;
#3162=EDGE_CURVE ( 'NONE', #20059, #23545, #13179, .T. ) ;
#3164=B_SPLINE_CURVE_WITH_KNOTS ( 'NONE', 3,
 ( #18329, #5836, #16330, #14159, #20791, #18927 ),
 .UNSPECIFIED., .F., .F.,
 ( 4, 2, 4 ),
 ( 8.239936510889833698E-18, 0.0006311636237756815130, 0.001262327247551354786 ),
 .UNSPECIFIED. ) ;
#3167=CLOSED_SHELL ( 'NONE', ( #18753, #4684, #22561, #27696, #11598, #26506, #7461, #16008, #9327, #16885, #16834, #22775, #20763, #6642, #18729, #23628, #8672, #27941, #12827, #25330, #21185, #19854, #25200, #8187, #8642, #8176, #3581, #6075, #3062, #25882, #1101, #13906, #7323, #16148, #15580, #4708, #2218, #24718, #12704, #2323, #18659, #7494, #8072, #14285, #5997, #26009, #5365, #18855, #11840, #8137, #4357, #19650, #20066, #18574, #15122, #751, #11151, #20659, #15636, #21842, #12574, #3066, #18459, #15255, #6582, #18763, #18811, #9280, #28479, #27051, #6381, #19809, #16253, #5568, #13477, #11668, #27335, #3678, #1211, #11744, #28209, #4000, #27883, #9234, #16179, #5093, #17129, #16936, #11575, #8033, #9503, #6285, #1150, #5910, #27254, #17820, #13023, #28274, #1569, #12932, #24520, #12897, #6813, #12764, #26962, #12811, #317, #15089, #17186, #8886, #13970, #14006, #27287, #9658, #17136, #3646, #14787, #14294, #26765, #12027, #11276, #22312, #25258, #3575, #24225, #4012, #26862, #19128, #10439, #19361, #27861, #2796, #11761, #20142, #19183, #12540, #19886, #4169, #13760, #4219, #6171, #14792, #23967, #26435, #20177, #3909, #20707, #21423, #5305, #5524, #4515, #1902, #17595, #5034, #15392, #23756, #21836, #14155, #4680, #21706, #25849, #12771, #9778, #10812, #19530, #22400, #4958, #21192, #3776, #11645, #13673, #2459, #3965, #171, #2043, #11464, #22912, #25171, #10442, #4899, #1187, #5859, #3487, #5344, #25911, #25335, #13060, #23294, #16734, #14878, #7973, #17910, #20923, #16261, #812, #15061, #1657, #9757, #11733, #22675, #16615, #9037, #4281, #16901, #23568, #17765, #21677, #27661, #4058, #14665, #4285, #13551, #903, #1029, #6606, #12192, #23937, #5833, #25749, #13057, #12877, #24812, #5029, #16316, #21957, #18629, #1796, #24686, #22048, #584, #953, #14495, #5096, #3323, #1439, #24096, #10423, #27929, #16699, #18919, #23624, #595, #21944, #7022, #13766, #12415, #11084, #25878, #22193, #4364, #24618, #9664, #9472, #23963, #8679, #21386, #22471, #17828, #24794, #8001, #15921, #20071, #2492, #9305, #9937, #7708, #13178, #2913, #23809, #15415, #26795, #26409, #25238, #15160, #11534, #27928, #15236, #16452, #8978, #13098, #15479, #9194, #5464, #7934, #14057, #14435, #4034, #26509, #27776, #4473, #26160, #14529, #27438, #19921, #25760, #20952, #6811, #21991, #8784, #18692, #16878, #4122, #21664, #25264, #1238, #12138, #6484, #5754, #9564, #5040, #15348, #11251, #27332, #4885, #22972, #12991, #20993, #7264, #17467, #14723, #4025, #3509, #486, #7002, #2007, #25974, #2759, #545, #5863, #20227, #2095, #2181, #2012, #15002, #15018, #783, #5240, #2384, #3061, #26241, #11436, #4973, #5133, #2165, #27030, #25048, #15029, #2784, #14858, #19469, #20202, #3356, #3457, #19081, #24091, #1117, #5672, #26866, #23995, #21166, #25376, #19052, #1880, #12043, #6706, #7389, #10107, #2016, #26511, #18526, #24840, #12678, #13093, #20349, #2557, #22430, #22475, #21455, #10401, #24040, #14031, #10646, #24982, #2103, #3877, #10303, #8616, #7612, #4296, #12349, #14218, #4541 ) ) ;
#3168=CARTESIAN_POINT ( 'NONE',  ( 24.01988960052065991, -73.52806416354015084, -108.4726924928705927 ) ) ;
#3169=CARTESIAN_POINT ( 'NONE',  ( 26.11404676487257603, -1.130420376097928115, 113.2169081140373947 ) ) ;
#3170=CARTESIAN_POINT ( 'NONE',  ( 10.93730112725982195, -145.2260730187404079, 42.00474393596209666 ) ) ;
#3171=CARTESIAN_POINT ( 'NONE',  ( 25.64699802086726876, 35.11755197949837992, 107.3112355540541643 ) ) ;
#3172=FACE_OUTER_BOUND ( 'NONE', #10825, .T. ) ;
#3176=FACE_OUTER_BOUND ( 'NONE', #8032, .T. ) ;
#3177=CARTESIAN_POINT ( 'NONE',  ( 28.43349137099832191, -76.27296957774061070, -98.08682467580860020 ) ) ;
#3178=DIRECTION ( 'NONE',  ( 0.000000000000000000, 0.000000000000000000, 1.000000000000000000 ) ) ;
#3179=CARTESIAN_POINT ( 'NONE',  ( 109.1586059443104944, 0.005555961672773770607, -0.004378796245590031722 ) ) ;
#3183=CARTESIAN_POINT ( 'NONE',  ( 109.1586900883932856, 0.005715190711481724431, -0.004277182003227242291 ) ) ;
#3184=B_SPLINE_CURVE_WITH_KNOTS ( 'NONE', 3,
 ( #19451, #28082, #14982, #14847 ),
 .UNSPECIFIED., .F., .F.,
 ( 4, 4 ),
 ( 3.254074918541991720E-16, 0.01077107486149803464 ),
 .UNSPECIFIED. ) ;
#3186=DIRECTION ( 'NONE',  ( 0.000000000000000000, 0.000000000000000000, 1.000000000000000000 ) ) ;
#3187=CARTESIAN_POINT ( 'NONE',  ( 25.64681081121879203, -110.3564950173083474, 23.88203588908045916 ) ) ;
#3189=ORIENTED_EDGE ( 'NONE', *, *, #4158, .T. ) ;
#3190=CARTESIAN_POINT ( 'NONE',  ( 1.833485406944057594, 145.1085452359073429, -0.5339064996889759662 ) ) ;
#3191=ORIENTED_EDGE ( 'NONE', *, *, #14098, .T. ) ;
#3192=ORIENTED_EDGE ( 'NONE', *, *, #24696, .T. ) ;
#3194=ORIENTED_EDGE ( 'NONE', *, *, #12570, .T. ) ;
#3195=CARTESIAN_POINT ( 'NONE',  ( 25.64681081121880624, 66.03065707438935306, 91.59071981940594753 ) ) ;
#3196=EDGE_CURVE ( 'NONE', #22961, #12630, #7044, .T. ) ;
#3197=( BOUNDED_SURFACE ( )  B_SPLINE_SURFACE ( 3, 1, ( 
 ( #23713, #21383 ),
 ( #12457, #27865 ),
 ( #8162, #10459 ),
 ( #25717, #6003 ) ),
 .UNSPECIFIED., .F., .F., .F. ) 
 B_SPLINE_SURFACE_WITH_KNOTS ( ( 4, 4 ),
 ( 2, 2 ),
 ( 0.000000000000000000, 1.000000000000000000 ),
 ( 0.000000000000000000, 1.000000000000000000 ),
 .UNSPECIFIED. ) 
 GEOMETRIC_REPRESENTATION_ITEM ( )  RATIONAL_B_SPLINE_SURFACE ( (
 ( 1.000000000000000000, 1.000000000000000000),
 ( 0.6386103224230316178, 0.9954351624131538845),
 ( 0.6386103224230316178, 0.9954351624131538845),
 ( 1.000000000000000000, 1.000000000000000000) ) ) 
 REPRESENTATION_ITEM ( '' )  SURFACE ( )  );
#3198=DIRECTION ( 'NONE',  ( 0.000000000000000000, 0.000000000000000000, 1.000000000000000000 ) ) ;
#3199=CARTESIAN_POINT ( 'NONE',  ( 32.73300124599732186, 0.000000000000000000, 0.000000000000000000 ) ) ;
#3202=CARTESIAN_POINT ( 'NONE',  ( 109.1587776205901861, -0.006305329297950526372, 0.003736572840496112016 ) ) ;
#3204=CARTESIAN_POINT ( 'NONE',  ( 6.224689322667630975, 12.92299475786958673, 147.4941644018828697 ) ) ;
#3205=CARTESIAN_POINT ( 'NONE',  ( 8.186469829614358318, -108.6390983847743854, -102.4860667297607222 ) ) ;
#3206=CARTESIAN_POINT ( 'NONE',  ( 1.833691583653525470, -85.00512109099176428, -117.6050685739178050 ) ) ;
#3207=CARTESIAN_POINT ( 'NONE',  ( 30.59141879584311852, -33.33270905817506957, -111.3296561588017113 ) ) ;
#3208=DIRECTION ( 'NONE',  ( -1.000000000000000000, -0.000000000000000000, -0.000000000000000000 ) ) ;
#3209=FACE_OUTER_BOUND ( 'NONE', #1734, .T. ) ;
#3211=CARTESIAN_POINT ( 'NONE',  ( 9.884929003653608603, -150.0922431698405717, 11.54837932062982198 ) ) ;
#3212=CARTESIAN_POINT ( 'NONE',  ( 6.224689322667630975, -100.9623537450659114, 108.2965163446070704 ) ) ;
#3213=CARTESIAN_POINT ( 'NONE',  ( 9.884929003653626367, 114.6392083957118047, 97.56484214660662246 ) ) ;
#3214=ORIENTED_EDGE ( 'NONE', *, *, #16014, .T. ) ;
#3216=EDGE_CURVE ( 'NONE', #6575, #15678, #5667, .T. ) ;
#3218=CARTESIAN_POINT ( 'NONE',  ( 1.831572820252008738, 138.3111855986067269, -43.90210991190477330 ) ) ;
#3219=ORIENTED_EDGE ( 'NONE', *, *, #26274, .T. ) ;
#3220=EDGE_CURVE ( 'NONE', #16392, #12695, #22447, .T. ) ;
#3221=EDGE_LOOP ( 'NONE', ( #10409, #1827, #15842, #20092 ) ) ;
#3222=EDGE_LOOP ( 'NONE', ( #23248, #16246, #21655, #23486 ) ) ;
#3223=EDGE_CURVE ( 'NONE', #4538, #14688, #17309, .T. ) ;
#3227=EDGE_CURVE ( 'NONE', #7560, #3533, #22492, .T. ) ;
#3228=DIRECTION ( 'NONE',  ( 0.5946245182733608248, -0.7999021332774035598, 0.08110646981858252169 ) ) ;
#3230=CARTESIAN_POINT ( 'NONE',  ( 24.01988960052059241, -129.8107982898200135, -17.94039809062754287 ) ) ;
#3232=CARTESIAN_POINT ( 'NONE',  ( 26.11404676487257603, -108.0249973236469572, 33.91085499298339556 ) ) ;
#3235=CARTESIAN_POINT ( 'NONE',  ( 25.70243777736188662, 35.59945151684219411, -107.1912711514951866 ) ) ;
#3238=CARTESIAN_POINT ( 'NONE',  ( 1.833485406944043827, -30.69200235379031838, 141.8265699653866250 ) ) ;
#3239=CARTESIAN_POINT ( 'NONE',  ( 2.263178113027039640, 60.41552743271138581, -132.2496129425953484 ) ) ;
#3240=CARTESIAN_POINT ( 'NONE',  ( 55.49584447822657296, 22.67407039687332215, -68.91748907713565586 ) ) ;
#3242=CIRCLE ( 'NONE', #20234, 117.6351876552689504 ) ;
#3244=ORIENTED_EDGE ( 'NONE', *, *, #9003, .F. ) ;
#3245=FACE_OUTER_BOUND ( 'NONE', #2739, .T. ) ;
#3246=LINE ( 'NONE', #18644, #27693 ) ;
#3247=B_SPLINE_CURVE_WITH_KNOTS ( 'NONE', 3,
 ( #23296, #1119, #18673, #12329, #7757, #20963, #3418 ),
 .UNSPECIFIED., .F., .F.,
 ( 4, 3, 4 ),
 ( 4.946183070983774510E-16, 0.02816610861753248568, 0.04000277880656268742 ),
 .UNSPECIFIED. ) ;
#3249=FACE_OUTER_BOUND ( 'NONE', #2821, .T. ) ;
#3252=CARTESIAN_POINT ( 'NONE',  ( 1.833691583653573209, 44.50270951807548414, 138.1170938425793224 ) ) ;
#3253=CARTESIAN_POINT ( 'NONE',  ( 25.64681081121879203, -35.28660243342475411, -107.2555980796244910 ) ) ;
#3254=CARTESIAN_POINT ( 'NONE',  ( 109.1592201516379674, 0.001934867487021726170, 0.007620268632971113378 ) ) ;
#3257=EDGE_CURVE ( 'NONE', #26408, #19554, #26588, .T. ) ;
#3259=CARTESIAN_POINT ( 'NONE',  ( 25.98107933586750917, -112.6229961579372230, 10.73978443746694289 ) ) ;
#3265=CARTESIAN_POINT ( 'NONE',  ( 109.1586059443104944, 0.001740416220259405171, 0.006856640434643077389 ) ) ;
#3266=AXIS2_PLACEMENT_3D ( 'NONE', #13498, #6894, #15223 ) ;
#3269=CARTESIAN_POINT ( 'NONE',  ( 25.64660436782558861, 112.3516544824819334, 11.22538561721926342 ) ) ;
#3270=ORIENTED_EDGE ( 'NONE', *, *, #20098, .T. ) ;
#3272=CARTESIAN_POINT ( 'NONE',  ( 30.59138290137872218, 101.9665464510086537, 55.75105126023953517 ) ) ;
#3274=CARTESIAN_POINT ( 'NONE',  ( 24.01988960052032951, 123.2441023955621091, 44.53753990739565438 ) ) ;
#3277=CARTESIAN_POINT ( 'NONE',  ( 1.833691583653537016, 85.58103979054644128, -117.1866391460177397 ) ) ;
#3280=ORIENTED_EDGE ( 'NONE', *, *, #7138, .T. ) ;
#3282=ORIENTED_EDGE ( 'NONE', *, *, #18431, .F. ) ;
#3284=CARTESIAN_POINT ( 'NONE',  ( 32.73300124599735028, 66.00340565729339914, 97.37344512919882789 ) ) ;
#3285=DIRECTION ( 'NONE',  ( 0.000000000000000000, 0.000000000000000000, 1.000000000000000000 ) ) ;
#3286=CARTESIAN_POINT ( 'NONE',  ( 2.433796855181205476, -142.0211193075553524, -31.67151202413115385 ) ) ;
#3287=VECTOR ( 'NONE', #5979, 1000.000000000000227 ) ;
#3288=CARTESIAN_POINT ( 'NONE',  ( 25.64681081121879203, -11.38886654529598275, -112.3352186517031726 ) ) ;
#3290=CARTESIAN_POINT ( 'NONE',  ( 1.833838850855487923, 107.7780290788696789, 97.16351016225925719 ) ) ;
#3291=CARTESIAN_POINT ( 'NONE',  ( 10.93730112725972781, -92.80059208661754155, 119.3442956573269100 ) ) ;
#3296=CARTESIAN_POINT ( 'NONE',  ( 25.73574536432414206, 74.99093179013968324, 84.49061642666495686 ) ) ;
#3297=CARTESIAN_POINT ( 'NONE',  ( 109.1586900883932856, 0.005371970278523967128, -0.004701023939953873770 ) ) ;
#3298=CARTESIAN_POINT ( 'NONE',  ( 8.186469829614264171, -122.8338389144551996, 84.95702201190503899 ) ) ;
#3299=EDGE_CURVE ( 'NONE', #7211, #22124, #6037, .T. ) ;
#3300=ORIENTED_EDGE ( 'NONE', *, *, #15709, .F. ) ;
#3301=CARTESIAN_POINT ( 'NONE',  ( 1.831572820252009626, -137.7011124121620469, 45.77972211429768379 ) ) ;
#3302=CARTESIAN_POINT ( 'NONE',  ( 28.37599760073042532, -45.02094138570515014, -105.5302221302111150 ) ) ;
#3304=CARTESIAN_POINT ( 'NONE',  ( 21.16825799904930605, 59.09063383105323908, 121.8625396241595240 ) ) ;
#3305=EDGE_CURVE ( 'NONE', #27642, #17966, #16686, .T. ) ;
#3307=ORIENTED_EDGE ( 'NONE', *, *, #4289, .T. ) ;
#3308=VECTOR ( 'NONE', #12721, 1000.000000000000000 ) ;
#3310=CARTESIAN_POINT ( 'NONE',  ( 109.1589550718174877, 0.0005685167901298389739, 0.007553890059312249293 ) ) ;
#3311=CIRCLE ( 'NONE', #6996, 117.6351876552689504 ) ;
#3312=CARTESIAN_POINT ( 'NONE',  ( 109.1721716018069515, -0.001984900887706775655, 0.01695288006056417870 ) ) ;
#3313=CARTESIAN_POINT ( 'NONE',  ( 25.64681081121879203, 97.57530875170684226, -56.81519825470653018 ) ) ;
#3314=CARTESIAN_POINT ( 'NONE',  ( 2.430230287190581429, 145.5073573687466819, 1.451610819318244650 ) ) ;
#3316=CARTESIAN_POINT ( 'NONE',  ( 25.87036335909429496, -45.07965203034989798, 103.6841944152904489 ) ) ;
#3317=ORIENTED_EDGE ( 'NONE', *, *, #26214, .T. ) ;
#3319=ORIENTED_EDGE ( 'NONE', *, *, #2099, .F. ) ;
#3321=FACE_OUTER_BOUND ( 'NONE', #24203, .T. ) ;
#3322=CARTESIAN_POINT ( 'NONE',  ( 109.1586059443104944, 0.004935564877218401141, -0.005067816690893759031 ) ) ;
#3323=ADVANCED_FACE ( 'NONE', ( #15951 ), #25528, .F. ) ;
#3328=DIRECTION ( 'NONE',  ( -1.000000000000000000, -0.000000000000000000, -0.000000000000000000 ) ) ;
#3332=VECTOR ( 'NONE', #3853, 1000.000000000000000 ) ;
#3333=VERTEX_POINT ( 'NONE', #25176 ) ;
#3334=CARTESIAN_POINT ( 'NONE',  ( 25.69398547355839213, -57.11291030433587679, -97.43788956976209192 ) ) ;
#3335=CARTESIAN_POINT ( 'NONE',  ( 32.73300124599739291, -105.8473486001047235, -51.32617430725011332 ) ) ;
#3338=VERTEX_POINT ( 'NONE', #9624 ) ;
#3339=CARTESIAN_POINT ( 'NONE',  ( 25.64670758986457955, -107.5375791514045574, 34.41755235608707864 ) ) ;
#3340=CARTESIAN_POINT ( 'NONE',  ( 32.73300124599732186, 0.000000000000000000, 0.000000000000000000 ) ) ;
#3342=CARTESIAN_POINT ( 'NONE',  ( 2.433796855181205476, -133.5135467655521779, 57.85512797797844087 ) ) ;
#3343=CARTESIAN_POINT ( 'NONE',  ( 1.833485406944057594, -125.9346397303430223, -72.09189602597842850 ) ) ;
#3344=AXIS2_PLACEMENT_3D ( 'NONE', #19606, #15272, #2316 ) ;
#3345=VECTOR ( 'NONE', #4434, 1000.000000000000000 ) ;
#3346=CARTESIAN_POINT ( 'NONE',  ( 16.05277956358235159, 142.9335921074867315, 10.32496049470132782 ) ) ;
#3347=CARTESIAN_POINT ( 'NONE',  ( 26.11404676487257603, 108.0249973236472130, -33.91085499298264239 ) ) ;
#3348=CARTESIAN_POINT ( 'NONE',  ( 8.186469777910776457, 49.43817851234059191, 140.9315935720371158 ) ) ;
#3349=EDGE_CURVE ( 'NONE', #3421, #2445, #11509, .T. ) ;
#3350=CARTESIAN_POINT ( 'NONE',  ( 10.93730112725990367, -142.1801301103781157, -51.37919228020433593 ) ) ;
#3353=EDGE_CURVE ( 'NONE', #11913, #4019, #14574, .T. ) ;
#3354=B_SPLINE_CURVE_WITH_KNOTS ( 'NONE', 3,
 ( #3681, #21521, #19220, #19360 ),
 .UNSPECIFIED., .F., .F.,
 ( 4, 4 ),
 ( 0.000000000000000000, 0.008383560773332708604 ),
 .UNSPECIFIED. ) ;
#3355=CARTESIAN_POINT ( 'NONE',  ( 26.11404676487259024, -83.38016054979834735, 76.59696442953165274 ) ) ;
#3356=ADVANCED_FACE ( 'NONE', ( #22595 ), #11545, .F. ) ;
#3357=CARTESIAN_POINT ( 'NONE',  ( 26.04756280548355463, -22.44333019059074985, 110.9306483680202007 ) ) ;
#3358=CARTESIAN_POINT ( 'NONE',  ( 109.1778270068192853, -0.004958088776549044938, -0.007885345421917355421 ) ) ;
#3359=B_SPLINE_CURVE_WITH_KNOTS ( 'NONE', 3,
 ( #16162, #5224, #13996, #16598, #22809, #20909, #1198 ),
 .UNSPECIFIED., .F., .F.,
 ( 4, 3, 4 ),
 ( 4.718224631282382674E-16, 0.02816610861753243364, 0.04000277880656261109 ),
 .UNSPECIFIED. ) ;
#3362=ORIENTED_EDGE ( 'NONE', *, *, #18564, .F. ) ;
#3365=ORIENTED_EDGE ( 'NONE', *, *, #19125, .F. ) ;
#3368=ORIENTED_EDGE ( 'NONE', *, *, #18461, .T. ) ;
#3369=( BOUNDED_SURFACE ( )  B_SPLINE_SURFACE ( 3, 1, ( 
 ( #24659, #7092 ),
 ( #20306, #15852 ),
 ( #5049, #20159 ),
 ( #13541, #4915 ) ),
 .UNSPECIFIED., .F., .F., .F. ) 
 B_SPLINE_SURFACE_WITH_KNOTS ( ( 4, 4 ),
 ( 2, 2 ),
 ( 0.000000000000000000, 1.000000000000000000 ),
 ( 0.000000000000000000, 1.000000000000000000 ),
 .UNSPECIFIED. ) 
 GEOMETRIC_REPRESENTATION_ITEM ( )  RATIONAL_B_SPLINE_SURFACE ( (
 ( 1.000000000000000000, 1.000000000000000000),
 ( 0.9956975270656955868, 0.8568959468854907557),
 ( 0.9956975270656955868, 0.8568959468854907557),
 ( 1.000000000000000000, 1.000000000000000000) ) ) 
 REPRESENTATION_ITEM ( '' )  SURFACE ( )  );
#3371=VECTOR ( 'NONE', #4270, 1000.000000000000114 ) ;
#3372=ORIENTED_EDGE ( 'NONE', *, *, #13795, .F. ) ;
#3373=CARTESIAN_POINT ( 'NONE',  ( 2.430230287190581429, -16.65331920325836634, 144.5585181921885294 ) ) ;
#3374=B_SPLINE_CURVE_WITH_KNOTS ( 'NONE', 3,
 ( #19117, #16679, #14643, #25473, #3562, #5747 ),
 .UNSPECIFIED., .F., .F.,
 ( 4, 2, 4 ),
 ( 1.344410693882025498E-17, 0.0006311636237756689362, 0.001262327247551324428 ),
 .UNSPECIFIED. ) ;
#3375=AXIS2_PLACEMENT_3D ( 'NONE', #16537, #22602, #5309 ) ;
#3376=LINE ( 'NONE', #12159, #17698 ) ;
#3381=CARTESIAN_POINT ( 'NONE',  ( 1.831572820252009626, -31.13525033585391100, -141.7320553118909174 ) ) ;
#3383=CARTESIAN_POINT ( 'NONE',  ( 2.108393763691196021, 57.92353377304286965, 133.2474712570796100 ) ) ;
#3384=EDGE_CURVE ( 'NONE', #4901, #342, #23517, .T. ) ;
#3385=ORIENTED_EDGE ( 'NONE', *, *, #10867, .F. ) ;
#3386=ORIENTED_EDGE ( 'NONE', *, *, #9896, .T. ) ;
#3387=CARTESIAN_POINT ( 'NONE',  ( 2.433796855181205476, 144.8571464219891141, -13.76554153471544417 ) ) ;
#3388=CARTESIAN_POINT ( 'NONE',  ( 25.64708010899965984, 66.32331961783506813, -91.37928813995102928 ) ) ;
#3390=CARTESIAN_POINT ( 'NONE',  ( 2.433796855181233454, 109.1007109081226076, 96.28145139437721411 ) ) ;
#3392=( NAMED_UNIT ( * ) PLANE_ANGLE_UNIT ( ) SI_UNIT ( $, .RADIAN. ) );
#3393=VERTEX_POINT ( 'NONE', #20124 ) ;
#3395=ORIENTED_EDGE ( 'NONE', *, *, #10331, .F. ) ;
#3396=CARTESIAN_POINT ( 'NONE',  ( 1.894214914920974380, 137.7482714433630520, -45.75988301372497347 ) ) ;
#3398=CARTESIAN_POINT ( 'NONE',  ( 10.93730112725990011, -146.7718404940640653, -36.23586118136687162 ) ) ;
#3399=ORIENTED_EDGE ( 'NONE', *, *, #672, .T. ) ;
#3401=DIRECTION ( 'NONE',  ( 0.5914120900931444380, -0.6942916636548135401, -0.4101107478122094641 ) ) ;
#3408=CARTESIAN_POINT ( 'NONE',  ( 109.1589550718174877, -0.004632048724973759565, 0.005994046294307789347 ) ) ;
#3409=B_SPLINE_CURVE_WITH_KNOTS ( 'NONE', 3,
 ( #5869, #10195, #23579, #969, #16661, #5426, #18669, #9905, #14628, #12466 ),
 .UNSPECIFIED., .F., .F.,
 ( 4, 3, 3, 4 ),
 ( 3.925231146709437917E-17, 0.0002669559177086530829, 0.0005339118354151471939, 0.001067817517169176392 ),
 .UNSPECIFIED. ) ;
#3410=B_SPLINE_CURVE_WITH_KNOTS ( 'NONE', 3,
 ( #9258, #6967, #24533, #4932, #11271, #8976, #2770 ),
 .UNSPECIFIED., .F., .F.,
 ( 4, 3, 4 ),
 ( 0.000000000000000000, 0.02398743853561340067, 0.04000277880656219476 ),
 .UNSPECIFIED. ) ;
#3412=EDGE_CURVE ( 'NONE', #2885, #16498, #2914, .T. ) ;
#3413=CARTESIAN_POINT ( 'NONE',  ( 13.36082413113061307, -94.94363694444135149, 119.8836995922723219 ) ) ;
#3414=CARTESIAN_POINT ( 'NONE',  ( 1.831572820252009626, 31.13525033585493418, 141.7320553118907185 ) ) ;
#3415=EDGE_CURVE ( 'NONE', #11749, #16457, #3618, .T. ) ;
#3416=ORIENTED_EDGE ( 'NONE', *, *, #27147, .T. ) ;
#3418=CARTESIAN_POINT ( 'NONE',  ( 32.73300124599737160, -117.3295799645428872, -8.473903470907334423 ) ) ;
#3419=CARTESIAN_POINT ( 'NONE',  ( 109.1778270068192853, 0.007885345421917369299, -0.004958088776549021519 ) ) ;
#3420=DIRECTION ( 'NONE',  ( 1.000000000000000000, 0.000000000000000000, 0.000000000000000000 ) ) ;
#3421=VERTEX_POINT ( 'NONE', #23180 ) ;
#3424=ORIENTED_EDGE ( 'NONE', *, *, #24280, .F. ) ;
#3426=CARTESIAN_POINT ( 'NONE',  ( 1.832998868059890096, -137.8420662456167065, -45.34898734666185049 ) ) ;
#3427=CARTESIAN_POINT ( 'NONE',  ( 2.430230287190589422, 16.65331920325738935, 144.5585181921886715 ) ) ;
#3435=ORIENTED_EDGE ( 'NONE', *, *, #22243, .T. ) ;
#3439=CARTESIAN_POINT ( 'NONE',  ( 109.1586900883932856, 0.004701023939953854688, 0.005371970278523982741 ) ) ;
#3440=CARTESIAN_POINT ( 'NONE',  ( 25.64681081121879203, -110.5293738517610080, 23.06870491922286348 ) ) ;
#3443=B_SPLINE_CURVE_WITH_KNOTS ( 'NONE', 3,
 ( #12890, #21535, #13171, #4261, #13042, #8587, #26140 ),
 .UNSPECIFIED., .F., .F.,
 ( 4, 3, 4 ),
 ( 3.642919299551294898E-17, 0.02816610861753245099, 0.04000277880656211149 ),
 .UNSPECIFIED. ) ;
#3444=CARTESIAN_POINT ( 'NONE',  ( 25.98552792386798771, 110.4352299692913419, -24.57669147553878020 ) ) ;
#3445=CARTESIAN_POINT ( 'NONE',  ( 6.224689322667647851, -57.86870174583520310, 136.2818611715188979 ) ) ;
#3446=ORIENTED_EDGE ( 'NONE', *, *, #815, .T. ) ;
#3448=CARTESIAN_POINT ( 'NONE',  ( 109.1592201516379674, -0.007856029051022764623, 0.0003082430542016628347 ) ) ;
#3449=CARTESIAN_POINT ( 'NONE',  ( 2.263178113027040972, 73.90841366068559637, -125.2099934853443415 ) ) ;
#3450=CARTESIAN_POINT ( 'NONE',  ( 1.832998868059858122, 108.1944082009157455, 96.70023740551157232 ) ) ;
#3451=CARTESIAN_POINT ( 'NONE',  ( 25.64708228042120197, -23.51409906510289005, 110.4357030047557231 ) ) ;
#3452=CARTESIAN_POINT ( 'NONE',  ( 28.43349137099834678, 58.58376153369862038, -109.5743306972600664 ) ) ;
#3453=CARTESIAN_POINT ( 'NONE',  ( 25.98552792386798060, 74.89816102339827353, -84.79516057869801671 ) ) ;
#3455=CARTESIAN_POINT ( 'NONE',  ( 8.186469777910909684, -77.65916160569824456, -127.5731248346295672 ) ) ;
#3456=DIRECTION ( 'NONE',  ( -1.000000000000000000, -0.000000000000000000, -0.000000000000000000 ) ) ;
#3457=ADVANCED_FACE ( 'NONE', ( #12346 ), #14482, .F. ) ;
#3459=CARTESIAN_POINT ( 'NONE',  ( 1.833603222531986487, -30.60504697399307261, 141.8454679205786420 ) ) ;
#3461=CARTESIAN_POINT ( 'NONE',  ( 55.79472521941426777, 23.17337251492855188, -68.96476385670641207 ) ) ;
#3462=EDGE_CURVE ( 'NONE', #213, #174, #10294, .T. ) ;
#3464=CARTESIAN_POINT ( 'NONE',  ( 109.1589550718175161, 0.007270618150635350940, 0.002126635388718555592 ) ) ;
#3467=CARTESIAN_POINT ( 'NONE',  ( 25.64681081121879203, 107.2555980796245905, -35.28660243342437752 ) ) ;
#3468=CARTESIAN_POINT ( 'NONE',  ( 1.831572820252008738, -137.7011124121613932, -45.77972211429954541 ) ) ;
#3469=DIRECTION ( 'NONE',  ( 0.5914120900931444380, -0.2415416038592965442, -0.7693434820005542463 ) ) ;
#3470=EDGE_LOOP ( 'NONE', ( #13657, #215, #12701, #12281 ) ) ;
#3471=CARTESIAN_POINT ( 'NONE',  ( 25.64699802086723679, -75.37548011155783456, 84.06830990999306152 ) ) ;
#3472=CARTESIAN_POINT ( 'NONE',  ( 109.1589550718174877, 0.004632048724973717932, -0.005994046294307822306 ) ) ;
#3473=ORIENTED_EDGE ( 'NONE', *, *, #13404, .T. ) ;
#3474=VERTEX_POINT ( 'NONE', #16530 ) ;
#3475=ORIENTED_EDGE ( 'NONE', *, *, #22028, .F. ) ;
#3476=CARTESIAN_POINT ( 'NONE',  ( 26.11404676487257603, -108.0249973236469572, 33.91085499298339556 ) ) ;
#3477=CARTESIAN_POINT ( 'NONE',  ( 109.1587776205901577, 0.007297420966928596861, -0.0006832286435102698360 ) ) ;
#3479=EDGE_CURVE ( 'NONE', #20262, #15935, #14841, .T. ) ;
#3480=B_SPLINE_CURVE_WITH_KNOTS ( 'NONE', 3,
 ( #15717, #4796, #468, #22362 ),
 .UNSPECIFIED., .F., .F.,
 ( 4, 4 ),
 ( 3.360511874109859618E-16, 0.01077107486149756280 ),
 .UNSPECIFIED. ) ;
#3485=CARTESIAN_POINT ( 'NONE',  ( 1.833721034905629654, 132.7087680342067983, 58.69612512971652052 ) ) ;
#3486=CARTESIAN_POINT ( 'NONE',  ( 25.64681081121879203, -84.18689316040098447, 75.24277141833462679 ) ) ;
#3487=ADVANCED_FACE ( 'NONE', ( #11420 ), #17418, .F. ) ;
#3490=CARTESIAN_POINT ( 'NONE',  ( 25.64681081121879203, 97.99105938548001404, -56.09509703373240797 ) ) ;
#3491=CARTESIAN_POINT ( 'NONE',  ( 109.1592201516379674, 0.001934867487012827689, -0.007620268632968149602 ) ) ;
#3494=CARTESIAN_POINT ( 'NONE',  ( 25.64681081121879203, -0.4157506337719985012, -112.9102952884414606 ) ) ;
#3496=CARTESIAN_POINT ( 'NONE',  ( 32.73300124599741423, 113.0038235389606314, -32.68291970228113996 ) ) ;
#3498=CARTESIAN_POINT ( 'NONE',  ( 9.884929003653626367, 35.39789245780329452, 146.3148513795968029 ) ) ;
#3501=CARTESIAN_POINT ( 'NONE',  ( 109.1589550718175161, -0.005477029346534963497, 0.005233222325307145852 ) ) ;
#3502=ORIENTED_EDGE ( 'NONE', *, *, #5174, .T. ) ;
#3503=B_SPLINE_CURVE_WITH_KNOTS ( 'NONE', 3,
 ( #21568, #10641, #5770, #19409, #14527, #4291, #17663, #21856, #6460, #13071 ),
 .UNSPECIFIED., .F., .F.,
 ( 4, 3, 3, 4 ),
 ( 3.469446951953614189E-17, 0.0002669559177086241347, 0.0005339118354150929838, 0.001067817517169170104 ),
 .UNSPECIFIED. ) ;
#3505=ORIENTED_EDGE ( 'NONE', *, *, #11144, .F. ) ;
#3506=EDGE_CURVE ( 'NONE', #16392, #15825, #496, .T. ) ;
#3509=ADVANCED_FACE ( 'NONE', ( #12693 ), #14660, .F. ) ;
#3511=CARTESIAN_POINT ( 'NONE',  ( 28.37599760073041821, -109.6580863494832272, 33.74340001061066374 ) ) ;
#3514=CARTESIAN_POINT ( 'NONE',  ( 2.063896406836605024, -145.2631347824382431, -1.344106060021882598 ) ) ;
#3515=CARTESIAN_POINT ( 'NONE',  ( 25.81918753295377300, -112.5005889664128631, -10.88546493098971268 ) ) ;
#3516=ORIENTED_EDGE ( 'NONE', *, *, #5650, .T. ) ;
#3518=CARTESIAN_POINT ( 'NONE',  ( 25.64699802086727587, -107.4581924007662082, -34.66526531169749603 ) ) ;
#3520=CARTESIAN_POINT ( 'NONE',  ( 109.1586900883932856, -0.005371970278528676035, -0.004701023939945692814 ) ) ;
#3522=B_SPLINE_CURVE_WITH_KNOTS ( 'NONE', 3,
 ( #27917, #16273, #25355, #16419 ),
 .UNSPECIFIED., .F., .F.,
 ( 4, 4 ),
 ( 0.000000000000000000, 0.008383560773332699931 ),
 .UNSPECIFIED. ) ;
#3523=CARTESIAN_POINT ( 'NONE',  ( 2.430230287190589422, -1.451610819316722312, -145.5073573687467103 ) ) ;
#3525=( BOUNDED_SURFACE ( )  B_SPLINE_SURFACE ( 3, 1, ( 
 ( #13622, #11615 ),
 ( #2686, #20236 ),
 ( #674, #9323 ),
 ( #25582, #10461 ) ),
 .UNSPECIFIED., .F., .F., .F. ) 
 B_SPLINE_SURFACE_WITH_KNOTS ( ( 4, 4 ),
 ( 2, 2 ),
 ( 0.000000000000000000, 1.000000000000000000 ),
 ( 0.000000000000000000, 1.000000000000000000 ),
 .UNSPECIFIED. ) 
 GEOMETRIC_REPRESENTATION_ITEM ( )  RATIONAL_B_SPLINE_SURFACE ( (
 ( 1.000000000000000000, 1.000000000000000000),
 ( 0.9960225298536222738, 0.9999952330161893110),
 ( 0.9960225298536222738, 0.9999952330161893110),
 ( 1.000000000000000000, 1.000000000000000000) ) ) 
 REPRESENTATION_ITEM ( '' )  SURFACE ( )  );
#3526=VERTEX_POINT ( 'NONE', #10549 ) ;
#3528=CARTESIAN_POINT ( 'NONE',  ( 6.224689322667630975, 43.30635742325379312, 141.5842213414014736 ) ) ;
#3529=CARTESIAN_POINT ( 'NONE',  ( 1.833691583653539903, -15.52203496789013748, 144.2771263798446739 ) ) ;
#3530=ORIENTED_EDGE ( 'NONE', *, *, #8951, .T. ) ;
#3531=CARTESIAN_POINT ( 'NONE',  ( 25.64681081121879203, -97.57530875170644435, 56.81519825470720519 ) ) ;
#3533=VERTEX_POINT ( 'NONE', #10291 ) ;
#3535=EDGE_CURVE ( 'NONE', #15977, #5184, #2415, .T. ) ;
#3536=EDGE_CURVE ( 'NONE', #16728, #27632, #25901, .T. ) ;
#3538=VERTEX_POINT ( 'NONE', #12410 ) ;
#3539=DIRECTION ( 'NONE',  ( 0.5946245182733607137, -0.7870422510449677223, 0.1642747008466114989 ) ) ;
#3542=CARTESIAN_POINT ( 'NONE',  ( 32.73300124599732186, 0.000000000000000000, 0.000000000000000000 ) ) ;
#3543=CARTESIAN_POINT ( 'NONE',  ( 1.894214914920972603, 138.3376769255508520, 43.94587946447450832 ) ) ;
#3545=CARTESIAN_POINT ( 'NONE',  ( 10.93730112725936898, 142.1801301103782578, 51.37919228020297879 ) ) ;
#3547=CARTESIAN_POINT ( 'NONE',  ( 2.430230287190572103, -13.76600171652544624, -144.8619874886008176 ) ) ;
#3551=ORIENTED_EDGE ( 'NONE', *, *, #1109, .F. ) ;
#3552=B_SPLINE_CURVE_WITH_KNOTS ( 'NONE', 3,
 ( #18730, #24935, #27060, #5486 ),
 .UNSPECIFIED., .F., .F.,
 ( 4, 4 ),
 ( 1.606470082347908540E-16, 0.008383748772659627146 ),
 .UNSPECIFIED. ) ;
#3554=ORIENTED_EDGE ( 'NONE', *, *, #24357, .T. ) ;
#3555=LINE ( 'NONE', #20969, #19339 ) ;
#3556=CARTESIAN_POINT ( 'NONE',  ( 10.93730112725932635, 0.000000000000000000, 0.000000000000000000 ) ) ;
#3558=CARTESIAN_POINT ( 'NONE',  ( 2.433796855181205476, 46.34326152018925171, -137.9325382748280333 ) ) ;
#3562=CARTESIAN_POINT ( 'NONE',  ( 1.833206308920056538, 71.90885838897399651, 126.0392061186624773 ) ) ;
#3563=CARTESIAN_POINT ( 'NONE',  ( 109.1586900883932856, -0.005371970278528676035, -0.004701023939945692814 ) ) ;
#3565=CARTESIAN_POINT ( 'NONE',  ( 9.884929003653608603, 139.1775604444711973, -57.36421526887020406 ) ) ;
#3569=CARTESIAN_POINT ( 'NONE',  ( 109.1586900883932856, -0.002995460350180849298, 0.006479576224403778457 ) ) ;
#3571=CARTESIAN_POINT ( 'NONE',  ( 1.833485406944043827, -108.1939177044932592, 96.69979900902130510 ) ) ;
#3572=CARTESIAN_POINT ( 'NONE',  ( 25.69398547355841345, -84.42756928260523352, -75.02007992711791928 ) ) ;
#3573=ORIENTED_EDGE ( 'NONE', *, *, #10163, .F. ) ;
#3574=CARTESIAN_POINT ( 'NONE',  ( 10.93730112726002623, 65.95960219663321311, -136.0306644680977683 ) ) ;
#3575=ADVANCED_FACE ( 'NONE', ( #21201 ), #26250, .F. ) ;
#3576=CARTESIAN_POINT ( 'NONE',  ( 1.833485406944043827, 144.3694338680886915, -14.63699153649211127 ) ) ;
#3577=CARTESIAN_POINT ( 'NONE',  ( 16.05277956358197144, 128.9466020665984161, -62.52511797225994172 ) ) ;
#3578=EDGE_CURVE ( 'NONE', #5939, #2880, #26079, .T. ) ;
#3581=ADVANCED_FACE ( 'NONE', ( #10419 ), #19445, .T. ) ;
#3582=CARTESIAN_POINT ( 'NONE',  ( 26.11404676487257603, -67.46175819463425682, 90.92995828888176391 ) ) ;
#3583=FACE_OUTER_BOUND ( 'NONE', #24155, .T. ) ;
#3586=CARTESIAN_POINT ( 'NONE',  ( 2.430230287190592531, -145.5073573687466819, 1.451610819317235013 ) ) ;
#3587=CARTESIAN_POINT ( 'NONE',  ( 1.833838848569431246, 137.9525894882063426, -45.01064392477788800 ) ) ;
#3588=CARTESIAN_POINT ( 'NONE',  ( 19.66333377628701840, 99.30798531455356226, 95.46107873288919166 ) ) ;
#3590=LINE ( 'NONE', #5216, #22185 ) ;
#3591=AXIS2_PLACEMENT_3D ( 'NONE', #3601, #12799, #16566 ) ;
#3592=CARTESIAN_POINT ( 'NONE',  ( 2.108393763691167155, -16.46048390411897344, 144.3574619851892180 ) ) ;
#3593=ORIENTED_EDGE ( 'NONE', *, *, #19676, .F. ) ;
#3594=ORIENTED_EDGE ( 'NONE', *, *, #22532, .F. ) ;
#3596=CARTESIAN_POINT ( 'NONE',  ( 10.93730112725990367, -92.80059208661606363, -119.3442956573281748 ) ) ;
#3598=CARTESIAN_POINT ( 'NONE',  ( 2.430230287190581429, 137.9371479820462696, 46.34481016236870943 ) ) ;
#3599=CARTESIAN_POINT ( 'NONE',  ( 55.79472521941426777, 72.27573336313952268, 8.328398066092010055 ) ) ;
#3601=CARTESIAN_POINT ( 'NONE',  ( 10.93730112725932635, 0.000000000000000000, 0.000000000000000000 ) ) ;
#3602=CARTESIAN_POINT ( 'NONE',  ( 21.16825799904904315, -59.09063383105261380, -121.8625396241603056 ) ) ;
#3603=CARTESIAN_POINT ( 'NONE',  ( 109.1592201516379674, 0.007566779963318552571, -0.002134489919774391464 ) ) ;
#3606=CARTESIAN_POINT ( 'NONE',  ( 55.49584447822657296, 62.96491934286042635, -36.04376091928477166 ) ) ;
#3607=CARTESIAN_POINT ( 'NONE',  ( 16.75465622695661239, -140.0080030360328180, 25.01894884133809427 ) ) ;
#3608=VERTEX_POINT ( 'NONE', #17429 ) ;
#3609=CARTESIAN_POINT ( 'NONE',  ( 2.263178607246689733, -46.26071628252355339, -137.8402782326816123 ) ) ;
#3610=CARTESIAN_POINT ( 'NONE',  ( 32.73300124599735739, 51.32617430724909013, 105.8473486001052777 ) ) ;
#3611=ORIENTED_EDGE ( 'NONE', *, *, #223, .T. ) ;
#3614=ORIENTED_EDGE ( 'NONE', *, *, #8710, .F. ) ;
#3617=EDGE_CURVE ( 'NONE', #8000, #11148, #8373, .T. ) ;
#3618=B_SPLINE_CURVE_WITH_KNOTS ( 'NONE', 3,
 ( #15295, #27758, #23447, #20852, #8555, #3710 ),
 .UNSPECIFIED., .F., .F.,
 ( 4, 2, 4 ),
 ( 9.875766617722657020E-18, 0.0006311571484586093669, 0.001262314296917208976 ),
 .UNSPECIFIED. ) ;
#3620=CARTESIAN_POINT ( 'NONE',  ( 32.73300124599741423, -92.86301839379967760, -72.21147546950645335 ) ) ;
#3621=CARTESIAN_POINT ( 'NONE',  ( 55.49584447822657296, -14.82242356767884672, -71.02133150427270891 ) ) ;
#3622=CARTESIAN_POINT ( 'NONE',  ( 109.1624594426973118, -0.01263706729759551950, 0.009754804742280919622 ) ) ;
#3624=CARTESIAN_POINT ( 'NONE',  ( 109.1721716018069657, 0.009868622090676173672, -0.01392660302850758265 ) ) ;
#3625=DIRECTION ( 'NONE',  ( 0.000000000000000000, 0.000000000000000000, 1.000000000000000000 ) ) ;
#3626=DIRECTION ( 'NONE',  ( -1.000000000000000000, -0.000000000000000000, -0.000000000000000000 ) ) ;
#3628=CARTESIAN_POINT ( 'NONE',  ( 25.64681081121879203, -12.21581276189883170, 112.2483031020013016 ) ) ;
#3629=CARTESIAN_POINT ( 'NONE',  ( 25.64681081121879203, -112.9102952884414464, -0.4157506337739698132 ) ) ;
#3630=DIRECTION ( 'NONE',  ( 0.000000000000000000, 0.000000000000000000, 1.000000000000000000 ) ) ;
#3631=CARTESIAN_POINT ( 'NONE',  ( 13.36082413113061307, -151.2941478187906341, -22.28175172543715732 ) ) ;
#3632=CARTESIAN_POINT ( 'NONE',  ( 2.433796855181233454, 125.2830755159764777, -74.00833731765430912 ) ) ;
#3634=CARTESIAN_POINT ( 'NONE',  ( 1.833485406944043827, -0.5339064996894915538, 145.1085452359073145 ) ) ;
#3635=ORIENTED_EDGE ( 'NONE', *, *, #19535, .T. ) ;
#3637=CARTESIAN_POINT ( 'NONE',  ( 32.73300124599735739, -20.69176323058707823, 115.8010721414082980 ) ) ;
#3638=CARTESIAN_POINT ( 'NONE',  ( 1.832998868059858122, 138.1720401012273101, -44.33343224355090939 ) ) ;
#3640=ORIENTED_EDGE ( 'NONE', *, *, #10331, .T. ) ;
#3641=EDGE_CURVE ( 'NONE', #27505, #2120, #5290, .T. ) ;
#3642=EDGE_LOOP ( 'NONE', ( #11235, #26460, #7786, #1287 ) ) ;
#3643=B_SPLINE_CURVE_WITH_KNOTS ( 'NONE', 3,
 ( #13570, #26949, #19912, #11280, #22373, #15573, #17604, #26387 ),
 .UNSPECIFIED., .F., .F.,
 ( 4, 2, 2, 4 ),
 ( 0.000000000000000000, 0.0002429588503611229482, 0.0004859177007222458965, 0.0009718354014444972140 ),
 .UNSPECIFIED. ) ;
#3646=ADVANCED_FACE ( 'NONE', ( #2164 ), #6770, .F. ) ;
#3647=VECTOR ( 'NONE', #5153, 1000.000000000000114 ) ;
#3648=CARTESIAN_POINT ( 'NONE',  ( 2.433796855181219243, -74.00833731765649759, 125.2830755159751703 ) ) ;
#3649=B_SPLINE_CURVE_WITH_KNOTS ( 'NONE', 3,
 ( #13742, #22549, #15330, #2817, #11592, #20370, #19794, #18201 ),
 .UNSPECIFIED., .F., .F.,
 ( 4, 2, 2, 4 ),
 ( 6.938893903907228378E-18, 0.0002429588503611282337, 0.0004859177007222495286, 0.0009718354014444800836 ),
 .UNSPECIFIED. ) ;
#3653=DIRECTION ( 'NONE',  ( 0.000000000000000000, 0.000000000000000000, -1.000000000000000000 ) ) ;
#3655=CARTESIAN_POINT ( 'NONE',  ( 2.430230287190589422, -31.67257033707400637, -142.0258656395025412 ) ) ;
#3656=CARTESIAN_POINT ( 'NONE',  ( 1.893872463202053824, 58.16604752596723671, 132.9857054814982291 ) ) ;
#3657=DIRECTION ( 'NONE',  ( 0.5914120900931444380, -0.7643865440136106137, -0.2567974902965117767 ) ) ;
#3658=VERTEX_POINT ( 'NONE', #15853 ) ;
#3660=ORIENTED_EDGE ( 'NONE', *, *, #21996, .F. ) ;
#3661=CARTESIAN_POINT ( 'NONE',  ( 25.64692872815573210, -107.2850779876532101, -35.19724814978025051 ) ) ;
#3662=CARTESIAN_POINT ( 'NONE',  ( 2.108393763691184919, 144.6252321290184284, -13.91282116576829608 ) ) ;
#3664=DIRECTION ( 'NONE',  ( 0.000000000000000000, 0.000000000000000000, 1.000000000000000000 ) ) ;
#3665=DIRECTION ( 'NONE',  ( -1.000000000000000000, -0.000000000000000000, -0.000000000000000000 ) ) ;
#3666=CARTESIAN_POINT ( 'NONE',  ( 1.833206310202337042, 96.54250248081145003, -108.3342540861869168 ) ) ;
#3668=VERTEX_POINT ( 'NONE', #26780 ) ;
#3669=DIRECTION ( 'NONE',  ( -1.000000000000000000, -0.000000000000000000, -0.000000000000000000 ) ) ;
#3670=CARTESIAN_POINT ( 'NONE',  ( 26.04756280548353686, -36.02883009343563714, -107.2904246402798663 ) ) ;
#3671=CARTESIAN_POINT ( 'NONE',  ( 25.64681081121879203, -66.03065707438874199, -91.59071981940638807 ) ) ;
#3673=VERTEX_POINT ( 'NONE', #7094 ) ;
#3674=EDGE_CURVE ( 'NONE', #10482, #16310, #4916, .T. ) ;
#3676=B_SPLINE_CURVE_WITH_KNOTS ( 'NONE', 3,
 ( #1057, #3357, #22665, #12144, #18614, #1199, #9845, #27384 ),
 .UNSPECIFIED., .F., .F.,
 ( 4, 2, 2, 4 ),
 ( 3.469446951953614189E-18, 0.0002429592666046704447, 0.0004859185332093374199, 0.0009718370664186920787 ),
 .UNSPECIFIED. ) ;
#3678=ADVANCED_FACE ( 'NONE', ( #11527 ), #6941, .F. ) ;
#3679=ORIENTED_EDGE ( 'NONE', *, *, #12290, .T. ) ;
#3680=VERTEX_POINT ( 'NONE', #18144 ) ;
#3681=CARTESIAN_POINT ( 'NONE',  ( 26.11404676487257603, -1.130420376097928115, 113.2169081140373947 ) ) ;
#3682=ORIENTED_EDGE ( 'NONE', *, *, #24001, .F. ) ;
#3683=CARTESIAN_POINT ( 'NONE',  ( 109.1586900883932856, 0.007109207791180751322, 0.0006456433529069300226 ) ) ;
#3684=CARTESIAN_POINT ( 'NONE',  ( 26.11404676487257603, 112.7148551500680469, 10.71016160607605627 ) ) ;
#3685=VECTOR ( 'NONE', #23861, 1000.000000000000114 ) ;
#3689=CARTESIAN_POINT ( 'NONE',  ( 2.263178113027048521, -60.41552743271048342, 132.2496129425957747 ) ) ;
#3691=CARTESIAN_POINT ( 'NONE',  ( 25.98107933586724982, -47.01057192495340331, 102.9042679418247417 ) ) ;
#3693=( BOUNDED_SURFACE ( )  B_SPLINE_SURFACE ( 3, 1, ( 
 ( #12042, #22713 ),
 ( #2981, #5854 ),
 ( #27429, #23415 ),
 ( #25575, #27860 ) ),
 .UNSPECIFIED., .F., .F., .F. ) 
 B_SPLINE_SURFACE_WITH_KNOTS ( ( 4, 4 ),
 ( 2, 2 ),
 ( 0.000000000000000000, 1.000000000000000000 ),
 ( 0.000000000000000000, 1.000000000000000000 ),
 .UNSPECIFIED. ) 
 GEOMETRIC_REPRESENTATION_ITEM ( )  RATIONAL_B_SPLINE_SURFACE ( (
 ( 1.000000000000000000, 1.000000000000000000),
 ( 0.9956975270656955868, 0.8568959468854907557),
 ( 0.9956975270656955868, 0.8568959468854907557),
 ( 1.000000000000000000, 1.000000000000000000) ) ) 
 REPRESENTATION_ITEM ( '' )  SURFACE ( )  );
#3694=CARTESIAN_POINT ( 'NONE',  ( 28.37599760073042887, -105.5302221302109729, 45.02094138570548409 ) ) ;
#3695=CARTESIAN_POINT ( 'NONE',  ( 25.64703792032470631, -97.85829113439916682, -56.32669596053541028 ) ) ;
#3698=ORIENTED_EDGE ( 'NONE', *, *, #21079, .T. ) ;
#3699=ORIENTED_EDGE ( 'NONE', *, *, #25952, .F. ) ;
#3700=CARTESIAN_POINT ( 'NONE',  ( 8.186469777910943435, -49.43817851233971084, -140.9315935720375421 ) ) ;
#3702=CARTESIAN_POINT ( 'NONE',  ( 109.1586900883932856, -0.007109207791180745251, -0.0006456433529069797875 ) ) ;
#3703=CARTESIAN_POINT ( 'NONE',  ( 16.75465622695653423, 53.58152542127676554, 131.7467602971410656 ) ) ;
#3705=EDGE_LOOP ( 'NONE', ( #13581, #9028, #12256, #23948 ) ) ;
#3710=CARTESIAN_POINT ( 'NONE',  ( 2.433796855181233454, -1.451562450948615135, -145.5024947199069913 ) ) ;
#3712=CARTESIAN_POINT ( 'NONE',  ( 25.64670758986457599, -66.76959937251515953, 91.05338785329418272 ) ) ;
#3713=CARTESIAN_POINT ( 'NONE',  ( 6.224689322667647851, 97.14981701196477104, -111.7293398381254974 ) ) ;
#3716=CARTESIAN_POINT ( 'NONE',  ( 109.1592201516379674, 0.006957642258155071965, 0.003661068210032695190 ) ) ;
#3717=CARTESIAN_POINT ( 'NONE',  ( 32.73300124599735739, 75.82012867748483131, 89.94078864464094636 ) ) ;
#3718=AXIS2_PLACEMENT_3D ( 'NONE', #18897, #27669, #3625 ) ;
#3719=ORIENTED_EDGE ( 'NONE', *, *, #24230, .T. ) ;
#3722=CARTESIAN_POINT ( 'NONE',  ( 109.1721716018069515, -0.01665253177025269662, -0.003746085893651981968 ) ) ;
#3723=AXIS2_PLACEMENT_3D ( 'NONE', #27035, #24914, #13952 ) ;
#3724=CARTESIAN_POINT ( 'NONE',  ( 1.833485406944057594, -137.8414413349088932, 45.34878176254188276 ) ) ;
#3725=ORIENTED_EDGE ( 'NONE', *, *, #21466, .T. ) ;
#3727=ORIENTED_EDGE ( 'NONE', *, *, #13944, .F. ) ;
#3729=EDGE_LOOP ( 'NONE', ( #6444, #19866, #25623, #2355 ) ) ;
#3730=CARTESIAN_POINT ( 'NONE',  ( 2.263178607246678187, -71.48082837426089498, 126.6115608827435892 ) ) ;
#3732=CONICAL_SURFACE ( 'NONE', #4180, 117.6351876552689504, 0.9945805576725580410 ) ;
#3733=FACE_OUTER_BOUND ( 'NONE', #19088, .T. ) ;
#3735=CARTESIAN_POINT ( 'NONE',  ( 28.37644542392843405, 123.1691345231582773, 17.02293047611404475 ) ) ;
#3738=CARTESIAN_POINT ( 'NONE',  ( 32.73300124599735739, -55.46353551262085091, 103.7392577722174565 ) ) ;
#3739=CARTESIAN_POINT ( 'NONE',  ( 10.93730112725985926, -150.7858122213662853, 10.89264110824944609 ) ) ;
#3741=( BOUNDED_SURFACE ( )  B_SPLINE_SURFACE ( 3, 1, ( 
 ( #2090, #19653 ),
 ( #3980, #26280 ),
 ( #6577, #15328 ),
 ( #12476, #10475 ) ),
 .UNSPECIFIED., .F., .F., .F. ) 
 B_SPLINE_SURFACE_WITH_KNOTS ( ( 4, 4 ),
 ( 2, 2 ),
 ( 0.000000000000000000, 1.000000000000000000 ),
 ( 0.000000000000000000, 1.000000000000000000 ),
 .UNSPECIFIED. ) 
 GEOMETRIC_REPRESENTATION_ITEM ( )  RATIONAL_B_SPLINE_SURFACE ( (
 ( 1.000000000000000000, 1.000000000000000000),
 ( 0.9956975270656954757, 0.8568959468854893125),
 ( 0.9956975270656954757, 0.8568959468854893125),
 ( 1.000000000000000000, 1.000000000000000000) ) ) 
 REPRESENTATION_ITEM ( '' )  SURFACE ( )  );
#3742=EDGE_CURVE ( 'NONE', #22569, #3673, #20595, .T. ) ;
#3746=CARTESIAN_POINT ( 'NONE',  ( 109.1586059443104944, -0.006260042619939258299, 0.003294606663363219227 ) ) ;
#3749=LINE ( 'NONE', #8629, #24071 ) ;
#3752=CARTESIAN_POINT ( 'NONE',  ( 13.84597867724973597, 112.1633818588838949, -94.55652763153713636 ) ) ;
#3755=EDGE_CURVE ( 'NONE', #2053, #5932, #17622, .T. ) ;
#3757=FACE_OUTER_BOUND ( 'NONE', #7184, .T. ) ;
#3758=CARTESIAN_POINT ( 'NONE',  ( 26.11404676487257603, 65.63269960453241936, 92.25884714080432047 ) ) ;
#3759=EDGE_CURVE ( 'NONE', #9428, #27430, #3552, .T. ) ;
#3760=ORIENTED_EDGE ( 'NONE', *, *, #22807, .T. ) ;
#3761=CARTESIAN_POINT ( 'NONE',  ( 25.64704443564078318, -112.2786464378872751, -11.93517308299253443 ) ) ;
#3765=CONICAL_SURFACE ( 'NONE', #25371, 117.6351876552689504, 0.9945805576725580410 ) ;
#3766=ORIENTED_EDGE ( 'NONE', *, *, #6319, .T. ) ;
#3767=ORIENTED_EDGE ( 'NONE', *, *, #3882, .T. ) ;
#3769=FACE_OUTER_BOUND ( 'NONE', #14476, .T. ) ;
#3770=CARTESIAN_POINT ( 'NONE',  ( 1.833838850855462610, 30.25705358195048689, -141.9202662332485261 ) ) ;
#3771=CARTESIAN_POINT ( 'NONE',  ( 109.1624594426973260, -0.01531968460305926580, 0.004489871836309038827 ) ) ;
#3772=ORIENTED_EDGE ( 'NONE', *, *, #6145, .F. ) ;
#3773=EDGE_CURVE ( 'NONE', #10268, #9673, #7715, .T. ) ;
#3776=ADVANCED_FACE ( 'NONE', ( #11964 ), #6994, .F. ) ;
#3777=VECTOR ( 'NONE', #25871, 1000.000000000000000 ) ;
#3780=CARTESIAN_POINT ( 'NONE',  ( 25.81918753295378721, -110.3582118788978903, 24.41190151229222138 ) ) ;
#3781=CARTESIAN_POINT ( 'NONE',  ( 13.36082413113063083, 53.25066407421806502, 143.3553710183991541 ) ) ;
#3782=VECTOR ( 'NONE', #5373, 1000.000000000000000 ) ;
#3787=CARTESIAN_POINT ( 'NONE',  ( 28.37644542392844116, 124.0168596762487567, -8.957364412598916914 ) ) ;
#3788=CARTESIAN_POINT ( 'NONE',  ( 21.16825799904902539, -133.3214686481436217, -23.82367662027958133 ) ) ;
#3790=ORIENTED_EDGE ( 'NONE', *, *, #10132, .F. ) ;
#3791=ORIENTED_EDGE ( 'NONE', *, *, #13652, .F. ) ;
#3792=CARTESIAN_POINT ( 'NONE',  ( 1.833206310202338152, -108.3342540861872294, -96.54250248081103791 ) ) ;
#3793=CARTESIAN_POINT ( 'NONE',  ( 28.43349137099834323, 34.52178142065691446, -119.3601175884732015 ) ) ;
#3795=ORIENTED_EDGE ( 'NONE', *, *, #17061, .F. ) ;
#3797=CIRCLE ( 'NONE', #25851, 151.1787379149930359 ) ;
#3798=CIRCLE ( 'NONE', #110, 12.50000000000000178 ) ;
#3799=CARTESIAN_POINT ( 'NONE',  ( 1.833721034905649194, -141.8643653601972119, 30.51809396650970996 ) ) ;
#3800=LINE ( 'NONE', #27972, #18050 ) ;
#3801=DIRECTION ( 'NONE',  ( -0.5914120900931443270, -0.7023121577978098662, -0.3962188444547314337 ) ) ;
#3802=CARTESIAN_POINT ( 'NONE',  ( 26.11404676487257603, 55.62948129436244926, 98.61392875273382685 ) ) ;
#3803=EDGE_CURVE ( 'NONE', #6049, #24611, #9393, .T. ) ;
#3804=CARTESIAN_POINT ( 'NONE',  ( 6.224689322667630975, -139.9988794244329142, -48.18553814190173057 ) ) ;
#3805=CARTESIAN_POINT ( 'NONE',  ( 26.04756280548355463, -112.6689254848258344, -10.72497307632908736 ) ) ;
#3808=ORIENTED_EDGE ( 'NONE', *, *, #1369, .T. ) ;
#3812=EDGE_CURVE ( 'NONE', #531, #9093, #19158, .T. ) ;
#3813=CARTESIAN_POINT ( 'NONE',  ( 25.64692872815574631, -103.0182448446671089, -46.21877827526664362 ) ) ;
#3814=DIRECTION ( 'NONE',  ( 0.5946245182733607137, 0.08697490616139455510, -0.7992853357633870059 ) ) ;
#3815=CARTESIAN_POINT ( 'NONE',  ( 1.833206308920057426, -71.90885838897311544, -126.0392061186629888 ) ) ;
#3818=CARTESIAN_POINT ( 'NONE',  ( 25.64681081121879203, 91.10197563708035773, -66.70335573067774249 ) ) ;
#3820=( BOUNDED_SURFACE ( )  B_SPLINE_SURFACE ( 3, 1, ( 
 ( #18339, #27557 ),
 ( #14030, #14313 ),
 ( #11743, #5402 ),
 ( #3520, #9878 ) ),
 .UNSPECIFIED., .F., .F., .F. ) 
 B_SPLINE_SURFACE_WITH_KNOTS ( ( 4, 4 ),
 ( 2, 2 ),
 ( 0.000000000000000000, 1.000000000000000000 ),
 ( 0.000000000000000000, 1.000000000000000000 ),
 .UNSPECIFIED. ) 
 GEOMETRIC_REPRESENTATION_ITEM ( )  RATIONAL_B_SPLINE_SURFACE ( (
 ( 1.000000000000000000, 1.000000000000000000),
 ( 0.9956975270656954757, 0.8568959468854893125),
 ( 0.9956975270656954757, 0.8568959468854893125),
 ( 1.000000000000000000, 1.000000000000000000) ) ) 
 REPRESENTATION_ITEM ( '' )  SURFACE ( )  );
#3823=ORIENTED_EDGE ( 'NONE', *, *, #25489, .F. ) ;
#3825=B_SPLINE_CURVE_WITH_KNOTS ( 'NONE', 3,
 ( #25706, #19492, #23552, #5987, #14888, #10171, #23702, #16789 ),
 .UNSPECIFIED., .F., .F.,
 ( 4, 2, 2, 4 ),
 ( 1.387778780781445676E-17, 0.0002429588503611381271, 0.0004859177007222623764, 0.0009718354014445054539 ),
 .UNSPECIFIED. ) ;
#3828=ORIENTED_EDGE ( 'NONE', *, *, #5615, .T. ) ;
#3829=CARTESIAN_POINT ( 'NONE',  ( 2.108393763691200462, -13.91282116576881300, -144.6252321290183147 ) ) ;
#3831=CARTESIAN_POINT ( 'NONE',  ( 25.86096068574580897, -45.07009591924492753, -103.6815822123523390 ) ) ;
#3832=CARTESIAN_POINT ( 'NONE',  ( 1.831572820252009626, 29.20415387690763609, -142.1425225354577435 ) ) ;
#3834=CARTESIAN_POINT ( 'NONE',  ( 2.263178607246671081, -73.90841395012498083, -125.2099936970375609 ) ) ;
#3835=AXIS2_PLACEMENT_3D ( 'NONE', #8901, #26575, #2392 ) ;
#3836=CARTESIAN_POINT ( 'NONE',  ( 28.37644542392838432, -76.32685750075070530, 98.15613422114063269 ) ) ;
#3838=CARTESIAN_POINT ( 'NONE',  ( 8.186469777911000278, 134.9918587298873547, -63.89871389959332504 ) ) ;
#3839=CARTESIAN_POINT ( 'NONE',  ( 6.224689322667647851, -118.2566963816776848, 89.08920297664174370 ) ) ;
#3840=CARTESIAN_POINT ( 'NONE',  ( 25.98107933586711127, 55.61918067932742815, 98.51796269673089057 ) ) ;
#3841=CARTESIAN_POINT ( 'NONE',  ( 32.73300124599735028, 72.21147546950551543, 92.86301839380053025 ) ) ;
#3842=EDGE_CURVE ( 'NONE', #12210, #19484, #3900, .T. ) ;
#3844=CARTESIAN_POINT ( 'NONE',  ( 25.64700659047694842, -97.67001118499064205, -56.65258046470359687 ) ) ;
#3845=CARTESIAN_POINT ( 'NONE',  ( 25.69398547355839213, -11.06723946918835644, 112.3990349503584838 ) ) ;
#3847=VERTEX_POINT ( 'NONE', #1864 ) ;
#3848=VERTEX_POINT ( 'NONE', #23915 ) ;
#3849=CARTESIAN_POINT ( 'NONE',  ( 25.64692232868534560, 56.17236075412082386, -97.94691534265373889 ) ) ;
#3850=DIRECTION ( 'NONE',  ( -0.5946245182733607137, -0.08697490616138379982, -0.7992853357633882272 ) ) ;
#3851=CARTESIAN_POINT ( 'NONE',  ( 32.73300124599735028, 66.00340565729339914, 97.37344512919882789 ) ) ;
#3853=DIRECTION ( 'NONE',  ( 0.5914120900931444380, -0.4674599267565346938, -0.6570486713847260019 ) ) ;
#3854=ORIENTED_EDGE ( 'NONE', *, *, #8521, .F. ) ;
#3857=ORIENTED_EDGE ( 'NONE', *, *, #935, .F. ) ;
#3859=CARTESIAN_POINT ( 'NONE',  ( 1.832998868059890096, 142.0492247521722788, 29.64765804470122745 ) ) ;
#3861=CARTESIAN_POINT ( 'NONE',  ( 25.64681081121879203, 107.5125461021402486, 34.49579773461821475 ) ) ;
#3862=CARTESIAN_POINT ( 'NONE',  ( 109.1592201516379674, 0.003661068210032671338, -0.006957642258155084976 ) ) ;
#3863=CARTESIAN_POINT ( 'NONE',  ( 1.833485406944043827, -45.34878176254329674, 137.8414413349084100 ) ) ;
#3865=CARTESIAN_POINT ( 'NONE',  ( 2.430230287190572103, 28.83279105684426113, 142.6294793592098813 ) ) ;
#3868=CARTESIAN_POINT ( 'NONE',  ( 2.430230287190572103, -145.5073573687466819, -1.451610819319274270 ) ) ;
#3869=VERTEX_POINT ( 'NONE', #27800 ) ;
#3870=CARTESIAN_POINT ( 'NONE',  ( 10.93730112725990189, -97.44200844886194091, -115.5857507957714461 ) ) ;
#3871=ORIENTED_EDGE ( 'NONE', *, *, #19884, .T. ) ;
#3872=B_SPLINE_CURVE_WITH_KNOTS ( 'NONE', 3,
 ( #1179, #15893, #20060, #18039 ),
 .UNSPECIFIED., .F., .F.,
 ( 4, 4 ),
 ( 1.422050084071091177E-16, 0.008383748772659580309 ),
 .UNSPECIFIED. ) ;
#3873=CARTESIAN_POINT ( 'NONE',  ( 2.433796855181233454, -1.451562450948615135, -145.5024947199069913 ) ) ;
#3875=( BOUNDED_SURFACE ( )  B_SPLINE_SURFACE ( 3, 1, ( 
 ( #10943, #19708 ),
 ( #8782, #17547 ),
 ( #12224, #20864 ),
 ( #11799, #9498 ) ),
 .UNSPECIFIED., .F., .F., .F. ) 
 B_SPLINE_SURFACE_WITH_KNOTS ( ( 4, 4 ),
 ( 2, 2 ),
 ( 0.000000000000000000, 1.000000000000000000 ),
 ( 0.000000000000000000, 1.000000000000000000 ),
 .UNSPECIFIED. ) 
 GEOMETRIC_REPRESENTATION_ITEM ( )  RATIONAL_B_SPLINE_SURFACE ( (
 ( 1.000000000000000000, 1.000000000000000000),
 ( 0.9956975270656954757, 0.8568959468854893125),
 ( 0.9956975270656954757, 0.8568959468854893125),
 ( 1.000000000000000000, 1.000000000000000000) ) ) 
 REPRESENTATION_ITEM ( '' )  SURFACE ( )  );
#3877=ADVANCED_FACE ( 'NONE', ( #16869, #8226 ), #4171, .F. ) ;
#3879=EDGE_CURVE ( 'NONE', #20144, #9116, #22115, .T. ) ;
#3880=CARTESIAN_POINT ( 'NONE',  ( 13.36082413113063083, -152.7944199136427983, 6.345145185217505812 ) ) ;
#3881=CARTESIAN_POINT ( 'NONE',  ( 109.1589550718175161, -0.006826119083824107661, 0.003284595046935108106 ) ) ;
#3882=EDGE_CURVE ( 'NONE', #14688, #17616, #10111, .T. ) ;
#3885=CARTESIAN_POINT ( 'NONE',  ( 1.833206310202334599, -58.34025049825039844, 132.8652722326996809 ) ) ;
#3887=ORIENTED_EDGE ( 'NONE', *, *, #16584, .F. ) ;
#3888=ORIENTED_EDGE ( 'NONE', *, *, #25609, .F. ) ;
#3889=CARTESIAN_POINT ( 'NONE',  ( 28.37599760073042887, -112.5845136272806997, 22.09615888373918935 ) ) ;
#3893=CARTESIAN_POINT ( 'NONE',  ( 1.832998868059890096, -142.0492247521720799, -29.64765804470219024 ) ) ;
#3899=B_SPLINE_CURVE_WITH_KNOTS ( 'NONE', 3,
 ( #21992, #26310, #4014, #12785 ),
 .UNSPECIFIED., .F., .F.,
 ( 4, 4 ),
 ( 0.000000000000000000, 0.008383560773332720747 ),
 .UNSPECIFIED. ) ;
#3900=LINE ( 'NONE', #10259, #25906 ) ;
#3901=ORIENTED_EDGE ( 'NONE', *, *, #12736, .T. ) ;
#3902=CARTESIAN_POINT ( 'NONE',  ( 25.64692232868535626, -45.62640214192334298, 103.2819624397966294 ) ) ;
#3903=DIRECTION ( 'NONE',  ( -0.000000000000000000, 1.000000000000000000, -0.000000000000000000 ) ) ;
#3905=ORIENTED_EDGE ( 'NONE', *, *, #21718, .F. ) ;
#3906=ORIENTED_EDGE ( 'NONE', *, *, #10775, .T. ) ;
#3909=ADVANCED_FACE ( 'NONE', ( #3757 ), #9943, .F. ) ;
#3910=DIRECTION ( 'NONE',  ( 0.5914120900931444380, -0.8063295922669342364, -0.008020494142999035764 ) ) ;
#3914=CARTESIAN_POINT ( 'NONE',  ( 1.833206308920065197, -132.8652726225756737, 58.34024961171186874 ) ) ;
#3916=CARTESIAN_POINT ( 'NONE',  ( 26.28373643307405771, 82.21796085350790406, -97.52903534490786797 ) ) ;
#3919=CARTESIAN_POINT ( 'NONE',  ( 109.1778270068192853, 0.007323887274071894798, 0.005755170886745451797 ) ) ;
#3920=CARTESIAN_POINT ( 'NONE',  ( 28.37599760073042887, -25.60640155549242181, 111.8383885143454393 ) ) ;
#3923=B_SPLINE_CURVE_WITH_KNOTS ( 'NONE', 3,
 ( #25052, #23037, #9633, #20272, #9495, #3155, #5016, #564 ),
 .UNSPECIFIED., .F., .F.,
 ( 4, 2, 2, 4 ),
 ( 7.757919228897728493E-18, 0.0002429592666046773836, 0.0004859185332093470151, 0.0009718370664186765746 ),
 .UNSPECIFIED. ) ;
#3924=CARTESIAN_POINT ( 'NONE',  ( 109.1624594426973260, -0.01595733256931099533, -0.0004639210235577357917 ) ) ;
#3925=CARTESIAN_POINT ( 'NONE',  ( 30.58324630866342986, -95.47492154584209345, 74.24222250960207248 ) ) ;
#3926=CARTESIAN_POINT ( 'NONE',  ( 13.84597867724971643, 140.9259526407714986, -40.76072889493610774 ) ) ;
#3927=ORIENTED_EDGE ( 'NONE', *, *, #8523, .F. ) ;
#3930=CARTESIAN_POINT ( 'NONE',  ( 2.433796855181233454, -57.85512797797981932, 133.5135467655516095 ) ) ;
#3931=ORIENTED_EDGE ( 'NONE', *, *, #23934, .T. ) ;
#3932=EDGE_LOOP ( 'NONE', ( #16801, #9094, #17016, #19192 ) ) ;
#3933=VERTEX_POINT ( 'NONE', #8370 ) ;
#3936=EDGE_CURVE ( 'NONE', #813, #11599, #5970, .T. ) ;
#3937=CARTESIAN_POINT ( 'NONE',  ( 1.833838848569415925, -141.9017642089167168, 30.34409872482189030 ) ) ;
#3944=CARTESIAN_POINT ( 'NONE',  ( 109.1721716018069657, 0.003350975118864183214, -0.01673651515803010678 ) ) ;
#3945=CARTESIAN_POINT ( 'NONE',  ( 9.884929003653626367, -135.7578851563890510, 65.04493172071430251 ) ) ;
#3946=CARTESIAN_POINT ( 'NONE',  ( 2.433796855181219243, -126.7346379669260443, 71.49415740225030902 ) ) ;
#3947=ORIENTED_EDGE ( 'NONE', *, *, #12228, .F. ) ;
#3948=ORIENTED_EDGE ( 'NONE', *, *, #4783, .F. ) ;
#3949=CARTESIAN_POINT ( 'NONE',  ( 25.64708228042121263, 112.9112740241346984, 0.03938584558032432598 ) ) ;
#3951=CARTESIAN_POINT ( 'NONE',  ( 10.93730112726003156, 97.44200844886434254, -115.5857507957695276 ) ) ;
#3952=LINE ( 'NONE', #27712, #3308 ) ;
#3953=FACE_OUTER_BOUND ( 'NONE', #10490, .T. ) ;
#3954=ORIENTED_EDGE ( 'NONE', *, *, #13971, .F. ) ;
#3955=DIRECTION ( 'NONE',  ( -1.000000000000000000, -0.000000000000000000, -0.000000000000000000 ) ) ;
#3959=EDGE_LOOP ( 'NONE', ( #16487, #12051, #5829, #21502 ) ) ;
#3960=B_SPLINE_CURVE_WITH_KNOTS ( 'NONE', 3,
 ( #6195, #28450, #13335, #10918, #23895, #22134, #21987 ),
 .UNSPECIFIED., .F., .F.,
 ( 4, 3, 4 ),
 ( 0.000000000000000000, 0.02398743853561339720, 0.04000277880656220864 ),
 .UNSPECIFIED. ) ;
#3961=ORIENTED_EDGE ( 'NONE', *, *, #13253, .T. ) ;
#3963=ORIENTED_EDGE ( 'NONE', *, *, #27151, .T. ) ;
#3964=ORIENTED_EDGE ( 'NONE', *, *, #22023, .T. ) ;
#3965=ADVANCED_FACE ( 'NONE', ( #12947 ), #17586, .F. ) ;
#3966=ORIENTED_EDGE ( 'NONE', *, *, #21382, .F. ) ;
#3968=CARTESIAN_POINT ( 'NONE',  ( 2.108985857320913038, -73.75356715683001596, -125.1820688103229884 ) ) ;
#3969=CARTESIAN_POINT ( 'NONE',  ( 25.64681081121879203, -0.4157506337719985012, -112.9102952884414606 ) ) ;
#3970=DIRECTION ( 'NONE',  ( 0.000000000000000000, 0.000000000000000000, 1.000000000000000000 ) ) ;
#3971=CARTESIAN_POINT ( 'NONE',  ( 2.108985857320924584, 138.5727354014057084, 43.67763756616700022 ) ) ;
#3973=B_SPLINE_CURVE_WITH_KNOTS ( 'NONE', 3,
 ( #25845, #23555, #60, #8559, #19628, #14891 ),
 .UNSPECIFIED., .F., .F.,
 ( 4, 2, 4 ),
 ( 3.035766082959412415E-18, 0.0006311636237756726225, 0.001262327247551342860 ),
 .UNSPECIFIED. ) ;
#3975=CARTESIAN_POINT ( 'NONE',  ( 1.833485406944043827, -117.7091014914955309, 84.86072343962528919 ) ) ;
#3976=CARTESIAN_POINT ( 'NONE',  ( 1.833485406944057594, 30.69200235378934849, 141.8265699653868523 ) ) ;
#3977=EDGE_LOOP ( 'NONE', ( #15739, #7297, #1489, #12788 ) ) ;
#3978=VERTEX_POINT ( 'NONE', #24188 ) ;
#3980=CARTESIAN_POINT ( 'NONE',  ( 109.1589550718174877, 0.001354998915261331188, 0.007453082872776644989 ) ) ;
#3981=CARTESIAN_POINT ( 'NONE',  ( 6.224689322667630975, -28.26953958630515018, -145.3353551538644126 ) ) ;
#3982=CARTESIAN_POINT ( 'NONE',  ( 25.64670758986457599, -98.03181353150523591, 56.02376616805386789 ) ) ;
#3986=LINE ( 'NONE', #53, #7534 ) ;
#3988=CARTESIAN_POINT ( 'NONE',  ( 25.64708228042122684, -112.2968511928419986, 11.76327187353777859 ) ) ;
#3989=FACE_OUTER_BOUND ( 'NONE', #1437, .T. ) ;
#3994=B_SPLINE_CURVE_WITH_KNOTS ( 'NONE', 3,
 ( #17774, #22544, #505, #24572, #26550, #9440, #6714, #18196 ),
 .UNSPECIFIED., .F., .F.,
 ( 4, 2, 2, 4 ),
 ( 5.421010862427522170E-20, 0.0002429588503611193433, 0.0004859177007222386323, 0.0009718354014444823604 ),
 .UNSPECIFIED. ) ;
#3995=CARTESIAN_POINT ( 'NONE',  ( 13.84597867724971287, 64.00674338126026441, -132.0026437215594228 ) ) ;
#3996=CARTESIAN_POINT ( 'NONE',  ( 109.1589550718174877, 0.003980125429499884598, -0.006445391216542585913 ) ) ;
#3997=EDGE_CURVE ( 'NONE', #20945, #23678, #16618, .T. ) ;
#4000=ADVANCED_FACE ( 'NONE', ( #28338 ), #18747, .F. ) ;
#4003=CARTESIAN_POINT ( 'NONE',  ( 2.108985857320888613, -116.7869613039525518, 86.43462668039097707 ) ) ;
#4006=LINE ( 'NONE', #8612, #18059 ) ;
#4007=CARTESIAN_POINT ( 'NONE',  ( 10.93730112725990722, -136.0306644680979389, -65.95960219663263047 ) ) ;
#4008=DIRECTION ( 'NONE',  ( -1.000000000000000000, 0.000000000000000000, -0.000000000000000000 ) ) ;
#4009=CARTESIAN_POINT ( 'NONE',  ( 25.64708228042120908, 110.4357030047557799, 23.51409906510251346 ) ) ;
#4010=B_SPLINE_CURVE_WITH_KNOTS ( 'NONE', 3,
 ( #12646, #2396, #4145, #15355, #13070, #24031 ),
 .UNSPECIFIED., .F., .F.,
 ( 4, 2, 4 ),
 ( 6.942281208919283290E-18, 0.0006311571484586124027, 0.001262314296917217216 ),
 .UNSPECIFIED. ) ;
#4012=ADVANCED_FACE ( 'NONE', ( #13359 ), #20534, .F. ) ;
#4014=CARTESIAN_POINT ( 'NONE',  ( 30.59141879584319312, 70.47510900703926495, -92.40465812955481795 ) ) ;
#4019=VERTEX_POINT ( 'NONE', #20130 ) ;
#4020=CARTESIAN_POINT ( 'NONE',  ( 32.73300124599736449, -115.8010721414085253, 20.69176323058589162 ) ) ;
#4023=FACE_OUTER_BOUND ( 'NONE', #15491, .T. ) ;
#4024=CARTESIAN_POINT ( 'NONE',  ( 21.16825799904906447, 134.1581724640165305, -18.54093663547691051 ) ) ;
#4025=ADVANCED_FACE ( 'NONE', ( #9201 ), #23509, .F. ) ;
#4026=CARTESIAN_POINT ( 'NONE',  ( 1.831572820252008738, 132.9644823688603310, -58.11906524360346538 ) ) ;
#4027=CARTESIAN_POINT ( 'NONE',  ( 1.831572820252009626, -0.9871191512904484711, -145.1082523917587537 ) ) ;
#4028=VERTEX_POINT ( 'NONE', #15959 ) ;
#4029=CARTESIAN_POINT ( 'NONE',  ( 10.93730112726003156, 115.5857507957718440, -97.44200844886164248 ) ) ;
#4032=B_SPLINE_CURVE_WITH_KNOTS ( 'NONE', 3,
 ( #20162, #13976, #16283, #4917, #15854, #22787, #27208, #25082, #879, #24936 ),
 .UNSPECIFIED., .F., .F.,
 ( 4, 3, 3, 4 ),
 ( 0.000000000000000000, 0.0002669560319015713877, 0.0005492286108966342980, 0.0008315040496093477167 ),
 .UNSPECIFIED. ) ;
#4034=ADVANCED_FACE ( 'NONE', ( #4881 ), #9884, .F. ) ;
#4037=CARTESIAN_POINT ( 'NONE',  ( 10.93730112725932635, 0.000000000000000000, 0.000000000000000000 ) ) ;
#4039=EDGE_CURVE ( 'NONE', #11142, #14288, #847, .T. ) ;
#4041=EDGE_CURVE ( 'NONE', #3038, #9740, #3923, .T. ) ;
#4043=EDGE_LOOP ( 'NONE', ( #19556, #7045, #11501, #19826 ) ) ;
#4044=CARTESIAN_POINT ( 'NONE',  ( 109.1587776205901577, -0.006388631651928916751, 0.003592288931009581399 ) ) ;
#4045=CARTESIAN_POINT ( 'NONE',  ( 32.73300124599740002, 66.00340565729470654, -97.37344512919790418 ) ) ;
#4047=CARTESIAN_POINT ( 'NONE',  ( 32.73300124599734318, 115.8010721414084117, 20.69176323058669809 ) ) ;
#4048=ORIENTED_EDGE ( 'NONE', *, *, #17410, .T. ) ;
#4052=CARTESIAN_POINT ( 'NONE',  ( 10.93730112725943293, 128.3908183996590537, 79.81734490845931873 ) ) ;
#4053=CARTESIAN_POINT ( 'NONE',  ( 28.37603512858453669, 98.45183098818061751, -58.91311972676436426 ) ) ;
#4054=CARTESIAN_POINT ( 'NONE',  ( 1.834118845439484335, 85.43746956709850338, 117.2918069668803724 ) ) ;
#4055=VECTOR ( 'NONE', #12893, 1000.000000000000000 ) ;
#4056=EDGE_CURVE ( 'NONE', #4028, #7451, #24537, .T. ) ;
#4057=EDGE_LOOP ( 'NONE', ( #21116, #1829, #11427, #63 ) ) ;
#4058=ADVANCED_FACE ( 'NONE', ( #9359 ), #876, .F. ) ;
#4065=ORIENTED_EDGE ( 'NONE', *, *, #20012, .T. ) ;
#4066=ORIENTED_EDGE ( 'NONE', *, *, #3220, .F. ) ;
#4067=( BOUNDED_SURFACE ( )  B_SPLINE_SURFACE ( 3, 1, ( 
 ( #4299, #28454 ),
 ( #1709, #23898 ),
 ( #14947, #17249 ),
 ( #28048, #26173 ) ),
 .UNSPECIFIED., .F., .F., .F. ) 
 B_SPLINE_SURFACE_WITH_KNOTS ( ( 4, 4 ),
 ( 2, 2 ),
 ( 0.000000000000000000, 1.000000000000000000 ),
 ( 0.000000000000000000, 1.000000000000000000 ),
 .UNSPECIFIED. ) 
 GEOMETRIC_REPRESENTATION_ITEM ( )  RATIONAL_B_SPLINE_SURFACE ( (
 ( 1.000000000000000000, 1.000000000000000000),
 ( 0.6386103224230302855, 0.9954351624131538845),
 ( 0.6386103224230302855, 0.9954351624131538845),
 ( 1.000000000000000000, 1.000000000000000000) ) ) 
 REPRESENTATION_ITEM ( '' )  SURFACE ( )  );
#4068=CARTESIAN_POINT ( 'NONE',  ( 8.186469777910888368, -122.8338388711456872, -84.95702201436542111 ) ) ;
#4069=B_SPLINE_CURVE_WITH_KNOTS ( 'NONE', 3,
 ( #24631, #13655, #8781, #22455, #2428, #2723 ),
 .UNSPECIFIED., .F., .F.,
 ( 4, 2, 4 ),
 ( 2.602085213965210642E-18, 0.0006311636237756740320, 0.001262327247551345679 ),
 .UNSPECIFIED. ) ;
#4071=VECTOR ( 'NONE', #13855, 1000.000000000000114 ) ;
#4078=CARTESIAN_POINT ( 'NONE',  ( 109.1586900883932856, 0.002301750759607898694, 0.006757191295056137574 ) ) ;
#4080=CARTESIAN_POINT ( 'NONE',  ( 2.063896406836609909, -46.16709813092528947, -137.7380992975107290 ) ) ;
#4081=EDGE_CURVE ( 'NONE', #5582, #21108, #16737, .T. ) ;
#4082=ORIENTED_EDGE ( 'NONE', *, *, #16857, .F. ) ;
#4083=VERTEX_POINT ( 'NONE', #18116 ) ;
#4084=EDGE_CURVE ( 'NONE', #12482, #20441, #705, .T. ) ;
#4085=FACE_OUTER_BOUND ( 'NONE', #16480, .T. ) ;
#4086=CARTESIAN_POINT ( 'NONE',  ( 25.64692872815577118, -91.53575854059458550, 66.10702795113384411 ) ) ;
#4089=CARTESIAN_POINT ( 'NONE',  ( 26.11404676487257603, 110.5078194225161070, 24.64483677384886917 ) ) ;
#4094=CARTESIAN_POINT ( 'NONE',  ( 25.64681081121879203, -91.59071981940616070, 66.03065707438906884 ) ) ;
#4096=ORIENTED_EDGE ( 'NONE', *, *, #21188, .T. ) ;
#4097=ORIENTED_EDGE ( 'NONE', *, *, #13412, .T. ) ;
#4098=DIRECTION ( 'NONE',  ( -0.000000000000000000, 1.000000000000000000, 0.000000000000000000 ) ) ;
#4099=EDGE_CURVE ( 'NONE', #8520, #24828, #7345, .T. ) ;
#4100=VERTEX_POINT ( 'NONE', #20860 ) ;
#4102=ORIENTED_EDGE ( 'NONE', *, *, #27827, .T. ) ;
#4106=( BOUNDED_SURFACE ( )  B_SPLINE_SURFACE ( 3, 1, ( 
 ( #27111, #2808 ),
 ( #20360, #3097 ),
 ( #12684, #27409 ),
 ( #11874, #28084 ) ),
 .UNSPECIFIED., .F., .F., .F. ) 
 B_SPLINE_SURFACE_WITH_KNOTS ( ( 4, 4 ),
 ( 2, 2 ),
 ( 0.000000000000000000, 1.000000000000000000 ),
 ( 0.000000000000000000, 1.000000000000000000 ),
 .UNSPECIFIED. ) 
 GEOMETRIC_REPRESENTATION_ITEM ( )  RATIONAL_B_SPLINE_SURFACE ( (
 ( 1.000000000000000000, 1.000000000000000000),
 ( 0.6386103224230316178, 0.9954351624131538845),
 ( 0.6386103224230316178, 0.9954351624131538845),
 ( 1.000000000000000000, 1.000000000000000000) ) ) 
 REPRESENTATION_ITEM ( '' )  SURFACE ( )  );
#4107=CARTESIAN_POINT ( 'NONE',  ( 109.1721716018069657, -0.01706748904932341507, 0.0002019688922674831401 ) ) ;
#4110=CARTESIAN_POINT ( 'NONE',  ( 26.11404676487257603, -112.4785329405481065, -12.95861723607569438 ) ) ;
#4111=ORIENTED_EDGE ( 'NONE', *, *, #26802, .T. ) ;
#4113=B_SPLINE_CURVE_WITH_KNOTS ( 'NONE', 3,
 ( #8427, #8697, #2197, #22229, #17461, #26395, #19349, #11004, #25980, #1923 ),
 .UNSPECIFIED., .F., .F.,
 ( 4, 3, 3, 4 ),
 ( 1.962615573354718958E-17, 0.0002669560319015810371, 0.0005492286108966412369, 0.0008315040496093431630 ),
 .UNSPECIFIED. ) ;
#4114=DIRECTION ( 'NONE',  ( -1.000000000000000000, -0.000000000000000000, -0.000000000000000000 ) ) ;
#4116=DIRECTION ( 'NONE',  ( 0.000000000000000000, 0.000000000000000000, 1.000000000000000000 ) ) ;
#4118=ORIENTED_EDGE ( 'NONE', *, *, #6864, .T. ) ;
#4119=ORIENTED_EDGE ( 'NONE', *, *, #16176, .T. ) ;
#4122=ADVANCED_FACE ( 'NONE', ( #21281 ), #18402, .F. ) ;
#4125=CARTESIAN_POINT ( 'NONE',  ( 5.340103556456569756, 100.3626145793577678, -108.0219267027620447 ) ) ;
#4127=DIRECTION ( 'NONE',  ( -0.5914120900931443270, -0.008020494142990605008, -0.8063295922669344584 ) ) ;
#4130=EDGE_CURVE ( 'NONE', #23678, #3338, #11107, .T. ) ;
#4133=CARTESIAN_POINT ( 'NONE',  ( 1.833809397773873640, 117.2915757704557080, 85.43729755723188646 ) ) ;
#4134=ORIENTED_EDGE ( 'NONE', *, *, #5570, .T. ) ;
#4135=CARTESIAN_POINT ( 'NONE',  ( 2.430230287190572103, -133.5180086894995100, 57.85706160874098458 ) ) ;
#4137=ORIENTED_EDGE ( 'NONE', *, *, #3641, .F. ) ;
#4138=CARTESIAN_POINT ( 'NONE',  ( 19.66333377628710366, -88.78556591841228851, -105.3186440504705104 ) ) ;
#4139=CARTESIAN_POINT ( 'NONE',  ( 26.11404676487257603, -90.92995828888153653, -67.46175819463459788 ) ) ;
#4140=FACE_BOUND ( 'NONE', #26124, .T. ) ;
#4142=CARTESIAN_POINT ( 'NONE',  ( 32.73300124599732186, 0.000000000000000000, 0.000000000000000000 ) ) ;
#4144=( BOUNDED_SURFACE ( )  B_SPLINE_SURFACE ( 3, 1, ( 
 ( #20270, #2272 ),
 ( #22451, #7059 ),
 ( #8932, #24625 ),
 ( #26743, #562 ) ),
 .UNSPECIFIED., .F., .F., .F. ) 
 B_SPLINE_SURFACE_WITH_KNOTS ( ( 4, 4 ),
 ( 2, 2 ),
 ( 0.000000000000000000, 1.000000000000000000 ),
 ( 0.000000000000000000, 1.000000000000000000 ),
 .UNSPECIFIED. ) 
 GEOMETRIC_REPRESENTATION_ITEM ( )  RATIONAL_B_SPLINE_SURFACE ( (
 ( 1.000000000000000000, 1.000000000000000000),
 ( 0.6386103224230302855, 0.9954351624131538845),
 ( 0.6386103224230302855, 0.9954351624131538845),
 ( 1.000000000000000000, 1.000000000000000000) ) ) 
 REPRESENTATION_ITEM ( '' )  SURFACE ( )  );
#4145=CARTESIAN_POINT ( 'NONE',  ( 1.894214914920965276, 132.2104617488244855, -59.90782071839061729 ) ) ;
#4146=CARTESIAN_POINT ( 'NONE',  ( 13.36082413113063083, 142.1654513177088006, 56.35051087435012818 ) ) ;
#4147=CARTESIAN_POINT ( 'NONE',  ( 16.05277956358201763, 25.20902801311569164, -141.0713346807232824 ) ) ;
#4148=CARTESIAN_POINT ( 'NONE',  ( 109.1592201516379674, 0.007376275279030877242, 0.002720803050361335265 ) ) ;
#4153=ORIENTED_EDGE ( 'NONE', *, *, #24527, .F. ) ;
#4156=CARTESIAN_POINT ( 'NONE',  ( 25.64703792032471341, 103.2099561461823924, 45.78915563622597062 ) ) ;
#4157=CARTESIAN_POINT ( 'NONE',  ( 21.16825799904898986, -121.8625396241600782, 59.09063383105294776 ) ) ;
#4158=EDGE_CURVE ( 'NONE', #28263, #1461, #18987, .T. ) ;
#4159=CARTESIAN_POINT ( 'NONE',  ( 1.832998868059890096, -85.72499093308179852, 117.0819875546692685 ) ) ;
#4160=CARTESIAN_POINT ( 'NONE',  ( 1.832998868059858122, 59.50898020732511640, 132.3466930259795618 ) ) ;
#4162=CARTESIAN_POINT ( 'NONE',  ( 1.834118845439484335, -141.9759513273462517, -29.99597360113214961 ) ) ;
#4163=CARTESIAN_POINT ( 'NONE',  ( 30.58324630866341209, -45.56259622822436484, 112.0331114996533870 ) ) ;
#4164=ORIENTED_EDGE ( 'NONE', *, *, #20786, .T. ) ;
#4167=CIRCLE ( 'NONE', #30, 12.50000000000000178 ) ;
#4168=CARTESIAN_POINT ( 'NONE',  ( 25.64692872815576052, 23.79008960806752881, -110.3764733653606100 ) ) ;
#4169=ADVANCED_FACE ( 'NONE', ( #8068 ), #15447, .F. ) ;
#4171=PLANE ( 'NONE',  #15311 ) ;
#4172=ORIENTED_EDGE ( 'NONE', *, *, #492, .F. ) ;
#4173=CARTESIAN_POINT ( 'NONE',  ( 2.108393763691172040, 43.67806918959143303, 138.5721856399486569 ) ) ;
#4178=VERTEX_POINT ( 'NONE', #5760 ) ;
#4180=AXIS2_PLACEMENT_3D ( 'NONE', #15022, #12860, #2198 ) ;
#4182=CARTESIAN_POINT ( 'NONE',  ( 10.93730112725932635, 0.000000000000000000, 0.000000000000000000 ) ) ;
#4185=CARTESIAN_POINT ( 'NONE',  ( 10.93730112725932635, 0.000000000000000000, 0.000000000000000000 ) ) ;
#4186=DIRECTION ( 'NONE',  ( -0.5946245182733608248, -0.5994612328333145390, -0.5357871896547512502 ) ) ;
#4187=EDGE_LOOP ( 'NONE', ( #24508, #21758, #21090, #24399 ) ) ;
#4188=EDGE_LOOP ( 'NONE', ( #17368, #5551, #26613, #20631 ) ) ;
#4193=CARTESIAN_POINT ( 'NONE',  ( 109.1586900883932856, 0.006819617742893400482, 0.002109621908814826672 ) ) ;
#4195=CIRCLE ( 'NONE', #24429, 151.1787379149930359 ) ;
#4196=VECTOR ( 'NONE', #21161, 999.9999999999998863 ) ;
#4199=ORIENTED_EDGE ( 'NONE', *, *, #19249, .T. ) ;
#4200=CIRCLE ( 'NONE', #2354, 37.50000000000001421 ) ;
#4202=FACE_OUTER_BOUND ( 'NONE', #3222, .T. ) ;
#4203=CARTESIAN_POINT ( 'NONE',  ( 26.11404676487257603, -36.06104232266378062, -107.3263591096434197 ) ) ;
#4207=ORIENTED_EDGE ( 'NONE', *, *, #26690, .F. ) ;
#4209=CARTESIAN_POINT ( 'NONE',  ( 1.832998868059890096, -85.72499093308022111, -117.0819875546704054 ) ) ;
#4210=CARTESIAN_POINT ( 'NONE',  ( 109.1586900883932856, 0.006231977675084991036, 0.003481399864218453783 ) ) ;
#4212=CARTESIAN_POINT ( 'NONE',  ( 109.1586059443104944, -0.001740416220250516881, 0.006856640434645976979 ) ) ;
#4213=EDGE_CURVE ( 'NONE', #24090, #4630, #14146, .T. ) ;
#4216=CARTESIAN_POINT ( 'NONE',  ( 109.1589550718175161, -0.007453082872782207380, -0.001354998915253747844 ) ) ;
#4217=CARTESIAN_POINT ( 'NONE',  ( 10.93730112725932635, 0.000000000000000000, 0.000000000000000000 ) ) ;
#4219=ADVANCED_FACE ( 'NONE', ( #13056 ), #19659, .F. ) ;
#4220=CARTESIAN_POINT ( 'NONE',  ( 2.430230287190572103, -137.9371479820459570, -46.34481016236966155 ) ) ;
#4223=ORIENTED_EDGE ( 'NONE', *, *, #14943, .T. ) ;
#4224=CARTESIAN_POINT ( 'NONE',  ( 25.98107933586721074, -57.50946808479307037, 97.42660475433937961 ) ) ;
#4226=CARTESIAN_POINT ( 'NONE',  ( 109.1592201516379674, 0.002720803050370466849, 0.007376275279032907736 ) ) ;
#4227=DIRECTION ( 'NONE',  ( -1.000000000000000000, -0.000000000000000000, -0.000000000000000000 ) ) ;
#4228=CARTESIAN_POINT ( 'NONE',  ( 55.79472521941426777, 54.55111121764146986, -48.13855120843829383 ) ) ;
#4230=CARTESIAN_POINT ( 'NONE',  ( 5.340103579038292025, 146.3832392131354538, -17.70136536264517346 ) ) ;
#4232=CARTESIAN_POINT ( 'NONE',  ( 28.37603512858358101, 113.9023475466376993, -13.77584568114176911 ) ) ;
#4233=ORIENTED_EDGE ( 'NONE', *, *, #14255, .F. ) ;
#4235=B_SPLINE_CURVE_WITH_KNOTS ( 'NONE', 3,
 ( #13600, #2517, #11309, #7506 ),
 .UNSPECIFIED., .F., .F.,
 ( 4, 4 ),
 ( 1.309227883336067538E-16, 0.008383748772659583778 ),
 .UNSPECIFIED. ) ;
#4238=CARTESIAN_POINT ( 'NONE',  ( 1.832998868059858122, 117.7096351258387870, 84.86110816369641441 ) ) ;
#4239=CIRCLE ( 'NONE', #6118, 151.1787379149930359 ) ;
#4241=CARTESIAN_POINT ( 'NONE',  ( 2.433796855181219243, -125.2830755159749003, -74.00833731765692391 ) ) ;
#4243=EDGE_LOOP ( 'NONE', ( #17406, #14074, #28264, #6167 ) ) ;
#4244=CARTESIAN_POINT ( 'NONE',  ( 1.833485406944043827, 125.9346397303445286, -72.09189602597577107 ) ) ;
#4245=CARTESIAN_POINT ( 'NONE',  ( 109.1624594426973118, -0.003771499231554190090, -0.01551217196237749882 ) ) ;
#4246=EDGE_CURVE ( 'NONE', #10890, #1025, #8601, .T. ) ;
#4248=B_SPLINE_CURVE_WITH_KNOTS ( 'NONE', 3,
 ( #1349, #19063, #4068, #5685 ),
 .UNSPECIFIED., .F., .F.,
 ( 4, 4 ),
 ( 3.406435548571490246E-16, 0.01077107486149829138 ),
 .UNSPECIFIED. ) ;
#4249=CARTESIAN_POINT ( 'NONE',  ( 1.833485406944057594, -125.9346397303430223, -72.09189602597842850 ) ) ;
#4251=LINE ( 'NONE', #26270, #6966 ) ;
#4252=ORIENTED_EDGE ( 'NONE', *, *, #25667, .F. ) ;
#4255=CARTESIAN_POINT ( 'NONE',  ( 2.433796855181205476, 145.5024947199069629, 1.451562450950146133 ) ) ;
#4257=CARTESIAN_POINT ( 'NONE',  ( 25.64681081121880624, -56.81519825470823548, 97.57530875170583329 ) ) ;
#4258=CONICAL_SURFACE ( 'NONE', #10278, 117.6351876552689504, 0.9945805576725580410 ) ;
#4259=ORIENTED_EDGE ( 'NONE', *, *, #21504, .F. ) ;
#4260=EDGE_LOOP ( 'NONE', ( #28343, #1817, #15465, #11529 ) ) ;
#4261=CARTESIAN_POINT ( 'NONE',  ( 26.28373643307439167, 122.5382646256984600, 35.44121223574892099 ) ) ;
#4262=CARTESIAN_POINT ( 'NONE',  ( 1.833838850093452599, -72.55487854850780138, 125.6687428896156575 ) ) ;
#4263=CARTESIAN_POINT ( 'NONE',  ( 25.98552792386800903, -76.50165414343506143, -83.35136888841310565 ) ) ;
#4265=CARTESIAN_POINT ( 'NONE',  ( 1.893872463202044054, -137.7483215415845450, -45.75900850850141666 ) ) ;
#4267=CARTESIAN_POINT ( 'NONE',  ( 109.1586900883932856, -0.004113747441000954568, -0.005833932871487501094 ) ) ;
#4269=CARTESIAN_POINT ( 'NONE',  ( 109.1587776205901577, -0.005880209827417018538, -0.004375189885414149799 ) ) ;
#4270=DIRECTION ( 'NONE',  ( -0.5914120900931443270, -0.6045864222316674752, -0.5335794202785283380 ) ) ;
#4271=CARTESIAN_POINT ( 'NONE',  ( 25.64692232868535626, 75.30916867847216167, -84.12764974007949093 ) ) ;
#4274=CARTESIAN_POINT ( 'NONE',  ( 1.833809397773842553, 15.34508223002640293, -144.2961330457378324 ) ) ;
#4278=EDGE_LOOP ( 'NONE', ( #2965, #23842, #21093, #10180 ) ) ;
#4279=CARTESIAN_POINT ( 'NONE',  ( 26.11404676487257603, 33.91085499298520034, -108.0249973236464314 ) ) ;
#4280=CIRCLE ( 'NONE', #19920, 151.1787379149930359 ) ;
#4281=ADVANCED_FACE ( 'NONE', ( #23882 ), #921, .F. ) ;
#4282=CARTESIAN_POINT ( 'NONE',  ( 2.430230287190572103, -57.85706160874057247, -133.5180086894997089 ) ) ;
#4283=DIRECTION ( 'NONE',  ( -1.000000000000000000, -0.000000000000000000, -0.000000000000000000 ) ) ;
#4284=AXIS2_PLACEMENT_3D ( 'NONE', #20582, #3456, #9378 ) ;
#4285=ADVANCED_FACE ( 'NONE', ( #6870 ), #15606, .F. ) ;
#4287=CARTESIAN_POINT ( 'NONE',  ( 1.833485406944057594, -117.0814567582550154, 85.72460230293657446 ) ) ;
#4289=EDGE_CURVE ( 'NONE', #20108, #24250, #4884, .T. ) ;
#4290=CARTESIAN_POINT ( 'NONE',  ( 26.11404676487257603, -76.59696442953135431, -83.38016054979861735 ) ) ;
#4291=CARTESIAN_POINT ( 'NONE',  ( 1.833838850855474600, -137.9800888515320025, -44.92600961247803326 ) ) ;
#4292=CARTESIAN_POINT ( 'NONE',  ( 26.28373643307403285, 22.43832507403829979, -125.5716026420345628 ) ) ;
#4294=B_SPLINE_CURVE_WITH_KNOTS ( 'NONE', 3,
 ( #26012, #23873, #1959, #6300, #26284, #22110 ),
 .UNSPECIFIED., .F., .F.,
 ( 4, 2, 4 ),
 ( 1.734723475976806902E-18, 0.0006311636237756703457, 0.001262327247551338957 ),
 .UNSPECIFIED. ) ;
#4295=CARTESIAN_POINT ( 'NONE',  ( 109.1592201516379674, 0.001934867487012827689, -0.007620268632968149602 ) ) ;
#4296=ADVANCED_FACE ( 'NONE', ( #26991 ), #952, .T. ) ;
#4297=AXIS2_PLACEMENT_3D ( 'NONE', #18698, #9933, #20423 ) ;
#4298=CARTESIAN_POINT ( 'NONE',  ( 6.224689322667630975, 97.14981701196322206, 111.7293398381268332 ) ) ;
#4299=CARTESIAN_POINT ( 'NONE',  ( 109.1592201516379674, -0.004194960840990111066, -0.006649399203953448162 ) ) ;
#4302=ORIENTED_EDGE ( 'NONE', *, *, #5207, .F. ) ;
#4306=CARTESIAN_POINT ( 'NONE',  ( 30.59141879584286627, -95.58042137919495929, 66.10404588653759106 ) ) ;
#4307=CARTESIAN_POINT ( 'NONE',  ( 26.11404676487259024, 103.8885755249569485, 45.01677474591446781 ) ) ;
#4308=CARTESIAN_POINT ( 'NONE',  ( 26.11404676487259024, -12.95861723607377414, -112.4785329405483338 ) ) ;
#4312=CARTESIAN_POINT ( 'NONE',  ( 6.224689322667630975, 57.86870174583425808, 136.2818611715192390 ) ) ;
#4316=VERTEX_POINT ( 'NONE', #810 ) ;
#4317=DIRECTION ( 'NONE',  ( 0.000000000000000000, 0.000000000000000000, 1.000000000000000000 ) ) ;
#4319=VERTEX_POINT ( 'NONE', #2830 ) ;
#4320=B_SPLINE_CURVE_WITH_KNOTS ( 'NONE', 3,
 ( #9038, #4991, #26577, #18089, #387, #6881, #26867, #15625, #7176, #13767 ),
 .UNSPECIFIED., .F., .F.,
 ( 4, 3, 3, 4 ),
 ( 6.938893903907228378E-18, 0.0002669560319015712793, 0.0005492286108966453568, 0.0008315040496093611608 ),
 .UNSPECIFIED. ) ;
#4321=ORIENTED_EDGE ( 'NONE', *, *, #4888, .T. ) ;
#4323=EDGE_CURVE ( 'NONE', #24455, #4923, #10042, .T. ) ;
#4325=CARTESIAN_POINT ( 'NONE',  ( 109.1624594426973260, -0.01154818537150952180, -0.01102230012606015934 ) ) ;
#4327=EDGE_CURVE ( 'NONE', #6430, #24062, #26830, .T. ) ;
#4328=B_SPLINE_CURVE_WITH_KNOTS ( 'NONE', 3,
 ( #2679, #9458, #26855, #26993, #14044, #16063, #24864 ),
 .UNSPECIFIED., .F., .F.,
 ( 4, 3, 4 ),
 ( 0.000000000000000000, 0.02398743853561337291, 0.04000277880656209761 ),
 .UNSPECIFIED. ) ;
#4329=VERTEX_POINT ( 'NONE', #18511 ) ;
#4331=CARTESIAN_POINT ( 'NONE',  ( 5.340103556456461398, -111.1041836730285013, 96.93942141426026637 ) ) ;
#4334=CARTESIAN_POINT ( 'NONE',  ( 1.833691583653552115, -44.50270951807451070, -138.1170938425796351 ) ) ;
#4335=CARTESIAN_POINT ( 'NONE',  ( 2.433796855181205476, -96.28145139437610567, -109.1007109081235882 ) ) ;
#4336=CARTESIAN_POINT ( 'NONE',  ( 1.831572820252009626, -144.4165162501762154, -14.18623102066916175 ) ) ;
#4337=CARTESIAN_POINT ( 'NONE',  ( 1.833809397773857208, 97.22957127128982791, -107.7184108265653748 ) ) ;
#4340=FACE_OUTER_BOUND ( 'NONE', #25012, .T. ) ;
#4341=CARTESIAN_POINT ( 'NONE',  ( 1.894214914920945070, 141.7768822502890487, -31.11059045488991970 ) ) ;
#4342=CARTESIAN_POINT ( 'NONE',  ( 109.1624594426973118, 0.007576898892907089726, -0.01405141589344816727 ) ) ;
#4343=VERTEX_POINT ( 'NONE', #22854 ) ;
#4344=ORIENTED_EDGE ( 'NONE', *, *, #23367, .F. ) ;
#4345=CARTESIAN_POINT ( 'NONE',  ( 25.98552792386799482, -24.57669147553907152, -110.4352299692912851 ) ) ;
#4346=DIRECTION ( 'NONE',  ( 0.000000000000000000, 0.000000000000000000, 1.000000000000000000 ) ) ;
#4348=B_SPLINE_CURVE_WITH_KNOTS ( 'NONE', 3,
 ( #17709, #6794, #162, #15538, #24353, #26626 ),
 .UNSPECIFIED., .F., .F.,
 ( 4, 2, 4 ),
 ( 1.389302603484999005E-17, 0.0006311571484586108848, 0.001262314296917207892 ),
 .UNSPECIFIED. ) ;
#4349=ORIENTED_EDGE ( 'NONE', *, *, #16479, .F. ) ;
#4350=ORIENTED_EDGE ( 'NONE', *, *, #3879, .F. ) ;
#4351=EDGE_CURVE ( 'NONE', #25928, #16492, #5613, .T. ) ;
#4352=B_SPLINE_CURVE_WITH_KNOTS ( 'NONE', 3,
 ( #16486, #27274, #1091, #1509 ),
 .UNSPECIFIED., .F., .F.,
 ( 4, 4 ),
 ( 3.743959683027022744E-16, 0.01077107486149797219 ),
 .UNSPECIFIED. ) ;
#4353=CARTESIAN_POINT ( 'NONE',  ( 109.1592201516379674, 0.007748443302128555504, -0.001331853079208340871 ) ) ;
#4355=CARTESIAN_POINT ( 'NONE',  ( 1.894214914920941739, -144.2521558665608836, 16.12044375672241614 ) ) ;
#4356=CARTESIAN_POINT ( 'NONE',  ( 8.186469777910877710, -148.8557359139593359, -12.15801985874125712 ) ) ;
#4357=ADVANCED_FACE ( 'NONE', ( #25014 ), #21787, .T. ) ;
#4360=CARTESIAN_POINT ( 'NONE',  ( 109.1587776205901861, -0.004240403845331913203, 0.005978137617721826502 ) ) ;
#4361=B_SPLINE_CURVE_WITH_KNOTS ( 'NONE', 3,
 ( #17009, #15116, #1747, #14856, #4337, #8393, #17289, #26076, #21901, #10 ),
 .UNSPECIFIED., .F., .F.,
 ( 4, 3, 3, 4 ),
 ( 5.003707553108401214E-17, 0.0002669559177086260862, 0.0005339118354151285457, 0.001067817517169155576 ),
 .UNSPECIFIED. ) ;
#4362=CARTESIAN_POINT ( 'NONE',  ( 5.340103579038192549, -133.7487108093468180, 62.06990748397801383 ) ) ;
#4364=ADVANCED_FACE ( 'NONE', ( #24862 ), #3693, .F. ) ;
#4366=CARTESIAN_POINT ( 'NONE',  ( 25.81918753295378366, 113.0221398901142180, -0.9336804662331048554 ) ) ;
#4367=CARTESIAN_POINT ( 'NONE',  ( 25.64681081121879203, -107.5125461021405044, 34.49579773461748999 ) ) ;
#4369=ORIENTED_EDGE ( 'NONE', *, *, #1466, .F. ) ;
#4372=DIRECTION ( 'NONE',  ( -1.000000000000000000, -0.000000000000000000, -0.000000000000000000 ) ) ;
#4378=B_SPLINE_CURVE_WITH_KNOTS ( 'NONE', 3,
 ( #25364, #27799, #14548, #12115 ),
 .UNSPECIFIED., .F., .F.,
 ( 4, 4 ),
 ( 3.408235012970691066E-16, 0.01077107486149795484 ),
 .UNSPECIFIED. ) ;
#4381=ORIENTED_EDGE ( 'NONE', *, *, #23992, .F. ) ;
#4382=CARTESIAN_POINT ( 'NONE',  ( 109.1586059443104944, 0.0004635842312796052884, -0.007058870754606104241 ) ) ;
#4385=CARTESIAN_POINT ( 'NONE',  ( 25.64670758986456889, 107.2298587623395747, 35.36461833156559464 ) ) ;
#4386=ORIENTED_EDGE ( 'NONE', *, *, #22231, .T. ) ;
#4387=EDGE_CURVE ( 'NONE', #3680, #14349, #16798, .T. ) ;
#4390=EDGE_LOOP ( 'NONE', ( #12911, #6574, #19206, #11360 ) ) ;
#4393=CARTESIAN_POINT ( 'NONE',  ( 109.1589550718174877, -0.003980125429499926232, 0.006445391216542559892 ) ) ;
#4394=CARTESIAN_POINT ( 'NONE',  ( 26.11404676487257603, 55.62948129436244926, 98.61392875273382685 ) ) ;
#4395=CARTESIAN_POINT ( 'NONE',  ( 25.65782528836479415, -112.2379831684171592, -12.37768345530092162 ) ) ;
#4396=CARTESIAN_POINT ( 'NONE',  ( 25.64681081121879203, -103.3177883989776547, -45.54494737132326776 ) ) ;
#4398=CARTESIAN_POINT ( 'NONE',  ( 25.64708010899963853, -56.40825696968328629, 97.81137751680981296 ) ) ;
#4399=CARTESIAN_POINT ( 'NONE',  ( 26.11404676487259024, -67.46175819463304890, -90.92995828888270182 ) ) ;
#4402=CARTESIAN_POINT ( 'NONE',  ( 16.75465622695659818, 67.05928661304356808, 125.4242432475195272 ) ) ;
#4403=CARTESIAN_POINT ( 'NONE',  ( 24.01988960052077005, 129.0012934948648535, -23.05141021591152750 ) ) ;
#4405=EDGE_LOOP ( 'NONE', ( #25662, #3057, #2102, #24293 ) ) ;
#4406=CARTESIAN_POINT ( 'NONE',  ( 25.64692232868534560, -35.20209749635233720, -107.2834780834839137 ) ) ;
#4407=CARTESIAN_POINT ( 'NONE',  ( 109.1592201516379674, 0.002720803050370466849, 0.007376275279032907736 ) ) ;
#4409=CARTESIAN_POINT ( 'NONE',  ( 25.64708010899965984, 112.2984447178532719, 11.74803558238322410 ) ) ;
#4410=CARTESIAN_POINT ( 'NONE',  ( 25.64704443564075120, 110.4715096490036075, -23.34498572103212410 ) ) ;
#4412=CARTESIAN_POINT ( 'NONE',  ( 1.831572820252008738, 29.20415387690568210, 142.1425225354580846 ) ) ;
#4415=CARTESIAN_POINT ( 'NONE',  ( 9.884929003653608603, -97.56484214660547138, -114.6392083957127994 ) ) ;
#4418=CARTESIAN_POINT ( 'NONE',  ( 2.433796855181219243, 31.67151202413165478, -142.0211193075552956 ) ) ;
#4419=CARTESIAN_POINT ( 'NONE',  ( 2.063896406836609909, -98.19887492195788070, -107.0521644432427593 ) ) ;
#4422=CARTESIAN_POINT ( 'NONE',  ( 2.433796855181233454, -98.43889364293788447, -107.1581411821795626 ) ) ;
#4424=CARTESIAN_POINT ( 'NONE',  ( 55.49584447822657296, -48.74506217377918205, 53.73688382046248080 ) ) ;
#4425=CARTESIAN_POINT ( 'NONE',  ( 28.37599760073042532, 22.09615888373955528, 112.5845136272806428 ) ) ;
#4426=CARTESIAN_POINT ( 'NONE',  ( 1.833809397773871419, -132.6366580004811340, 58.85883548850542013 ) ) ;
#4427=CARTESIAN_POINT ( 'NONE',  ( 25.64681081121880624, -112.3352186517031441, 11.38886654529637887 ) ) ;
#4429=DIRECTION ( 'NONE',  ( 0.5914120900931444380, 0.7023121577978154173, -0.3962188444547216082 ) ) ;
#4434=DIRECTION ( 'NONE',  ( 0.5914120900931444380, -0.3352908775637255534, 0.7333565075147320256 ) ) ;
#4437=DIRECTION ( 'NONE',  ( -1.000000000000000000, -0.000000000000000000, -0.000000000000000000 ) ) ;
#4438=CARTESIAN_POINT ( 'NONE',  ( 25.64692872815577473, -91.15762468787696093, -66.62748454953252519 ) ) ;
#4444=CARTESIAN_POINT ( 'NONE',  ( 109.1624594426973118, 0.008380433676412918365, 0.01358749486988785130 ) ) ;
#4446=CARTESIAN_POINT ( 'NONE',  ( 1.833691583653554336, -0.3559373310805032387, 145.1092556475514073 ) ) ;
#4447=CARTESIAN_POINT ( 'NONE',  ( 32.73300124599738581, 51.32617430725051832, -105.8473486001045387 ) ) ;
#4448=( BOUNDED_SURFACE ( )  B_SPLINE_SURFACE ( 3, 1, ( 
 ( #13585, #22384 ),
 ( #26540, #22241 ),
 ( #9000, #343 ),
 ( #20062, #2649 ) ),
 .UNSPECIFIED., .F., .F., .F. ) 
 B_SPLINE_SURFACE_WITH_KNOTS ( ( 4, 4 ),
 ( 2, 2 ),
 ( 0.000000000000000000, 1.000000000000000000 ),
 ( 0.000000000000000000, 1.000000000000000000 ),
 .UNSPECIFIED. ) 
 GEOMETRIC_REPRESENTATION_ITEM ( )  RATIONAL_B_SPLINE_SURFACE ( (
 ( 1.000000000000000000, 1.000000000000000000),
 ( 0.9956975270656955868, 0.8568959468854907557),
 ( 0.9956975270656955868, 0.8568959468854907557),
 ( 1.000000000000000000, 1.000000000000000000) ) ) 
 REPRESENTATION_ITEM ( '' )  SURFACE ( )  );
#4453=EDGE_CURVE ( 'NONE', #3161, #21238, #25714, .T. ) ;
#4454=ORIENTED_EDGE ( 'NONE', *, *, #26196, .T. ) ;
#4455=ORIENTED_EDGE ( 'NONE', *, *, #4745, .F. ) ;
#4457=CARTESIAN_POINT ( 'NONE',  ( 2.063896406836605024, 98.19887492196005496, -107.0521644432407129 ) ) ;
#4460=CARTESIAN_POINT ( 'NONE',  ( 55.49584447822657296, 42.42793568432957585, 58.85239198729202315 ) ) ;
#4464=CARTESIAN_POINT ( 'NONE',  ( 25.64681081121879203, 91.59071981940572016, 66.03065707438965148 ) ) ;
#4465=ORIENTED_EDGE ( 'NONE', *, *, #21086, .T. ) ;
#4468=DIRECTION ( 'NONE',  ( 0.000000000000000000, 0.000000000000000000, 1.000000000000000000 ) ) ;
#4470=LINE ( 'NONE', #2298, #16619 ) ;
#4473=ADVANCED_FACE ( 'NONE', ( #1521 ), #11775, .F. ) ;
#4475=DIRECTION ( 'NONE',  ( -1.000000000000000000, -0.000000000000000000, -0.000000000000000000 ) ) ;
#4476=CARTESIAN_POINT ( 'NONE',  ( 2.263178607246655982, -43.59477707254128376, 138.7064943909644228 ) ) ;
#4477=ORIENTED_EDGE ( 'NONE', *, *, #561, .F. ) ;
#4480=DIRECTION ( 'NONE',  ( -1.000000000000000000, -0.000000000000000000, -0.000000000000000000 ) ) ;
#4482=CARTESIAN_POINT ( 'NONE',  ( 32.73300124599740002, 97.37344512919945316, -66.00340565729239017 ) ) ;
#4484=EDGE_LOOP ( 'NONE', ( #10422, #24697, #1564, #454 ) ) ;
#4486=CARTESIAN_POINT ( 'NONE',  ( 1.834118845439484335, -85.43746956709772178, -117.2918069668809409 ) ) ;
#4487=B_SPLINE_CURVE_WITH_KNOTS ( 'NONE', 3,
 ( #25618, #14514, #3016, #11796, #14365, #3572, #5894, #12353 ),
 .UNSPECIFIED., .F., .F.,
 ( 4, 2, 2, 4 ),
 ( 6.938893903907228378E-18, 0.0002429592666046848646, 0.0004859185332093627903, 0.0009718370664186809114 ),
 .UNSPECIFIED. ) ;
#4488=CARTESIAN_POINT ( 'NONE',  ( 1.831572820252009626, -138.3111855986058174, -43.90210991190762257 ) ) ;
#4489=CARTESIAN_POINT ( 'NONE',  ( 109.1624594426973260, 0.005372302061310704584, -0.01503296564240499435 ) ) ;
#4490=CARTESIAN_POINT ( 'NONE',  ( 1.832998868059858122, -145.1092030902949830, 0.5339089137742969449 ) ) ;
#4495=CARTESIAN_POINT ( 'NONE',  ( 30.58324630866342275, -102.7123253644120240, 63.85566901681581697 ) ) ;
#4498=ORIENTED_EDGE ( 'NONE', *, *, #2627, .T. ) ;
#4499=ORIENTED_EDGE ( 'NONE', *, *, #21053, .T. ) ;
#4500=CARTESIAN_POINT ( 'NONE',  ( 25.64681081121879203, 91.10197563707947666, 66.70335573067896462 ) ) ;
#4503=CARTESIAN_POINT ( 'NONE',  ( 28.37599760073042887, 78.09498850373518053, -84.05168479399007708 ) ) ;
#4506=CARTESIAN_POINT ( 'NONE',  ( 26.28373643307404706, -119.9673604189460150, 43.35364178852736217 ) ) ;
#4507=ORIENTED_EDGE ( 'NONE', *, *, #14591, .T. ) ;
#4508=CARTESIAN_POINT ( 'NONE',  ( 1.833206308920111161, 145.1075835660717530, 0.7447049373416791962 ) ) ;
#4509=ORIENTED_EDGE ( 'NONE', *, *, #26096, .F. ) ;
#4510=CARTESIAN_POINT ( 'NONE',  ( 2.430230287190581429, 84.35270093935257307, 118.5711603495684301 ) ) ;
#4513=ORIENTED_EDGE ( 'NONE', *, *, #25597, .F. ) ;
#4514=ORIENTED_EDGE ( 'NONE', *, *, #18115, .T. ) ;
#4515=ADVANCED_FACE ( 'NONE', ( #13019 ), #24479, .F. ) ;
#4518=EDGE_LOOP ( 'NONE', ( #10149, #3727, #9614, #26366 ) ) ;
#4520=AXIS2_PLACEMENT_3D ( 'NONE', #21412, #10484, #12625 ) ;
#4523=CIRCLE ( 'NONE', #4982, 117.6351876552689504 ) ;
#4524=ORIENTED_EDGE ( 'NONE', *, *, #23885, .T. ) ;
#4525=CARTESIAN_POINT ( 'NONE',  ( 2.063896406836609909, 98.19887492195857703, 107.0521644432420771 ) ) ;
#4526=EDGE_CURVE ( 'NONE', #14115, #18577, #22426, .T. ) ;
#4529=CARTESIAN_POINT ( 'NONE',  ( -90.83090735639699176, 0.000000000000000000, 0.000000000000000000 ) ) ;
#4534=CARTESIAN_POINT ( 'NONE',  ( 109.1587776205901577, 0.007151389024634738009, 0.001605238040359060429 ) ) ;
#4535=CARTESIAN_POINT ( 'NONE',  ( 6.224689322667647851, -28.26953958630718944, 145.3353551538640716 ) ) ;
#4536=CARTESIAN_POINT ( 'NONE',  ( 32.73300124599732186, 0.000000000000000000, 0.000000000000000000 ) ) ;
#4538=VERTEX_POINT ( 'NONE', #23844 ) ;
#4541=ADVANCED_FACE ( 'NONE', ( #19500 ), #21945, .T. ) ;
#4542=CARTESIAN_POINT ( 'NONE',  ( 10.93730112725990367, -145.2260730187398678, -42.00474393596407197 ) ) ;
#4543=FACE_OUTER_BOUND ( 'NONE', #4746, .T. ) ;
#4546=ORIENTED_EDGE ( 'NONE', *, *, #22833, .F. ) ;
#4549=CARTESIAN_POINT ( 'NONE',  ( 109.1586059443104944, -0.004378796245583073746, 0.005555961672780045102 ) ) ;
#4553=VERTEX_POINT ( 'NONE', #8997 ) ;
#4554=CARTESIAN_POINT ( 'NONE',  ( 25.64699802086726166, -112.9109702078779804, 0.2377811728593887397 ) ) ;
#4555=DIRECTION ( 'NONE',  ( 0.5946245182733607137, -0.3297108033645317349, 0.7332888028688893112 ) ) ;
#4556=CARTESIAN_POINT ( 'NONE',  ( 2.433796855181233454, 74.00833731765563073, 125.2830755159756677 ) ) ;
#4558=CARTESIAN_POINT ( 'NONE',  ( 10.93730112725932813, 146.7718404940640085, 36.23586118136551448 ) ) ;
#4559=EDGE_CURVE ( 'NONE', #1868, #8689, #22246, .T. ) ;
#4560=CARTESIAN_POINT ( 'NONE',  ( 25.81918753295378721, 55.70247894228311480, -98.34688456803341694 ) ) ;
#4562=DIRECTION ( 'NONE',  ( 0.5914120900931444380, -0.5335794202785220097, -0.6045864222316730263 ) ) ;
#4563=CARTESIAN_POINT ( 'NONE',  ( 10.93730112725932635, 149.7554878793145576, 20.69552240458357062 ) ) ;
#4567=CARTESIAN_POINT ( 'NONE',  ( 109.1586900883932856, -0.0008465529156635612316, -0.007088091345229652514 ) ) ;
#4569=CARTESIAN_POINT ( 'NONE',  ( 109.1592201516379674, 0.001934867487021726170, 0.007620268632971113378 ) ) ;
#4570=DIRECTION ( 'NONE',  ( 0.000000000000000000, -1.000000000000000000, -3.469446951953603342E-16 ) ) ;
#4571=CARTESIAN_POINT ( 'NONE',  ( 25.69398547355839924, -98.18017599249800753, -55.82723250638873225 ) ) ;
#4572=ORIENTED_EDGE ( 'NONE', *, *, #17863, .F. ) ;
#4574=ORIENTED_EDGE ( 'NONE', *, *, #22168, .F. ) ;
#4575=ORIENTED_EDGE ( 'NONE', *, *, #7110, .T. ) ;
#4576=CARTESIAN_POINT ( 'NONE',  ( 25.64699802086725811, 103.2460182674617073, 45.70780507840472495 ) ) ;
#4577=CARTESIAN_POINT ( 'NONE',  ( 2.433796855181205476, -43.58222566461547132, -138.8296532063092457 ) ) ;
#4580=CARTESIAN_POINT ( 'NONE',  ( 109.1587776205901577, 0.005978137617714225811, -0.004240403845337380184 ) ) ;
#4582=CARTESIAN_POINT ( 'NONE',  ( 32.73300124599738581, -97.37344512919901263, 66.00340565729310072 ) ) ;
#4583=EDGE_LOOP ( 'NONE', ( #7020, #24783, #23179, #25598 ) ) ;
#4584=CARTESIAN_POINT ( 'NONE',  ( 25.64681081121879203, -34.49579773461710630, -107.5125461021406181 ) ) ;
#4586=CARTESIAN_POINT ( 'NONE',  ( 25.64704443564076897, -0.1334765861211750504, 112.9111375659905718 ) ) ;
#4587=CARTESIAN_POINT ( 'NONE',  ( 109.1586900883932856, 0.002301750759599777586, -0.006757191295060853420 ) ) ;
#4588=CARTESIAN_POINT ( 'NONE',  ( 55.49584447822657296, 72.55110015779771970, 0.2676470673959223112 ) ) ;
#4589=CARTESIAN_POINT ( 'NONE',  ( 13.36082413113063083, 150.7747251079861996, 25.56125765253504412 ) ) ;
#4594=ORIENTED_EDGE ( 'NONE', *, *, #25940, .T. ) ;
#4595=ORIENTED_EDGE ( 'NONE', *, *, #22315, .T. ) ;
#4596=ORIENTED_EDGE ( 'NONE', *, *, #5243, .T. ) ;
#4597=DIRECTION ( 'NONE',  ( -1.000000000000000000, -0.000000000000000000, -0.000000000000000000 ) ) ;
#4600=EDGE_CURVE ( 'NONE', #6599, #9129, #3872, .T. ) ;
#4603=EDGE_LOOP ( 'NONE', ( #3516, #20386, #5146, #158 ) ) ;
#4607=ORIENTED_EDGE ( 'NONE', *, *, #3162, .T. ) ;
#4610=ORIENTED_EDGE ( 'NONE', *, *, #24001, .T. ) ;
#4611=CARTESIAN_POINT ( 'NONE',  ( 1.833485406944057594, 141.8265699653871366, -30.69200235378795227 ) ) ;
#4612=CARTESIAN_POINT ( 'NONE',  ( 25.64708228042122329, -45.88917180166207288, -103.1656011680036897 ) ) ;
#4613=CARTESIAN_POINT ( 'NONE',  ( 26.11404676487257603, 84.89295829319590325, -74.91683232330889552 ) ) ;
#4616=CARTESIAN_POINT ( 'NONE',  ( 28.37603512858449761, 104.0705994281843090, -48.29936889363852259 ) ) ;
#4617=( BOUNDED_SURFACE ( )  B_SPLINE_SURFACE ( 3, 1, ( 
 ( #16890, #25682 ),
 ( #12409, #14577 ),
 ( #16756, #7698 ),
 ( #1335, #14709 ) ),
 .UNSPECIFIED., .F., .F., .F. ) 
 B_SPLINE_SURFACE_WITH_KNOTS ( ( 4, 4 ),
 ( 2, 2 ),
 ( 0.000000000000000000, 1.000000000000000000 ),
 ( 0.000000000000000000, 1.000000000000000000 ),
 .UNSPECIFIED. ) 
 GEOMETRIC_REPRESENTATION_ITEM ( )  RATIONAL_B_SPLINE_SURFACE ( (
 ( 1.000000000000000000, 1.000000000000000000),
 ( 0.9956975270656954757, 0.8568959468854893125),
 ( 0.9956975270656954757, 0.8568959468854893125),
 ( 1.000000000000000000, 1.000000000000000000) ) ) 
 REPRESENTATION_ITEM ( '' )  SURFACE ( )  );
#4618=EDGE_CURVE ( 'NONE', #449, #6339, #5238, .T. ) ;
#4619=CARTESIAN_POINT ( 'NONE',  ( 109.1778270068192853, -0.008743876326153485548, -0.003210287141656848614 ) ) ;
#4620=FACE_OUTER_BOUND ( 'NONE', #6202, .T. ) ;
#4624=CARTESIAN_POINT ( 'NONE',  ( 25.64670758986456889, -65.96397693491100256, -91.63870681572889509 ) ) ;
#4626=VERTEX_POINT ( 'NONE', #25369 ) ;
#4627=ORIENTED_EDGE ( 'NONE', *, *, #5300, .T. ) ;
#4630=VERTEX_POINT ( 'NONE', #5646 ) ;
#4634=VECTOR ( 'NONE', #20101, 1000.000000000000000 ) ;
#4635=CARTESIAN_POINT ( 'NONE',  ( 2.063896406836609909, -138.5688025270875698, -43.61045647697833516 ) ) ;
#4638=DIRECTION ( 'NONE',  ( 0.5946245182733607137, -0.6521823330503053739, 0.4701913299128708257 ) ) ;
#4640=FACE_OUTER_BOUND ( 'NONE', #20196, .T. ) ;
#4642=CARTESIAN_POINT ( 'NONE',  ( 25.64692232868535626, 66.63160215461263647, 91.15460455808850782 ) ) ;
#4647=B_SPLINE_CURVE_WITH_KNOTS ( 'NONE', 3,
 ( #10479, #8592, #25874, #23739 ),
 .UNSPECIFIED., .F., .F.,
 ( 4, 4 ),
 ( 3.371304645218077370E-16, 0.01077107486149766341 ),
 .UNSPECIFIED. ) ;
#4649=CARTESIAN_POINT ( 'NONE',  ( 10.93730112726006176, 142.1801301103792809, -51.37919228020152929 ) ) ;
#4650=CARTESIAN_POINT ( 'NONE',  ( 1.831572820252008738, -97.82994539998453831, 107.1759352627503148 ) ) ;
#4652=( BOUNDED_SURFACE ( )  B_SPLINE_SURFACE ( 3, 1, ( 
 ( #5219, #18296 ),
 ( #3070, #9682 ),
 ( #27229, #7543 ),
 ( #16300, #25095 ) ),
 .UNSPECIFIED., .F., .F., .F. ) 
 B_SPLINE_SURFACE_WITH_KNOTS ( ( 4, 4 ),
 ( 2, 2 ),
 ( 0.000000000000000000, 1.000000000000000000 ),
 ( 0.000000000000000000, 1.000000000000000000 ),
 .UNSPECIFIED. ) 
 GEOMETRIC_REPRESENTATION_ITEM ( )  RATIONAL_B_SPLINE_SURFACE ( (
 ( 1.000000000000000000, 1.000000000000000000),
 ( 0.9956975270656954757, 0.8568959468854893125),
 ( 0.9956975270656954757, 0.8568959468854893125),
 ( 1.000000000000000000, 1.000000000000000000) ) ) 
 REPRESENTATION_ITEM ( '' )  SURFACE ( )  );
#4653=CIRCLE ( 'NONE', #1897, 117.6351876552689504 ) ;
#4655=FACE_OUTER_BOUND ( 'NONE', #18444, .T. ) ;
#4656=CARTESIAN_POINT ( 'NONE',  ( 109.1592201516379674, 0.006174480289200316024, 0.004867031887010233454 ) ) ;
#4660=CARTESIAN_POINT ( 'NONE',  ( 21.16825799904900052, -127.3716170292826746, 46.02882515936445174 ) ) ;
#4661=ORIENTED_EDGE ( 'NONE', *, *, #20627, .T. ) ;
#4665=CARTESIAN_POINT ( 'NONE',  ( 1.893872463202059153, 141.7768406633803693, 31.10971550360632421 ) ) ;
#4669=VERTEX_POINT ( 'NONE', #3335 ) ;
#4671=B_SPLINE_CURVE_WITH_KNOTS ( 'NONE', 3,
 ( #6843, #6992, #24704, #2502, #4950, #24557, #18043, #13440, #26827, #4819 ),
 .UNSPECIFIED., .F., .F.,
 ( 4, 3, 3, 4 ),
 ( 1.962615573354718958E-17, 0.0002669559177086215868, 0.0005339118354150813829, 0.001067817517169175959 ),
 .UNSPECIFIED. ) ;
#4672=B_SPLINE_CURVE_WITH_KNOTS ( 'NONE', 3,
 ( #9072, #15830, #5316, #16107 ),
 .UNSPECIFIED., .F., .F.,
 ( 4, 4 ),
 ( 2.133075126106637135E-16, 0.008383748772659693066 ),
 .UNSPECIFIED. ) ;
#4674=CARTESIAN_POINT ( 'NONE',  ( 26.11404676487259024, 67.46175819463365997, 90.92995828888226129 ) ) ;
#4675=VECTOR ( 'NONE', #25742, 1000.000000000000114 ) ;
#4678=CARTESIAN_POINT ( 'NONE',  ( 1.833485406944043827, 137.8414413349085521, 45.34878176254281357 ) ) ;
#4680=ADVANCED_FACE ( 'NONE', ( #13722 ), #23564, .F. ) ;
#4681=B_SPLINE_CURVE_WITH_KNOTS ( 'NONE', 3,
 ( #24501, #4770, #24655, #18429, #13676, #7363, #3048, #14243, #9966, #18587 ),
 .UNSPECIFIED., .F., .F.,
 ( 4, 3, 3, 4 ),
 ( 4.443059973708341306E-17, 0.0002669559177086373619, 0.0005339118354151127163, 0.001067817517169160346 ),
 .UNSPECIFIED. ) ;
#4682=CARTESIAN_POINT ( 'NONE',  ( 1.833809397773874750, -72.40070666294502644, -125.7576368866150887 ) ) ;
#4683=DIRECTION ( 'NONE',  ( -1.000000000000000000, -0.000000000000000000, -0.000000000000000000 ) ) ;
#4684=ADVANCED_FACE ( 'NONE', ( #19025 ), #21172, .F. ) ;
#4685=CARTESIAN_POINT ( 'NONE',  ( 25.86096068574578410, -110.3716997142157084, -24.48003142199199544 ) ) ;
#4688=CARTESIAN_POINT ( 'NONE',  ( 32.73300124599738581, -44.31599526637883457, -108.9684813982493097 ) ) ;
#4689=ORIENTED_EDGE ( 'NONE', *, *, #24151, .T. ) ;
#4690=CARTESIAN_POINT ( 'NONE',  ( 32.73300124599739291, 81.52272205837319063, -84.80615050150287004 ) ) ;
#4693=B_SPLINE_CURVE_WITH_KNOTS ( 'NONE', 3,
 ( #11711, #24962, #7839, #27086, #10134, #9692, #5225, #13998 ),
 .UNSPECIFIED., .F., .F.,
 ( 4, 2, 2, 4 ),
 ( 3.469446951953614189E-18, 0.0002429592666046825878, 0.0004859185332093617061, 0.0009718370664187031376 ),
 .UNSPECIFIED. ) ;
#4695=ORIENTED_EDGE ( 'NONE', *, *, #26959, .F. ) ;
#4697=CONICAL_SURFACE ( 'NONE', #7466, 117.6351876552689504, 0.9945805576725580410 ) ;
#4699=DIRECTION ( 'NONE',  ( 0.5914120900931444380, -0.5455001977188131956, 0.5938529060132602400 ) ) ;
#4700=LINE ( 'NONE', #4978, #24308 ) ;
#4701=ORIENTED_EDGE ( 'NONE', *, *, #23071, .F. ) ;
#4702=CARTESIAN_POINT ( 'NONE',  ( 1.834118845439484335, -137.9527673765108489, 45.01070051384546389 ) ) ;
#4703=( BOUNDED_SURFACE ( )  B_SPLINE_SURFACE ( 3, 1, ( 
 ( #6120, #14726 ),
 ( #19196, #23820 ),
 ( #5830, #12708 ),
 ( #14448, #21060 ) ),
 .UNSPECIFIED., .F., .F., .F. ) 
 B_SPLINE_SURFACE_WITH_KNOTS ( ( 4, 4 ),
 ( 2, 2 ),
 ( 0.000000000000000000, 1.000000000000000000 ),
 ( 0.000000000000000000, 1.000000000000000000 ),
 .UNSPECIFIED. ) 
 GEOMETRIC_REPRESENTATION_ITEM ( )  RATIONAL_B_SPLINE_SURFACE ( (
 ( 1.000000000000000000, 1.000000000000000000),
 ( 0.9960225298536222738, 0.9999952330161893110),
 ( 0.9960225298536222738, 0.9999952330161893110),
 ( 1.000000000000000000, 1.000000000000000000) ) ) 
 REPRESENTATION_ITEM ( '' )  SURFACE ( )  );
#4705=ORIENTED_EDGE ( 'NONE', *, *, #19676, .T. ) ;
#4706=CARTESIAN_POINT ( 'NONE',  ( 25.64681081121879203, -112.9102952884414464, -0.4157506337739698132 ) ) ;
#4707=CARTESIAN_POINT ( 'NONE',  ( 10.93730112725932635, 0.000000000000000000, 0.000000000000000000 ) ) ;
#4708=ADVANCED_FACE ( 'NONE', ( #17405 ), #15253, .T. ) ;
#4710=AXIS2_PLACEMENT_3D ( 'NONE', #2622, #21921, #11405 ) ;
#4713=EDGE_CURVE ( 'NONE', #16334, #25087, #10411, .T. ) ;
#4714=CARTESIAN_POINT ( 'NONE',  ( 10.93730112725983439, -148.8212007290663621, 26.59437931460704263 ) ) ;
#4717=CARTESIAN_POINT ( 'NONE',  ( 1.834118845439484335, -58.85894970555005301, 132.6369225636072144 ) ) ;
#4718=ORIENTED_EDGE ( 'NONE', *, *, #16727, .F. ) ;
#4720=CARTESIAN_POINT ( 'NONE',  ( 10.93730112725932990, 151.0983828010088530, 4.928439153520527860 ) ) ;
#4722=ORIENTED_EDGE ( 'NONE', *, *, #20997, .F. ) ;
#4723=ORIENTED_EDGE ( 'NONE', *, *, #22907, .T. ) ;
#4725=ORIENTED_EDGE ( 'NONE', *, *, #27288, .F. ) ;
#4727=CARTESIAN_POINT ( 'NONE',  ( 2.263178113027026761, -43.59477710889630231, -138.7064940342182808 ) ) ;
#4731=CARTESIAN_POINT ( 'NONE',  ( 10.93730112725978287, -125.1380233598484182, 84.82621002473399585 ) ) ;
#4733=CARTESIAN_POINT ( 'NONE',  ( 26.11404676487257603, 1.130420376097130086, 113.2169081140374090 ) ) ;
#4735=CARTESIAN_POINT ( 'NONE',  ( 2.430230287190589422, 145.5073573687466819, -1.451610819318246648 ) ) ;
#4736=CARTESIAN_POINT ( 'NONE',  ( 13.36082413113061307, 106.9547846563650637, -109.3026516754221547 ) ) ;
#4737=CARTESIAN_POINT ( 'NONE',  ( 2.108985857320907265, 142.3791757917253165, 28.95357181520875045 ) ) ;
#4739=CARTESIAN_POINT ( 'NONE',  ( 109.1586900883932856, -0.004701023939953894587, -0.005371970278523948913 ) ) ;
#4740=AXIS2_PLACEMENT_3D ( 'NONE', #15340, #2233, #12902 ) ;
#4741=( BOUNDED_SURFACE ( )  B_SPLINE_SURFACE ( 3, 1, ( 
 ( #9927, #23451 ),
 ( #5753, #16532 ),
 ( #3150, #3713 ),
 ( #27319, #12350 ) ),
 .UNSPECIFIED., .F., .F., .F. ) 
 B_SPLINE_SURFACE_WITH_KNOTS ( ( 4, 4 ),
 ( 2, 2 ),
 ( 0.000000000000000000, 1.000000000000000000 ),
 ( 0.000000000000000000, 1.000000000000000000 ),
 .UNSPECIFIED. ) 
 GEOMETRIC_REPRESENTATION_ITEM ( )  RATIONAL_B_SPLINE_SURFACE ( (
 ( 1.000000000000000000, 1.000000000000000000),
 ( 0.6386103224230316178, 0.9954351624131538845),
 ( 0.6386103224230316178, 0.9954351624131538845),
 ( 1.000000000000000000, 1.000000000000000000) ) ) 
 REPRESENTATION_ITEM ( '' )  SURFACE ( )  );
#4743=CARTESIAN_POINT ( 'NONE',  ( 25.64681081121879203, -56.81519825470687834, -97.57530875170664331 ) ) ;
#4745=EDGE_CURVE ( 'NONE', #27833, #18502, #8103, .T. ) ;
#4746=EDGE_LOOP ( 'NONE', ( #11477, #6519, #21372, #20747 ) ) ;
#4747=EDGE_CURVE ( 'NONE', #19015, #21184, #26058, .T. ) ;
#4748=EDGE_CURVE ( 'NONE', #15804, #13619, #12963, .T. ) ;
#4750=CARTESIAN_POINT ( 'NONE',  ( 25.64692872815574631, -23.16082795281176843, -110.5102270591925588 ) ) ;
#4753=CARTESIAN_POINT ( 'NONE',  ( 25.87036335909428075, 57.38512068813009392, 97.41424496619539752 ) ) ;
#4755=ORIENTED_EDGE ( 'NONE', *, *, #24190, .T. ) ;
#4758=CARTESIAN_POINT ( 'NONE',  ( 1.893872463202035616, -142.1730500379302100, 29.24569695044196749 ) ) ;
#4759=ORIENTED_EDGE ( 'NONE', *, *, #14124, .F. ) ;
#4760=CARTESIAN_POINT ( 'NONE',  ( 30.59141879584324997, 107.2355637993510413, -44.78722686469095038 ) ) ;
#4762=LINE ( 'NONE', #13239, #25853 ) ;
#4764=CARTESIAN_POINT ( 'NONE',  ( 1.833485406944043827, -145.1085452359073145, -0.5339064996899981486 ) ) ;
#4765=LINE ( 'NONE', #18422, #16109 ) ;
#4768=DIRECTION ( 'NONE',  ( -0.5946245182733607137, 0.7637359336799438569, -0.2512550613902095331 ) ) ;
#4770=CARTESIAN_POINT ( 'NONE',  ( 1.833603222531971833, 58.61467103263744605, 132.7445893798459906 ) ) ;
#4777=EDGE_CURVE ( 'NONE', #15104, #5027, #22651, .T. ) ;
#4778=ORIENTED_EDGE ( 'NONE', *, *, #22391, .F. ) ;
#4779=CARTESIAN_POINT ( 'NONE',  ( 26.04756280548352976, 24.61655718144339389, 110.4687147111160357 ) ) ;
#4780=FACE_OUTER_BOUND ( 'NONE', #14497, .T. ) ;
#4781=ORIENTED_EDGE ( 'NONE', *, *, #10805, .F. ) ;
#4782=VERTEX_POINT ( 'NONE', #1867 ) ;
#4783=EDGE_CURVE ( 'NONE', #9740, #10557, #13290, .T. ) ;
#4784=VERTEX_POINT ( 'NONE', #3610 ) ;
#4785=CARTESIAN_POINT ( 'NONE',  ( 109.1586900883932856, 0.005236795036868161120, 0.004851151255031871216 ) ) ;
#4786=CARTESIAN_POINT ( 'NONE',  ( 109.1721716018069657, -0.01699510305644696614, -0.001583175916619995001 ) ) ;
#4789=CARTESIAN_POINT ( 'NONE',  ( 109.1586900883932856, -0.006757191295056145380, 0.002301750759607874407 ) ) ;
#4792=( BOUNDED_SURFACE ( )  B_SPLINE_SURFACE ( 3, 1, ( 
 ( #4941, #2638 ),
 ( #13573, #16308 ),
 ( #13714, #14135 ),
 ( #6980, #22957 ) ),
 .UNSPECIFIED., .F., .F., .F. ) 
 B_SPLINE_SURFACE_WITH_KNOTS ( ( 4, 4 ),
 ( 2, 2 ),
 ( 0.000000000000000000, 1.000000000000000000 ),
 ( 0.000000000000000000, 1.000000000000000000 ),
 .UNSPECIFIED. ) 
 GEOMETRIC_REPRESENTATION_ITEM ( )  RATIONAL_B_SPLINE_SURFACE ( (
 ( 1.000000000000000000, 1.000000000000000000),
 ( 0.9956975270656954757, 0.8568959468854893125),
 ( 0.9956975270656954757, 0.8568959468854893125),
 ( 1.000000000000000000, 1.000000000000000000) ) ) 
 REPRESENTATION_ITEM ( '' )  SURFACE ( )  );
#4794=CARTESIAN_POINT ( 'NONE',  ( 109.1586900883932856, -0.004851151255031892033, 0.005236795036868142038 ) ) ;
#4795=DIRECTION ( 'NONE',  ( 0.000000000000000000, 0.000000000000000000, 1.000000000000000000 ) ) ;
#4796=CARTESIAN_POINT ( 'NONE',  ( 5.340103579038074422, 140.9275371836310455, 43.36842539899422633 ) ) ;
#4798=CARTESIAN_POINT ( 'NONE',  ( 2.063896406836609909, -118.3103904147675962, -84.29612368209275530 ) ) ;
#4799=CARTESIAN_POINT ( 'NONE',  ( 26.04756280548354397, -65.62256188141788016, 92.21166514879074327 ) ) ;
#4800=CARTESIAN_POINT ( 'NONE',  ( 6.224689322667630975, -126.9212313063839588, -76.23997225729401350 ) ) ;
#4802=VERTEX_POINT ( 'NONE', #5934 ) ;
#4803=CARTESIAN_POINT ( 'NONE',  ( 109.1586900883932856, -0.004277182003220990347, 0.005715190711488705826 ) ) ;
#4804=CARTESIAN_POINT ( 'NONE',  ( 25.64699802086725811, -66.55977212001099019, -91.20712948285722632 ) ) ;
#4805=CARTESIAN_POINT ( 'NONE',  ( 109.1624594426973260, -0.003771499231549682845, 0.01551217196236918082 ) ) ;
#4807=CARTESIAN_POINT ( 'NONE',  ( 10.93730112725978287, -136.0306644680987915, 65.95960219663069779 ) ) ;
#4810=CARTESIAN_POINT ( 'NONE',  ( 1.833721034905646752, -15.52204855105742176, -144.2772269874177198 ) ) ;
#4812=VERTEX_POINT ( 'NONE', #9066 ) ;
#4813=CARTESIAN_POINT ( 'NONE',  ( 1.833485406944043827, 117.7091014914961420, -84.86072343962446496 ) ) ;
#4815=ORIENTED_EDGE ( 'NONE', *, *, #6490, .F. ) ;
#4816=EDGE_CURVE ( 'NONE', #1490, #7808, #8168, .T. ) ;
#4817=CARTESIAN_POINT ( 'NONE',  ( 13.84597867724963294, 129.3717503931862325, -69.17016226638924081 ) ) ;
#4818=ORIENTED_EDGE ( 'NONE', *, *, #23496, .F. ) ;
#4819=CARTESIAN_POINT ( 'NONE',  ( 1.833485406944043827, -97.49333871408619245, -107.4794113447419477 ) ) ;
#4822=CARTESIAN_POINT ( 'NONE',  ( 1.893872463202060485, -125.2243573918629096, -73.39855082356775995 ) ) ;
#4824=LINE ( 'NONE', #14935, #957 ) ;
#4825=CARTESIAN_POINT ( 'NONE',  ( 1.893872463202018963, 137.7483215415849713, 45.75900850850049295 ) ) ;
#4831=FACE_OUTER_BOUND ( 'NONE', #8783, .T. ) ;
#4836=CARTESIAN_POINT ( 'NONE',  ( 26.11404676487256893, -110.9778746459748362, 22.43340081644731043 ) ) ;
#4838=VERTEX_POINT ( 'NONE', #17823 ) ;
#4839=CARTESIAN_POINT ( 'NONE',  ( 1.833721034905662295, 45.17977675814314864, 137.8972080590633027 ) ) ;
#4840=CARTESIAN_POINT ( 'NONE',  ( 24.01988960052062794, -49.36855864442049580, -121.3896480498355714 ) ) ;
#4841=CARTESIAN_POINT ( 'NONE',  ( 55.79472521941426777, 49.22042574086499656, -53.57698701322163970 ) ) ;
#4842=ORIENTED_EDGE ( 'NONE', *, *, #24981, .T. ) ;
#4843=CARTESIAN_POINT ( 'NONE',  ( 25.64704443564078673, 75.65149037849873537, -83.82001435192547945 ) ) ;
#4844=EDGE_CURVE ( 'NONE', #18428, #11607, #2644, .T. ) ;
#4845=ORIENTED_EDGE ( 'NONE', *, *, #28444, .F. ) ;
#4846=CARTESIAN_POINT ( 'NONE',  ( 119.2224693531408803, -6.245004513516543405E-14, 20.00000000000018119 ) ) ;
#4847=EDGE_CURVE ( 'NONE', #12354, #4901, #17068, .T. ) ;
#4849=DIRECTION ( 'NONE',  ( -1.000000000000000000, -0.000000000000000000, -0.000000000000000000 ) ) ;
#4851=CARTESIAN_POINT ( 'NONE',  ( 25.81918753295377655, 112.3053965977763511, -12.74259626488037256 ) ) ;
#4852=ORIENTED_EDGE ( 'NONE', *, *, #10092, .F. ) ;
#4853=ORIENTED_EDGE ( 'NONE', *, *, #13308, .F. ) ;
#4856=CARTESIAN_POINT ( 'NONE',  ( 30.59138290137870442, 111.3296280985502165, 33.33271994911384439 ) ) ;
#4860=ORIENTED_EDGE ( 'NONE', *, *, #24344, .T. ) ;
#4861=CARTESIAN_POINT ( 'NONE',  ( 13.36082413113061307, 53.25066407421994796, -143.3553710183984435 ) ) ;
#4862=CARTESIAN_POINT ( 'NONE',  ( 2.433796855181205476, 145.5024947199069629, 1.451562450950146133 ) ) ;
#4865=ORIENTED_EDGE ( 'NONE', *, *, #189, .T. ) ;
#4868=CARTESIAN_POINT ( 'NONE',  ( 26.11404676487259024, -47.08215554553450488, -102.9690087468806325 ) ) ;
#4870=DIRECTION ( 'NONE',  ( 0.5946245182733608248, 0.4701913299128731016, 0.6521823330503037086 ) ) ;
#4871=CARTESIAN_POINT ( 'NONE',  ( 10.93730112726024117, 133.3192575531818136, -71.28103789254788580 ) ) ;
#4872=( BOUNDED_SURFACE ( )  B_SPLINE_SURFACE ( 3, 1, ( 
 ( #7825, #28080 ),
 ( #8385, #6228 ),
 ( #20898, #9983 ),
 ( #16585, #25379 ) ),
 .UNSPECIFIED., .F., .F., .F. ) 
 B_SPLINE_SURFACE_WITH_KNOTS ( ( 4, 4 ),
 ( 2, 2 ),
 ( 0.000000000000000000, 1.000000000000000000 ),
 ( 0.000000000000000000, 1.000000000000000000 ),
 .UNSPECIFIED. ) 
 GEOMETRIC_REPRESENTATION_ITEM ( )  RATIONAL_B_SPLINE_SURFACE ( (
 ( 1.000000000000000000, 1.000000000000000000),
 ( 0.6386103224230316178, 0.9954351624131538845),
 ( 0.6386103224230316178, 0.9954351624131538845),
 ( 1.000000000000000000, 1.000000000000000000) ) ) 
 REPRESENTATION_ITEM ( '' )  SURFACE ( )  );
#4873=CARTESIAN_POINT ( 'NONE',  ( 1.832998868059858122, 72.09222286251082323, 125.9352106559986311 ) ) ;
#4874=VERTEX_POINT ( 'NONE', #26333 ) ;
#4877=CARTESIAN_POINT ( 'NONE',  ( 1.833809397773905614, -145.1096615951801141, -0.1779672212515608920 ) ) ;
#4878=CARTESIAN_POINT ( 'NONE',  ( 25.86096068574581963, 102.8701285401541696, 46.89265070732157881 ) ) ;
#4880=ORIENTED_EDGE ( 'NONE', *, *, #5427, .F. ) ;
#4881=FACE_OUTER_BOUND ( 'NONE', #8965, .T. ) ;
#4882=VERTEX_POINT ( 'NONE', #11497 ) ;
#4883=DIRECTION ( 'NONE',  ( 0.000000000000000000, 0.000000000000000000, 1.000000000000000000 ) ) ;
#4884=B_SPLINE_CURVE_WITH_KNOTS ( 'NONE', 3,
 ( #15775, #5269, #20523, #7298, #3115, #24586, #3259, #26854 ),
 .UNSPECIFIED., .F., .F.,
 ( 4, 2, 2, 4 ),
 ( 0.000000000000000000, 0.0002429588503611208340, 0.0004859177007222416681, 0.0009718354014444833362 ),
 .UNSPECIFIED. ) ;
#4885=ADVANCED_FACE ( 'NONE', ( #21883 ), #3875, .F. ) ;
#4886=CARTESIAN_POINT ( 'NONE',  ( 25.64700659047694842, -56.25842064176025303, -97.89757946487067386 ) ) ;
#4888=EDGE_CURVE ( 'NONE', #5555, #26700, #9936, .T. ) ;
#4889=ORIENTED_EDGE ( 'NONE', *, *, #4056, .F. ) ;
#4890=ORIENTED_EDGE ( 'NONE', *, *, #7357, .T. ) ;
#4891=DIRECTION ( 'NONE',  ( 0.000000000000000000, 0.000000000000000000, 1.000000000000000000 ) ) ;
#4892=CARTESIAN_POINT ( 'NONE',  ( 109.1721716018069657, -0.009868622090676078262, 0.01392660302850765031 ) ) ;
#4893=DIRECTION ( 'NONE',  ( 0.000000000000000000, 0.000000000000000000, 1.000000000000000000 ) ) ;
#4894=CARTESIAN_POINT ( 'NONE',  ( 109.1587776205901577, 0.003592288931009604384, 0.006388631651928904608 ) ) ;
#4898=CARTESIAN_POINT ( 'NONE',  ( 1.832998868059858122, -15.69902610990277836, -144.2584710144581948 ) ) ;
#4899=ADVANCED_FACE ( 'NONE', ( #708 ), #27224, .F. ) ;
#4900=CARTESIAN_POINT ( 'NONE',  ( 1.833485406944043827, -142.0485807715647297, 29.64752363041495542 ) ) ;
#4901=VERTEX_POINT ( 'NONE', #25055 ) ;
#4903=VERTEX_POINT ( 'NONE', #16397 ) ;
#4905=CARTESIAN_POINT ( 'NONE',  ( 25.64681081121879203, -46.30456157731261868, -102.9795863647033229 ) ) ;
#4906=CARTESIAN_POINT ( 'NONE',  ( 1.832998868059890096, -144.3700883710216090, -14.63705790014157060 ) ) ;
#4911=CYLINDRICAL_SURFACE ( 'NONE', #10220, 12.50000000000000178 ) ;
#4912=( BOUNDED_SURFACE ( )  B_SPLINE_SURFACE ( 3, 1, ( 
 ( #6920, #13230 ),
 ( #6636, #15524 ),
 ( #24483, #2435 ),
 ( #9071, #24200 ) ),
 .UNSPECIFIED., .F., .F., .F. ) 
 B_SPLINE_SURFACE_WITH_KNOTS ( ( 4, 4 ),
 ( 2, 2 ),
 ( 0.000000000000000000, 1.000000000000000000 ),
 ( 0.000000000000000000, 1.000000000000000000 ),
 .UNSPECIFIED. ) 
 GEOMETRIC_REPRESENTATION_ITEM ( )  RATIONAL_B_SPLINE_SURFACE ( (
 ( 1.000000000000000000, 1.000000000000000000),
 ( 0.6386103224230302855, 0.9954351624131538845),
 ( 0.6386103224230302855, 0.9954351624131538845),
 ( 1.000000000000000000, 1.000000000000000000) ) ) 
 REPRESENTATION_ITEM ( '' )  SURFACE ( )  );
#4915=CARTESIAN_POINT ( 'NONE',  ( 2.430230287190581429, 107.1617224697464366, 98.44218333480804972 ) ) ;
#4916=LINE ( 'NONE', #22488, #6177 ) ;
#4917=CARTESIAN_POINT ( 'NONE',  ( 25.64703792032471341, -107.3388703233124346, 35.03296646432524142 ) ) ;
#4919=VERTEX_POINT ( 'NONE', #13945 ) ;
#4920=CARTESIAN_POINT ( 'NONE',  ( 1.893872463202054046, -126.1771883101041851, 71.74819926215134558 ) ) ;
#4921=CARTESIAN_POINT ( 'NONE',  ( 1.834118845439484335, -117.5010238212692855, -85.14950727125977892 ) ) ;
#4923=VERTEX_POINT ( 'NONE', #16539 ) ;
#4925=CARTESIAN_POINT ( 'NONE',  ( 9.884929003653608603, -35.39789245780430349, 146.3148513795965755 ) ) ;
#4927=CARTESIAN_POINT ( 'NONE',  ( 21.16825799904901473, 51.02216409572741895, -125.4548537968708786 ) ) ;
#4928=CARTESIAN_POINT ( 'NONE',  ( 119.2224693531407382, -90.00000000000005684, 20.00000000000004263 ) ) ;
#4930=FACE_OUTER_BOUND ( 'NONE', #5192, .T. ) ;
#4932=CARTESIAN_POINT ( 'NONE',  ( 19.66333377628716406, 4.491394265034155175, -137.6761449113041920 ) ) ;
#4933=EDGE_CURVE ( 'NONE', #16681, #4784, #3020, .T. ) ;
#4935=CARTESIAN_POINT ( 'NONE',  ( 30.58324630866341209, 87.19147450740472038, -83.81536267638863080 ) ) ;
#4937=VERTEX_POINT ( 'NONE', #3021 ) ;
#4939=CARTESIAN_POINT ( 'NONE',  ( 26.11404676487257603, 76.59696442953305962, -83.38016054979703995 ) ) ;
#4940=CARTESIAN_POINT ( 'NONE',  ( 1.832998868059890096, -125.4013017422225857, -73.01698022778485608 ) ) ;
#4941=CARTESIAN_POINT ( 'NONE',  ( 109.1592201516379674, -0.007302213399779945366, 0.002913740842108614778 ) ) ;
#4944=CARTESIAN_POINT ( 'NONE',  ( 10.93730112725991432, -71.28103789254845424, -133.3192575531807620 ) ) ;
#4950=CARTESIAN_POINT ( 'NONE',  ( 1.833809397773860095, -96.96506043213376813, -107.9565774559021349 ) ) ;
#4952=B_SPLINE_CURVE_WITH_KNOTS ( 'NONE', 3,
 ( #25972, #23698, #18933, #25836, #6131, #3949, #19343, #14602, #6262, #23830 ),
 .UNSPECIFIED., .F., .F.,
 ( 4, 3, 3, 4 ),
 ( 8.944667923005411581E-18, 0.0002669560319015738814, 0.0005492286108966413453, 0.0008315040496093442472 ),
 .UNSPECIFIED. ) ;
#4953=B_SPLINE_CURVE_WITH_KNOTS ( 'NONE', 3,
 ( #17361, #24285, #17648, #2377 ),
 .UNSPECIFIED., .F., .F.,
 ( 4, 4 ),
 ( 5.689046731696576935E-16, 0.008383748772660036541 ),
 .UNSPECIFIED. ) ;
#4955=CARTESIAN_POINT ( 'NONE',  ( 26.11404676487257603, -113.2169081140373947, -1.130420376098323576 ) ) ;
#4958=ADVANCED_FACE ( 'NONE', ( #3158 ), #27569, .F. ) ;
#4959=FACE_OUTER_BOUND ( 'NONE', #17435, .T. ) ;
#4960=CARTESIAN_POINT ( 'NONE',  ( 25.64681081121879203, 110.3564950173084895, -23.88203588907973085 ) ) ;
#4961=EDGE_CURVE ( 'NONE', #26564, #3869, #245, .T. ) ;
#4962=CARTESIAN_POINT ( 'NONE',  ( 2.433796855181219243, -125.2830755159749003, -74.00833731765692391 ) ) ;
#4963=CARTESIAN_POINT ( 'NONE',  ( 32.73300124599732186, 0.000000000000000000, 0.000000000000000000 ) ) ;
#4964=CARTESIAN_POINT ( 'NONE',  ( 109.1586900883932856, 0.005715190711488721438, 0.004277182003220971265 ) ) ;
#4968=CARTESIAN_POINT ( 'NONE',  ( 1.833485406944057594, -72.09189602597798796, 125.9346397303433065 ) ) ;
#4970=CARTESIAN_POINT ( 'NONE',  ( 109.1586900883932856, 0.003481399864218433400, -0.006231977675085001445 ) ) ;
#4971=CARTESIAN_POINT ( 'NONE',  ( 1.834118845439484335, -44.67218053242488196, 138.0627591860428254 ) ) ;
#4972=CARTESIAN_POINT ( 'NONE',  ( 26.11404676487259024, -112.4785329405482912, 12.95861723607416671 ) ) ;
#4973=ADVANCED_FACE ( 'NONE', ( #23460 ), #26472, .F. ) ;
#4974=CARTESIAN_POINT ( 'NONE',  ( 21.16825799904934158, 135.3612955721062860, -4.416019842158871889 ) ) ;
#4975=CARTESIAN_POINT ( 'NONE',  ( 1.833485406944043827, 45.34878176254236593, 137.8414413349087511 ) ) ;
#4976=CARTESIAN_POINT ( 'NONE',  ( 109.1624594426973260, 0.01503296564240497526, 0.005372302061310759227 ) ) ;
#4977=ORIENTED_EDGE ( 'NONE', *, *, #23231, .T. ) ;
#4978=CARTESIAN_POINT ( 'NONE',  ( 55.79472521941428198, 23.17337251492763883, 68.96476385670672471 ) ) ;
#4979=B_SPLINE_CURVE_WITH_KNOTS ( 'NONE', 3,
 ( #5323, #14096, #18714, #5183, #20723, #27485 ),
 .UNSPECIFIED., .F., .F.,
 ( 4, 2, 4 ),
 ( 3.469446951953613804E-18, 0.0006311636237756778267, 0.001262327247551352401 ),
 .UNSPECIFIED. ) ;
#4981=AXIS2_PLACEMENT_3D ( 'NONE', #8062, #7481, #16833 ) ;
#4982=AXIS2_PLACEMENT_3D ( 'NONE', #8847, #6544, #24393 ) ;
#4986=EDGE_LOOP ( 'NONE', ( #6716, #22119, #10590, #21995 ) ) ;
#4989=CARTESIAN_POINT ( 'NONE',  ( 10.93730112725990367, -104.7670965581004054, -108.9902118373752842 ) ) ;
#4991=CARTESIAN_POINT ( 'NONE',  ( 25.64692232868535626, -34.58055111992117503, 107.4854307433085978 ) ) ;
#4992=CARTESIAN_POINT ( 'NONE',  ( 25.64704443564078318, 110.4160069635933894, 23.60610532596994915 ) ) ;
#4993=EDGE_CURVE ( 'NONE', #8105, #25030, #19129, .T. ) ;
#4994=ORIENTED_EDGE ( 'NONE', *, *, #23226, .F. ) ;
#4995=CARTESIAN_POINT ( 'NONE',  ( 26.11404676487259024, -45.01677474591480888, 103.8885755249567922 ) ) ;
#5000=ORIENTED_EDGE ( 'NONE', *, *, #4993, .F. ) ;
#5006=B_SPLINE_CURVE_WITH_KNOTS ( 'NONE', 3,
 ( #9235, #26778, #7091, #15849 ),
 .UNSPECIFIED., .F., .F.,
 ( 4, 4 ),
 ( 0.000000000000000000, 0.01077107196513881274 ),
 .UNSPECIFIED. ) ;
#5008=CARTESIAN_POINT ( 'NONE',  ( 25.87036335909430207, 46.88819766600106931, 102.8789780196089936 ) ) ;
#5010=CARTESIAN_POINT ( 'NONE',  ( 2.433796855181219243, 118.5671979538068257, -84.34988187690807138 ) ) ;
#5012=CARTESIAN_POINT ( 'NONE',  ( 109.1592201516379674, -0.004194960840990111066, -0.006649399203953448162 ) ) ;
#5015=ORIENTED_EDGE ( 'NONE', *, *, #15033, .T. ) ;
#5016=CARTESIAN_POINT ( 'NONE',  ( 25.64660436782554598, -12.37913844082964410, -112.2303901742707950 ) ) ;
#5018=CARTESIAN_POINT ( 'NONE',  ( 26.04756280548352976, 110.4687147111163199, -24.61655718144232097 ) ) ;
#5019=CARTESIAN_POINT ( 'NONE',  ( 32.73300124599735739, 51.32617430724909013, 105.8473486001052777 ) ) ;
#5020=EDGE_LOOP ( 'NONE', ( #22422, #18386, #10870, #19373 ) ) ;
#5021=VERTEX_POINT ( 'NONE', #6185 ) ;
#5023=CARTESIAN_POINT ( 'NONE',  ( 32.73300124599732186, 0.000000000000000000, 0.000000000000000000 ) ) ;
#5024=CARTESIAN_POINT ( 'NONE',  ( 2.430230287190581429, 96.28466919684099423, 109.1043569252017420 ) ) ;
#5025=CARTESIAN_POINT ( 'NONE',  ( 32.73300124599732186, 0.000000000000000000, 0.000000000000000000 ) ) ;
#5026=CARTESIAN_POINT ( 'NONE',  ( 19.66333377628702195, 18.85786579350133607, -136.4524620437342435 ) ) ;
#5027=VERTEX_POINT ( 'NONE', #1695 ) ;
#5029=ADVANCED_FACE ( 'NONE', ( #28167 ), #6817, .F. ) ;
#5030=CARTESIAN_POINT ( 'NONE',  ( 1.833603222531970944, 45.26427810763087933, -137.8693250773473267 ) ) ;
#5031=( BOUNDED_SURFACE ( )  B_SPLINE_SURFACE ( 3, 1, ( 
 ( #28024, #8324 ),
 ( #17230, #19955 ),
 ( #18207, #2671 ),
 ( #664, #2824 ) ),
 .UNSPECIFIED., .F., .F., .F. ) 
 B_SPLINE_SURFACE_WITH_KNOTS ( ( 4, 4 ),
 ( 2, 2 ),
 ( 0.000000000000000000, 1.000000000000000000 ),
 ( 0.000000000000000000, 1.000000000000000000 ),
 .UNSPECIFIED. ) 
 GEOMETRIC_REPRESENTATION_ITEM ( )  RATIONAL_B_SPLINE_SURFACE ( (
 ( 1.000000000000000000, 1.000000000000000000),
 ( 0.9960225298536222738, 0.9999952330161893110),
 ( 0.9960225298536222738, 0.9999952330161893110),
 ( 1.000000000000000000, 1.000000000000000000) ) ) 
 REPRESENTATION_ITEM ( '' )  SURFACE ( )  );
#5033=ORIENTED_EDGE ( 'NONE', *, *, #10867, .T. ) ;
#5034=ADVANCED_FACE ( 'NONE', ( #19259 ), #27401, .F. ) ;
#5035=B_SPLINE_CURVE_WITH_KNOTS ( 'NONE', 3,
 ( #14687, #23493, #27359, #9970, #1595, #27503, #12254 ),
 .UNSPECIFIED., .F., .F.,
 ( 4, 3, 4 ),
 ( 0.0004157520161266013833, 0.0005492286108966324548, 0.0008315040496093446809 ),
 .UNSPECIFIED. ) ;
#5036=ORIENTED_EDGE ( 'NONE', *, *, #14570, .T. ) ;
#5038=CARTESIAN_POINT ( 'NONE',  ( 32.73300124599741423, 114.2056417606551406, -28.19767303745493336 ) ) ;
#5040=ADVANCED_FACE ( 'NONE', ( #10077 ), #8830, .F. ) ;
#5041=CARTESIAN_POINT ( 'NONE',  ( 109.1778270068192853, 0.004958088776550212406, -0.007885345421907750257 ) ) ;
#5043=ORIENTED_EDGE ( 'NONE', *, *, #12995, .T. ) ;
#5046=CARTESIAN_POINT ( 'NONE',  ( 109.1586900883932856, 0.007088091345232578125, 0.0008465529156546095163 ) ) ;
#5047=B_SPLINE_CURVE_WITH_KNOTS ( 'NONE', 3,
 ( #17313, #26102, #6391, #26656, #15722, #16750, #23376 ),
 .UNSPECIFIED., .F., .F.,
 ( 4, 3, 4 ),
 ( 0.000000000000000000, 0.02398743853561295311, 0.04000277880656212537 ),
 .UNSPECIFIED. ) ;
#5048=B_SPLINE_CURVE_WITH_KNOTS ( 'NONE', 3,
 ( #3861, #25180, #8063, #25480, #14210, #14512, #21413, #18983, #27761, #1686 ),
 .UNSPECIFIED., .F., .F.,
 ( 4, 3, 3, 4 ),
 ( 0.000000000000000000, 0.0002669560319015692193, 0.0005492286108966405863, 0.0008315040496093498851 ),
 .UNSPECIFIED. ) ;
#5049=CARTESIAN_POINT ( 'NONE',  ( 109.1589550718175161, -0.007270618150635364818, -0.002126635388718505718 ) ) ;
#5050=CARTESIAN_POINT ( 'NONE',  ( 25.73574536432415982, -76.18908113044813035, 83.41179791497836504 ) ) ;
#5051=CARTESIAN_POINT ( 'NONE',  ( 9.884929003653626367, 109.0134320167746722, -103.8128997986846827 ) ) ;
#5052=ORIENTED_EDGE ( 'NONE', *, *, #19812, .T. ) ;
#5056=VERTEX_POINT ( 'NONE', #27892 ) ;
#5057=CARTESIAN_POINT ( 'NONE',  ( 55.49584447822657296, -68.91748907713572692, -22.67407039687311610 ) ) ;
#5058=CIRCLE ( 'NONE', #2760, 117.6351876552689504 ) ;
#5059=CARTESIAN_POINT ( 'NONE',  ( 10.93730112725932635, 0.000000000000000000, 0.000000000000000000 ) ) ;
#5064=CARTESIAN_POINT ( 'NONE',  ( 1.833206308920067196, -97.64934899952775993, 107.3376449983724541 ) ) ;
#5066=DIRECTION ( 'NONE',  ( 0.000000000000000000, 0.000000000000000000, 1.000000000000000000 ) ) ;
#5067=CARTESIAN_POINT ( 'NONE',  ( 25.98107933586745588, 113.1286487641198022, 1.091357942390989155 ) ) ;
#5068=FACE_OUTER_BOUND ( 'NONE', #25578, .T. ) ;
#5069=CARTESIAN_POINT ( 'NONE',  ( 25.86096068574578410, 33.98552076022196644, 107.8247115223743435 ) ) ;
#5071=CARTESIAN_POINT ( 'NONE',  ( 2.430230287190581429, -98.44218333480841920, 107.1617224697460955 ) ) ;
#5072=CARTESIAN_POINT ( 'NONE',  ( 55.79472521941428198, 49.22042574086425759, 53.57698701322232893 ) ) ;
#5074=VECTOR ( 'NONE', #27927, 999.9999999999998863 ) ;
#5076=CARTESIAN_POINT ( 'NONE',  ( 109.1778270068192853, 0.006682187084639316411, 0.006489198140358653361 ) ) ;
#5077=AXIS2_PLACEMENT_3D ( 'NONE', #1981, #10782, #22388 ) ;
#5078=CARTESIAN_POINT ( 'NONE',  ( 1.833691583653552115, -144.2771263798445887, -15.52203496789063664 ) ) ;
#5079=CARTESIAN_POINT ( 'NONE',  ( 55.49584447822657296, -42.86099773636501453, -58.53775398922299900 ) ) ;
#5082=ORIENTED_EDGE ( 'NONE', *, *, #13272, .F. ) ;
#5083=CARTESIAN_POINT ( 'NONE',  ( 32.73300124599735739, 28.19767303745605602, 114.2056417606549132 ) ) ;
#5084=CONICAL_SURFACE ( 'NONE', #12876, 117.6351876552689504, 0.9945805576725580410 ) ;
#5085=ORIENTED_EDGE ( 'NONE', *, *, #8590, .F. ) ;
#5086=CARTESIAN_POINT ( 'NONE',  ( 25.86096068574583029, 103.6815822123525095, -45.07009591924456515 ) ) ;
#5088=ORIENTED_EDGE ( 'NONE', *, *, #10523, .F. ) ;
#5089=ORIENTED_EDGE ( 'NONE', *, *, #1113, .F. ) ;
#5090=ORIENTED_EDGE ( 'NONE', *, *, #886, .F. ) ;
#5091=CARTESIAN_POINT ( 'NONE',  ( 109.1592201516379674, -0.0005146241775983334847, -0.007845213074654432128 ) ) ;
#5093=ADVANCED_FACE ( 'NONE', ( #15338 ), #9761, .F. ) ;
#5096=ADVANCED_FACE ( 'NONE', ( #3989 ), #10849, .F. ) ;
#5098=CARTESIAN_POINT ( 'NONE',  ( 1.832998868059890096, -132.3466930259797891, 59.50898020732464744 ) ) ;
#5101=CARTESIAN_POINT ( 'NONE',  ( 109.1721716018069515, 0.01629455849719223248, -0.005082060336465326310 ) ) ;
#5103=LINE ( 'NONE', #1080, #544 ) ;
#5107=CARTESIAN_POINT ( 'NONE',  ( 30.59138290137891047, -88.14703743378190381, -75.73279410806814838 ) ) ;
#5108=CARTESIAN_POINT ( 'NONE',  ( 25.70243777736190083, 83.44449745408539343, 76.12033502296544896 ) ) ;
#5112=DIRECTION ( 'NONE',  ( 0.000000000000000000, 0.000000000000000000, 1.000000000000000000 ) ) ;
#5114=CARTESIAN_POINT ( 'NONE',  ( 30.58324630866339078, -116.1819705588610816, -33.60235057864094443 ) ) ;
#5115=B_SPLINE_CURVE_WITH_KNOTS ( 'NONE', 3,
 ( #10959, #17561, #9081, #19869, #19723, #24495, #26768, #26349, #20151, #4611 ),
 .UNSPECIFIED., .F., .F.,
 ( 4, 3, 3, 4 ),
 ( 3.816391647148975608E-17, 0.0002669559177086135637, 0.0005339118354150864786, 0.001067817517169152757 ),
 .UNSPECIFIED. ) ;
#5118=ORIENTED_EDGE ( 'NONE', *, *, #10105, .F. ) ;
#5119=CARTESIAN_POINT ( 'NONE',  ( 1.833485406944043827, 45.34878176254236593, 137.8414413349087511 ) ) ;
#5120=AXIS2_PLACEMENT_3D ( 'NONE', #4185, #24341, #12818 ) ;
#5122=CARTESIAN_POINT ( 'NONE',  ( 109.1592201516379674, 0.007302213399779926284, -0.002913740842108661615 ) ) ;
#5125=AXIS2_PLACEMENT_3D ( 'NONE', #9733, #7585, #22846 ) ;
#5126=ORIENTED_EDGE ( 'NONE', *, *, #10304, .T. ) ;
#5127=DIRECTION ( 'NONE',  ( 0.000000000000000000, 0.000000000000000000, 1.000000000000000000 ) ) ;
#5128=EDGE_CURVE ( 'NONE', #22381, #22329, #21907, .T. ) ;
#5130=CARTESIAN_POINT ( 'NONE',  ( 2.108985857320890389, -132.2056553747750343, 60.26444811757351516 ) ) ;
#5133=ADVANCED_FACE ( 'NONE', ( #17717 ), #6655, .F. ) ;
#5136=B_SPLINE_CURVE_WITH_KNOTS ( 'NONE', 3,
 ( #10119, #25666, #5655, #5945, #21465, #3770, #10407, #1738, #18890, #10537 ),
 .UNSPECIFIED., .F., .F.,
 ( 4, 3, 3, 4 ),
 ( 3.816391647148975608E-17, 0.0002669559177086172500, 0.0005339118354150979712, 0.001067817517169165550 ),
 .UNSPECIFIED. ) ;
#5137=ORIENTED_EDGE ( 'NONE', *, *, #16551, .T. ) ;
#5138=CARTESIAN_POINT ( 'NONE',  ( 28.43349137099829349, -94.99961975860206564, -80.08535015164004278 ) ) ;
#5140=CARTESIAN_POINT ( 'NONE',  ( 28.37599760073043242, -75.42809173301549208, -86.45296943207098650 ) ) ;
#5142=VERTEX_POINT ( 'NONE', #17574 ) ;
#5145=CARTESIAN_POINT ( 'NONE',  ( 25.98552792386799126, 98.51438617140739495, 55.63155129532967891 ) ) ;
#5146=ORIENTED_EDGE ( 'NONE', *, *, #25133, .F. ) ;
#5147=VECTOR ( 'NONE', #17005, 1000.000000000000000 ) ;
#5149=ORIENTED_EDGE ( 'NONE', *, *, #14886, .T. ) ;
#5151=CARTESIAN_POINT ( 'NONE',  ( 1.831572820252008738, -132.9644823688599331, 58.11906524360431803 ) ) ;
#5153=DIRECTION ( 'NONE',  ( -0.5946245182733608248, -0.4045541647807384122, -0.6948076064830700505 ) ) ;
#5155=CARTESIAN_POINT ( 'NONE',  ( 1.833809397773845662, 107.7184108265663980, 97.22957127128873367 ) ) ;
#5160=CARTESIAN_POINT ( 'NONE',  ( 109.1592201516379674, -0.006174480289199440856, 0.004867031887019522031 ) ) ;
#5161=CARTESIAN_POINT ( 'NONE',  ( 109.1586059443104944, -0.004935564877218434968, 0.005067816690893726939 ) ) ;
#5163=ORIENTED_EDGE ( 'NONE', *, *, #10092, .T. ) ;
#5165=EDGE_CURVE ( 'NONE', #19216, #26175, #5792, .T. ) ;
#5167=CARTESIAN_POINT ( 'NONE',  ( 109.1586900883932856, 0.002995460350180810267, -0.006479576224403795805 ) ) ;
#5168=ORIENTED_EDGE ( 'NONE', *, *, #25133, .T. ) ;
#5169=EDGE_CURVE ( 'NONE', #21319, #15966, #13252, .T. ) ;
#5170=CIRCLE ( 'NONE', #10688, 117.6351876552689504 ) ;
#5171=ORIENTED_EDGE ( 'NONE', *, *, #21445, .F. ) ;
#5173=VECTOR ( 'NONE', #6362, 1000.000000000000227 ) ;
#5174=EDGE_CURVE ( 'NONE', #15441, #17576, #9167, .T. ) ;
#5175=CARTESIAN_POINT ( 'NONE',  ( 26.11404676487257603, 84.89295829319495112, 74.91683232331003239 ) ) ;
#5176=EDGE_CURVE ( 'NONE', #10776, #2577, #4032, .T. ) ;
#5177=CARTESIAN_POINT ( 'NONE',  ( 24.22246935314087324, -69.99999999999998579, -40.00000000000002132 ) ) ;
#5178=CARTESIAN_POINT ( 'NONE',  ( 2.433796855181233454, 144.8571464219889151, 13.76554153471742481 ) ) ;
#5179=CARTESIAN_POINT ( 'NONE',  ( 5.340103556456345046, 108.0219267027630252, 100.3626145793565172 ) ) ;
#5182=CARTESIAN_POINT ( 'NONE',  ( 25.64703792032473118, 35.03296646432561090, 107.3388703233122783 ) ) ;
#5183=CARTESIAN_POINT ( 'NONE',  ( 1.893872463202041612, -116.8661275359691700, -86.08597552418997623 ) ) ;
#5184=VERTEX_POINT ( 'NONE', #6947 ) ;
#5185=VERTEX_POINT ( 'NONE', #9668 ) ;
#5188=CARTESIAN_POINT ( 'NONE',  ( 109.1592201516379674, 0.007376275279030877242, 0.002720803050361335265 ) ) ;
#5189=DIRECTION ( 'NONE',  ( 0.000000000000000000, 0.000000000000000000, 1.000000000000000000 ) ) ;
#5190=CARTESIAN_POINT ( 'NONE',  ( 1.831572820252008738, 137.7011124121617058, 45.77972211429861460 ) ) ;
#5192=EDGE_LOOP ( 'NONE', ( #4574, #13786, #23413, #13637 ) ) ;
#5197=CARTESIAN_POINT ( 'NONE',  ( 25.70243777736191859, -76.12033502296576160, 83.44449745408508079 ) ) ;
#5199=VERTEX_POINT ( 'NONE', #18145 ) ;
#5201=EDGE_LOOP ( 'NONE', ( #16212, #25599, #17051, #27369 ) ) ;
#5202=CARTESIAN_POINT ( 'NONE',  ( 1.833838850855489255, 145.1097630809417467, 0.08898185259624630250 ) ) ;
#5203=ORIENTED_EDGE ( 'NONE', *, *, #7633, .T. ) ;
#5207=EDGE_CURVE ( 'NONE', #12120, #4838, #12946, .T. ) ;
#5209=( BOUNDED_SURFACE ( )  B_SPLINE_SURFACE ( 3, 1, ( 
 ( #21847, #11325 ),
 ( #11046, #379 ),
 ( #2386, #2683 ),
 ( #24294, #15619 ) ),
 .UNSPECIFIED., .F., .F., .F. ) 
 B_SPLINE_SURFACE_WITH_KNOTS ( ( 4, 4 ),
 ( 2, 2 ),
 ( 0.000000000000000000, 1.000000000000000000 ),
 ( 0.000000000000000000, 1.000000000000000000 ),
 .UNSPECIFIED. ) 
 GEOMETRIC_REPRESENTATION_ITEM ( )  RATIONAL_B_SPLINE_SURFACE ( (
 ( 1.000000000000000000, 1.000000000000000000),
 ( 0.6386103224230302855, 0.9954351624131538845),
 ( 0.6386103224230302855, 0.9954351624131538845),
 ( 1.000000000000000000, 1.000000000000000000) ) ) 
 REPRESENTATION_ITEM ( '' )  SURFACE ( )  );
#5212=CARTESIAN_POINT ( 'NONE',  ( 109.1592201516379674, 0.006174480289199407029, -0.004867031887019566266 ) ) ;
#5214=B_SPLINE_CURVE_WITH_KNOTS ( 'NONE', 3,
 ( #666, #6589, #13469, #17915, #24148, #20224, #4410, #520, #22266, #13614 ),
 .UNSPECIFIED., .F., .F.,
 ( 4, 3, 3, 4 ),
 ( 3.469446951953614189E-18, 0.0002669560319015759414, 0.0005492286108966491515, 0.0008315040496093429462 ),
 .UNSPECIFIED. ) ;
#5216=CARTESIAN_POINT ( 'NONE',  ( 119.2224693531408803, 90.00000000000005684, 39.99999999999999289 ) ) ;
#5218=CARTESIAN_POINT ( 'NONE',  ( 10.93730112725995873, 4.928439153522441885, -151.0983828010091656 ) ) ;
#5219=CARTESIAN_POINT ( 'NONE',  ( 109.1592201516379674, -0.007620268632968129653, -0.001934867487012907703 ) ) ;
#5224=CARTESIAN_POINT ( 'NONE',  ( 16.05277956358209579, -25.20902801311468266, 141.0713346807233393 ) ) ;
#5225=CARTESIAN_POINT ( 'NONE',  ( 25.64660436782543940, 75.98230157781860328, 83.52001792470919384 ) ) ;
#5226=CARTESIAN_POINT ( 'NONE',  ( 25.64704443564077252, 45.80316013050833135, 103.2037466592375807 ) ) ;
#5227=CARTESIAN_POINT ( 'NONE',  ( 13.36082413113061307, -152.6206443696329416, 9.660980093454195838 ) ) ;
#5228=CARTESIAN_POINT ( 'NONE',  ( 13.36082413113063083, 117.7941133658638790, 97.52406103376794988 ) ) ;
#5229=ORIENTED_EDGE ( 'NONE', *, *, #4041, .T. ) ;
#5230=DIRECTION ( 'NONE',  ( -0.5946245182733607137, 0.7332888028688970827, -0.3297108033645145819 ) ) ;
#5231=ORIENTED_EDGE ( 'NONE', *, *, #21295, .T. ) ;
#5233=CARTESIAN_POINT ( 'NONE',  ( 1.893872463202043832, 0.9528309182417881162, -145.1467500857187929 ) ) ;
#5234=VERTEX_POINT ( 'NONE', #3187 ) ;
#5238=B_SPLINE_CURVE_WITH_KNOTS ( 'NONE', 3,
 ( #12258, #7967, #16574, #2647, #7133, #4817, #2792 ),
 .UNSPECIFIED., .F., .F.,
 ( 4, 3, 4 ),
 ( 0.000000000000000000, 0.02398743853561391762, 0.04000277880656258334 ),
 .UNSPECIFIED. ) ;
#5240=ADVANCED_FACE ( 'NONE', ( #24662 ), #12688, .F. ) ;
#5243=EDGE_CURVE ( 'NONE', #19356, #12270, #5035, .T. ) ;
#5245=CARTESIAN_POINT ( 'NONE',  ( 1.833721034905634317, 144.2772269874178050, -15.52204855105691905 ) ) ;
#5247=CARTESIAN_POINT ( 'NONE',  ( 10.93730112725970294, 65.95960219663110990, 136.0306644680985642 ) ) ;
#5248=CARTESIAN_POINT ( 'NONE',  ( 32.73300124599735028, 84.80615050150375112, 81.52272205837232377 ) ) ;
#5249=CARTESIAN_POINT ( 'NONE',  ( 1.833838848569416147, -59.18404309081275017, -132.4919773286275415 ) ) ;
#5251=LINE ( 'NONE', #3240, #20810 ) ;
#5252=CARTESIAN_POINT ( 'NONE',  ( 26.11404676487257603, 83.38016054979783576, 76.59696442953219275 ) ) ;
#5258=FACE_OUTER_BOUND ( 'NONE', #24, .T. ) ;
#5259=CARTESIAN_POINT ( 'NONE',  ( 1.833206310202336153, 144.3905118062894530, 14.42724831649402617 ) ) ;
#5260=EDGE_CURVE ( 'NONE', #5291, #25128, #12289, .T. ) ;
#5261=ORIENTED_EDGE ( 'NONE', *, *, #27085, .T. ) ;
#5265=ORIENTED_EDGE ( 'NONE', *, *, #18518, .T. ) ;
#5267=EDGE_CURVE ( 'NONE', #26744, #27903, #6419, .T. ) ;
#5269=CARTESIAN_POINT ( 'NONE',  ( 25.64670758986456889, -112.3434365398309041, 11.30712635241953024 ) ) ;
#5274=CARTESIAN_POINT ( 'NONE',  ( 109.1624594426973260, 0.001206615835671176864, 0.01591840958352308891 ) ) ;
#5275=ORIENTED_EDGE ( 'NONE', *, *, #9945, .T. ) ;
#5277=B_SPLINE_CURVE_WITH_KNOTS ( 'NONE', 3,
 ( #25861, #19642, #2216, #1945, #17070, #80, #3840, #4394 ),
 .UNSPECIFIED., .F., .F.,
 ( 4, 2, 2, 4 ),
 ( 6.938893903907228378E-18, 0.0002429588503611338987, 0.0004859177007222608585, 0.0009718354014444862635 ),
 .UNSPECIFIED. ) ;
#5279=B_SPLINE_CURVE_WITH_KNOTS ( 'NONE', 3,
 ( #9578, #22985, #3104, #27272 ),
 .UNSPECIFIED., .F., .F.,
 ( 4, 4 ),
 ( 0.000000000000000000, 0.01077107196513891682 ),
 .UNSPECIFIED. ) ;
#5281=CARTESIAN_POINT ( 'NONE',  ( 32.73300124599733607, 103.7392577722176270, 55.46353551262048853 ) ) ;
#5282=CARTESIAN_POINT ( 'NONE',  ( 25.64681081121879203, 107.5125461021407318, -34.49579773461672971 ) ) ;
#5285=EDGE_LOOP ( 'NONE', ( #781, #27994, #23543, #23280 ) ) ;
#5289=EDGE_LOOP ( 'NONE', ( #9575, #7580, #17038, #17449 ) ) ;
#5290=B_SPLINE_CURVE_WITH_KNOTS ( 'NONE', 3,
 ( #13391, #15695, #22190, #2457, #4476, #15 ),
 .UNSPECIFIED., .F., .F.,
 ( 4, 2, 4 ),
 ( 6.952433221959954168E-18, 0.0006311571484585832377, 0.001262314296917159536 ),
 .UNSPECIFIED. ) ;
#5291=VERTEX_POINT ( 'NONE', #25653 ) ;
#5292=ORIENTED_EDGE ( 'NONE', *, *, #7679, .F. ) ;
#5295=CARTESIAN_POINT ( 'NONE',  ( 1.833691583653511925, 108.0753610255266466, -96.83253123394105444 ) ) ;
#5296=CARTESIAN_POINT ( 'NONE',  ( 25.64681081121879203, 11.38886654529823694, -112.3352186517029594 ) ) ;
#5299=CARTESIAN_POINT ( 'NONE',  ( 26.28373643307403995, -127.4927519498667010, 4.159810388345953847 ) ) ;
#5300=EDGE_CURVE ( 'NONE', #25430, #3869, #14407, .T. ) ;
#5304=CARTESIAN_POINT ( 'NONE',  ( 109.1589550718174877, -0.007453082872776649326, 0.001354998915261305167 ) ) ;
#5305=ADVANCED_FACE ( 'NONE', ( #19021 ), #13770, .F. ) ;
#5308=ORIENTED_EDGE ( 'NONE', *, *, #21224, .T. ) ;
#5309=DIRECTION ( 'NONE',  ( 0.000000000000000000, 0.000000000000000000, 1.000000000000000000 ) ) ;
#5310=CARTESIAN_POINT ( 'NONE',  ( 1.833809397773803918, -29.99591688576986570, -141.9756687985007204 ) ) ;
#5312=ORIENTED_EDGE ( 'NONE', *, *, #23726, .F. ) ;
#5313=EDGE_LOOP ( 'NONE', ( #3446, #3300, #11572, #1170 ) ) ;
#5315=EDGE_CURVE ( 'NONE', #16951, #27330, #4378, .T. ) ;
#5316=CARTESIAN_POINT ( 'NONE',  ( 28.37603512858449406, -111.8384105897143570, 25.60641750873868361 ) ) ;
#5317=CARTESIAN_POINT ( 'NONE',  ( 25.64681081121879203, 56.81519825470756047, 97.57530875170624540 ) ) ;
#5319=CARTESIAN_POINT ( 'NONE',  ( 32.73300124599738581, 16.10546300444979195, -116.5274707358853163 ) ) ;
#5320=ORIENTED_EDGE ( 'NONE', *, *, #11233, .F. ) ;
#5321=CARTESIAN_POINT ( 'NONE',  ( 26.11404676487257603, 67.46175819463486789, -90.92995828888132337 ) ) ;
#5322=CARTESIAN_POINT ( 'NONE',  ( 25.64708228042121618, -103.1656011680036045, 45.88917180166242815 ) ) ;
#5323=CARTESIAN_POINT ( 'NONE',  ( 2.433796855181205476, -116.8607839509050734, -86.69855925934092511 ) ) ;
#5324=ORIENTED_EDGE ( 'NONE', *, *, #13308, .T. ) ;
#5325=EDGE_CURVE ( 'NONE', #24050, #14114, #18727, .T. ) ;
#5326=ORIENTED_EDGE ( 'NONE', *, *, #8529, .T. ) ;
#5330=DIRECTION ( 'NONE',  ( 1.000000000000000000, 0.000000000000000000, 0.000000000000000000 ) ) ;
#5334=ORIENTED_EDGE ( 'NONE', *, *, #16210, .T. ) ;
#5335=DIRECTION ( 'NONE',  ( 0.5914120900931444380, 0.5455001977188090878, -0.5938529060132641257 ) ) ;
#5336=CARTESIAN_POINT ( 'NONE',  ( 1.833485406944057594, 138.1714136985308699, 44.33323125129973619 ) ) ;
#5337=CARTESIAN_POINT ( 'NONE',  ( 2.063896406836609909, -96.20114399516467074, 108.8509294491461787 ) ) ;
#5339=B_SPLINE_CURVE_WITH_KNOTS ( 'NONE', 3,
 ( #14486, #16509, #6013, #16809, #12465, #10044, #3691, #27441 ),
 .UNSPECIFIED., .F., .F.,
 ( 4, 2, 2, 4 ),
 ( 6.938893903907228378E-18, 0.0002429588503611250624, 0.0004859177007222431860, 0.0009718354014444615437 ),
 .UNSPECIFIED. ) ;
#5341=CARTESIAN_POINT ( 'NONE',  ( 2.063896406836609909, -60.31174178979723166, -132.1577797566312142 ) ) ;
#5342=CARTESIAN_POINT ( 'NONE',  ( 109.1592201516379674, -0.007051465909552739365, 0.003476928926134781935 ) ) ;
#5344=ADVANCED_FACE ( 'NONE', ( #5790 ), #14703, .F. ) ;
#5345=ORIENTED_EDGE ( 'NONE', *, *, #15749, .F. ) ;
#5352=B_SPLINE_CURVE_WITH_KNOTS ( 'NONE', 3,
 ( #1614, #25948, #12275, #26077, #21191, #12405, #19180, #12826, #5815, #19042 ),
 .UNSPECIFIED., .F., .F.,
 ( 4, 3, 3, 4 ),
 ( 3.122502256758252770E-17, 0.0002669559177086221831, 0.0005339118354151072953, 0.001067817517169176392 ),
 .UNSPECIFIED. ) ;
#5356=FACE_OUTER_BOUND ( 'NONE', #17512, .T. ) ;
#5357=CARTESIAN_POINT ( 'NONE',  ( 2.263178607246642660, -13.80342482180185115, 144.7392885066942654 ) ) ;
#5360=CARTESIAN_POINT ( 'NONE',  ( 1.833691583653512369, 132.4191286035306518, 59.34641645332686011 ) ) ;
#5361=EDGE_CURVE ( 'NONE', #1807, #27476, #9538, .T. ) ;
#5362=CARTESIAN_POINT ( 'NONE',  ( 32.73300124599732186, 0.000000000000000000, 0.000000000000000000 ) ) ;
#5364=CARTESIAN_POINT ( 'NONE',  ( 30.58324630866342275, -106.6567942264192368, -57.02364853894589203 ) ) ;
#5365=ADVANCED_FACE ( 'NONE', ( #18589 ), #11063, .T. ) ;
#5366=CARTESIAN_POINT ( 'NONE',  ( 13.36082413113063083, -9.660980093455732387, 152.6206443696328563 ) ) ;
#5367=CARTESIAN_POINT ( 'NONE',  ( 109.1721716018069515, -0.01550977894511840725, -0.007126480965768139213 ) ) ;
#5368=CARTESIAN_POINT ( 'NONE',  ( 32.73300124599737160, -89.94078864464117373, 75.82012867748450446 ) ) ;
#5370=CARTESIAN_POINT ( 'NONE',  ( 32.73300124599740002, 103.7392577722183660, -55.46353551261898218 ) ) ;
#5371=CARTESIAN_POINT ( 'NONE',  ( 25.64699802086726521, 83.75009658924095390, -75.72889180797035635 ) ) ;
#5372=ORIENTED_EDGE ( 'NONE', *, *, #17569, .F. ) ;
#5373=DIRECTION ( 'NONE',  ( 0.5946245182733607137, 0.7999021332774030046, -0.08110646981858811444 ) ) ;
#5376=CARTESIAN_POINT ( 'NONE',  ( 10.93730112725971715, 20.69552240458328995, 149.7554878793148703 ) ) ;
#5377=ORIENTED_EDGE ( 'NONE', *, *, #15924, .T. ) ;
#5382=FACE_OUTER_BOUND ( 'NONE', #19250, .T. ) ;
#5383=CARTESIAN_POINT ( 'NONE',  ( 1.833485406944043827, 85.72460230293849293, -117.0814567582535659 ) ) ;
#5384=B_SPLINE_CURVE_WITH_KNOTS ( 'NONE', 3,
 ( #13693, #14117, #462, #18006 ),
 .UNSPECIFIED., .F., .F.,
 ( 4, 4 ),
 ( 9.837579971998123693E-17, 0.008383748772659571635 ),
 .UNSPECIFIED. ) ;
#5386=B_SPLINE_CURVE_WITH_KNOTS ( 'NONE', 3,
 ( #2410, #18101, #13348, #8920, #11346, #2855, #125, #11481, #17677, #26456 ),
 .UNSPECIFIED., .F., .F.,
 ( 4, 3, 3, 4 ),
 ( 0.000000000000000000, 0.0002669560319015801698, 0.0005492286108966397190, 0.0008315040496093522703 ),
 .UNSPECIFIED. ) ;
#5388=CARTESIAN_POINT ( 'NONE',  ( 19.66333377628710366, -137.6761449113042772, -4.491394265033680000 ) ) ;
#5389=CARTESIAN_POINT ( 'NONE',  ( 2.433796855181205476, -137.9325382748282038, -46.34326152018883249 ) ) ;
#5390=CARTESIAN_POINT ( 'NONE',  ( 109.1589550718175161, -0.001354998915253822220, 0.007453082872782193502 ) ) ;
#5391=CARTESIAN_POINT ( 'NONE',  ( 1.831572820252008738, -43.90210991190526357, -138.3111855986065564 ) ) ;
#5392=EDGE_CURVE ( 'NONE', #10557, #26958, #11936, .T. ) ;
#5396=LINE ( 'NONE', #10313, #12456 ) ;
#5397=EDGE_CURVE ( 'NONE', #9920, #1176, #16111, .T. ) ;
#5398=EDGE_LOOP ( 'NONE', ( #4048, #7638, #27241, #563 ) ) ;
#5400=CARTESIAN_POINT ( 'NONE',  ( 32.73300124599739291, -99.90245962373785460, -62.10906484417343165 ) ) ;
#5401=CARTESIAN_POINT ( 'NONE',  ( 2.433796855181205476, -16.65276281464661423, 144.5536872373191102 ) ) ;
#5402=CARTESIAN_POINT ( 'NONE',  ( 1.831572820252009626, 126.1609924456730170, 71.69925593429853450 ) ) ;
#5404=CARTESIAN_POINT ( 'NONE',  ( 32.73300124599738581, -32.68291970228155918, -113.0038235389605461 ) ) ;
#5405=CYLINDRICAL_SURFACE ( 'NONE', #5125, 12.50000000000000178 ) ;
#5406=ORIENTED_EDGE ( 'NONE', *, *, #7093, .T. ) ;
#5407=EDGE_LOOP ( 'NONE', ( #19419, #8984, #23779, #16565 ) ) ;
#5409=CARTESIAN_POINT ( 'NONE',  ( 9.884929003653608603, 42.50195158091032965, 144.4113244745773272 ) ) ;
#5410=CARTESIAN_POINT ( 'NONE',  ( 16.75465622695650936, -138.0797984721905323, -34.09043808962561428 ) ) ;
#5412=CARTESIAN_POINT ( 'NONE',  ( 25.64708010899964208, -97.75667227735131348, 56.50300922386559677 ) ) ;
#5413=DIRECTION ( 'NONE',  ( -1.000000000000000000, -0.000000000000000000, -0.000000000000000000 ) ) ;
#5414=( BOUNDED_SURFACE ( )  B_SPLINE_SURFACE ( 3, 1, ( 
 ( #12555, #17160 ),
 ( #10695, #23806 ),
 ( #12829, #19461 ),
 ( #19047, #6799 ) ),
 .UNSPECIFIED., .F., .F., .F. ) 
 B_SPLINE_SURFACE_WITH_KNOTS ( ( 4, 4 ),
 ( 2, 2 ),
 ( 0.000000000000000000, 1.000000000000000000 ),
 ( 0.000000000000000000, 1.000000000000000000 ),
 .UNSPECIFIED. ) 
 GEOMETRIC_REPRESENTATION_ITEM ( )  RATIONAL_B_SPLINE_SURFACE ( (
 ( 1.000000000000000000, 1.000000000000000000),
 ( 0.6386103224230316178, 0.9954351624131538845),
 ( 0.6386103224230316178, 0.9954351624131538845),
 ( 1.000000000000000000, 1.000000000000000000) ) ) 
 REPRESENTATION_ITEM ( '' )  SURFACE ( )  );
#5415=ORIENTED_EDGE ( 'NONE', *, *, #13652, .T. ) ;
#5416=CARTESIAN_POINT ( 'NONE',  ( 1.832998868059890096, -44.33343224355141388, -138.1720401012271395 ) ) ;
#5418=CARTESIAN_POINT ( 'NONE',  ( 25.73574536432414916, -45.21157800100239399, -103.5288236655400027 ) ) ;
#5419=DIRECTION ( 'NONE',  ( 0.5946245182733607137, -0.1642747008466192427, -0.7870422510449660569 ) ) ;
#5425=CARTESIAN_POINT ( 'NONE',  ( 109.1592201516379674, -0.007376275279032879113, 0.002720803050370542309 ) ) ;
#5426=CARTESIAN_POINT ( 'NONE',  ( 1.833838850855475044, -107.7780290788690536, -97.16351016226002457 ) ) ;
#5427=EDGE_CURVE ( 'NONE', #20744, #25928, #8369, .T. ) ;
#5432=CARTESIAN_POINT ( 'NONE',  ( 28.37644542392845892, -17.02293047611445687, 123.1691345231581352 ) ) ;
#5433=ORIENTED_EDGE ( 'NONE', *, *, #25952, .T. ) ;
#5436=CARTESIAN_POINT ( 'NONE',  ( 10.93730112725996406, 10.89264110825190457, -150.7858122213661716 ) ) ;
#5438=DIRECTION ( 'NONE',  ( -1.000000000000000000, -0.000000000000000000, -0.000000000000000000 ) ) ;
#5439=LINE ( 'NONE', #8727, #4055 ) ;
#5440=CARTESIAN_POINT ( 'NONE',  ( 26.11404676487257603, -110.9778746459745520, -22.43340081644882389 ) ) ;
#5445=CARTESIAN_POINT ( 'NONE',  ( 19.66333377628716406, -129.5498775999581085, -46.81583828063196506 ) ) ;
#5446=CARTESIAN_POINT ( 'NONE',  ( 109.1592201516379674, -0.006044422199831509662, -0.005027640251764362717 ) ) ;
#5447=CARTESIAN_POINT ( 'NONE',  ( 25.64681081121879203, 110.3564950173081769, 23.88203588908119457 ) ) ;
#5448=CARTESIAN_POINT ( 'NONE',  ( 109.1586059443104944, -0.003774052605959072812, 0.005983234375919664789 ) ) ;
#5450=FACE_BOUND ( 'NONE', #15960, .T. ) ;
#5451=B_SPLINE_CURVE_WITH_KNOTS ( 'NONE', 3,
 ( #22097, #11165, #11732, #17772 ),
 .UNSPECIFIED., .F., .F.,
 ( 4, 4 ),
 ( 0.000000000000000000, 0.01077107196513816395 ),
 .UNSPECIFIED. ) ;
#5453=ORIENTED_EDGE ( 'NONE', *, *, #1726, .T. ) ;
#5454=B_SPLINE_CURVE_WITH_KNOTS ( 'NONE', 3,
 ( #12074, #27596, #986, #27014, #7327, #12212, #14358, #3009, #1263, #22888 ),
 .UNSPECIFIED., .F., .F.,
 ( 4, 3, 3, 4 ),
 ( 0.000000000000000000, 0.0002669560319015888434, 0.0005492286108966463326, 0.0008315040496093561734 ),
 .UNSPECIFIED. ) ;
#5455=CARTESIAN_POINT ( 'NONE',  ( 2.108985857320942348, 28.95357181521022127, -142.3791757917249186 ) ) ;
#5458=VERTEX_POINT ( 'NONE', #12666 ) ;
#5464=ADVANCED_FACE ( 'NONE', ( #13090 ), #11597, .F. ) ;
#5465=CARTESIAN_POINT ( 'NONE',  ( 25.64681081121880624, -23.88203588908156760, 110.3564950173080916 ) ) ;
#5466=CARTESIAN_POINT ( 'NONE',  ( 25.69398547355840989, 97.43788956976230509, -57.11291030433552152 ) ) ;
#5467=ORIENTED_EDGE ( 'NONE', *, *, #11247, .T. ) ;
#5468=CARTESIAN_POINT ( 'NONE',  ( 1.893872463202055600, -144.4512189534318622, 14.22435552397961978 ) ) ;
#5471=CARTESIAN_POINT ( 'NONE',  ( 25.64704443564076541, 34.76451658509533615, 107.4261196778963949 ) ) ;
#5472=CARTESIAN_POINT ( 'NONE',  ( 1.833485406944057594, -45.34878176254139248, -137.8414413349090637 ) ) ;
#5473=ORIENTED_EDGE ( 'NONE', *, *, #8645, .F. ) ;
#5474=ORIENTED_EDGE ( 'NONE', *, *, #13305, .T. ) ;
#5477=CARTESIAN_POINT ( 'NONE',  ( 1.833206308920100724, 107.3376449983727809, 97.64934899952737624 ) ) ;
#5478=CARTESIAN_POINT ( 'NONE',  ( 25.64681081121879203, 56.09509703373481670, -97.99105938547863559 ) ) ;
#5481=CARTESIAN_POINT ( 'NONE',  ( 24.22246935314087324, -90.00000000000005684, 39.99999999999997158 ) ) ;
#5483=CARTESIAN_POINT ( 'NONE',  ( 2.433796855181233454, 43.58222566461826375, -138.8296532063083646 ) ) ;
#5485=DIRECTION ( 'NONE',  ( -1.000000000000000000, -0.000000000000000000, -0.000000000000000000 ) ) ;
#5486=CARTESIAN_POINT ( 'NONE',  ( 26.11404676487259024, -45.01677474591480888, 103.8885755249567922 ) ) ;
#5487=CARTESIAN_POINT ( 'NONE',  ( 109.1592201516379674, 0.004194960840980690650, -0.006649399203953405661 ) ) ;
#5488=CARTESIAN_POINT ( 'NONE',  ( 25.64708010899963853, -75.51173009720581319, 83.94602815988648103 ) ) ;
#5492=ORIENTED_EDGE ( 'NONE', *, *, #23041, .T. ) ;
#5493=EDGE_CURVE ( 'NONE', #7441, #1461, #23461, .T. ) ;
#5495=CARTESIAN_POINT ( 'NONE',  ( 19.66333377628679813, -108.7423656420555460, -84.55762186019691740 ) ) ;
#5497=B_SPLINE_CURVE_WITH_KNOTS ( 'NONE', 3,
 ( #8483, #17245, #24167, #28181, #4426, #13073, #11056, #2399, #19549, #14942 ),
 .UNSPECIFIED., .F., .F.,
 ( 4, 3, 3, 4 ),
 ( 2.775557561562891351E-17, 0.0002669559177086104737, 0.0005339118354150823587, 0.001067817517169155576 ),
 .UNSPECIFIED. ) ;
#5499=CARTESIAN_POINT ( 'NONE',  ( 8.186469777910884815, -143.0750864738775192, -42.84118569629491446 ) ) ;
#5506=CARTESIAN_POINT ( 'NONE',  ( 1.833485406944043827, -59.50871042846314651, 132.3460930279889567 ) ) ;
#5507=CARTESIAN_POINT ( 'NONE',  ( 109.1586900883932856, -0.004701023939945749193, 0.005371970278528625728 ) ) ;
#5510=B_SPLINE_CURVE_WITH_KNOTS ( 'NONE', 3,
 ( #24252, #24830, #6985, #11146, #9556, #5086, #11425, #22521 ),
 .UNSPECIFIED., .F., .F.,
 ( 4, 2, 2, 4 ),
 ( 1.430489624538199204E-17, 0.0002429588503611245745, 0.0004859177007222348376, 0.0009718354014444673984 ),
 .UNSPECIFIED. ) ;
#5511=CARTESIAN_POINT ( 'NONE',  ( 9.884929003653608603, 148.0628878137283948, -27.17402761732198613 ) ) ;
#5522=ORIENTED_EDGE ( 'NONE', *, *, #9562, .F. ) ;
#5524=ADVANCED_FACE ( 'NONE', ( #21736 ), #21354, .F. ) ;
#5525=EDGE_CURVE ( 'NONE', #19015, #5056, #2156, .T. ) ;
#5526=CARTESIAN_POINT ( 'NONE',  ( 1.831572820252008738, 59.92262167723615107, -132.1614873090342712 ) ) ;
#5527=CIRCLE ( 'NONE', #6001, 151.1787379149930359 ) ;
#5528=EDGE_CURVE ( 'NONE', #15977, #13981, #22155, .T. ) ;
#5534=( BOUNDED_SURFACE ( )  B_SPLINE_SURFACE ( 3, 1, ( 
 ( #10981, #4209 ),
 ( #13128, #4486 ),
 ( #8823, #17860 ),
 ( #4785, #21779 ) ),
 .UNSPECIFIED., .F., .F., .F. ) 
 B_SPLINE_SURFACE_WITH_KNOTS ( ( 4, 4 ),
 ( 2, 2 ),
 ( 0.000000000000000000, 1.000000000000000000 ),
 ( 0.000000000000000000, 1.000000000000000000 ),
 .UNSPECIFIED. ) 
 GEOMETRIC_REPRESENTATION_ITEM ( )  RATIONAL_B_SPLINE_SURFACE ( (
 ( 1.000000000000000000, 1.000000000000000000),
 ( 0.9960225298536222738, 0.9999952330161893110),
 ( 0.9960225298536222738, 0.9999952330161893110),
 ( 1.000000000000000000, 1.000000000000000000) ) ) 
 REPRESENTATION_ITEM ( '' )  SURFACE ( )  );
#5535=CARTESIAN_POINT ( 'NONE',  ( 25.86096068574580542, 35.88291140784058797, -107.2082119295148459 ) ) ;
#5536=CARTESIAN_POINT ( 'NONE',  ( 109.1586900883932856, -0.002109621908824192878, -0.006819617742892434241 ) ) ;
#5537=CARTESIAN_POINT ( 'NONE',  ( 1.833485406944043827, -58.53321471326791681, -132.7804117027893938 ) ) ;
#5539=CARTESIAN_POINT ( 'NONE',  ( 10.93730112725945602, 104.7670965581007607, 108.9902118373744742 ) ) ;
#5540=CARTESIAN_POINT ( 'NONE',  ( 8.186469829614269500, -131.0413692472658340, 71.65198613712934161 ) ) ;
#5542=ORIENTED_EDGE ( 'NONE', *, *, #8750, .F. ) ;
#5544=CARTESIAN_POINT ( 'NONE',  ( 55.49584447822657296, 42.42793568433036455, -58.85239198729144761 ) ) ;
#5546=CARTESIAN_POINT ( 'NONE',  ( 26.11404676487257603, 57.58742681967585497, -97.48350837663548418 ) ) ;
#5547=CARTESIAN_POINT ( 'NONE',  ( 8.186469829614233973, 12.15801983495625116, 148.8557359502361805 ) ) ;
#5550=( BOUNDED_SURFACE ( )  B_SPLINE_SURFACE ( 3, 1, ( 
 ( #18585, #11823 ),
 ( #18723, #27641 ),
 ( #7665, #872 ),
 ( #16424, #7516 ) ),
 .UNSPECIFIED., .F., .F., .F. ) 
 B_SPLINE_SURFACE_WITH_KNOTS ( ( 4, 4 ),
 ( 2, 2 ),
 ( 0.000000000000000000, 1.000000000000000000 ),
 ( 0.000000000000000000, 1.000000000000000000 ),
 .UNSPECIFIED. ) 
 GEOMETRIC_REPRESENTATION_ITEM ( )  RATIONAL_B_SPLINE_SURFACE ( (
 ( 1.000000000000000000, 1.000000000000000000),
 ( 0.9956975270656954757, 0.8568959468854893125),
 ( 0.9956975270656954757, 0.8568959468854893125),
 ( 1.000000000000000000, 1.000000000000000000) ) ) 
 REPRESENTATION_ITEM ( '' )  SURFACE ( )  );
#5551=ORIENTED_EDGE ( 'NONE', *, *, #3227, .F. ) ;
#5552=CARTESIAN_POINT ( 'NONE',  ( 1.833206310202339262, 137.7753867363983886, -45.54896489827011408 ) ) ;
#5553=CARTESIAN_POINT ( 'NONE',  ( 109.1586900883932856, -0.007109207791181747921, 0.0006456433529163188882 ) ) ;
#5554=CARTESIAN_POINT ( 'NONE',  ( 32.73300124599738581, -114.2056417606545864, -28.19767303745721065 ) ) ;
#5555=VERTEX_POINT ( 'NONE', #2566 ) ;
#5556=CARTESIAN_POINT ( 'NONE',  ( 25.64703792032469920, -97.70949518026544922, 56.58441811305572600 ) ) ;
#5559=AXIS2_PLACEMENT_3D ( 'NONE', #5985, #4372, #19622 ) ;
#5561=AXIS2_PLACEMENT_3D ( 'NONE', #5579, #3420, #12201 ) ;
#5562=EDGE_CURVE ( 'NONE', #9016, #4553, #23159, .T. ) ;
#5563=CONICAL_SURFACE ( 'NONE', #16155, 117.6351876552689504, 0.9945805576725580410 ) ;
#5567=VERTEX_POINT ( 'NONE', #22748 ) ;
#5568=ADVANCED_FACE ( 'NONE', ( #24469 ), #22636, .F. ) ;
#5569=CARTESIAN_POINT ( 'NONE',  ( 109.1592201516379674, -0.005485778713193788063, 0.005631912476305676526 ) ) ;
#5570=EDGE_CURVE ( 'NONE', #2039, #5567, #20371, .T. ) ;
#5572=B_SPLINE_CURVE_WITH_KNOTS ( 'NONE', 3,
 ( #4047, #10683, #28353, #19035 ),
 .UNSPECIFIED., .F., .F.,
 ( 4, 4 ),
 ( 2.081668171172168513E-17, 0.008383748772659471021 ),
 .UNSPECIFIED. ) ;
#5573=CARTESIAN_POINT ( 'NONE',  ( 2.108985857320932578, -118.2933707022552454, -84.36123201973929042 ) ) ;
#5574=CARTESIAN_POINT ( 'NONE',  ( 16.75465622695635659, 133.7599617830029217, 48.33695624543378244 ) ) ;
#5575=ORIENTED_EDGE ( 'NONE', *, *, #19307, .F. ) ;
#5577=CARTESIAN_POINT ( 'NONE',  ( 10.93730112725945425, 115.5857507957700818, 97.44200844886312041 ) ) ;
#5579=CARTESIAN_POINT ( 'NONE',  ( 24.22246935314087324, 0.000000000000000000, 0.000000000000000000 ) ) ;
#5580=ORIENTED_EDGE ( 'NONE', *, *, #21590, .F. ) ;
#5581=VECTOR ( 'NONE', #2765, 1000.000000000000000 ) ;
#5582=VERTEX_POINT ( 'NONE', #20126 ) ;
#5584=AXIS2_PLACEMENT_3D ( 'NONE', #16241, #25047, #20696 ) ;
#5586=DIRECTION ( 'NONE',  ( 0.5914120900931444380, 0.8027508043202539190, -0.07630783613000559351 ) ) ;
#5588=CARTESIAN_POINT ( 'NONE',  ( 10.93730112726006176, 142.1801301103792809, -51.37919228020152929 ) ) ;
#5589=VECTOR ( 'NONE', #15372, 1000.000000000000000 ) ;
#5591=DIRECTION ( 'NONE',  ( -1.000000000000000000, 0.000000000000000000, 0.000000000000000000 ) ) ;
#5593=CARTESIAN_POINT ( 'NONE',  ( 1.833750490713684123, 107.6587173638747146, 97.29556423840173807 ) ) ;
#5594=DIRECTION ( 'NONE',  ( 0.000000000000000000, 0.000000000000000000, -1.000000000000000000 ) ) ;
#5595=ORIENTED_EDGE ( 'NONE', *, *, #13654, .T. ) ;
#5596=CARTESIAN_POINT ( 'NONE',  ( 8.186469777910868828, -137.8131828745823668, -57.56191611950443843 ) ) ;
#5598=( BOUNDED_SURFACE ( )  B_SPLINE_SURFACE ( 3, 1, ( 
 ( #24958, #9113 ),
 ( #22060, #4800 ),
 ( #22219, #24820 ),
 ( #6971, #19905 ) ),
 .UNSPECIFIED., .F., .F., .F. ) 
 B_SPLINE_SURFACE_WITH_KNOTS ( ( 4, 4 ),
 ( 2, 2 ),
 ( 0.000000000000000000, 1.000000000000000000 ),
 ( 0.000000000000000000, 1.000000000000000000 ),
 .UNSPECIFIED. ) 
 GEOMETRIC_REPRESENTATION_ITEM ( )  RATIONAL_B_SPLINE_SURFACE ( (
 ( 1.000000000000000000, 1.000000000000000000),
 ( 0.6386103224230302855, 0.9954351624131538845),
 ( 0.6386103224230302855, 0.9954351624131538845),
 ( 1.000000000000000000, 1.000000000000000000) ) ) 
 REPRESENTATION_ITEM ( '' )  SURFACE ( )  );
#5599=CONICAL_SURFACE ( 'NONE', #1462, 117.6351876552689504, 0.9945805576725580410 ) ;
#5600=CARTESIAN_POINT ( 'NONE',  ( 109.1624594426973260, -0.009004164758061298027, -0.01318243916934112685 ) ) ;
#5603=CARTESIAN_POINT ( 'NONE',  ( 25.73574536432414916, -110.6664861019685873, 22.69874377039401381 ) ) ;
#5604=CARTESIAN_POINT ( 'NONE',  ( 32.73300124599738581, 39.98094346392455378, -110.6325518752269517 ) ) ;
#5605=VERTEX_POINT ( 'NONE', #18109 ) ;
#5606=CARTESIAN_POINT ( 'NONE',  ( 16.75465622695653423, 62.05388459346063712, -127.9746229614479631 ) ) ;
#5607=CARTESIAN_POINT ( 'NONE',  ( 26.11404676487257603, 110.5078194225164481, -24.64483677384740545 ) ) ;
#5612=ORIENTED_EDGE ( 'NONE', *, *, #21079, .F. ) ;
#5613=B_SPLINE_CURVE_WITH_KNOTS ( 'NONE', 3,
 ( #24731, #20661, #27283, #7594, #16350, #16205 ),
 .UNSPECIFIED., .F., .F.,
 ( 4, 2, 4 ),
 ( 3.108012608937941465E-17, 0.0006311571484586140290, 0.001262314296917197484 ),
 .UNSPECIFIED. ) ;
#5614=EDGE_CURVE ( 'NONE', #23498, #13376, #14519, .T. ) ;
#5615=EDGE_CURVE ( 'NONE', #11790, #604, #8702, .T. ) ;
#5617=CARTESIAN_POINT ( 'NONE',  ( 25.81918753295378011, -102.8711004511196450, 46.82320532096481003 ) ) ;
#5620=CARTESIAN_POINT ( 'NONE',  ( 1.834118845439484335, 144.2964192726484214, -15.34511559672534986 ) ) ;
#5621=CARTESIAN_POINT ( 'NONE',  ( 1.833485406944043827, 138.1714136985314383, -44.33323125129781772 ) ) ;
#5622=CARTESIAN_POINT ( 'NONE',  ( 10.93730112725945247, 108.9902118373741331, 104.7670965581011302 ) ) ;
#5623=CARTESIAN_POINT ( 'NONE',  ( 1.833750490713697445, -125.5350013574264523, -72.78591676344089478 ) ) ;
#5624=CARTESIAN_POINT ( 'NONE',  ( 25.69398547355842766, -45.25878216557502043, 103.4778695380287559 ) ) ;
#5626=VERTEX_POINT ( 'NONE', #18691 ) ;
#5627=DIRECTION ( 'NONE',  ( 0.000000000000000000, 0.000000000000000000, 1.000000000000000000 ) ) ;
#5629=CARTESIAN_POINT ( 'NONE',  ( 2.263178607246703056, 84.32376080825709153, -118.4461883615806670 ) ) ;
#5631=CARTESIAN_POINT ( 'NONE',  ( 2.108393763691208012, -84.36147263237489824, -118.2927144690668086 ) ) ;
#5632=CARTESIAN_POINT ( 'NONE',  ( 1.833485406944057594, -137.8414413349088932, 45.34878176254188276 ) ) ;
#5633=ORIENTED_EDGE ( 'NONE', *, *, #818, .F. ) ;
#5634=CARTESIAN_POINT ( 'NONE',  ( 1.833603222531987598, -144.3605362014089337, 14.72553080638947343 ) ) ;
#5635=CARTESIAN_POINT ( 'NONE',  ( 8.186469777910941659, -34.43598809570042363, -145.3272523831807632 ) ) ;
#5638=B_SPLINE_CURVE_WITH_KNOTS ( 'NONE', 3,
 ( #4905, #24496, #11672, #11239, #727, #4612, #20011, #26769, #13533, #15844 ),
 .UNSPECIFIED., .F., .F.,
 ( 4, 3, 3, 4 ),
 ( 2.501853776554200607E-17, 0.0002669560319015822298, 0.0005492286108966468747, 0.0008315040496093393683 ),
 .UNSPECIFIED. ) ;
#5641=CARTESIAN_POINT ( 'NONE',  ( 25.64681081121880624, 66.03065707438935306, 91.59071981940594753 ) ) ;
#5643=VECTOR ( 'NONE', #14783, 1000.000000000000000 ) ;
#5644=EDGE_LOOP ( 'NONE', ( #26535, #17551, #25318, #6890 ) ) ;
#5645=CARTESIAN_POINT ( 'NONE',  ( 1.832998868059890096, -132.3466930259790217, -59.50898020732640958 ) ) ;
#5646=CARTESIAN_POINT ( 'NONE',  ( 10.93730112725972248, -36.23586118136624634, 146.7718404940640653 ) ) ;
#5647=ORIENTED_EDGE ( 'NONE', *, *, #14816, .F. ) ;
#5649=( BOUNDED_SURFACE ( )  B_SPLINE_SURFACE ( 3, 1, ( 
 ( #20576, #857 ),
 ( #9643, #22320 ),
 ( #18407, #20140 ),
 ( #27184, #715 ) ),
 .UNSPECIFIED., .F., .F., .F. ) 
 B_SPLINE_SURFACE_WITH_KNOTS ( ( 4, 4 ),
 ( 2, 2 ),
 ( 0.000000000000000000, 1.000000000000000000 ),
 ( 0.000000000000000000, 1.000000000000000000 ),
 .UNSPECIFIED. ) 
 GEOMETRIC_REPRESENTATION_ITEM ( )  RATIONAL_B_SPLINE_SURFACE ( (
 ( 1.000000000000000000, 1.000000000000000000),
 ( 0.6386103224230316178, 0.9954351624131538845),
 ( 0.6386103224230316178, 0.9954351624131538845),
 ( 1.000000000000000000, 1.000000000000000000) ) ) 
 REPRESENTATION_ITEM ( '' )  SURFACE ( )  );
#5650=EDGE_CURVE ( 'NONE', #21979, #11148, #7777, .T. ) ;
#5651=ORIENTED_EDGE ( 'NONE', *, *, #22098, .F. ) ;
#5652=ORIENTED_EDGE ( 'NONE', *, *, #28212, .T. ) ;
#5653=CARTESIAN_POINT ( 'NONE',  ( 26.28373643307412166, -30.57614217577372884, -123.8418562193901096 ) ) ;
#5654=CARTESIAN_POINT ( 'NONE',  ( 19.66333377628707879, -132.3257119126253940, 38.27269871461014361 ) ) ;
#5655=CARTESIAN_POINT ( 'NONE',  ( 1.833691583653541013, 30.51806994139792550, -141.8642667235905037 ) ) ;
#5658=VECTOR ( 'NONE', #3801, 1000.000000000000114 ) ;
#5661=CARTESIAN_POINT ( 'NONE',  ( 1.833838850855487035, 132.5281727421685787, 59.10274688031898904 ) ) ;
#5662=LINE ( 'NONE', #13993, #16718 ) ;
#5663=CARTESIAN_POINT ( 'NONE',  ( 32.73300124599735739, -103.7392577722179823, 55.46353551261974957 ) ) ;
#5664=CARTESIAN_POINT ( 'NONE',  ( 25.64681081121879203, -110.3564950173083474, 23.88203588908045916 ) ) ;
#5665=CARTESIAN_POINT ( 'NONE',  ( 5.340103556456292644, 143.7310399800117011, 32.90561046456755179 ) ) ;
#5666=EDGE_CURVE ( 'NONE', #8915, #22329, #11448, .T. ) ;
#5667=B_SPLINE_CURVE_WITH_KNOTS ( 'NONE', 3,
 ( #22302, #17398, #8632, #15375, #26598, #19565 ),
 .UNSPECIFIED., .F., .F.,
 ( 4, 2, 4 ),
 ( 3.469446951953614189E-18, 0.0006311636237756632984, 0.001262327247551323344 ),
 .UNSPECIFIED. ) ;
#5668=CARTESIAN_POINT ( 'NONE',  ( 25.64692872815577473, -66.10702795113353147, -91.53575854059484129 ) ) ;
#5669=CARTESIAN_POINT ( 'NONE',  ( 1.833485406944057594, 97.49333871408690300, 107.4794113447412940 ) ) ;
#5671=CARTESIAN_POINT ( 'NONE',  ( 32.73300124599738581, -115.8010721414081985, -20.69176323058746902 ) ) ;
#5672=ADVANCED_FACE ( 'NONE', ( #18981 ), #24661, .F. ) ;
#5673=VERTEX_POINT ( 'NONE', #7632 ) ;
#5674=CARTESIAN_POINT ( 'NONE',  ( 13.36082413113063083, 37.97423473099294000, 148.1362653801003830 ) ) ;
#5675=EDGE_CURVE ( 'NONE', #26606, #20294, #18455, .T. ) ;
#5676=ORIENTED_EDGE ( 'NONE', *, *, #23849, .F. ) ;
#5678=CARTESIAN_POINT ( 'NONE',  ( 28.37603512858440880, 105.5302493666427353, 45.02094145483413712 ) ) ;
#5679=ORIENTED_EDGE ( 'NONE', *, *, #4961, .F. ) ;
#5681=ORIENTED_EDGE ( 'NONE', *, *, #8143, .T. ) ;
#5682=VECTOR ( 'NONE', #871, 1000.000000000000000 ) ;
#5683=( BOUNDED_SURFACE ( )  B_SPLINE_SURFACE ( 3, 1, ( 
 ( #12379, #6072 ),
 ( #7809, #14961 ),
 ( #25921, #10662 ),
 ( #23351, #23487 ) ),
 .UNSPECIFIED., .F., .F., .F. ) 
 B_SPLINE_SURFACE_WITH_KNOTS ( ( 4, 4 ),
 ( 2, 2 ),
 ( 0.000000000000000000, 1.000000000000000000 ),
 ( 0.000000000000000000, 1.000000000000000000 ),
 .UNSPECIFIED. ) 
 GEOMETRIC_REPRESENTATION_ITEM ( )  RATIONAL_B_SPLINE_SURFACE ( (
 ( 1.000000000000000000, 1.000000000000000000),
 ( 0.9956975270656954757, 0.8568959468854893125),
 ( 0.9956975270656954757, 0.8568959468854893125),
 ( 1.000000000000000000, 1.000000000000000000) ) ) 
 REPRESENTATION_ITEM ( '' )  SURFACE ( )  );
#5685=CARTESIAN_POINT ( 'NONE',  ( 10.93730112725990367, -125.1380233598473950, -84.82621002473567273 ) ) ;
#5687=B_SPLINE_CURVE_WITH_KNOTS ( 'NONE', 3,
 ( #28016, #17082, #21688, #28156, #15050, #6580, #17355, #17225 ),
 .UNSPECIFIED., .F., .F.,
 ( 4, 2, 2, 4 ),
 ( 3.469446951953614189E-18, 0.0002429592666046748086, 0.0004859185332093461478, 0.0009718370664186862240 ),
 .UNSPECIFIED. ) ;
#5688=CARTESIAN_POINT ( 'NONE',  ( 16.75465622695653778, -142.1502242093126256, -4.637075857202995088 ) ) ;
#5689=CARTESIAN_POINT ( 'NONE',  ( 6.224689322667630975, 141.5842213414019568, -43.30635742325229387 ) ) ;
#5690=CARTESIAN_POINT ( 'NONE',  ( 25.64681081121879203, 35.28660243342691416, -107.2555980796237804 ) ) ;
#5695=CARTESIAN_POINT ( 'NONE',  ( 109.1721716018069657, 0.005082060336469409849, -0.01629455849720092692 ) ) ;
#5696=CARTESIAN_POINT ( 'NONE',  ( 1.833603222531999810, 132.7445893798465590, -58.61467103263608891 ) ) ;
#5698=EDGE_LOOP ( 'NONE', ( #3719, #15342, #17465, #15481 ) ) ;
#5700=DIRECTION ( 'NONE',  ( 0.000000000000000000, 0.000000000000000000, 1.000000000000000000 ) ) ;
#5701=EDGE_CURVE ( 'NONE', #4874, #9075, #7341, .T. ) ;
#5703=CARTESIAN_POINT ( 'NONE',  ( 25.64681081121879203, 75.86069728269103507, -83.63051021305824406 ) ) ;
#5704=CARTESIAN_POINT ( 'NONE',  ( 55.49584447822657296, 48.74506217377881967, 53.73688382046282186 ) ) ;
#5705=CARTESIAN_POINT ( 'NONE',  ( 1.831572820252008738, -116.8148281295963358, -86.09108691067891073 ) ) ;
#5706=DIRECTION ( 'NONE',  ( -1.000000000000000000, -0.000000000000000000, -0.000000000000000000 ) ) ;
#5707=ORIENTED_EDGE ( 'NONE', *, *, #23102, .T. ) ;
#5712=CARTESIAN_POINT ( 'NONE',  ( 1.833838848569429691, -14.99110384899624826, 144.3334397096298289 ) ) ;
#5714=B_SPLINE_CURVE_WITH_KNOTS ( 'NONE', 3,
 ( #27968, #10306, #19065, #8008, #16770, #23687, #27697, #3937, #3799, #25412 ),
 .UNSPECIFIED., .F., .F.,
 ( 4, 3, 3, 4 ),
 ( 2.428612866367529932E-17, 0.0002669559177086305315, 0.0005339118354151180289, 0.001067817517169162515 ),
 .UNSPECIFIED. ) ;
#5718=VECTOR ( 'NONE', #24019, 1000.000000000000114 ) ;
#5719=VERTEX_POINT ( 'NONE', #22226 ) ;
#5720=ORIENTED_EDGE ( 'NONE', *, *, #1960, .T. ) ;
#5723=CARTESIAN_POINT ( 'NONE',  ( 32.73300124599735739, -55.46353551262085091, 103.7392577722174565 ) ) ;
#5726=CARTESIAN_POINT ( 'NONE',  ( 1.833485406944043827, -59.50871042846314651, 132.3460930279889567 ) ) ;
#5727=CARTESIAN_POINT ( 'NONE',  ( 1.833485406944057594, -117.7091014914944225, -84.86072343962690923 ) ) ;
#5728=DIRECTION ( 'NONE',  ( 0.5914120900931444380, -0.7903769105750364510, 0.1598001217819286501 ) ) ;
#5729=CARTESIAN_POINT ( 'NONE',  ( 109.1586900883932856, -0.007137750914552287197, -0.0001010081143883946364 ) ) ;
#5730=CARTESIAN_POINT ( 'NONE',  ( 1.832998868059858122, 30.69214149074014841, 141.8272129421609691 ) ) ;
#5733=CARTESIAN_POINT ( 'NONE',  ( 28.43349137099835744, -4.052139611197551616, -124.1860347533534252 ) ) ;
#5738=ORIENTED_EDGE ( 'NONE', *, *, #6733, .T. ) ;
#5741=CARTESIAN_POINT ( 'NONE',  ( 10.93730112725945602, 84.82621002473440797, 125.1380233598478640 ) ) ;
#5742=EDGE_CURVE ( 'NONE', #5899, #25988, #2071, .T. ) ;
#5747=CARTESIAN_POINT ( 'NONE',  ( 1.833485406944043827, 72.09189602597706426, 125.9346397303438039 ) ) ;
#5748=DIRECTION ( 'NONE',  ( 0.000000000000000000, 0.000000000000000000, 1.000000000000000000 ) ) ;
#5749=ORIENTED_EDGE ( 'NONE', *, *, #20539, .F. ) ;
#5751=CARTESIAN_POINT ( 'NONE',  ( 13.84597867724974840, -25.80666409311465159, -144.4146018799366402 ) ) ;
#5753=CARTESIAN_POINT ( 'NONE',  ( 109.1721716018069515, -0.01127028715939363233, -0.01281875973823913897 ) ) ;
#5754=ADVANCED_FACE ( 'NONE', ( #13147 ), #1834, .F. ) ;
#5756=CARTESIAN_POINT ( 'NONE',  ( 109.1587776205901861, 0.004842060007769388025, -0.005502145856762321631 ) ) ;
#5757=CARTESIAN_POINT ( 'NONE',  ( 109.1586900883932856, 0.007109207791181753125, -0.0006456433529162696654 ) ) ;
#5759=B_SPLINE_CURVE_WITH_KNOTS ( 'NONE', 3,
 ( #21396, #21680, #23999, #14774, #10470, #3845, #21824, #2220 ),
 .UNSPECIFIED., .F., .F.,
 ( 4, 2, 2, 4 ),
 ( 2.030441771438897272E-17, 0.0002429592666046836720, 0.0004859185332093470693, 0.0009718370664186737557 ),
 .UNSPECIFIED. ) ;
#5760=CARTESIAN_POINT ( 'NONE',  ( 26.11404676487257603, -83.38016054979729574, -76.59696442953277540 ) ) ;
#5761=CARTESIAN_POINT ( 'NONE',  ( 109.1586059443104944, -0.005438258427231163275, -0.004524147648825544571 ) ) ;
#5762=CARTESIAN_POINT ( 'NONE',  ( 109.1624594426973260, -0.01263706729758975501, -0.009754804742273411738 ) ) ;
#5763=ORIENTED_EDGE ( 'NONE', *, *, #6361, .T. ) ;
#5764=FACE_OUTER_BOUND ( 'NONE', #4518, .T. ) ;
#5766=CARTESIAN_POINT ( 'NONE',  ( 109.1592201516379674, -0.0003082430541935533277, 0.007856029051018016685 ) ) ;
#5769=B_SPLINE_CURVE_WITH_KNOTS ( 'NONE', 3,
 ( #528, #13480, #22276, #24592, #4851, #13620, #26159, #22419 ),
 .UNSPECIFIED., .F., .F.,
 ( 4, 2, 2, 4 ),
 ( 1.250926888277100303E-17, 0.0002429592666046810699, 0.0004859185332093496172, 0.0009718370664186909945 ),
 .UNSPECIFIED. ) ;
#5770=CARTESIAN_POINT ( 'NONE',  ( 1.833691583653495716, -137.8971124741065637, -45.17974255430956276 ) ) ;
#5771=CARTESIAN_POINT ( 'NONE',  ( 5.340103579038303572, 117.9209211655070106, -88.52145169228850818 ) ) ;
#5772=B_SPLINE_CURVE_WITH_KNOTS ( 'NONE', 3,
 ( #8498, #1856, #19285, #12519, #15090, #2000, #23908 ),
 .UNSPECIFIED., .F., .F.,
 ( 4, 3, 4 ),
 ( 0.000000000000000000, 0.02398743853561418823, 0.04000277880656218088 ),
 .UNSPECIFIED. ) ;
#5773=CARTESIAN_POINT ( 'NONE',  ( 1.833838848569426139, -58.85887272891280730, 132.6367525013575346 ) ) ;
#5775=LINE ( 'NONE', #18857, #16876 ) ;
#5776=ORIENTED_EDGE ( 'NONE', *, *, #16868, .F. ) ;
#5777=( BOUNDED_SURFACE ( )  B_SPLINE_SURFACE ( 3, 1, ( 
 ( #14675, #23478 ),
 ( #6206, #25354 ),
 ( #21008, #10094 ),
 ( #14952, #5779 ) ),
 .UNSPECIFIED., .F., .F., .F. ) 
 B_SPLINE_SURFACE_WITH_KNOTS ( ( 4, 4 ),
 ( 2, 2 ),
 ( 0.000000000000000000, 1.000000000000000000 ),
 ( 0.000000000000000000, 1.000000000000000000 ),
 .UNSPECIFIED. ) 
 GEOMETRIC_REPRESENTATION_ITEM ( )  RATIONAL_B_SPLINE_SURFACE ( (
 ( 1.000000000000000000, 1.000000000000000000),
 ( 0.6386103224230316178, 0.9954351624131538845),
 ( 0.6386103224230316178, 0.9954351624131538845),
 ( 1.000000000000000000, 1.000000000000000000) ) ) 
 REPRESENTATION_ITEM ( '' )  SURFACE ( )  );
#5778=ORIENTED_EDGE ( 'NONE', *, *, #27657, .T. ) ;
#5779=CARTESIAN_POINT ( 'NONE',  ( 2.430230287190592531, 57.85706160874325832, -133.5180086894985436 ) ) ;
#5780=CARTESIAN_POINT ( 'NONE',  ( 1.893872463202045830, 107.2274879309827611, 97.83022426231997315 ) ) ;
#5782=CARTESIAN_POINT ( 'NONE',  ( 1.833485406944043827, 84.86072343962726450, -117.7091014914941809 ) ) ;
#5784=DIRECTION ( 'NONE',  ( -1.000000000000000000, -0.000000000000000000, -0.000000000000000000 ) ) ;
#5786=DIRECTION ( 'NONE',  ( -0.5946245182733607137, -0.5357871896547490298, 0.5994612328333164264 ) ) ;
#5788=CARTESIAN_POINT ( 'NONE',  ( 32.73300124599732186, 0.000000000000000000, 0.000000000000000000 ) ) ;
#5790=FACE_OUTER_BOUND ( 'NONE', #13400, .T. ) ;
#5792=B_SPLINE_CURVE_WITH_KNOTS ( 'NONE', 3,
 ( #26359, #6661, #9092, #20023 ),
 .UNSPECIFIED., .F., .F.,
 ( 4, 4 ),
 ( 1.534813690070764878E-16, 0.008383748772659597656 ),
 .UNSPECIFIED. ) ;
#5793=EDGE_CURVE ( 'NONE', #11289, #26082, #19644, .T. ) ;
#5794=CARTESIAN_POINT ( 'NONE',  ( 119.2224693531408803, 90.00000000000005684, 39.99999999999999289 ) ) ;
#5795=CARTESIAN_POINT ( 'NONE',  ( 10.93730112725983439, -148.8212007290663621, 26.59437931460704263 ) ) ;
#5797=CARTESIAN_POINT ( 'NONE',  ( 25.64704443564079739, -11.66968230815837337, -112.3065506427462736 ) ) ;
#5798=VERTEX_POINT ( 'NONE', #54 ) ;
#5800=ORIENTED_EDGE ( 'NONE', *, *, #12768, .F. ) ;
#5801=ORIENTED_EDGE ( 'NONE', *, *, #19929, .F. ) ;
#5802=CARTESIAN_POINT ( 'NONE',  ( 28.43349137099838586, -29.78331910005408645, -120.6297847406439985 ) ) ;
#5803=EDGE_CURVE ( 'NONE', #12270, #18370, #15892, .T. ) ;
#5806=CARTESIAN_POINT ( 'NONE',  ( 9.884929003653626367, -4.203795436551307496, -150.4771565009631047 ) ) ;
#5807=ORIENTED_EDGE ( 'NONE', *, *, #17627, .F. ) ;
#5808=CARTESIAN_POINT ( 'NONE',  ( 10.93730112725996051, 20.69552240458543224, -149.7554878793147282 ) ) ;
#5809=CARTESIAN_POINT ( 'NONE',  ( 5.340103556456536005, 88.52145167812754778, -117.9209211572677418 ) ) ;
#5810=EDGE_CURVE ( 'NONE', #27903, #26589, #13130, .T. ) ;
#5811=EDGE_CURVE ( 'NONE', #14545, #449, #20010, .T. ) ;
#5812=FACE_OUTER_BOUND ( 'NONE', #24437, .T. ) ;
#5815=CARTESIAN_POINT ( 'NONE',  ( 1.833721034905656744, -142.0123736691684542, -29.82176961967059370 ) ) ;
#5816=LINE ( 'NONE', #14575, #10062 ) ;
#5818=CARTESIAN_POINT ( 'NONE',  ( 30.59141879584289114, -115.8270959620729030, 9.457572341076161848 ) ) ;
#5820=CARTESIAN_POINT ( 'NONE',  ( 109.1778270068192853, -0.003465086990427028186, -0.008646067828078151524 ) ) ;
#5821=CARTESIAN_POINT ( 'NONE',  ( 55.49584447822657296, 72.55110015779771970, -0.2676470673959188695 ) ) ;
#5823=ORIENTED_EDGE ( 'NONE', *, *, #20701, .T. ) ;
#5824=ORIENTED_EDGE ( 'NONE', *, *, #5427, .T. ) ;
#5825=FACE_OUTER_BOUND ( 'NONE', #4603, .T. ) ;
#5827=ORIENTED_EDGE ( 'NONE', *, *, #5614, .F. ) ;
#5828=ORIENTED_EDGE ( 'NONE', *, *, #23955, .F. ) ;
#5829=ORIENTED_EDGE ( 'NONE', *, *, #24968, .T. ) ;
#5830=CARTESIAN_POINT ( 'NONE',  ( 109.1586059443104944, 0.003294606663363240043, 0.006260042619939244421 ) ) ;
#5832=CARTESIAN_POINT ( 'NONE',  ( 55.79472521941428198, -58.42842213658356343, 43.35047097963431639 ) ) ;
#5833=ADVANCED_FACE ( 'NONE', ( #27237 ), #28477, .F. ) ;
#5834=CARTESIAN_POINT ( 'NONE',  ( 28.37603512858448340, -98.45183098818029066, 58.91311972676509612 ) ) ;
#5835=CARTESIAN_POINT ( 'NONE',  ( 26.11404676487257603, -65.63269960453305885, 92.25884714080386573 ) ) ;
#5836=CARTESIAN_POINT ( 'NONE',  ( 2.263178113027032978, -86.59154384226256695, 116.7985471375928768 ) ) ;
#5837=CARTESIAN_POINT ( 'NONE',  ( 25.64708228042119842, 56.42152786924503260, 97.80372460135694723 ) ) ;
#5840=ORIENTED_EDGE ( 'NONE', *, *, #3412, .T. ) ;
#5841=CARTESIAN_POINT ( 'NONE',  ( 25.64708228042119487, -107.3728320282186530, -34.92896069507395396 ) ) ;
#5842=CARTESIAN_POINT ( 'NONE',  ( 2.433796855181205476, 144.8571464219891141, -13.76554153471544417 ) ) ;
#5845=CARTESIAN_POINT ( 'NONE',  ( 25.73574536432413851, 90.91878692682031726, 67.05280231777534539 ) ) ;
#5848=( BOUNDED_SURFACE ( )  B_SPLINE_SURFACE ( 3, 1, ( 
 ( #16559, #1443 ),
 ( #11954, #9813 ),
 ( #3746, #23480 ),
 ( #21303, #14238 ) ),
 .UNSPECIFIED., .F., .F., .F. ) 
 B_SPLINE_SURFACE_WITH_KNOTS ( ( 4, 4 ),
 ( 2, 2 ),
 ( 0.000000000000000000, 1.000000000000000000 ),
 ( 0.000000000000000000, 1.000000000000000000 ),
 .UNSPECIFIED. ) 
 GEOMETRIC_REPRESENTATION_ITEM ( )  RATIONAL_B_SPLINE_SURFACE ( (
 ( 1.000000000000000000, 1.000000000000000000),
 ( 0.9960225298536222738, 0.9999952330161893110),
 ( 0.9960225298536222738, 0.9999952330161893110),
 ( 1.000000000000000000, 1.000000000000000000) ) ) 
 REPRESENTATION_ITEM ( '' )  SURFACE ( )  );
#5850=CARTESIAN_POINT ( 'NONE',  ( 1.833485406944057594, -85.72460230293616235, -117.0814567582553281 ) ) ;
#5851=ORIENTED_EDGE ( 'NONE', *, *, #27117, .T. ) ;
#5852=ORIENTED_EDGE ( 'NONE', *, *, #5811, .F. ) ;
#5853=B_SPLINE_CURVE_WITH_KNOTS ( 'NONE', 3,
 ( #3802, #1637, #8270, #12575 ),
 .UNSPECIFIED., .F., .F.,
 ( 4, 4 ),
 ( 0.000000000000000000, 0.008383560773332712074 ),
 .UNSPECIFIED. ) ;
#5854=CARTESIAN_POINT ( 'NONE',  ( 1.831572820252008738, -125.1738732943805132, -73.40899645746137026 ) ) ;
#5855=ORIENTED_EDGE ( 'NONE', *, *, #9371, .T. ) ;
#5857=ORIENTED_EDGE ( 'NONE', *, *, #3415, .T. ) ;
#5858=CARTESIAN_POINT ( 'NONE',  ( 1.833838850093440387, 97.09738632349036891, 107.8375672471886020 ) ) ;
#5859=ADVANCED_FACE ( 'NONE', ( #24965 ), #2950, .F. ) ;
#5862=CARTESIAN_POINT ( 'NONE',  ( 32.73300124599732186, 0.000000000000000000, 0.000000000000000000 ) ) ;
#5863=ADVANCED_FACE ( 'NONE', ( #7551 ), #4792, .F. ) ;
#5865=EDGE_CURVE ( 'NONE', #28334, #20235, #11996, .T. ) ;
#5868=CARTESIAN_POINT ( 'NONE',  ( 1.832998868059858122, 141.8272129421608554, 30.69214149074063513 ) ) ;
#5869=CARTESIAN_POINT ( 'NONE',  ( 1.833485406944043827, -107.4794113447402566, -97.49333871408801144 ) ) ;
#5870=ORIENTED_EDGE ( 'NONE', *, *, #4526, .T. ) ;
#5873=CARTESIAN_POINT ( 'NONE',  ( 25.64681081121879203, -97.99105938547884875, -56.09509703373446854 ) ) ;
#5876=ORIENTED_EDGE ( 'NONE', *, *, #7736, .F. ) ;
#5879=CARTESIAN_POINT ( 'NONE',  ( 1.834118845439484335, -137.9527673765102520, -45.01070051384731130 ) ) ;
#5880=FACE_OUTER_BOUND ( 'NONE', #6594, .T. ) ;
#5881=CARTESIAN_POINT ( 'NONE',  ( 19.66333377628691892, -127.6002314355562675, 51.89484018353797268 ) ) ;
#5884=ORIENTED_EDGE ( 'NONE', *, *, #599, .F. ) ;
#5887=ORIENTED_EDGE ( 'NONE', *, *, #25756, .F. ) ;
#5889=CARTESIAN_POINT ( 'NONE',  ( 25.64699802086726166, -112.2675771984164754, 12.03888878460436729 ) ) ;
#5890=CARTESIAN_POINT ( 'NONE',  ( 55.79472521941428198, 71.00924468211177043, -15.83764557006200135 ) ) ;
#5892=CARTESIAN_POINT ( 'NONE',  ( 5.340103579038286696, 71.72120379026205228, -128.8311297206835206 ) ) ;
#5894=CARTESIAN_POINT ( 'NONE',  ( 25.64660436782575559, -84.29628170537181120, -75.12017330820542327 ) ) ;
#5896=CARTESIAN_POINT ( 'NONE',  ( 10.93730112725972248, -36.23586118136624634, 146.7718404940640653 ) ) ;
#5897=( BOUNDED_SURFACE ( )  B_SPLINE_SURFACE ( 3, 1, ( 
 ( #1708, #10922 ),
 ( #12927, #4298 ),
 ( #28453, #8619 ),
 ( #23765, #13201 ) ),
 .UNSPECIFIED., .F., .F., .F. ) 
 B_SPLINE_SURFACE_WITH_KNOTS ( ( 4, 4 ),
 ( 2, 2 ),
 ( 0.000000000000000000, 1.000000000000000000 ),
 ( 0.000000000000000000, 1.000000000000000000 ),
 .UNSPECIFIED. ) 
 GEOMETRIC_REPRESENTATION_ITEM ( )  RATIONAL_B_SPLINE_SURFACE ( (
 ( 1.000000000000000000, 1.000000000000000000),
 ( 0.6386103224230302855, 0.9954351624131538845),
 ( 0.6386103224230302855, 0.9954351624131538845),
 ( 1.000000000000000000, 1.000000000000000000) ) ) 
 REPRESENTATION_ITEM ( '' )  SURFACE ( )  );
#5898=CARTESIAN_POINT ( 'NONE',  ( 109.1592201516379674, -0.007845213074654437332, 0.0005146241775982539042 ) ) ;
#5899=VERTEX_POINT ( 'NONE', #4807 ) ;
#5904=EDGE_CURVE ( 'NONE', #7408, #12561, #27822, .T. ) ;
#5905=EDGE_LOOP ( 'NONE', ( #17236, #19187, #121, #12751 ) ) ;
#5909=FACE_OUTER_BOUND ( 'NONE', #16991, .T. ) ;
#5910=ADVANCED_FACE ( 'NONE', ( #23381 ), #4617, .F. ) ;
#5912=CARTESIAN_POINT ( 'NONE',  ( 109.1586900883932856, -0.0001010081143976501722, -0.007137750914550312215 ) ) ;
#5913=CARTESIAN_POINT ( 'NONE',  ( 1.833691583653523027, 141.8642667235908164, 30.51806994139646534 ) ) ;
#5917=ORIENTED_EDGE ( 'NONE', *, *, #10156, .T. ) ;
#5919=CARTESIAN_POINT ( 'NONE',  ( 28.37603512858448340, 86.45299531409462190, 75.42810021528123343 ) ) ;
#5920=CARTESIAN_POINT ( 'NONE',  ( 109.1624594426973118, -0.006914244825467878892, -0.01438905500501944622 ) ) ;
#5921=CARTESIAN_POINT ( 'NONE',  ( 9.884929003653608603, 135.7578851563885962, 65.04493172071525464 ) ) ;
#5922=DIRECTION ( 'NONE',  ( 0.000000000000000000, 0.000000000000000000, -1.000000000000000000 ) ) ;
#5924=CARTESIAN_POINT ( 'NONE',  ( 109.1589550718175161, -0.004900004919101272859, 0.005777059646713168448 ) ) ;
#5926=ORIENTED_EDGE ( 'NONE', *, *, #7937, .F. ) ;
#5927=FACE_OUTER_BOUND ( 'NONE', #27002, .T. ) ;
#5928=CARTESIAN_POINT ( 'NONE',  ( 32.73300124599769134, -51.32617430724849328, -105.8473486001054198 ) ) ;
#5929=CARTESIAN_POINT ( 'NONE',  ( 25.64670758986458310, -11.30712635241913766, -112.3434365398309751 ) ) ;
#5930=DIRECTION ( 'NONE',  ( 0.000000000000000000, 1.000000000000000000, 3.122502256758243698E-15 ) ) ;
#5931=CARTESIAN_POINT ( 'NONE',  ( 32.73300124599735739, -62.10906484417306928, 99.90245962373816724 ) ) ;
#5932=VERTEX_POINT ( 'NONE', #7992 ) ;
#5934=CARTESIAN_POINT ( 'NONE',  ( 10.93730112725990011, -115.5857507957697976, -97.44200844886394464 ) ) ;
#5936=VECTOR ( 'NONE', #19344, 1000.000000000000114 ) ;
#5938=VECTOR ( 'NONE', #25326, 1000.000000000000000 ) ;
#5939=VERTEX_POINT ( 'NONE', #16455 ) ;
#5940=EDGE_CURVE ( 'NONE', #15925, #2427, #6989, .T. ) ;
#5941=CARTESIAN_POINT ( 'NONE',  ( 1.833485406944043827, 29.64752363041542083, 142.0485807715646729 ) ) ;
#5945=CARTESIAN_POINT ( 'NONE',  ( 1.833750490713699444, 30.43107162406064603, -141.8829662951649482 ) ) ;
#5950=CARTESIAN_POINT ( 'NONE',  ( 1.833485406944043827, 59.50871042846404180, -132.3460930279885019 ) ) ;
#5952=CARTESIAN_POINT ( 'NONE',  ( 25.98552792386799482, -110.4352299692911572, 24.57669147553951206 ) ) ;
#5953=CARTESIAN_POINT ( 'NONE',  ( 109.1778270068192853, 0.008646067828082840481, 0.003465086990435519224 ) ) ;
#5954=CARTESIAN_POINT ( 'NONE',  ( 10.93730112725990011, -151.0983828010092225, 4.928439153519769356 ) ) ;
#5955=CARTESIAN_POINT ( 'NONE',  ( 25.64681081121879203, 75.24277141833607629, -84.18689316039970549 ) ) ;
#5956=CARTESIAN_POINT ( 'NONE',  ( 10.93730112726005999, 128.3908183996603327, -79.81734490845792607 ) ) ;
#5958=CARTESIAN_POINT ( 'NONE',  ( 109.1592201516379674, 0.0003082430541934987381, -0.007856029051018018419 ) ) ;
#5959=CARTESIAN_POINT ( 'NONE',  ( 25.70243777736189728, 12.53519966262632224, -112.2504268534933232 ) ) ;
#5960=VERTEX_POINT ( 'NONE', #19048 ) ;
#5963=FACE_OUTER_BOUND ( 'NONE', #18084, .T. ) ;
#5964=ORIENTED_EDGE ( 'NONE', *, *, #21843, .T. ) ;
#5965=EDGE_LOOP ( 'NONE', ( #16817, #18474, #12084, #435 ) ) ;
#5970=B_SPLINE_CURVE_WITH_KNOTS ( 'NONE', 3,
 ( #17265, #6342, #25517, #15821, #19849, #24329 ),
 .UNSPECIFIED., .F., .F.,
 ( 4, 2, 4 ),
 ( 1.144950348284594810E-17, 0.0006311636237756862835, 0.001262327247551361074 ),
 .UNSPECIFIED. ) ;
#5972=DIRECTION ( 'NONE',  ( -0.5946245182733607137, -0.08110646981859605253, 0.7999021332774021165 ) ) ;
#5974=CARTESIAN_POINT ( 'NONE',  ( 26.11404676487259024, 74.91683232331092768, -84.89295829319416953 ) ) ;
#5975=CARTESIAN_POINT ( 'NONE',  ( 2.433796855181205476, 142.6247129145651797, -28.83182736670396196 ) ) ;
#5977=CARTESIAN_POINT ( 'NONE',  ( 1.832998868059890096, -73.01698022778269603, -125.4013017422238363 ) ) ;
#5979=DIRECTION ( 'NONE',  ( 0.5946245182733607137, 0.3243201896541541562, 0.7356888587241667832 ) ) ;
#5980=ORIENTED_EDGE ( 'NONE', *, *, #135, .F. ) ;
#5982=CARTESIAN_POINT ( 'NONE',  ( 25.64704443564077252, -107.3436266109710999, -35.01840413910241523 ) ) ;
#5983=CARTESIAN_POINT ( 'NONE',  ( 109.1586059443104944, 0.001014167950289969608, 0.007001002073869790586 ) ) ;
#5985=CARTESIAN_POINT ( 'NONE',  ( 10.93730112725932635, 0.000000000000000000, 0.000000000000000000 ) ) ;
#5987=CARTESIAN_POINT ( 'NONE',  ( 25.70243777736189017, 91.80600962488489358, -65.79472741891171950 ) ) ;
#5992=CARTESIAN_POINT ( 'NONE',  ( 30.58324630866355420, 119.0579156359858786, 21.27395054437283761 ) ) ;
#5993=VERTEX_POINT ( 'NONE', #21340 ) ;
#5994=ORIENTED_EDGE ( 'NONE', *, *, #15572, .T. ) ;
#5995=B_SPLINE_CURVE_WITH_KNOTS ( 'NONE', 3,
 ( #20152, #293, #2447, #585, #439, #9226, #20586 ),
 .UNSPECIFIED., .F., .F.,
 ( 4, 3, 4 ),
 ( 0.000000000000000000, 0.02398743853561337638, 0.04000277880656218088 ),
 .UNSPECIFIED. ) ;
#5996=CARTESIAN_POINT ( 'NONE',  ( 1.831572820252008738, -29.20415387690465181, -142.1425225354583119 ) ) ;
#5997=ADVANCED_FACE ( 'NONE', ( #12146 ), #18655, .T. ) ;
#5998=ORIENTED_EDGE ( 'NONE', *, *, #21461, .T. ) ;
#5999=ORIENTED_EDGE ( 'NONE', *, *, #7641, .T. ) ;
#6001=AXIS2_PLACEMENT_3D ( 'NONE', #27226, #7541, #16297 ) ;
#6002=EDGE_CURVE ( 'NONE', #531, #21908, #6627, .T. ) ;
#6003=CARTESIAN_POINT ( 'NONE',  ( 2.430230287190592531, -16.65331920325641590, -144.5585181921887568 ) ) ;
#6004=ORIENTED_EDGE ( 'NONE', *, *, #18657, .F. ) ;
#6005=VECTOR ( 'NONE', #15139, 1000.000000000000114 ) ;
#6006=CARTESIAN_POINT ( 'NONE',  ( 32.73300124599738581, -55.46353551261936587, -103.7392577722181812 ) ) ;
#6007=CARTESIAN_POINT ( 'NONE',  ( 10.93730112725972425, -65.95960219663204782, 136.0306644680981094 ) ) ;
#6009=CARTESIAN_POINT ( 'NONE',  ( 32.73300124599738581, 108.9684813982494092, -44.31599526637845798 ) ) ;
#6010=CARTESIAN_POINT ( 'NONE',  ( 1.893872463202029843, 126.1771883101046825, -71.74819926215046451 ) ) ;
#6011=CARTESIAN_POINT ( 'NONE',  ( 109.1778270068192853, -0.009307953841270272949, 0.0003511581237513249575 ) ) ;
#6012=CARTESIAN_POINT ( 'NONE',  ( 109.1778270068192853, -0.0003511581237570398956, 0.009307953841262543021 ) ) ;
#6013=CARTESIAN_POINT ( 'NONE',  ( 25.65782528836479770, -46.45532072021256198, 102.9197507294674523 ) ) ;
#6014=CARTESIAN_POINT ( 'NONE',  ( 1.833485406944043827, 125.4007332306545379, 73.01664920993009389 ) ) ;
#6016=CARTESIAN_POINT ( 'NONE',  ( 26.04756280548352976, -103.8403168215172627, -45.01666824410871470 ) ) ;
#6021=ORIENTED_EDGE ( 'NONE', *, *, #13771, .T. ) ;
#6022=ORIENTED_EDGE ( 'NONE', *, *, #11157, .T. ) ;
#6024=LINE ( 'NONE', #23591, #27268 ) ;
#6026=CARTESIAN_POINT ( 'NONE',  ( 2.263178607246699503, 125.2099936970377740, -73.90841395012451187 ) ) ;
#6028=ORIENTED_EDGE ( 'NONE', *, *, #3997, .F. ) ;
#6029=CARTESIAN_POINT ( 'NONE',  ( 26.11404676487257603, -107.3263591096427945, -36.06104232266560672 ) ) ;
#6030=CARTESIAN_POINT ( 'NONE',  ( 1.834118845439484335, 125.7578880615045023, 72.40084790867372533 ) ) ;
#6033=CARTESIAN_POINT ( 'NONE',  ( 109.1589550718175161, 0.001793588804100394816, 0.007359857714025730933 ) ) ;
#6037=B_SPLINE_CURVE_WITH_KNOTS ( 'NONE', 3,
 ( #14206, #9353, #557, #7329, #988, #22445 ),
 .UNSPECIFIED., .F., .F.,
 ( 4, 2, 4 ),
 ( 9.659140056172959483E-18, 0.0006311571484586091501, 0.001262314296917208759 ),
 .UNSPECIFIED. ) ;
#6045=EDGE_CURVE ( 'NONE', #14195, #20657, #20670, .T. ) ;
#6046=ORIENTED_EDGE ( 'NONE', *, *, #6162, .T. ) ;
#6047=CARTESIAN_POINT ( 'NONE',  ( 2.433796855181219243, -142.0211193075558356, 31.67151202412923894 ) ) ;
#6048=CARTESIAN_POINT ( 'NONE',  ( 32.73300124599740002, -8.473903470905288060, -117.3295799645430151 ) ) ;
#6049=VERTEX_POINT ( 'NONE', #13809 ) ;
#6050=CARTESIAN_POINT ( 'NONE',  ( 25.64681081121879203, -103.3177883989776547, -45.54494737132326776 ) ) ;
#6055=CARTESIAN_POINT ( 'NONE',  ( 1.833603222531976273, 138.1443021179086941, -44.41798579679396397 ) ) ;
#6056=CARTESIAN_POINT ( 'NONE',  ( 2.433796855181205476, 43.58222566461644476, 138.8296532063089614 ) ) ;
#6060=CARTESIAN_POINT ( 'NONE',  ( 25.64681081121879203, 34.49579773461926635, -107.5125461021399218 ) ) ;
#6063=ORIENTED_EDGE ( 'NONE', *, *, #189, .F. ) ;
#6064=CARTESIAN_POINT ( 'NONE',  ( 26.11404676487256893, -110.9778746459748362, 22.43340081644731043 ) ) ;
#6065=CARTESIAN_POINT ( 'NONE',  ( 1.833485406944043827, 59.50871042846404180, -132.3460930279885019 ) ) ;
#6066=CARTESIAN_POINT ( 'NONE',  ( 25.64681081121879203, 34.49579773461785948, 107.5125461021403765 ) ) ;
#6067=LINE ( 'NONE', #25357, #25323 ) ;
#6069=CARTESIAN_POINT ( 'NONE',  ( 32.73300124599737160, -84.80615050150427692, 81.52272205837169849 ) ) ;
#6070=CARTESIAN_POINT ( 'NONE',  ( 2.433796855181205476, 98.43889364294005873, -107.1581411821775305 ) ) ;
#6071=ORIENTED_EDGE ( 'NONE', *, *, #18094, .F. ) ;
#6072=CARTESIAN_POINT ( 'NONE',  ( 2.430230287190589422, 107.1617224697477297, -98.44218333480664285 ) ) ;
#6074=CARTESIAN_POINT ( 'NONE',  ( 25.64708010899964918, 23.42206246795159430, -110.4552579818683427 ) ) ;
#6075=ADVANCED_FACE ( 'NONE', ( #1008 ), #14975, .T. ) ;
#6076=EDGE_CURVE ( 'NONE', #2443, #7281, #718, .T. ) ;
#6079=EDGE_LOOP ( 'NONE', ( #16994, #12421, #3435, #13684 ) ) ;
#6081=EDGE_CURVE ( 'NONE', #22569, #14235, #17587, .T. ) ;
#6082=B_SPLINE_CURVE_WITH_KNOTS ( 'NONE', 3,
 ( #13724, #15587, #7135, #17890 ),
 .UNSPECIFIED., .F., .F.,
 ( 4, 4 ),
 ( 5.988792064294042516E-16, 0.008383748772660088583 ),
 .UNSPECIFIED. ) ;
#6084=VERTEX_POINT ( 'NONE', #3169 ) ;
#6085=AXIS2_PLACEMENT_3D ( 'NONE', #16129, #26917, #7228 ) ;
#6088=ORIENTED_EDGE ( 'NONE', *, *, #14221, .T. ) ;
#6089=ORIENTED_EDGE ( 'NONE', *, *, #3755, .T. ) ;
#6090=VECTOR ( 'NONE', #9449, 1000.000000000000114 ) ;
#6091=CARTESIAN_POINT ( 'NONE',  ( 32.73300124599738581, -28.19767303745521758, -114.2056417606550696 ) ) ;
#6092=CARTESIAN_POINT ( 'NONE',  ( 16.75465622695631041, -112.2763423369177076, -87.30527857298577032 ) ) ;
#6093=B_SPLINE_CURVE_WITH_KNOTS ( 'NONE', 3,
 ( #28437, #10907, #13618, #8602, #4274, #17367, #26156, #6447, #17511, #13058 ),
 .UNSPECIFIED., .F., .F.,
 ( 4, 3, 3, 4 ),
 ( 3.816391647148975608E-17, 0.0002669559177086190931, 0.0005339118354150969954, 0.001067817517169159913 ),
 .UNSPECIFIED. ) ;
#6096=VERTEX_POINT ( 'NONE', #24642 ) ;
#6097=CARTESIAN_POINT ( 'NONE',  ( 119.2224693531408803, 0.000000000000000000, 0.000000000000000000 ) ) ;
#6098=DIRECTION ( 'NONE',  ( 0.000000000000000000, 0.000000000000000000, 1.000000000000000000 ) ) ;
#6100=VECTOR ( 'NONE', #20103, 1000.000000000000341 ) ;
#6101=CARTESIAN_POINT ( 'NONE',  ( 1.834118845439484335, 144.3336252355296949, 14.99112450600294721 ) ) ;
#6102=CARTESIAN_POINT ( 'NONE',  ( 26.11404676487259024, 24.64483677384848903, 110.5078194225162207 ) ) ;
#6103=CARTESIAN_POINT ( 'NONE',  ( 109.1624594426973260, 0.01318243916934103317, -0.009004164758061436805 ) ) ;
#6104=EDGE_CURVE ( 'NONE', #16608, #7408, #24109, .T. ) ;
#6105=CARTESIAN_POINT ( 'NONE',  ( 28.37599760073042532, 108.5491283158102078, 37.15642189426440467 ) ) ;
#6106=DIRECTION ( 'NONE',  ( -1.000000000000000000, 0.000000000000000000, 0.000000000000000000 ) ) ;
#6108=VERTEX_POINT ( 'NONE', #20869 ) ;
#6109=ORIENTED_EDGE ( 'NONE', *, *, #16965, .F. ) ;
#6110=CARTESIAN_POINT ( 'NONE',  ( 26.11404676487259024, -24.64483677384768967, -110.5078194225163912 ) ) ;
#6112=CARTESIAN_POINT ( 'NONE',  ( 26.04756280548353686, 36.02883009343639031, 107.2904246402795962 ) ) ;
#6113=EDGE_LOOP ( 'NONE', ( #4661, #3823, #8152, #20027 ) ) ;
#6114=EDGE_LOOP ( 'NONE', ( #5926, #22735, #27924, #13100 ) ) ;
#6115=VERTEX_POINT ( 'NONE', #8203 ) ;
#6117=CARTESIAN_POINT ( 'NONE',  ( 10.93730112725945247, 97.44200844886275092, 115.5857507957704087 ) ) ;
#6118=AXIS2_PLACEMENT_3D ( 'NONE', #13720, #774, #6986 ) ;
#6119=CARTESIAN_POINT ( 'NONE',  ( 25.73574536432417048, -83.41179791497809504, -76.18908113044840036 ) ) ;
#6120=CARTESIAN_POINT ( 'NONE',  ( 109.1586900883932856, 0.001582822706032828994, 0.006960773163852194793 ) ) ;
#6122=LINE ( 'NONE', #17308, #13913 ) ;
#6123=B_SPLINE_CURVE_WITH_KNOTS ( 'NONE', 3,
 ( #18360, #7603, #16068, #7025 ),
 .UNSPECIFIED., .F., .F.,
 ( 4, 4 ),
 ( 0.000000000000000000, 0.01077107196513893937 ),
 .UNSPECIFIED. ) ;
#6125=B_SPLINE_CURVE_WITH_KNOTS ( 'NONE', 3,
 ( #9189, #22443, #128, #5008, #26596, #13352, #17537, #2414 ),
 .UNSPECIFIED., .F., .F.,
 ( 4, 2, 2, 4 ),
 ( 3.469446951953614189E-18, 0.0002429592666046752423, 0.0004859185332093470151, 0.0009718370664186726715 ),
 .UNSPECIFIED. ) ;
#6126=FACE_OUTER_BOUND ( 'NONE', #27063, .T. ) ;
#6127=CARTESIAN_POINT ( 'NONE',  ( 109.1586900883932856, 0.001582822706032828994, 0.006960773163852194793 ) ) ;
#6128=CARTESIAN_POINT ( 'NONE',  ( 10.93730112725978287, -133.3192575531804209, 71.28103789254889477 ) ) ;
#6129=ORIENTED_EDGE ( 'NONE', *, *, #16347, .T. ) ;
#6131=CARTESIAN_POINT ( 'NONE',  ( 25.64708010899963853, 112.9112661935490252, -0.05470523945908801339 ) ) ;
#6132=CARTESIAN_POINT ( 'NONE',  ( 25.64681081121879203, -91.59071981940616070, 66.03065707438906884 ) ) ;
#6134=CARTESIAN_POINT ( 'NONE',  ( 25.64681081121880624, -102.9795863647025556, -46.30456157731431688 ) ) ;
#6135=DIRECTION ( 'NONE',  ( 0.000000000000000000, 0.000000000000000000, 1.000000000000000000 ) ) ;
#6138=ORIENTED_EDGE ( 'NONE', *, *, #5793, .F. ) ;
#6139=VECTOR ( 'NONE', #2344, 1000.000000000000114 ) ;
#6141=EDGE_CURVE ( 'NONE', #27833, #142, #16557, .T. ) ;
#6143=ORIENTED_EDGE ( 'NONE', *, *, #17857, .T. ) ;
#6144=ORIENTED_EDGE ( 'NONE', *, *, #27487, .F. ) ;
#6145=EDGE_CURVE ( 'NONE', #14235, #21908, #7793, .T. ) ;
#6147=ORIENTED_EDGE ( 'NONE', *, *, #22425, .T. ) ;
#6149=CARTESIAN_POINT ( 'NONE',  ( 1.833206308920070970, -14.42724735286750892, -144.3905119031281288 ) ) ;
#6150=ORIENTED_EDGE ( 'NONE', *, *, #778, .T. ) ;
#6156=AXIS2_PLACEMENT_3D ( 'NONE', #27922, #21730, #12661 ) ;
#6157=CARTESIAN_POINT ( 'NONE',  ( 25.87036335909428075, -110.7910326764400537, -22.53739730344160108 ) ) ;
#6158=CARTESIAN_POINT ( 'NONE',  ( 2.430230287190592531, -116.8646894862417867, 86.70145658344620188 ) ) ;
#6159=CARTESIAN_POINT ( 'NONE',  ( 13.36082413113061307, 152.7944199136427414, 6.345145185218579620 ) ) ;
#6160=CARTESIAN_POINT ( 'NONE',  ( 28.37644542392840563, -4.054996728115051852, 124.2737818798215130 ) ) ;
#6161=B_SPLINE_CURVE_WITH_KNOTS ( 'NONE', 3,
 ( #16298, #14425, #5360, #11984, #1049, #5661, #23234, #18162, #3485, #618 ),
 .UNSPECIFIED., .F., .F.,
 ( 4, 3, 3, 4 ),
 ( 4.443059973708341306E-17, 0.0002669559177086151358, 0.0005339118354150905986, 0.001067817517169165767 ),
 .UNSPECIFIED. ) ;
#6162=EDGE_CURVE ( 'NONE', #27119, #2065, #19302, .T. ) ;
#6163=CARTESIAN_POINT ( 'NONE',  ( 28.37599760073042532, 109.6580863494834688, -33.74340001060989636 ) ) ;
#6166=ORIENTED_EDGE ( 'NONE', *, *, #28005, .F. ) ;
#6167=ORIENTED_EDGE ( 'NONE', *, *, #26802, .F. ) ;
#6169=CARTESIAN_POINT ( 'NONE',  ( 1.833838850855474600, -72.63194208529564833, 125.6242502389383588 ) ) ;
#6171=ADVANCED_FACE ( 'NONE', ( #19270 ), #754, .F. ) ;
#6172=DIRECTION ( 'NONE',  ( -1.000000000000000000, 0.000000000000000000, -0.000000000000000000 ) ) ;
#6174=EDGE_LOOP ( 'NONE', ( #18149, #10810, #9898, #4845 ) ) ;
#6177=VECTOR ( 'NONE', #2751, 1000.000000000000227 ) ;
#6178=VERTEX_POINT ( 'NONE', #1430 ) ;
#6179=CARTESIAN_POINT ( 'NONE',  ( 25.64681081121880624, -112.3352186517031441, 11.38886654529637887 ) ) ;
#6180=CARTESIAN_POINT ( 'NONE',  ( 25.64681081121879203, -56.09509703373275613, -97.99105938547980088 ) ) ;
#6181=CARTESIAN_POINT ( 'NONE',  ( 26.11404676487256893, -110.9778746459748362, 22.43340081644731043 ) ) ;
#6183=EDGE_LOOP ( 'NONE', ( #8402, #27796, #21809, #2267 ) ) ;
#6184=CARTESIAN_POINT ( 'NONE',  ( 9.884929003653608603, 27.17402761732343919, 148.0628878137281390 ) ) ;
#6185=CARTESIAN_POINT ( 'NONE',  ( 26.11404676487259024, 22.43340081644921113, -110.9778746459744667 ) ) ;
#6186=ORIENTED_EDGE ( 'NONE', *, *, #12602, .T. ) ;
#6188=CARTESIAN_POINT ( 'NONE',  ( 1.833485406944043827, 96.69979900902318093, -108.1939177044916107 ) ) ;
#6189=CARTESIAN_POINT ( 'NONE',  ( 25.64692232868537758, 103.0161468101953517, -46.22343382108633136 ) ) ;
#6195=CARTESIAN_POINT ( 'NONE',  ( 32.73300124599741423, -84.80615050150312584, -81.52272205837286378 ) ) ;
#6196=DIRECTION ( 'NONE',  ( -1.000000000000000000, -0.000000000000000000, -0.000000000000000000 ) ) ;
#6199=CARTESIAN_POINT ( 'NONE',  ( 109.1587776205901861, -0.007297420966932451417, -0.0006832286435016619213 ) ) ;
#6200=CARTESIAN_POINT ( 'NONE',  ( 25.64681081121879203, -46.30456157731261868, -102.9795863647033229 ) ) ;
#6202=EDGE_LOOP ( 'NONE', ( #22759, #21348, #23197, #16355 ) ) ;
#6203=EDGE_CURVE ( 'NONE', #8387, #3421, #15514, .T. ) ;
#6205=ORIENTED_EDGE ( 'NONE', *, *, #8240, .F. ) ;
#6206=CARTESIAN_POINT ( 'NONE',  ( 109.1721716018069515, -0.01467989464938416512, -0.008708654716135893342 ) ) ;
#6207=CARTESIAN_POINT ( 'NONE',  ( 55.79472521941426777, 30.25520714117996590, -66.16469064668267208 ) ) ;
#6208=CARTESIAN_POINT ( 'NONE',  ( 109.1592201516379674, -0.006174480289200349852, -0.004867031887010190086 ) ) ;
#6209=DIRECTION ( 'NONE',  ( 0.000000000000000000, -1.000000000000000000, 0.000000000000000000 ) ) ;
#6211=LINE ( 'NONE', #10659, #21311 ) ;
#6214=DIRECTION ( 'NONE',  ( -1.000000000000000000, -0.000000000000000000, -0.000000000000000000 ) ) ;
#6216=CARTESIAN_POINT ( 'NONE',  ( 1.833603222531972499, 117.6571262511690037, -84.93295186324742474 ) ) ;
#6219=CARTESIAN_POINT ( 'NONE',  ( 2.263178113027048077, 43.59477710889728286, 138.7064940342179966 ) ) ;
#6221=VERTEX_POINT ( 'NONE', #4007 ) ;
#6223=ORIENTED_EDGE ( 'NONE', *, *, #10963, .T. ) ;
#6224=CARTESIAN_POINT ( 'NONE',  ( 1.834118845439484335, -117.2918069668806424, 85.43746956709813389 ) ) ;
#6226=EDGE_CURVE ( 'NONE', #5185, #26195, #3503, .T. ) ;
#6228=CARTESIAN_POINT ( 'NONE',  ( 9.884929003653626367, -91.84919534721861112, -119.2676479132383065 ) ) ;
#6229=FACE_OUTER_BOUND ( 'NONE', #6777, .T. ) ;
#6231=EDGE_CURVE ( 'NONE', #20099, #5993, #2397, .T. ) ;
#6232=CARTESIAN_POINT ( 'NONE',  ( 1.833691583653584978, 59.34641645332813198, -132.4191286035299413 ) ) ;
#6233=B_SPLINE_CURVE_WITH_KNOTS ( 'NONE', 3,
 ( #3496, #12280, #21046, #10139, #22010, #3926, #9995 ),
 .UNSPECIFIED., .F., .F.,
 ( 4, 3, 4 ),
 ( 0.000000000000000000, 0.02398743853561342496, 0.04000277880656223639 ),
 .UNSPECIFIED. ) ;
#6235=EDGE_CURVE ( 'NONE', #26116, #19494, #12419, .T. ) ;
#6236=DIRECTION ( 'NONE',  ( 0.000000000000000000, 0.000000000000000000, 1.000000000000000000 ) ) ;
#6238=FACE_OUTER_BOUND ( 'NONE', #27687, .T. ) ;
#6239=CARTESIAN_POINT ( 'NONE',  ( 1.832998868059890096, 84.86110816369605914, 117.7096351258390712 ) ) ;
#6240=CARTESIAN_POINT ( 'NONE',  ( 32.73300124599741423, 117.3295799645430435, -8.473903470904879498 ) ) ;
#6241=CARTESIAN_POINT ( 'NONE',  ( 55.79472521941426777, -43.35047097963490614, 58.42842213658313000 ) ) ;
#6243=ORIENTED_EDGE ( 'NONE', *, *, #3127, .F. ) ;
#6245=ORIENTED_EDGE ( 'NONE', *, *, #1076, .T. ) ;
#6246=ORIENTED_EDGE ( 'NONE', *, *, #6081, .T. ) ;
#6249=EDGE_CURVE ( 'NONE', #13718, #7372, #20317, .T. ) ;
#6251=CARTESIAN_POINT ( 'NONE',  ( 2.430230287190592531, 28.83279105684623644, -142.6294793592095118 ) ) ;
#6252=EDGE_CURVE ( 'NONE', #1405, #22236, #26578, .T. ) ;
#6254=B_SPLINE_CURVE_WITH_KNOTS ( 'NONE', 3,
 ( #18666, #3689, #12052, #25451, #10337, #5726 ),
 .UNSPECIFIED., .F., .F.,
 ( 4, 2, 4 ),
 ( 1.110764993427085326E-17, 0.0006311636237756891024, 0.001262327247551367146 ),
 .UNSPECIFIED. ) ;
#6256=LINE ( 'NONE', #15425, #18559 ) ;
#6260=ORIENTED_EDGE ( 'NONE', *, *, #21640, .T. ) ;
#6261=ORIENTED_EDGE ( 'NONE', *, *, #8531, .T. ) ;
#6262=CARTESIAN_POINT ( 'NONE',  ( 25.64692872815574631, 112.9107203549055924, 0.3216598674787775058 ) ) ;
#6263=CARTESIAN_POINT ( 'NONE',  ( 109.1592201516379674, 0.007856029051018016685, 0.0003082430541935266563 ) ) ;
#6266=CARTESIAN_POINT ( 'NONE',  ( 25.98107933586716456, 1.091357942392178204, -113.1286487641202569 ) ) ;
#6267=CARTESIAN_POINT ( 'NONE',  ( 1.893872463202039391, -71.74819926215087662, -126.1771883101044693 ) ) ;
#6272=CARTESIAN_POINT ( 'NONE',  ( 16.05277956358198566, -99.31161228512409878, -103.3141821208293578 ) ) ;
#6274=EDGE_LOOP ( 'NONE', ( #4199, #20343, #22437, #18264 ) ) ;
#6277=CARTESIAN_POINT ( 'NONE',  ( 1.832998868059890096, 117.0819875546695670, 85.72499093308135798 ) ) ;
#6281=ORIENTED_EDGE ( 'NONE', *, *, #25296, .F. ) ;
#6282=CARTESIAN_POINT ( 'NONE',  ( 26.11404676487257603, -76.59696442953247697, 83.38016054979757996 ) ) ;
#6283=EDGE_CURVE ( 'NONE', #26195, #14327, #8648, .T. ) ;
#6285=ADVANCED_FACE ( 'NONE', ( #6603 ), #10689, .F. ) ;
#6289=CARTESIAN_POINT ( 'NONE',  ( 1.831572820252008738, -132.1614873090345270, -59.92262167723569632 ) ) ;
#6290=EDGE_CURVE ( 'NONE', #8378, #10268, #13196, .T. ) ;
#6291=DIRECTION ( 'NONE',  ( 0.5914120900931444380, 0.7903769105750353408, -0.1598001217819338404 ) ) ;
#6292=DIRECTION ( 'NONE',  ( -1.000000000000000000, -0.000000000000000000, -0.000000000000000000 ) ) ;
#6293=CARTESIAN_POINT ( 'NONE',  ( 26.04756280548354752, -112.4366864265128640, 12.93458011762439419 ) ) ;
#6295=ORIENTED_EDGE ( 'NONE', *, *, #5361, .F. ) ;
#6296=CARTESIAN_POINT ( 'NONE',  ( 25.64692872815576052, 56.73392579406848313, -97.62272225320887742 ) ) ;
#6297=CARTESIAN_POINT ( 'NONE',  ( 2.263178607246673746, 118.4461883615815339, 84.32376080825592624 ) ) ;
#6298=CARTESIAN_POINT ( 'NONE',  ( 55.79472521941426777, -42.17269936297599031, -59.28412330436345457 ) ) ;
#6300=CARTESIAN_POINT ( 'NONE',  ( 1.893872463202063150, 84.54426271294425987, 117.9862474593099648 ) ) ;
#6303=CARTESIAN_POINT ( 'NONE',  ( 2.433796855181205476, -107.1581411821778858, -98.43889364293970345 ) ) ;
#6304=CARTESIAN_POINT ( 'NONE',  ( 109.1587776205901861, 0.0008489206734500592518, 0.007280006032835109955 ) ) ;
#6306=CARTESIAN_POINT ( 'NONE',  ( 10.93730112725932635, 0.000000000000000000, 0.000000000000000000 ) ) ;
#6307=CARTESIAN_POINT ( 'NONE',  ( 1.833721034905648972, 117.6051524288283758, 85.00517831633722210 ) ) ;
#6311=CARTESIAN_POINT ( 'NONE',  ( 1.831572820252009626, -14.18623102066865549, 144.4165162501762154 ) ) ;
#6312=( BOUNDED_SURFACE ( )  B_SPLINE_SURFACE ( 3, 1, ( 
 ( #5041, #22628 ),
 ( #1020, #11820 ),
 ( #22482, #9385 ),
 ( #11523, #11674 ) ),
 .UNSPECIFIED., .F., .F., .F. ) 
 B_SPLINE_SURFACE_WITH_KNOTS ( ( 4, 4 ),
 ( 2, 2 ),
 ( 0.000000000000000000, 1.000000000000000000 ),
 ( 0.000000000000000000, 1.000000000000000000 ),
 .UNSPECIFIED. ) 
 GEOMETRIC_REPRESENTATION_ITEM ( )  RATIONAL_B_SPLINE_SURFACE ( (
 ( 1.000000000000000000, 1.000000000000000000),
 ( 0.6386103224230316178, 0.9954351624131538845),
 ( 0.6386103224230316178, 0.9954351624131538845),
 ( 1.000000000000000000, 1.000000000000000000) ) ) 
 REPRESENTATION_ITEM ( '' )  SURFACE ( )  );
#6315=CARTESIAN_POINT ( 'NONE',  ( 25.64681081121879203, 97.57530875170684226, -56.81519825470653018 ) ) ;
#6316=CARTESIAN_POINT ( 'NONE',  ( 1.833485406944043827, 0.5339064996905048543, -145.1085452359073145 ) ) ;
#6317=CARTESIAN_POINT ( 'NONE',  ( 2.108985857320901935, 108.8271972979199944, 96.26411661813067155 ) ) ;
#6318=B_SPLINE_CURVE_WITH_KNOTS ( 'NONE', 3,
 ( #11957, #20731, #5631, #9657, #7663, #14397 ),
 .UNSPECIFIED., .F., .F.,
 ( 4, 2, 4 ),
 ( 8.673617379884035472E-18, 0.0006311636237756913792, 0.001262327247551374085 ),
 .UNSPECIFIED. ) ;
#6319=EDGE_CURVE ( 'NONE', #4812, #24848, #9173, .T. ) ;
#6321=CARTESIAN_POINT ( 'NONE',  ( 1.834118845439484335, 29.99597360113265054, -141.9759513273461664 ) ) ;
#6324=CARTESIAN_POINT ( 'NONE',  ( 109.1592201516379674, -0.004368284148529054563, -0.006536841731953389224 ) ) ;
#6331=DIRECTION ( 'NONE',  ( -0.000000000000000000, 1.000000000000000000, -0.000000000000000000 ) ) ;
#6332=ORIENTED_EDGE ( 'NONE', *, *, #24868, .T. ) ;
#6335=LINE ( 'NONE', #8763, #20826 ) ;
#6336=CARTESIAN_POINT ( 'NONE',  ( 1.834118845439484335, -85.14950727125936680, 117.5010238212695697 ) ) ;
#6337=CARTESIAN_POINT ( 'NONE',  ( 30.58324630866348670, 119.8048187378266505, -16.55818995381025616 ) ) ;
#6338=CARTESIAN_POINT ( 'NONE',  ( 19.66333377628713563, -137.3914191246404926, 9.924285918886006641 ) ) ;
#6339=VERTEX_POINT ( 'NONE', #17934 ) ;
#6340=CARTESIAN_POINT ( 'NONE',  ( 1.833206310202317946, 30.89799345102960970, 141.7818020564279493 ) ) ;
#6342=CARTESIAN_POINT ( 'NONE',  ( 2.263178113027036531, 46.26071604342251931, -137.8402779654365702 ) ) ;
#6343=VERTEX_POINT ( 'NONE', #11471 ) ;
#6344=CARTESIAN_POINT ( 'NONE',  ( 25.64699802086720481, -45.70780507840510865, 103.2460182674616362 ) ) ;
#6346=ORIENTED_EDGE ( 'NONE', *, *, #14189, .F. ) ;
#6349=EDGE_LOOP ( 'NONE', ( #17581, #26671, #547, #17859 ) ) ;
#6351=EDGE_CURVE ( 'NONE', #17891, #21070, #3376, .T. ) ;
#6352=EDGE_CURVE ( 'NONE', #9016, #13373, #12293, .T. ) ;
#6353=DIRECTION ( 'NONE',  ( -1.000000000000000000, -0.000000000000000000, -0.000000000000000000 ) ) ;
#6354=CARTESIAN_POINT ( 'NONE',  ( 6.224689322667630975, 139.9988794244332269, 48.18553814190077844 ) ) ;
#6356=CARTESIAN_POINT ( 'NONE',  ( 16.75465622695633883, 120.7871673903176912, 75.09093759626908593 ) ) ;
#6359=CARTESIAN_POINT ( 'NONE',  ( 2.430230287190592531, 1.451610819317743051, 145.5073573687466819 ) ) ;
#6361=EDGE_CURVE ( 'NONE', #1161, #24022, #12770, .T. ) ;
#6362=DIRECTION ( 'NONE',  ( 0.5946245182733607137, -0.3994439555666229325, -0.6977579871484549390 ) ) ;
#6366=B_SPLINE_CURVE_WITH_KNOTS ( 'NONE', 3,
 ( #16079, #24884, #5145, #2996, #11779, #9611, #19372, #23164 ),
 .UNSPECIFIED., .F., .F.,
 ( 4, 2, 2, 4 ),
 ( 1.551583845779545699E-17, 0.0002429592666046777902, 0.0004859185332093400762, 0.0009718370664186931629 ),
 .UNSPECIFIED. ) ;
#6367=CARTESIAN_POINT ( 'NONE',  ( 6.224689322667647851, 43.30635742325564763, -141.5842213414009336 ) ) ;
#6368=CARTESIAN_POINT ( 'NONE',  ( 32.73300124599738581, -92.86301839380070078, 72.21147546950520280 ) ) ;
#6369=CIRCLE ( 'NONE', #27969, 151.1787379149930359 ) ;
#6370=ORIENTED_EDGE ( 'NONE', *, *, #6778, .T. ) ;
#6371=CIRCLE ( 'NONE', #19252, 143.8872038478949946 ) ;
#6373=ORIENTED_EDGE ( 'NONE', *, *, #417, .F. ) ;
#6378=VERTEX_POINT ( 'NONE', #20785 ) ;
#6379=CARTESIAN_POINT ( 'NONE',  ( 109.1589550718174877, -0.001354998915261381278, -0.007453082872776636315 ) ) ;
#6381=ADVANCED_FACE ( 'NONE', ( #13628 ), #605, .T. ) ;
#6382=FACE_OUTER_BOUND ( 'NONE', #14801, .T. ) ;
#6384=CARTESIAN_POINT ( 'NONE',  ( 1.832998868059858122, 125.4013017422230831, 73.01698022778400343 ) ) ;
#6385=CARTESIAN_POINT ( 'NONE',  ( 109.1721716018069515, -0.01616973485710002101, -0.005466227998627423527 ) ) ;
#6388=CARTESIAN_POINT ( 'NONE',  ( 25.64692232868535982, -110.3753891203787987, 23.79507962493589801 ) ) ;
#6390=CARTESIAN_POINT ( 'NONE',  ( 25.81918753295378011, 102.8711004511199860, -46.82320532096414922 ) ) ;
#6391=CARTESIAN_POINT ( 'NONE',  ( 24.01988960052077360, -69.18817751538357186, 111.2910478357996169 ) ) ;
#6392=ORIENTED_EDGE ( 'NONE', *, *, #11541, .F. ) ;
#6393=VERTEX_POINT ( 'NONE', #14450 ) ;
#6396=CARTESIAN_POINT ( 'NONE',  ( 5.340103556456445411, -17.70136535450003734, 146.3832391989195401 ) ) ;
#6399=ORIENTED_EDGE ( 'NONE', *, *, #8029, .T. ) ;
#6401=EDGE_CURVE ( 'NONE', #6438, #12091, #22752, .T. ) ;
#6402=CARTESIAN_POINT ( 'NONE',  ( 2.433796855181219243, 118.5671979538068257, -84.34988187690807138 ) ) ;
#6404=ORIENTED_EDGE ( 'NONE', *, *, #27428, .T. ) ;
#6406=EDGE_CURVE ( 'NONE', #10758, #8004, #10040, .T. ) ;
#6408=CARTESIAN_POINT ( 'NONE',  ( 25.73574536432413495, 107.1893601970595142, 35.67555431182866954 ) ) ;
#6409=ORIENTED_EDGE ( 'NONE', *, *, #27548, .F. ) ;
#6417=CARTESIAN_POINT ( 'NONE',  ( 25.64681081121879203, -35.28660243342623204, 107.2555980796239936 ) ) ;
#6419=B_SPLINE_CURVE_WITH_KNOTS ( 'NONE', 3,
 ( #5641, #14831, #12669, #21454, #25518, #21168, #18592, #3758 ),
 .UNSPECIFIED., .F., .F.,
 ( 4, 2, 2, 4 ),
 ( 0.000000000000000000, 0.0002429588503611252793, 0.0004859177007222505586, 0.0009718354014444827941 ),
 .UNSPECIFIED. ) ;
#6420=CARTESIAN_POINT ( 'NONE',  ( 109.1721716018069657, -0.01368917435591426694, 0.01019541462303507999 ) ) ;
#6421=CARTESIAN_POINT ( 'NONE',  ( 2.430230287190572103, 145.5073573687466819, 1.451610819318258194 ) ) ;
#6422=CARTESIAN_POINT ( 'NONE',  ( 10.93730112725996229, -10.89264110824889364, -150.7858122213663989 ) ) ;
#6423=VERTEX_POINT ( 'NONE', #8542 ) ;
#6424=CARTESIAN_POINT ( 'NONE',  ( 1.833691583653537904, 125.4903330494899194, 72.86287859464628980 ) ) ;
#6425=CARTESIAN_POINT ( 'NONE',  ( 109.1589550718175161, 0.003980125429509219145, 0.006445391216541659571 ) ) ;
#6426=CARTESIAN_POINT ( 'NONE',  ( 10.93730112725945247, 97.44200844886275092, 115.5857507957704087 ) ) ;
#6429=ORIENTED_EDGE ( 'NONE', *, *, #11904, .F. ) ;
#6430=VERTEX_POINT ( 'NONE', #17442 ) ;
#6431=CARTESIAN_POINT ( 'NONE',  ( 32.73300124599738581, -72.21147546950486174, -92.86301839380092815 ) ) ;
#6436=CARTESIAN_POINT ( 'NONE',  ( 26.11404676487257603, -67.46175819463425682, 90.92995828888176391 ) ) ;
#6437=CARTESIAN_POINT ( 'NONE',  ( 2.263178113027061400, -137.8402779654366839, -46.26071604342208587 ) ) ;
#6438=VERTEX_POINT ( 'NONE', #27838 ) ;
#6439=CARTESIAN_POINT ( 'NONE',  ( 10.93730112725932635, 0.000000000000000000, 0.000000000000000000 ) ) ;
#6440=CARTESIAN_POINT ( 'NONE',  ( 109.1592201516379674, -0.001127733110588171120, -0.007780772729122754396 ) ) ;
#6442=CARTESIAN_POINT ( 'NONE',  ( 2.263178113027051186, -46.26071604342163113, 137.8402779654368260 ) ) ;
#6444=ORIENTED_EDGE ( 'NONE', *, *, #21940, .T. ) ;
#6446=EDGE_CURVE ( 'NONE', #10146, #26248, #3800, .T. ) ;
#6447=CARTESIAN_POINT ( 'NONE',  ( 1.833838848569444568, 14.99110384899719151, -144.3334397096296584 ) ) ;
#6449=CIRCLE ( 'NONE', #26202, 151.1787379149930359 ) ;
#6450=B_SPLINE_CURVE_WITH_KNOTS ( 'NONE', 3,
 ( #22673, #11568, #13580, #2943, #22819, #11426, #7404, #20347 ),
 .UNSPECIFIED., .F., .F.,
 ( 4, 2, 2, 4 ),
 ( 7.757919228897728493E-18, 0.0002429592666046789286, 0.0004859185332093501051, 0.0009718370664186827546 ),
 .UNSPECIFIED. ) ;
#6452=CARTESIAN_POINT ( 'NONE',  ( 10.93730112725936898, 142.1801301103782578, 51.37919228020297879 ) ) ;
#6453=VERTEX_POINT ( 'NONE', #19331 ) ;
#6455=CARTESIAN_POINT ( 'NONE',  ( 2.433796855181205476, -1.451562450950653949, 145.5024947199069629 ) ) ;
#6459=FACE_BOUND ( 'NONE', #1210, .T. ) ;
#6460=CARTESIAN_POINT ( 'NONE',  ( 1.833721034905639646, -138.1171912769427763, -44.50273803002078665 ) ) ;
#6462=CARTESIAN_POINT ( 'NONE',  ( 26.11404676487257603, 108.0249973236472130, -33.91085499298264239 ) ) ;
#6464=CARTESIAN_POINT ( 'NONE',  ( 16.05277956358235159, 99.31161228512438299, 103.3141821208282920 ) ) ;
#6465=FACE_OUTER_BOUND ( 'NONE', #19604, .T. ) ;
#6466=CARTESIAN_POINT ( 'NONE',  ( 109.1721716018069657, 0.01629455849720090610, 0.005082060336469467095 ) ) ;
#6467=ORIENTED_EDGE ( 'NONE', *, *, #23171, .T. ) ;
#6470=CARTESIAN_POINT ( 'NONE',  ( 25.64692872815577118, 103.0182448446673789, 46.21877827526595439 ) ) ;
#6472=CARTESIAN_POINT ( 'NONE',  ( 28.37599760073042532, -93.86375353586211645, 65.97809271467107806 ) ) ;
#6473=CIRCLE ( 'NONE', #5077, 117.6351876552689504 ) ;
#6474=CARTESIAN_POINT ( 'NONE',  ( 109.1721716018069515, -0.007126480965768089773, 0.01550977894511842634 ) ) ;
#6476=CARTESIAN_POINT ( 'NONE',  ( 28.37603512858356680, -13.77584568114216523, -113.9023475466376567 ) ) ;
#6477=CARTESIAN_POINT ( 'NONE',  ( 32.73300124599735739, -44.31599526638029118, 108.9684813982487412 ) ) ;
#6480=CARTESIAN_POINT ( 'NONE',  ( 109.1624594426973118, -0.01582142368019174780, 0.002129375066974411451 ) ) ;
#6481=VECTOR ( 'NONE', #26572, 999.9999999999998863 ) ;
#6483=CARTESIAN_POINT ( 'NONE',  ( 8.186469829614441807, 77.65916164626527518, -127.5731248499969439 ) ) ;
#6484=ADVANCED_FACE ( 'NONE', ( #8680 ), #12526, .F. ) ;
#6486=( BOUNDED_SURFACE ( )  B_SPLINE_SURFACE ( 3, 1, ( 
 ( #20048, #22514 ),
 ( #24542, #2781 ),
 ( #4805, #7123 ),
 ( #9416, #15880 ) ),
 .UNSPECIFIED., .F., .F., .F. ) 
 B_SPLINE_SURFACE_WITH_KNOTS ( ( 4, 4 ),
 ( 2, 2 ),
 ( 0.000000000000000000, 1.000000000000000000 ),
 ( 0.000000000000000000, 1.000000000000000000 ),
 .UNSPECIFIED. ) 
 GEOMETRIC_REPRESENTATION_ITEM ( )  RATIONAL_B_SPLINE_SURFACE ( (
 ( 1.000000000000000000, 1.000000000000000000),
 ( 0.6386103224230316178, 0.9954351624131538845),
 ( 0.6386103224230316178, 0.9954351624131538845),
 ( 1.000000000000000000, 1.000000000000000000) ) ) 
 REPRESENTATION_ITEM ( '' )  SURFACE ( )  );
#6488=AXIS2_PLACEMENT_3D ( 'NONE', #2769, #9407, #13559 ) ;
#6489=CARTESIAN_POINT ( 'NONE',  ( 2.108985857320915702, -46.11505917359347961, -137.7807691131292813 ) ) ;
#6490=EDGE_CURVE ( 'NONE', #18732, #25406, #25695, .T. ) ;
#6493=EDGE_CURVE ( 'NONE', #12120, #14327, #1635, .T. ) ;
#6494=EDGE_LOOP ( 'NONE', ( #5082, #15860, #3017, #1733 ) ) ;
#6495=VERTEX_POINT ( 'NONE', #1766 ) ;
#6498=CARTESIAN_POINT ( 'NONE',  ( 1.832998868059858122, 97.49378069860945573, -107.4798986104849803 ) ) ;
#6499=CARTESIAN_POINT ( 'NONE',  ( 5.340103579038066428, 144.6887562507423297, 28.39990973304521304 ) ) ;
#6502=CARTESIAN_POINT ( 'NONE',  ( 2.433796855181205476, 98.43889364294005873, -107.1581411821775305 ) ) ;
#6505=CARTESIAN_POINT ( 'NONE',  ( 13.36082413113061307, 6.345145185220180117, -152.7944199136426846 ) ) ;
#6507=CARTESIAN_POINT ( 'NONE',  ( 5.340103556456319289, 126.5279493230358270, 75.71042922800570807 ) ) ;
#6510=AXIS2_PLACEMENT_3D ( 'NONE', #1607, #23508, #10276 ) ;
#6511=VECTOR ( 'NONE', #16826, 1000.000000000000114 ) ;
#6513=FACE_OUTER_BOUND ( 'NONE', #23311, .T. ) ;
#6516=ORIENTED_EDGE ( 'NONE', *, *, #4081, .F. ) ;
#6517=( BOUNDED_SURFACE ( )  B_SPLINE_SURFACE ( 3, 1, ( 
 ( #8180, #12615 ),
 ( #27882, #8725 ),
 ( #21536, #1675 ),
 ( #25734, #17352 ) ),
 .UNSPECIFIED., .F., .F., .F. ) 
 B_SPLINE_SURFACE_WITH_KNOTS ( ( 4, 4 ),
 ( 2, 2 ),
 ( 0.000000000000000000, 1.000000000000000000 ),
 ( 0.000000000000000000, 1.000000000000000000 ),
 .UNSPECIFIED. ) 
 GEOMETRIC_REPRESENTATION_ITEM ( )  RATIONAL_B_SPLINE_SURFACE ( (
 ( 1.000000000000000000, 1.000000000000000000),
 ( 0.9960225298536222738, 0.9999952330161893110),
 ( 0.9960225298536222738, 0.9999952330161893110),
 ( 1.000000000000000000, 1.000000000000000000) ) ) 
 REPRESENTATION_ITEM ( '' )  SURFACE ( )  );
#6519=ORIENTED_EDGE ( 'NONE', *, *, #12197, .F. ) ;
#6521=DIRECTION ( 'NONE',  ( -1.000000000000000000, -0.000000000000000000, -0.000000000000000000 ) ) ;
#6522=ORIENTED_EDGE ( 'NONE', *, *, #10132, .T. ) ;
#6523=VERTEX_POINT ( 'NONE', #21360 ) ;
#6525=LINE ( 'NONE', #2176, #2823 ) ;
#6526=DIRECTION ( 'NONE',  ( -1.000000000000000000, -0.000000000000000000, -0.000000000000000000 ) ) ;
#6527=VECTOR ( 'NONE', #23541, 1000.000000000000000 ) ;
#6528=CARTESIAN_POINT ( 'NONE',  ( 13.36082413113063083, 25.56125765253660376, -150.7747251079859723 ) ) ;
#6529=CARTESIAN_POINT ( 'NONE',  ( 25.64692872815576408, 66.10702795113414254, 91.53575854059441497 ) ) ;
#6531=CARTESIAN_POINT ( 'NONE',  ( 109.1624594426973260, 0.006066618937909673721, 0.01476644236456053048 ) ) ;
#6534=CARTESIAN_POINT ( 'NONE',  ( 25.64681081121879203, 112.9102952884414464, -0.4157506337731811663 ) ) ;
#6538=ORIENTED_EDGE ( 'NONE', *, *, #14907, .T. ) ;
#6539=CARTESIAN_POINT ( 'NONE',  ( 25.64708010899964563, 91.37928813995172561, 66.32331961783411600 ) ) ;
#6541=CARTESIAN_POINT ( 'NONE',  ( 2.433796855181233454, 96.28145139437833677, -109.1007109081216129 ) ) ;
#6544=DIRECTION ( 'NONE',  ( -1.000000000000000000, -0.000000000000000000, -0.000000000000000000 ) ) ;
#6548=CARTESIAN_POINT ( 'NONE',  ( 28.43349137099833257, -86.10800331998733270, -89.57679848841901560 ) ) ;
#6549=ORIENTED_EDGE ( 'NONE', *, *, #8425, .F. ) ;
#6555=VECTOR ( 'NONE', #27266, 1000.000000000000114 ) ;
#6556=ORIENTED_EDGE ( 'NONE', *, *, #13903, .F. ) ;
#6562=CARTESIAN_POINT ( 'NONE',  ( 55.49584447822657296, -7.317474139116119325, 72.18163437663937998 ) ) ;
#6563=CARTESIAN_POINT ( 'NONE',  ( 1.833206308920113825, 126.0392061186632304, -71.90885838897261806 ) ) ;
#6566=CARTESIAN_POINT ( 'NONE',  ( 9.884929003653608603, -71.59798461011239112, -132.4189379373577822 ) ) ;
#6567=CARTESIAN_POINT ( 'NONE',  ( 1.894214914920933301, 144.2521558665609405, -16.12044375672139296 ) ) ;
#6569=VECTOR ( 'NONE', #14593, 1000.000000000000000 ) ;
#6574=ORIENTED_EDGE ( 'NONE', *, *, #5528, .T. ) ;
#6575=VERTEX_POINT ( 'NONE', #15421 ) ;
#6576=CARTESIAN_POINT ( 'NONE',  ( 25.64681081121879203, 83.63051021306002042, -75.86069728268907397 ) ) ;
#6577=CARTESIAN_POINT ( 'NONE',  ( 109.1587776205901577, 0.002185517590245255552, 0.006995903587858435038 ) ) ;
#6578=CARTESIAN_POINT ( 'NONE',  ( 5.340103579038293802, 143.7310399932982250, -32.90561047415462070 ) ) ;
#6579=CARTESIAN_POINT ( 'NONE',  ( 24.01988960052059241, 61.78678588190025778, 115.5642432877694290 ) ) ;
#6580=CARTESIAN_POINT ( 'NONE',  ( 25.69398547355838502, -90.93418986874847576, 66.98507266663722248 ) ) ;
#6581=CARTESIAN_POINT ( 'NONE',  ( 25.87036335909428075, 90.88222105969153120, -67.25332031939053934 ) ) ;
#6582=ADVANCED_FACE ( 'NONE', ( #13134 ), #20241, .T. ) ;
#6584=ORIENTED_EDGE ( 'NONE', *, *, #12391, .F. ) ;
#6585=CARTESIAN_POINT ( 'NONE',  ( 2.063896406836605024, 57.85593781835414973, 133.2511741302122346 ) ) ;
#6588=CARTESIAN_POINT ( 'NONE',  ( 25.64704443564077252, 112.2786464378873603, 11.93517308299176349 ) ) ;
#6589=CARTESIAN_POINT ( 'NONE',  ( 25.64692232868535626, 110.3753891203789266, -23.79507962493517326 ) ) ;
#6590=ORIENTED_EDGE ( 'NONE', *, *, #226, .F. ) ;
#6592=CARTESIAN_POINT ( 'NONE',  ( 109.1624594426973118, 0.01438905500501946530, -0.006914244825467830320 ) ) ;
#6594=EDGE_LOOP ( 'NONE', ( #8188, #4477, #13126, #16065 ) ) ;
#6595=CARTESIAN_POINT ( 'NONE',  ( 2.433796855181233454, -138.8296532063085351, -43.58222566461785163 ) ) ;
#6596=VECTOR ( 'NONE', #20188, 1000.000000000000114 ) ;
#6599=VERTEX_POINT ( 'NONE', #22211 ) ;
#6600=B_SPLINE_CURVE_WITH_KNOTS ( 'NONE', 3,
 ( #20563, #846, #25051, #9786, #21128, #1414, #18555 ),
 .UNSPECIFIED., .F., .F.,
 ( 4, 3, 4 ),
 ( 3.179800655392250756E-17, 0.02816610861753246833, 0.04000277880656213925 ),
 .UNSPECIFIED. ) ;
#6602=DIRECTION ( 'NONE',  ( 0.000000000000000000, 0.000000000000000000, -1.000000000000000000 ) ) ;
#6603=FACE_OUTER_BOUND ( 'NONE', #19119, .T. ) ;
#6604=CARTESIAN_POINT ( 'NONE',  ( 55.79472521941426777, 0.7279028900803861113, -72.75035398477135118 ) ) ;
#6605=CARTESIAN_POINT ( 'NONE',  ( 6.224689322667647851, -144.2687111683197543, 33.28770499679286843 ) ) ;
#6606=ADVANCED_FACE ( 'NONE', ( #4930 ), #2768, .F. ) ;
#6607=CARTESIAN_POINT ( 'NONE',  ( 25.64681081121879203, -91.10197563707990298, 66.70335573067838197 ) ) ;
#6608=VECTOR ( 'NONE', #7202, 1000.000000000000114 ) ;
#6609=CARTESIAN_POINT ( 'NONE',  ( 10.93730112725945602, 104.7670965581007607, 108.9902118373744742 ) ) ;
#6610=CARTESIAN_POINT ( 'NONE',  ( 99.22246935314079508, 90.00000000000005684, -40.00000000000000711 ) ) ;
#6615=B_SPLINE_CURVE_WITH_KNOTS ( 'NONE', 3,
 ( #8238, #23085, #12396, #5654, #27660, #8384, #9981 ),
 .UNSPECIFIED., .F., .F.,
 ( 4, 3, 4 ),
 ( 0.000000000000000000, 0.02398743853561352557, 0.04000277880656219476 ),
 .UNSPECIFIED. ) ;
#6620=CARTESIAN_POINT ( 'NONE',  ( 26.11404676487257603, 55.62948129436244926, 98.61392875273382685 ) ) ;
#6626=FACE_OUTER_BOUND ( 'NONE', #10019, .T. ) ;
#6627=B_SPLINE_CURVE_WITH_KNOTS ( 'NONE', 3,
 ( #2884, #18410, #20718, #11946, #13665, #7216, #7652, #24779, #18260, #27481 ),
 .UNSPECIFIED., .F., .F.,
 ( 4, 3, 3, 4 ),
 ( 1.387778780781445676E-17, 0.0002669559177086302604, 0.0005339118354151229078, 0.001067817517169169237 ),
 .UNSPECIFIED. ) ;
#6628=CARTESIAN_POINT ( 'NONE',  ( 26.28373643307407548, -125.5716026420346765, -22.43832507403785215 ) ) ;
#6630=CARTESIAN_POINT ( 'NONE',  ( 25.64681081121879203, 12.21581276189956711, -112.2483031020012305 ) ) ;
#6632=CARTESIAN_POINT ( 'NONE',  ( 1.833485406944043827, -117.0814567582538501, -85.72460230293812344 ) ) ;
#6636=CARTESIAN_POINT ( 'NONE',  ( 109.1624594426973118, 0.006914244825467785217, 0.01438905500501948959 ) ) ;
#6637=CARTESIAN_POINT ( 'NONE',  ( 109.1586900883932856, -0.003656351050324928211, 0.006130969560693650365 ) ) ;
#6639=( BOUNDED_SURFACE ( )  B_SPLINE_SURFACE ( 3, 1, ( 
 ( #20832, #3547 ),
 ( #12198, #1390 ),
 ( #27300, #10198 ),
 ( #1537, #9907 ) ),
 .UNSPECIFIED., .F., .F., .F. ) 
 B_SPLINE_SURFACE_WITH_KNOTS ( ( 4, 4 ),
 ( 2, 2 ),
 ( 0.000000000000000000, 1.000000000000000000 ),
 ( 0.000000000000000000, 1.000000000000000000 ),
 .UNSPECIFIED. ) 
 GEOMETRIC_REPRESENTATION_ITEM ( )  RATIONAL_B_SPLINE_SURFACE ( (
 ( 1.000000000000000000, 1.000000000000000000),
 ( 0.6386103224230302855, 0.9954351624131538845),
 ( 0.6386103224230302855, 0.9954351624131538845),
 ( 1.000000000000000000, 1.000000000000000000) ) ) 
 REPRESENTATION_ITEM ( '' )  SURFACE ( )  );
#6641=CARTESIAN_POINT ( 'NONE',  ( 1.833485406944043827, 72.09189602597706426, 125.9346397303438039 ) ) ;
#6642=ADVANCED_FACE ( 'NONE', ( #4640 ), #19327, .T. ) ;
#6643=CARTESIAN_POINT ( 'NONE',  ( 2.433796855181205476, -109.1007109081232471, 96.28145139437646094 ) ) ;
#6646=EDGE_CURVE ( 'NONE', #12003, #704, #779, .T. ) ;
#6647=B_SPLINE_CURVE_WITH_KNOTS ( 'NONE', 3,
 ( #1290, #13849, #20472, #11702, #757, #8207, #18856, #18293 ),
 .UNSPECIFIED., .F., .F.,
 ( 4, 2, 2, 4 ),
 ( 6.938893903907228378E-18, 0.0002429588503611289385, 0.0004859177007222509380, 0.0009718354014444895161 ),
 .UNSPECIFIED. ) ;
#6651=EDGE_CURVE ( 'NONE', #10661, #16635, #18628, .T. ) ;
#6653=CARTESIAN_POINT ( 'NONE',  ( 1.833485406944043827, -0.5339064996894915538, 145.1085452359073145 ) ) ;
#6655=( BOUNDED_SURFACE ( )  B_SPLINE_SURFACE ( 3, 1, ( 
 ( #1895, #19463 ),
 ( #13392, #23941 ),
 ( #16, #10972 ),
 ( #172, #12978 ) ),
 .UNSPECIFIED., .F., .F., .F. ) 
 B_SPLINE_SURFACE_WITH_KNOTS ( ( 4, 4 ),
 ( 2, 2 ),
 ( 0.000000000000000000, 1.000000000000000000 ),
 ( 0.000000000000000000, 1.000000000000000000 ),
 .UNSPECIFIED. ) 
 GEOMETRIC_REPRESENTATION_ITEM ( )  RATIONAL_B_SPLINE_SURFACE ( (
 ( 1.000000000000000000, 1.000000000000000000),
 ( 0.6386103224230302855, 0.9954351624131538845),
 ( 0.6386103224230302855, 0.9954351624131538845),
 ( 1.000000000000000000, 1.000000000000000000) ) ) 
 REPRESENTATION_ITEM ( '' )  SURFACE ( )  );
#6657=CARTESIAN_POINT ( 'NONE',  ( 26.11404676487257603, 33.91085499298377925, 108.0249973236468577 ) ) ;
#6660=CARTESIAN_POINT ( 'NONE',  ( 1.833603222531973831, 14.72553080638994594, 144.3605362014088769 ) ) ;
#6661=CARTESIAN_POINT ( 'NONE',  ( 30.59138290137879679, -9.457588828075969900, 115.8270707793589196 ) ) ;
#6662=EDGE_LOOP ( 'NONE', ( #8585, #27210, #21299, #17706 ) ) ;
#6663=ORIENTED_EDGE ( 'NONE', *, *, #9267, .T. ) ;
#6664=CARTESIAN_POINT ( 'NONE',  ( 2.108393763691192468, -126.4628696952924116, 71.53437599919774925 ) ) ;
#6665=LINE ( 'NONE', #12563, #15262 ) ;
#6670=B_SPLINE_CURVE_WITH_KNOTS ( 'NONE', 3,
 ( #14130, #1329, #18900, #27671, #7987, #11987, #23375 ),
 .UNSPECIFIED., .F., .F.,
 ( 4, 3, 4 ),
 ( 4.201076225734585017E-16, 0.02816610861753247180, 0.04000277880656250701 ),
 .UNSPECIFIED. ) ;
#6672=CARTESIAN_POINT ( 'NONE',  ( 1.832998868059858122, -107.4798986104866572, 97.49378069860762253 ) ) ;
#6673=B_SPLINE_CURVE_WITH_KNOTS ( 'NONE', 3,
 ( #11170, #6293, #8583, #6856, #26137, #28421, #360, #1950 ),
 .UNSPECIFIED., .F., .F.,
 ( 4, 2, 2, 4 ),
 ( 7.757919228897728493E-18, 0.0002429592666046767060, 0.0004859185332093456599, 0.0009718370664186836219 ),
 .UNSPECIFIED. ) ;
#6674=CARTESIAN_POINT ( 'NONE',  ( 25.73574536432415982, 11.00659994954150278, 112.4329083163018481 ) ) ;
#6676=CARTESIAN_POINT ( 'NONE',  ( 2.430230287190589422, -145.5073573687466819, 1.451610819317230572 ) ) ;
#6677=CARTESIAN_POINT ( 'NONE',  ( 109.1587776205901861, 0.006305329297950502086, -0.003736572840496154083 ) ) ;
#6679=B_SPLINE_CURVE_WITH_KNOTS ( 'NONE', 3,
 ( #10255, #5634, #21018, #14826, #1302, #19016, #12250, #25361, #27797, #23639 ),
 .UNSPECIFIED., .F., .F.,
 ( 4, 3, 3, 4 ),
 ( 3.295974604355933479E-17, 0.0002669559177086193642, 0.0005339118354150988385, 0.001067817517169165550 ),
 .UNSPECIFIED. ) ;
#6682=CARTESIAN_POINT ( 'NONE',  ( 28.43349137099830415, -105.5221910860621932, 65.60227321965550118 ) ) ;
#6684=CARTESIAN_POINT ( 'NONE',  ( 16.05277956358200342, 103.3141821208296562, -99.31161228512374350 ) ) ;
#6685=( BOUNDED_SURFACE ( )  B_SPLINE_SURFACE ( 3, 1, ( 
 ( #19151, #3893 ),
 ( #17260, #4162 ),
 ( #17123, #14823 ),
 ( #21446, #16861 ) ),
 .UNSPECIFIED., .F., .F., .F. ) 
 B_SPLINE_SURFACE_WITH_KNOTS ( ( 4, 4 ),
 ( 2, 2 ),
 ( 0.000000000000000000, 1.000000000000000000 ),
 ( 0.000000000000000000, 1.000000000000000000 ),
 .UNSPECIFIED. ) 
 GEOMETRIC_REPRESENTATION_ITEM ( )  RATIONAL_B_SPLINE_SURFACE ( (
 ( 1.000000000000000000, 1.000000000000000000),
 ( 0.9960225298536222738, 0.9999952330161893110),
 ( 0.9960225298536222738, 0.9999952330161893110),
 ( 1.000000000000000000, 1.000000000000000000) ) ) 
 REPRESENTATION_ITEM ( '' )  SURFACE ( )  );
#6686=ORIENTED_EDGE ( 'NONE', *, *, #18420, .F. ) ;
#6688=CARTESIAN_POINT ( 'NONE',  ( 25.64704443564076541, 91.26857357624568579, 66.47548630737885844 ) ) ;
#6690=CARTESIAN_POINT ( 'NONE',  ( 1.833838850855461500, -144.3055354793886522, -15.25659494068255384 ) ) ;
#6692=CARTESIAN_POINT ( 'NONE',  ( 25.70243777736187241, 0.7331659071611001943, -112.9457924277214005 ) ) ;
#6693=CARTESIAN_POINT ( 'NONE',  ( 32.73300124599737160, -75.82012867748541396, 89.94078864464039214 ) ) ;
#6694=ORIENTED_EDGE ( 'NONE', *, *, #17960, .F. ) ;
#6695=CARTESIAN_POINT ( 'NONE',  ( 2.108393763691204903, 145.2872457912032758, 1.280847988472279431 ) ) ;
#6697=CARTESIAN_POINT ( 'NONE',  ( 28.37644542392835234, 86.16884085958076867, -89.64009552702822248 ) ) ;
#6699=ORIENTED_EDGE ( 'NONE', *, *, #4961, .T. ) ;
#6700=ORIENTED_EDGE ( 'NONE', *, *, #10589, .T. ) ;
#6701=CARTESIAN_POINT ( 'NONE',  ( 119.2224693531408803, 0.000000000000000000, 19.99999999999997513 ) ) ;
#6704=VERTEX_POINT ( 'NONE', #12269 ) ;
#6705=CARTESIAN_POINT ( 'NONE',  ( 25.87036335909428786, 67.25332031939144883, 90.88222105969083486 ) ) ;
#6706=ADVANCED_FACE ( 'NONE', ( #25381 ), #24298, .F. ) ;
#6709=CARTESIAN_POINT ( 'NONE',  ( 1.833485406944043827, 144.3694338680886915, -14.63699153649211127 ) ) ;
#6711=CARTESIAN_POINT ( 'NONE',  ( 109.1592201516379674, -0.006649399203953433417, 0.004194960840990133617 ) ) ;
#6712=CARTESIAN_POINT ( 'NONE',  ( -90.83090735639699176, 2.449293598294706119E-15, 20.00000000000000000 ) ) ;
#6713=CARTESIAN_POINT ( 'NONE',  ( 109.1721716018069657, -0.007126480965770814156, -0.01550977894512763945 ) ) ;
#6714=CARTESIAN_POINT ( 'NONE',  ( 25.98107933586726404, -1.091357942391386615, 113.1286487641201006 ) ) ;
#6716=ORIENTED_EDGE ( 'NONE', *, *, #22245, .F. ) ;
#6717=CARTESIAN_POINT ( 'NONE',  ( 25.87036335909426654, 83.35447252092961890, -76.38467849957065425 ) ) ;
#6720=B_SPLINE_CURVE_WITH_KNOTS ( 'NONE', 3,
 ( #5, #13377, #4760, #11236 ),
 .UNSPECIFIED., .F., .F.,
 ( 4, 4 ),
 ( 1.040834085586084257E-17, 0.008383560773332680849 ),
 .UNSPECIFIED. ) ;
#6722=CARTESIAN_POINT ( 'NONE',  ( 19.66333377628701840, 127.6002314355565659, -51.89484018353712003 ) ) ;
#6725=CARTESIAN_POINT ( 'NONE',  ( 1.833206308920100058, -107.3376449983721130, -97.64934899952810099 ) ) ;
#6726=CARTESIAN_POINT ( 'NONE',  ( 28.37603512858356325, 114.7183465482399782, -1.794342805483269965 ) ) ;
#6727=CARTESIAN_POINT ( 'NONE',  ( 25.64681081121879203, 112.3352186517030731, 11.38886654529711961 ) ) ;
#6728=CARTESIAN_POINT ( 'NONE',  ( 109.1586900883932856, 0.004851151255031855604, -0.005236795036868175865 ) ) ;
#6729=B_SPLINE_CURVE_WITH_KNOTS ( 'NONE', 3,
 ( #6060, #26040, #12652, #16976, #28049, #8208, #25767, #14814, #23475, #21436 ),
 .UNSPECIFIED., .F., .F.,
 ( 4, 3, 3, 4 ),
 ( 1.387778780781445676E-17, 0.0002669560319015715504, 0.0005492286108966297443, 0.0008315040496093390431 ),
 .UNSPECIFIED. ) ;
#6730=ORIENTED_EDGE ( 'NONE', *, *, #12160, .F. ) ;
#6731=CARTESIAN_POINT ( 'NONE',  ( 55.49584447822657296, -14.82242356767984326, 71.02133150427250996 ) ) ;
#6732=( BOUNDED_SURFACE ( )  B_SPLINE_SURFACE ( 3, 1, ( 
 ( #23575, #19507 ),
 ( #1941, #2074 ),
 ( #4107, #10879 ),
 ( #15168, #28411 ) ),
 .UNSPECIFIED., .F., .F., .F. ) 
 B_SPLINE_SURFACE_WITH_KNOTS ( ( 4, 4 ),
 ( 2, 2 ),
 ( 0.000000000000000000, 1.000000000000000000 ),
 ( 0.000000000000000000, 1.000000000000000000 ),
 .UNSPECIFIED. ) 
 GEOMETRIC_REPRESENTATION_ITEM ( )  RATIONAL_B_SPLINE_SURFACE ( (
 ( 1.000000000000000000, 1.000000000000000000),
 ( 0.6386103224230302855, 0.9954351624131538845),
 ( 0.6386103224230302855, 0.9954351624131538845),
 ( 1.000000000000000000, 1.000000000000000000) ) ) 
 REPRESENTATION_ITEM ( '' )  SURFACE ( )  );
#6733=EDGE_CURVE ( 'NONE', #22385, #13658, #420, .T. ) ;
#6734=CARTESIAN_POINT ( 'NONE',  ( 10.93730112725990367, -142.1801301103781157, -51.37919228020433593 ) ) ;
#6735=CARTESIAN_POINT ( 'NONE',  ( 1.833809397773885630, -97.22957127128904631, 107.7184108265659859 ) ) ;
#6736=ORIENTED_EDGE ( 'NONE', *, *, #14506, .T. ) ;
#6741=B_SPLINE_CURVE_WITH_KNOTS ( 'NONE', 3,
 ( #16921, #3670, #27424, #16343, #10030, #22992, #16490, #3253 ),
 .UNSPECIFIED., .F., .F.,
 ( 4, 2, 2, 4 ),
 ( 1.250926888277100303E-17, 0.0002429592666046815307, 0.0004859185332093505388, 0.0009718370664186885008 ),
 .UNSPECIFIED. ) ;
#6743=CARTESIAN_POINT ( 'NONE',  ( 25.69398547355838502, 55.82723250638906620, -98.18017599249780858 ) ) ;
#6744=PLANE ( 'NONE',  #9361 ) ;
#6745=DIRECTION ( 'NONE',  ( -0.5946245182733607137, -0.6487139525627746428, 0.4749651461092231908 ) ) ;
#6747=CARTESIAN_POINT ( 'NONE',  ( 25.64681081121879203, 110.5293738517608375, 23.06870491922360245 ) ) ;
#6748=VERTEX_POINT ( 'NONE', #18292 ) ;
#6749=CARTESIAN_POINT ( 'NONE',  ( 109.1589550718174877, 0.001014448720240637355, -0.007507020724817408015 ) ) ;
#6751=CARTESIAN_POINT ( 'NONE',  ( 25.98552792386801258, -47.00040718953707142, -102.9121737515625199 ) ) ;
#6752=FACE_OUTER_BOUND ( 'NONE', #21366, .T. ) ;
#6753=ORIENTED_EDGE ( 'NONE', *, *, #5615, .F. ) ;
#6754=ORIENTED_EDGE ( 'NONE', *, *, #3257, .T. ) ;
#6755=ORIENTED_EDGE ( 'NONE', *, *, #8248, .T. ) ;
#6757=VECTOR ( 'NONE', #7948, 1000.000000000000114 ) ;
#6759=CARTESIAN_POINT ( 'NONE',  ( 25.73574536432417403, -24.27578079247234299, 110.3312765349292164 ) ) ;
#6760=CARTESIAN_POINT ( 'NONE',  ( 2.430230287190589422, -84.35270093935336888, 118.5711603495678474 ) ) ;
#6764=CARTESIAN_POINT ( 'NONE',  ( 2.108985857320877955, 31.46042399111245658, 141.8463279126002590 ) ) ;
#6766=CARTESIAN_POINT ( 'NONE',  ( 25.64707127832796019, -0.04449220797097835911, 112.9112343549835487 ) ) ;
#6768=CARTESIAN_POINT ( 'NONE',  ( 25.70243777736189728, -75.03063812271992106, -84.42566495012526673 ) ) ;
#6770=( BOUNDED_SURFACE ( )  B_SPLINE_SURFACE ( 3, 1, ( 
 ( #8810, #447 ),
 ( #11111, #19731 ),
 ( #15407, #9091 ),
 ( #13682, #26635 ) ),
 .UNSPECIFIED., .F., .F., .F. ) 
 B_SPLINE_SURFACE_WITH_KNOTS ( ( 4, 4 ),
 ( 2, 2 ),
 ( 0.000000000000000000, 1.000000000000000000 ),
 ( 0.000000000000000000, 1.000000000000000000 ),
 .UNSPECIFIED. ) 
 GEOMETRIC_REPRESENTATION_ITEM ( )  RATIONAL_B_SPLINE_SURFACE ( (
 ( 1.000000000000000000, 1.000000000000000000),
 ( 0.9960225298536222738, 0.9999952330161893110),
 ( 0.9960225298536222738, 0.9999952330161893110),
 ( 1.000000000000000000, 1.000000000000000000) ) ) 
 REPRESENTATION_ITEM ( '' )  SURFACE ( )  );
#6772=CARTESIAN_POINT ( 'NONE',  ( 10.93730112725932635, 0.000000000000000000, 0.000000000000000000 ) ) ;
#6773=CARTESIAN_POINT ( 'NONE',  ( 1.833721034905647862, -117.6051524288277790, -85.00517831633806054 ) ) ;
#6774=EDGE_LOOP ( 'NONE', ( #4759, #7242, #2571, #7910 ) ) ;
#6776=ORIENTED_EDGE ( 'NONE', *, *, #599, .T. ) ;
#6777=EDGE_LOOP ( 'NONE', ( #2607, #12413, #11492, #3365 ) ) ;
#6778=EDGE_CURVE ( 'NONE', #7362, #6115, #5527, .T. ) ;
#6779=B_SPLINE_CURVE_WITH_KNOTS ( 'NONE', 3,
 ( #15454, #28407, #15589, #6705, #8708, #24263, #9002, #17894 ),
 .UNSPECIFIED., .F., .F.,
 ( 4, 2, 2, 4 ),
 ( 3.469446951953614189E-18, 0.0002429592666046763265, 0.0004859185332093491835, 0.0009718370664186922955 ),
 .UNSPECIFIED. ) ;
#6782=CARTESIAN_POINT ( 'NONE',  ( 1.831572820252008738, 97.82994539998530570, -107.1759352627496185 ) ) ;
#6784=ORIENTED_EDGE ( 'NONE', *, *, #713, .T. ) ;
#6791=LINE ( 'NONE', #15535, #12992 ) ;
#6792=CARTESIAN_POINT ( 'NONE',  ( 109.1586059443104944, 0.006971743774739760056, 0.001198897580739020224 ) ) ;
#6794=CARTESIAN_POINT ( 'NONE',  ( 1.833206310202336153, 73.19872434058787292, 125.2945016693813045 ) ) ;
#6795=CARTESIAN_POINT ( 'NONE',  ( 32.73300124599739291, 105.8473486001057466, -51.32617430724801721 ) ) ;
#6796=CARTESIAN_POINT ( 'NONE',  ( 30.59141879584280588, 33.33270905817592933, 111.3296561588013134 ) ) ;
#6798=B_SPLINE_CURVE_WITH_KNOTS ( 'NONE', 3,
 ( #25135, #11594, #18067, #16195, #20374, #26846 ),
 .UNSPECIFIED., .F., .F.,
 ( 4, 2, 4 ),
 ( 4.336808689942017255E-19, 0.0006311571484585985249, 0.001262314296917196399 ),
 .UNSPECIFIED. ) ;
#6799=CARTESIAN_POINT ( 'NONE',  ( 2.430230287190592531, -109.1043569252007615, -96.28466919684210268 ) ) ;
#6802=CARTESIAN_POINT ( 'NONE',  ( 25.98552792386801968, -1.078856412010039678, -113.1317367103340104 ) ) ;
#6803=ORIENTED_EDGE ( 'NONE', *, *, #24011, .F. ) ;
#6804=ORIENTED_EDGE ( 'NONE', *, *, #14816, .T. ) ;
#6807=ORIENTED_EDGE ( 'NONE', *, *, #5614, .T. ) ;
#6808=EDGE_CURVE ( 'NONE', #2120, #422, #3184, .T. ) ;
#6809=ORIENTED_EDGE ( 'NONE', *, *, #7597, .F. ) ;
#6811=ADVANCED_FACE ( 'NONE', ( #14122 ), #17469, .F. ) ;
#6812=( BOUNDED_SURFACE ( )  B_SPLINE_SURFACE ( 3, 1, ( 
 ( #2364, #8873 ),
 ( #15461, #20211 ),
 ( #6713, #11304 ),
 ( #17773, #2511 ) ),
 .UNSPECIFIED., .F., .F., .F. ) 
 B_SPLINE_SURFACE_WITH_KNOTS ( ( 4, 4 ),
 ( 2, 2 ),
 ( 0.000000000000000000, 1.000000000000000000 ),
 ( 0.000000000000000000, 1.000000000000000000 ),
 .UNSPECIFIED. ) 
 GEOMETRIC_REPRESENTATION_ITEM ( )  RATIONAL_B_SPLINE_SURFACE ( (
 ( 1.000000000000000000, 1.000000000000000000),
 ( 0.6386103224230302855, 0.9954351624131538845),
 ( 0.6386103224230302855, 0.9954351624131538845),
 ( 1.000000000000000000, 1.000000000000000000) ) ) 
 REPRESENTATION_ITEM ( '' )  SURFACE ( )  );
#6813=ADVANCED_FACE ( 'NONE', ( #6229 ), #16571, .F. ) ;
#6815=CARTESIAN_POINT ( 'NONE',  ( 25.65782528836482257, 11.22838748007616338, 112.3587790429870950 ) ) ;
#6817=( BOUNDED_SURFACE ( )  B_SPLINE_SURFACE ( 3, 1, ( 
 ( #21282, #3868 ),
 ( #1563, #1825 ),
 ( #19130, #8196 ),
 ( #21698, #25750 ) ),
 .UNSPECIFIED., .F., .F., .F. ) 
 B_SPLINE_SURFACE_WITH_KNOTS ( ( 4, 4 ),
 ( 2, 2 ),
 ( 0.000000000000000000, 1.000000000000000000 ),
 ( 0.000000000000000000, 1.000000000000000000 ),
 .UNSPECIFIED. ) 
 GEOMETRIC_REPRESENTATION_ITEM ( )  RATIONAL_B_SPLINE_SURFACE ( (
 ( 1.000000000000000000, 1.000000000000000000),
 ( 0.6386103224230302855, 0.9954351624131538845),
 ( 0.6386103224230302855, 0.9954351624131538845),
 ( 1.000000000000000000, 1.000000000000000000) ) ) 
 REPRESENTATION_ITEM ( '' )  SURFACE ( )  );
#6818=CARTESIAN_POINT ( 'NONE',  ( 1.833206310202321720, 44.13245377365817035, -138.2356391007178331 ) ) ;
#6820=CARTESIAN_POINT ( 'NONE',  ( 10.93730112725978287, -136.0306644680987915, 65.95960219663069779 ) ) ;
#6821=LINE ( 'NONE', #10853, #11188 ) ;
#6825=CARTESIAN_POINT ( 'NONE',  ( 1.833603222531971388, -117.6571262511684068, 84.93295186324824897 ) ) ;
#6827=DIRECTION ( 'NONE',  ( -0.5946245182733607137, 0.7655593692109006199, 0.2456431038754836038 ) ) ;
#6828=CARTESIAN_POINT ( 'NONE',  ( 109.1778270068192853, -0.006489198140358675912, 0.006682187084639293860 ) ) ;
#6831=CARTESIAN_POINT ( 'NONE',  ( 25.73574536432415982, 110.3312765349293159, 24.27578079247199128 ) ) ;
#6832=CARTESIAN_POINT ( 'NONE',  ( 16.05277956358206026, -92.36732600443268382, 109.5668455727256969 ) ) ;
#6833=ORIENTED_EDGE ( 'NONE', *, *, #21088, .F. ) ;
#6837=CARTESIAN_POINT ( 'NONE',  ( 25.98107933586717166, -12.91054317625193448, 112.3948402207513766 ) ) ;
#6840=EDGE_CURVE ( 'NONE', #9703, #19171, #5572, .T. ) ;
#6841=CARTESIAN_POINT ( 'NONE',  ( 1.832998868059890096, 0.5339089137747921043, 145.1092030902949830 ) ) ;
#6843=CARTESIAN_POINT ( 'NONE',  ( 1.833485406944043827, -96.69979900902094982, -108.1939177044935860 ) ) ;
#6844=ORIENTED_EDGE ( 'NONE', *, *, #1767, .F. ) ;
#6845=EDGE_CURVE ( 'NONE', #7588, #22237, #26508, .T. ) ;
#6847=CIRCLE ( 'NONE', #14647, 20.00000000000000000 ) ;
#6848=B_SPLINE_CURVE_WITH_KNOTS ( 'NONE', 3,
 ( #20260, #13644, #553, #9350, #17536, #26182, #13084 ),
 .UNSPECIFIED., .F., .F.,
 ( 4, 3, 4 ),
 ( 5.601733421463777940E-16, 0.02816610861753245099, 0.04000277880656276375 ),
 .UNSPECIFIED. ) ;
#6850=( BOUNDED_SURFACE ( )  B_SPLINE_SURFACE ( 3, 1, ( 
 ( #21207, #3638 ),
 ( #25688, #3218 ),
 ( #3501, #18912 ),
 ( #20630, #12152 ) ),
 .UNSPECIFIED., .F., .F., .F. ) 
 B_SPLINE_SURFACE_WITH_KNOTS ( ( 4, 4 ),
 ( 2, 2 ),
 ( 0.000000000000000000, 1.000000000000000000 ),
 ( 0.000000000000000000, 1.000000000000000000 ),
 .UNSPECIFIED. ) 
 GEOMETRIC_REPRESENTATION_ITEM ( )  RATIONAL_B_SPLINE_SURFACE ( (
 ( 1.000000000000000000, 1.000000000000000000),
 ( 0.9956975270656955868, 0.8568959468854907557),
 ( 0.9956975270656955868, 0.8568959468854907557),
 ( 1.000000000000000000, 1.000000000000000000) ) ) 
 REPRESENTATION_ITEM ( '' )  SURFACE ( )  );
#6853=FACE_OUTER_BOUND ( 'NONE', #18916, .T. ) ;
#6855=CARTESIAN_POINT ( 'NONE',  ( 25.98552792386800192, -33.93357582585569787, 107.9280603639525538 ) ) ;
#6856=CARTESIAN_POINT ( 'NONE',  ( 25.87036335909428786, -112.3329723497411123, 12.80197335559923388 ) ) ;
#6857=FACE_OUTER_BOUND ( 'NONE', #21120, .T. ) ;
#6860=CARTESIAN_POINT ( 'NONE',  ( 26.11404676487257603, 110.5078194225161070, 24.64483677384886917 ) ) ;
#6864=EDGE_CURVE ( 'NONE', #174, #1609, #14851, .T. ) ;
#6865=CARTESIAN_POINT ( 'NONE',  ( 26.11404676487257603, 110.9778746459749641, -22.43340081644658213 ) ) ;
#6866=CARTESIAN_POINT ( 'NONE',  ( 25.64703792032471696, 112.3081285890370111, 11.65444440562218276 ) ) ;
#6867=FACE_OUTER_BOUND ( 'NONE', #5407, .T. ) ;
#6868=EDGE_CURVE ( 'NONE', #8671, #15588, #15109, .T. ) ;
#6870=FACE_OUTER_BOUND ( 'NONE', #873, .T. ) ;
#6874=CARTESIAN_POINT ( 'NONE',  ( 32.73300124599740002, 97.37344512919945316, -66.00340565729239017 ) ) ;
#6876=B_SPLINE_CURVE_WITH_KNOTS ( 'NONE', 3,
 ( #24604, #2545, #22728, #13630, #2991, #11622, #822, #7459, #20394, #15628 ),
 .UNSPECIFIED., .F., .F.,
 ( 4, 3, 3, 4 ),
 ( 5.003707553108401214E-17, 0.0002669559177086285799, 0.0005339118354151193300, 0.001067817517169137144 ),
 .UNSPECIFIED. ) ;
#6877=ORIENTED_EDGE ( 'NONE', *, *, #22325, .F. ) ;
#6878=CARTESIAN_POINT ( 'NONE',  ( 0.000000000000000000, 0.000000000000000000, 0.000000000000000000 ) ) ;
#6881=CARTESIAN_POINT ( 'NONE',  ( 25.64708228042118776, -34.92896069507359869, 107.3728320282187951 ) ) ;
#6883=CARTESIAN_POINT ( 'NONE',  ( 10.93730112725977932, -104.7670965581018123, 108.9902118373738062 ) ) ;
#6884=CARTESIAN_POINT ( 'NONE',  ( 109.1586059443104944, 0.003294606663354653162, -0.006260042619943061680 ) ) ;
#6886=CARTESIAN_POINT ( 'NONE',  ( 30.59138290137888916, -95.58039132682486638, -66.10404757334158887 ) ) ;
#6889=CARTESIAN_POINT ( 'NONE',  ( 55.49584447822657296, 7.317474139115629939, 72.18163437663943682 ) ) ;
#6890=ORIENTED_EDGE ( 'NONE', *, *, #10926, .F. ) ;
#6892=ORIENTED_EDGE ( 'NONE', *, *, #6252, .T. ) ;
#6893=ORIENTED_EDGE ( 'NONE', *, *, #1278, .T. ) ;
#6894=DIRECTION ( 'NONE',  ( -1.000000000000000000, -0.000000000000000000, -0.000000000000000000 ) ) ;
#6895=B_SPLINE_CURVE_WITH_KNOTS ( 'NONE', 3,
 ( #23359, #741, #25216, #3054, #18876, #3334, #10110, #9972 ),
 .UNSPECIFIED., .F., .F.,
 ( 4, 2, 2, 4 ),
 ( 3.469446951953614189E-18, 0.0002429592666046710139, 0.0004859185332093385584, 0.0009718370664186956566 ),
 .UNSPECIFIED. ) ;
#6896=CARTESIAN_POINT ( 'NONE',  ( 28.37603512858441590, 45.02094145483519583, -105.5302493666422379 ) ) ;
#6899=DIRECTION ( 'NONE',  ( 0.5946245182733607137, 0.7870422510449666120, -0.1642747008466166614 ) ) ;
#6900=CARTESIAN_POINT ( 'NONE',  ( 5.340103556456712752, 128.8311297043957495, -71.72120378849476197 ) ) ;
#6901=( BOUNDED_SURFACE ( )  B_SPLINE_SURFACE ( 3, 1, ( 
 ( #26646, #22646 ),
 ( #2918, #24518 ),
 ( #4786, #4925 ),
 ( #23611, #16842 ) ),
 .UNSPECIFIED., .F., .F., .F. ) 
 B_SPLINE_SURFACE_WITH_KNOTS ( ( 4, 4 ),
 ( 2, 2 ),
 ( 0.000000000000000000, 1.000000000000000000 ),
 ( 0.000000000000000000, 1.000000000000000000 ),
 .UNSPECIFIED. ) 
 GEOMETRIC_REPRESENTATION_ITEM ( )  RATIONAL_B_SPLINE_SURFACE ( (
 ( 1.000000000000000000, 1.000000000000000000),
 ( 0.6386103224230302855, 0.9954351624131538845),
 ( 0.6386103224230302855, 0.9954351624131538845),
 ( 1.000000000000000000, 1.000000000000000000) ) ) 
 REPRESENTATION_ITEM ( '' )  SURFACE ( )  );
#6902=CARTESIAN_POINT ( 'NONE',  ( 26.11404676487257603, -112.7148551500681037, 10.71016160607530310 ) ) ;
#6904=ORIENTED_EDGE ( 'NONE', *, *, #14456, .T. ) ;
#6905=CARTESIAN_POINT ( 'NONE',  ( 26.11404676487257603, -33.91085499298301897, -108.0249973236470993 ) ) ;
#6908=CARTESIAN_POINT ( 'NONE',  ( 1.832998868059858122, -73.01698022778447239, 125.4013017422228558 ) ) ;
#6909=EDGE_CURVE ( 'NONE', #4019, #20724, #13668, .T. ) ;
#6910=CARTESIAN_POINT ( 'NONE',  ( 109.1624594426973118, 0.009754804742280794722, 0.01263706729759561664 ) ) ;
#6912=B_SPLINE_CURVE_WITH_KNOTS ( 'NONE', 3,
 ( #25995, #1663, #3543, #3971, #10465, #1385 ),
 .UNSPECIFIED., .F., .F.,
 ( 4, 2, 4 ),
 ( 2.168404344971008868E-19, 0.0006311571484586053554, 0.001262314296917210494 ),
 .UNSPECIFIED. ) ;
#6913=CARTESIAN_POINT ( 'NONE',  ( 109.1586059443104944, -0.003930911098393256690, -0.005881369279875392833 ) ) ;
#6915=CARTESIAN_POINT ( 'NONE',  ( 55.49584447822657296, 0.2676470673966822589, -72.55110015779771970 ) ) ;
#6917=EDGE_LOOP ( 'NONE', ( #18003, #18477, #22789, #19958 ) ) ;
#6918=VERTEX_POINT ( 'NONE', #6502 ) ;
#6920=CARTESIAN_POINT ( 'NONE',  ( 109.1592201516379674, -0.002134489919768192863, 0.007566779963325561721 ) ) ;
#6922=CARTESIAN_POINT ( 'NONE',  ( 25.81918753295381208, 57.31966094783204113, 97.41320410180104261 ) ) ;
#6923=VECTOR ( 'NONE', #22149, 1000.000000000000114 ) ;
#6928=EDGE_CURVE ( 'NONE', #21439, #20282, #17837, .T. ) ;
#6930=ORIENTED_EDGE ( 'NONE', *, *, #18094, .T. ) ;
#6931=DIRECTION ( 'NONE',  ( 0.000000000000000000, 0.000000000000000000, 1.000000000000000000 ) ) ;
#6936=CARTESIAN_POINT ( 'NONE',  ( 109.1589550718174877, 0.006445391216542572903, 0.003980125429499906282 ) ) ;
#6937=CARTESIAN_POINT ( 'NONE',  ( 16.05277956358206382, -75.66118899150433208, -121.7045645913025282 ) ) ;
#6938=CARTESIAN_POINT ( 'NONE',  ( 2.430230287190592531, -46.34481016236730255, -137.9371479820467243 ) ) ;
#6939=CARTESIAN_POINT ( 'NONE',  ( 25.64681081121879203, 110.5293738517611501, -23.06870491922213873 ) ) ;
#6941=( BOUNDED_SURFACE ( )  B_SPLINE_SURFACE ( 3, 1, ( 
 ( #5342, #3051 ),
 ( #18434, #11682 ),
 ( #7522, #13975 ),
 ( #11828, #7233 ) ),
 .UNSPECIFIED., .F., .F., .F. ) 
 B_SPLINE_SURFACE_WITH_KNOTS ( ( 4, 4 ),
 ( 2, 2 ),
 ( 0.000000000000000000, 1.000000000000000000 ),
 ( 0.000000000000000000, 1.000000000000000000 ),
 .UNSPECIFIED. ) 
 GEOMETRIC_REPRESENTATION_ITEM ( )  RATIONAL_B_SPLINE_SURFACE ( (
 ( 1.000000000000000000, 1.000000000000000000),
 ( 0.6386103224230302855, 0.9954351624131538845),
 ( 0.6386103224230302855, 0.9954351624131538845),
 ( 1.000000000000000000, 1.000000000000000000) ) ) 
 REPRESENTATION_ITEM ( '' )  SURFACE ( )  );
#6944=B_SPLINE_CURVE_WITH_KNOTS ( 'NONE', 3,
 ( #13427, #6981, #13011, #22227 ),
 .UNSPECIFIED., .F., .F.,
 ( 4, 4 ),
 ( 0.000000000000000000, 0.01077107196513893764 ),
 .UNSPECIFIED. ) ;
#6947=CARTESIAN_POINT ( 'NONE',  ( -40.00000000000000000, 0.000000000000000000, -80.00000000000000000 ) ) ;
#6954=ORIENTED_EDGE ( 'NONE', *, *, #24378, .T. ) ;
#6957=ORIENTED_EDGE ( 'NONE', *, *, #22788, .T. ) ;
#6958=VECTOR ( 'NONE', #2840, 1000.000000000000227 ) ;
#6960=CARTESIAN_POINT ( 'NONE',  ( 109.1587776205901861, 0.003592288931003351140, -0.006388631651935905084 ) ) ;
#6961=EDGE_LOOP ( 'NONE', ( #8878, #22559, #3854, #26484 ) ) ;
#6962=CARTESIAN_POINT ( 'NONE',  ( 26.11404676487257603, -98.61392875273325842, -55.62948129436350087 ) ) ;
#6963=CARTESIAN_POINT ( 'NONE',  ( 25.98107933586751273, -107.2544904356366402, -35.99661810150961827 ) ) ;
#6965=CARTESIAN_POINT ( 'NONE',  ( 25.64681081121880624, 66.03065707438935306, 91.59071981940594753 ) ) ;
#6966=VECTOR ( 'NONE', #15039, 999.9999999999998863 ) ;
#6967=CARTESIAN_POINT ( 'NONE',  ( 28.37644542392844471, 4.054996728115944471, -124.2737818798214136 ) ) ;
#6968=EDGE_CURVE ( 'NONE', #5199, #26221, #26941, .T. ) ;
#6969=CONICAL_SURFACE ( 'NONE', #10644, 117.6351876552689504, 0.9945805576725580410 ) ;
#6971=CARTESIAN_POINT ( 'NONE',  ( 109.1778270068192853, -0.001322180554001336399, -0.009220257877180839182 ) ) ;
#6972=FACE_OUTER_BOUND ( 'NONE', #22679, .T. ) ;
#6973=CONICAL_SURFACE ( 'NONE', #8814, 117.6351876552689504, 0.9945805576725580410 ) ;
#6974=EDGE_CURVE ( 'NONE', #12695, #22316, #7386, .T. ) ;
#6975=ORIENTED_EDGE ( 'NONE', *, *, #20765, .F. ) ;
#6978=CARTESIAN_POINT ( 'NONE',  ( 32.73300124599732186, 0.000000000000000000, 0.000000000000000000 ) ) ;
#6979=CARTESIAN_POINT ( 'NONE',  ( 30.59141879584286627, -79.74795589902086590, 84.53180090073648500 ) ) ;
#6980=CARTESIAN_POINT ( 'NONE',  ( 109.1586900883932856, -0.005236795036860577776, 0.004851151255037344269 ) ) ;
#6981=CARTESIAN_POINT ( 'NONE',  ( 8.186469829614468452, 148.8557359502364932, -12.15801983495463467 ) ) ;
#6982=ORIENTED_EDGE ( 'NONE', *, *, #5325, .F. ) ;
#6985=CARTESIAN_POINT ( 'NONE',  ( 25.65782528836482612, 103.3897864210302373, -45.39960327191509037 ) ) ;
#6986=DIRECTION ( 'NONE',  ( 0.000000000000000000, 0.000000000000000000, 1.000000000000000000 ) ) ;
#6987=ORIENTED_EDGE ( 'NONE', *, *, #2518, .T. ) ;
#6989=B_SPLINE_CURVE_WITH_KNOTS ( 'NONE', 3,
 ( #10290, #27533, #27386, #27677 ),
 .UNSPECIFIED., .F., .F.,
 ( 4, 4 ),
 ( 2.619375006920453660E-16, 0.008383748772659739903 ),
 .UNSPECIFIED. ) ;
#6991=VERTEX_POINT ( 'NONE', #2442 ) ;
#6992=CARTESIAN_POINT ( 'NONE',  ( 1.833603222531958954, -96.76619886578252761, -108.1346772638456457 ) ) ;
#6994=( BOUNDED_SURFACE ( )  B_SPLINE_SURFACE ( 3, 1, ( 
 ( #1174, #9822 ),
 ( #18590, #16430 ),
 ( #25214, #14248 ),
 ( #23070, #14406 ) ),
 .UNSPECIFIED., .F., .F., .F. ) 
 B_SPLINE_SURFACE_WITH_KNOTS ( ( 4, 4 ),
 ( 2, 2 ),
 ( 0.000000000000000000, 1.000000000000000000 ),
 ( 0.000000000000000000, 1.000000000000000000 ),
 .UNSPECIFIED. ) 
 GEOMETRIC_REPRESENTATION_ITEM ( )  RATIONAL_B_SPLINE_SURFACE ( (
 ( 1.000000000000000000, 1.000000000000000000),
 ( 0.9956975270656954757, 0.8568959468854893125),
 ( 0.9956975270656954757, 0.8568959468854893125),
 ( 1.000000000000000000, 1.000000000000000000) ) ) 
 REPRESENTATION_ITEM ( '' )  SURFACE ( )  );
#6995=CARTESIAN_POINT ( 'NONE',  ( 2.430230287190581429, -138.8342928068223046, 43.58368230469343985 ) ) ;
#6996=AXIS2_PLACEMENT_3D ( 'NONE', #22031, #15254, #6931 ) ;
#7002=ADVANCED_FACE ( 'NONE', ( #22326 ), #22459, .F. ) ;
#7003=CARTESIAN_POINT ( 'NONE',  ( 55.49584447822657296, -62.96491934286019188, 36.04376091928521220 ) ) ;
#7004=CARTESIAN_POINT ( 'NONE',  ( 2.430230287190592531, -28.83279105684524168, 142.6294793592097108 ) ) ;
#7008=CARTESIAN_POINT ( 'NONE',  ( 2.063896406836605024, 144.6078654718903636, -13.84738934186042059 ) ) ;
#7009=CARTESIAN_POINT ( 'NONE',  ( 2.433796855181219243, -144.5536872373193376, 16.65276281464516828 ) ) ;
#7010=EDGE_CURVE ( 'NONE', #18831, #5021, #18381, .T. ) ;
#7013=VECTOR ( 'NONE', #26766, 1000.000000000000114 ) ;
#7015=VECTOR ( 'NONE', #4429, 1000.000000000000000 ) ;
#7017=CARTESIAN_POINT ( 'NONE',  ( 26.11404676487257603, 112.4785329405482059, 12.95861723607491456 ) ) ;
#7020=ORIENTED_EDGE ( 'NONE', *, *, #13131, .F. ) ;
#7022=ADVANCED_FACE ( 'NONE', ( #3172 ), #7587, .F. ) ;
#7024=VERTEX_POINT ( 'NONE', #7656 ) ;
#7025=CARTESIAN_POINT ( 'NONE',  ( 2.433796855181219243, 133.5135467655526043, -57.85512797797757401 ) ) ;
#7026=B_SPLINE_CURVE_WITH_KNOTS ( 'NONE', 3,
 ( #28415, #19785, #6567, #8716, #26413, #28142 ),
 .UNSPECIFIED., .F., .F.,
 ( 4, 2, 4 ),
 ( 6.952433221959954168E-18, 0.0006311571484586013438, 0.001262314296917195749 ),
 .UNSPECIFIED. ) ;
#7027=ORIENTED_EDGE ( 'NONE', *, *, #5570, .F. ) ;
#7029=AXIS2_PLACEMENT_3D ( 'NONE', #7622, #5438, #3285 ) ;
#7030=EDGE_CURVE ( 'NONE', #27786, #1490, #4979, .T. ) ;
#7031=LINE ( 'NONE', #26576, #21643 ) ;
#7033=AXIS2_PLACEMENT_3D ( 'NONE', #22265, #7294, #16058 ) ;
#7034=CARTESIAN_POINT ( 'NONE',  ( 25.64708010899964208, 107.3680906278376881, -34.94352788466177628 ) ) ;
#7035=CARTESIAN_POINT ( 'NONE',  ( 25.98552792386799837, 107.9280603639527101, 33.93357582585531418 ) ) ;
#7043=ORIENTED_EDGE ( 'NONE', *, *, #428, .F. ) ;
#7044=B_SPLINE_CURVE_WITH_KNOTS ( 'NONE', 3,
 ( #24051, #2130, #11212, #17813 ),
 .UNSPECIFIED., .F., .F.,
 ( 4, 4 ),
 ( 7.152448122690996019E-18, 0.008383560773332731156 ),
 .UNSPECIFIED. ) ;
#7045=ORIENTED_EDGE ( 'NONE', *, *, #13372, .F. ) ;
#7046=CARTESIAN_POINT ( 'NONE',  ( 1.833485406944043827, 73.01664920992966756, 125.4007332306548221 ) ) ;
#7048=CARTESIAN_POINT ( 'NONE',  ( 55.49584447822657296, -36.50733923851154117, -62.69727227546439963 ) ) ;
#7053=AXIS2_PLACEMENT_3D ( 'NONE', #12977, #21768, #19185 ) ;
#7054=VERTEX_POINT ( 'NONE', #5472 ) ;
#7055=CARTESIAN_POINT ( 'NONE',  ( 5.340103579038239623, -144.6887562507422729, -28.39990973304617583 ) ) ;
#7056=CARTESIAN_POINT ( 'NONE',  ( 109.1587776205901577, -0.007297420966928602065, 0.0006832286435102221311 ) ) ;
#7057=CARTESIAN_POINT ( 'NONE',  ( 25.64700659047694487, -0.2275682798794833872, 112.9110011064639565 ) ) ;
#7059=CARTESIAN_POINT ( 'NONE',  ( 6.224689322667630975, 76.23997225729445404, -126.9212313063836461 ) ) ;
#7060=ORIENTED_EDGE ( 'NONE', *, *, #27, .T. ) ;
#7061=CARTESIAN_POINT ( 'NONE',  ( 109.1586900883932856, -0.004113747440992365084, 0.005833932871491302741 ) ) ;
#7062=VECTOR ( 'NONE', #9796, 1000.000000000000227 ) ;
#7063=CIRCLE ( 'NONE', #1975, 117.6351876552689504 ) ;
#7064=CARTESIAN_POINT ( 'NONE',  ( 32.73300124599732186, 0.000000000000000000, 0.000000000000000000 ) ) ;
#7065=CARTESIAN_POINT ( 'NONE',  ( 1.833691583653551227, -117.1866391460179813, -85.58103979054610022 ) ) ;
#7067=ORIENTED_EDGE ( 'NONE', *, *, #28102, .T. ) ;
#7071=EDGE_CURVE ( 'NONE', #25105, #8696, #25025, .T. ) ;
#7072=CARTESIAN_POINT ( 'NONE',  ( 25.98552792386800903, 57.50018541500425329, 97.43552975939633143 ) ) ;
#7074=CARTESIAN_POINT ( 'NONE',  ( 2.433796855181205476, 126.7346379669265843, -71.49415740224942795 ) ) ;
#7076=CARTESIAN_POINT ( 'NONE',  ( 28.43349137099832902, 105.5221910860626764, -65.60227321965477643 ) ) ;
#7077=CARTESIAN_POINT ( 'NONE',  ( 25.81918753295377655, 45.11728622333284733, -103.6306245682010712 ) ) ;
#7078=( BOUNDED_SURFACE ( )  B_SPLINE_SURFACE ( 3, 1, ( 
 ( #8859, #25486 ),
 ( #26403, #18989 ),
 ( #7931, #68 ),
 ( #8565, #11012 ) ),
 .UNSPECIFIED., .F., .F., .F. ) 
 B_SPLINE_SURFACE_WITH_KNOTS ( ( 4, 4 ),
 ( 2, 2 ),
 ( 0.000000000000000000, 1.000000000000000000 ),
 ( 0.000000000000000000, 1.000000000000000000 ),
 .UNSPECIFIED. ) 
 GEOMETRIC_REPRESENTATION_ITEM ( )  RATIONAL_B_SPLINE_SURFACE ( (
 ( 1.000000000000000000, 1.000000000000000000),
 ( 0.6386103224230316178, 0.9954351624131538845),
 ( 0.6386103224230316178, 0.9954351624131538845),
 ( 1.000000000000000000, 1.000000000000000000) ) ) 
 REPRESENTATION_ITEM ( '' )  SURFACE ( )  );
#7083=CARTESIAN_POINT ( 'NONE',  ( 1.833206308920082073, 30.89799439741820564, -141.7818018507499289 ) ) ;
#7084=CARTESIAN_POINT ( 'NONE',  ( 25.64681081121879203, -112.3352186517029878, -11.38886654529789233 ) ) ;
#7087=CARTESIAN_POINT ( 'NONE',  ( 30.59138290137918403, 105.0379801549016463, -49.72302320601711756 ) ) ;
#7090=B_SPLINE_CURVE_WITH_KNOTS ( 'NONE', 3,
 ( #16180, #11726, #3230, #7142, #18631, #7274, #15902 ),
 .UNSPECIFIED., .F., .F.,
 ( 4, 3, 4 ),
 ( 0.000000000000000000, 0.02398743853561347006, 0.04000277880656215312 ),
 .UNSPECIFIED. ) ;
#7091=CARTESIAN_POINT ( 'NONE',  ( 5.340103556456526235, 17.70136535450102500, -146.3832391989194548 ) ) ;
#7092=CARTESIAN_POINT ( 'NONE',  ( 1.832998868059858122, 107.4798986104860177, 97.49378069860833307 ) ) ;
#7093=EDGE_CURVE ( 'NONE', #27430, #16711, #19064, .T. ) ;
#7094=CARTESIAN_POINT ( 'NONE',  ( 2.433796855181233454, 125.2830755159764777, -74.00833731765430912 ) ) ;
#7097=ORIENTED_EDGE ( 'NONE', *, *, #348, .F. ) ;
#7098=CARTESIAN_POINT ( 'NONE',  ( 2.263178113027020544, -126.6115605262343422, 71.48082833565020167 ) ) ;
#7099=CARTESIAN_POINT ( 'NONE',  ( 5.340103556456450740, 71.72120378849609779, 128.8311297043948116 ) ) ;
#7102=ORIENTED_EDGE ( 'NONE', *, *, #18486, .T. ) ;
#7103=EDGE_CURVE ( 'NONE', #4802, #22173, #18063, .T. ) ;
#7106=CARTESIAN_POINT ( 'NONE',  ( 109.1592201516379674, -0.007856029051018016685, -0.0003082430541935813001 ) ) ;
#7107=CARTESIAN_POINT ( 'NONE',  ( 8.186469777910737378, 34.43598809570138997, 145.3272523831804790 ) ) ;
#7109=CARTESIAN_POINT ( 'NONE',  ( 9.884929003653626367, -109.0134320167740043, 103.8128997986854074 ) ) ;
#7110=EDGE_CURVE ( 'NONE', #19505, #21234, #9483, .T. ) ;
#7114=CARTESIAN_POINT ( 'NONE',  ( 10.93730112725932635, 0.000000000000000000, 0.000000000000000000 ) ) ;
#7115=CARTESIAN_POINT ( 'NONE',  ( 26.28373643307409324, 4.159810388346418364, 127.4927519498666726 ) ) ;
#7116=CARTESIAN_POINT ( 'NONE',  ( 25.73574536432413495, 34.14219540448133472, 107.6875787074508537 ) ) ;
#7117=DIRECTION ( 'NONE',  ( -0.5914120900931443270, 0.5335794202785305584, -0.6045864222316656988 ) ) ;
#7118=DIRECTION ( 'NONE',  ( 0.8320502949607718746, 6.793118186493350437E-17, 0.5547001952908368061 ) ) ;
#7123=CARTESIAN_POINT ( 'NONE',  ( 6.224689322667647851, -129.4863684118282379, -71.79702446228439783 ) ) ;
#7124=LINE ( 'NONE', #5079, #13481 ) ;
#7125=CARTESIAN_POINT ( 'NONE',  ( 109.1592201516379674, 0.006174480289199407029, -0.004867031887019566266 ) ) ;
#7129=ORIENTED_EDGE ( 'NONE', *, *, #16291, .T. ) ;
#7131=CARTESIAN_POINT ( 'NONE',  ( 1.833838848569441238, -29.99593366454849175, 141.9757689770220281 ) ) ;
#7132=ORIENTED_EDGE ( 'NONE', *, *, #18065, .T. ) ;
#7133=CARTESIAN_POINT ( 'NONE',  ( 16.75465622695631751, 125.4242432475205220, -67.05928661304241700 ) ) ;
#7134=ORIENTED_EDGE ( 'NONE', *, *, #21843, .F. ) ;
#7135=CARTESIAN_POINT ( 'NONE',  ( 28.37603512858453669, 91.75440368550030712, -68.88140609180105400 ) ) ;
#7136=ORIENTED_EDGE ( 'NONE', *, *, #10926, .T. ) ;
#7138=EDGE_CURVE ( 'NONE', #27364, #24182, #6729, .T. ) ;
#7140=CARTESIAN_POINT ( 'NONE',  ( 109.1592201516379674, 0.003476928926125392744, -0.007051465909551727154 ) ) ;
#7141=EDGE_CURVE ( 'NONE', #13619, #28480, #17363, .T. ) ;
#7142=CARTESIAN_POINT ( 'NONE',  ( 19.66333377628707169, -136.4524620437342719, -18.85786579350090619 ) ) ;
#7143=B_SPLINE_CURVE_WITH_KNOTS ( 'NONE', 3,
 ( #23871, #3982, #24007, #23440, #21404, #12478, #17221, #21539 ),
 .UNSPECIFIED., .F., .F.,
 ( 4, 2, 2, 4 ),
 ( 0.000000000000000000, 0.0002429588503611217285, 0.0004859177007222434570, 0.0009718354014444869141 ),
 .UNSPECIFIED. ) ;
#7144=DIRECTION ( 'NONE',  ( -1.000000000000000000, -0.000000000000000000, -0.000000000000000000 ) ) ;
#7152=CARTESIAN_POINT ( 'NONE',  ( 25.64681081121879203, 23.88203588908081443, 110.3564950173082480 ) ) ;
#7153=CARTESIAN_POINT ( 'NONE',  ( 26.11404676487257603, -84.89295829319543429, 74.91683232330944975 ) ) ;
#7158=CARTESIAN_POINT ( 'NONE',  ( 26.28373643307435614, 78.30371666786363960, 100.6987277884683323 ) ) ;
#7160=CARTESIAN_POINT ( 'NONE',  ( 1.831572820252008738, -117.9752562883672482, 84.49389457294098804 ) ) ;
#7161=ORIENTED_EDGE ( 'NONE', *, *, #27918, .T. ) ;
#7162=B_SPLINE_CURVE_WITH_KNOTS ( 'NONE', 3,
 ( #11883, #14034, #2973, #4972 ),
 .UNSPECIFIED., .F., .F.,
 ( 4, 4 ),
 ( 2.212843619328882373E-16, 0.008383748772659684392 ),
 .UNSPECIFIED. ) ;
#7163=CARTESIAN_POINT ( 'NONE',  ( 10.93730112725986281, -149.7554878793150408, 20.69552240458288850 ) ) ;
#7166=ORIENTED_EDGE ( 'NONE', *, *, #20627, .F. ) ;
#7167=CARTESIAN_POINT ( 'NONE',  ( 109.1721716018069515, -0.005466227998627365414, 0.01616973485710003489 ) ) ;
#7168=ORIENTED_EDGE ( 'NONE', *, *, #20345, .F. ) ;
#7169=EDGE_CURVE ( 'NONE', #19892, #28095, #5775, .T. ) ;
#7170=CARTESIAN_POINT ( 'NONE',  ( 2.433796855181219243, -71.49415740225165905, 126.7346379669253622 ) ) ;
#7171=ORIENTED_EDGE ( 'NONE', *, *, #8590, .T. ) ;
#7175=CARTESIAN_POINT ( 'NONE',  ( 32.73300124599740002, -89.94078864464006529, -75.82012867748569818 ) ) ;
#7176=CARTESIAN_POINT ( 'NONE',  ( 25.64692872815574631, -35.19724814977989524, 107.2850779876533238 ) ) ;
#7177=DIRECTION ( 'NONE',  ( -0.5914120900931443270, -0.6476200150380216902, 0.4804373588864745970 ) ) ;
#7180=ORIENTED_EDGE ( 'NONE', *, *, #23044, .F. ) ;
#7181=CARTESIAN_POINT ( 'NONE',  ( 8.186469829614360094, -134.9918587494109659, -63.89871393833158919 ) ) ;
#7182=CARTESIAN_POINT ( 'NONE',  ( 25.64681081121879203, 34.49579773461926635, -107.5125461021399218 ) ) ;
#7183=CARTESIAN_POINT ( 'NONE',  ( 1.832998868059890096, 142.0492247521726199, -29.64765804469936583 ) ) ;
#7184=EDGE_LOOP ( 'NONE', ( #1388, #3594, #16106, #7027 ) ) ;
#7185=EDGE_LOOP ( 'NONE', ( #26847, #5542, #4546, #13344 ) ) ;
#7186=ORIENTED_EDGE ( 'NONE', *, *, #3299, .T. ) ;
#7188=CARTESIAN_POINT ( 'NONE',  ( 109.1586900883932856, 0.006231977675084991036, 0.003481399864218453783 ) ) ;
#7192=CARTESIAN_POINT ( 'NONE',  ( 25.64699802086725811, -83.75009658924048495, 75.72889180797095321 ) ) ;
#7193=CARTESIAN_POINT ( 'NONE',  ( 55.79472521941428198, 59.28412330436302113, 42.17269936297659427 ) ) ;
#7194=ORIENTED_EDGE ( 'NONE', *, *, #2731, .F. ) ;
#7197=CARTESIAN_POINT ( 'NONE',  ( 109.1589550718174877, -0.006826119083824097253, -0.003284595046925634348 ) ) ;
#7199=CARTESIAN_POINT ( 'NONE',  ( 109.1586059443104944, -0.005555961672773799230, 0.004378796245589994425 ) ) ;
#7200=LINE ( 'NONE', #2569, #13707 ) ;
#7202=DIRECTION ( 'NONE',  ( -0.5914120900931443270, -0.7870418015781058818, 0.1754905759872819881 ) ) ;
#7205=VERTEX_POINT ( 'NONE', #23340 ) ;
#7207=CARTESIAN_POINT ( 'NONE',  ( 16.05277956358233027, 62.52511797226105728, 128.9466020665973076 ) ) ;
#7209=EDGE_CURVE ( 'NONE', #20165, #21162, #1291, .T. ) ;
#7210=ORIENTED_EDGE ( 'NONE', *, *, #9532, .F. ) ;
#7211=VERTEX_POINT ( 'NONE', #12508 ) ;
#7214=CARTESIAN_POINT ( 'NONE',  ( 2.063896406836605024, 96.20114399516394599, 108.8509294491468182 ) ) ;
#7216=CARTESIAN_POINT ( 'NONE',  ( 1.833838850855474600, 125.7132320915358719, -72.47782099564513203 ) ) ;
#7218=CARTESIAN_POINT ( 'NONE',  ( 2.433796855181205476, -138.8296532063090751, 43.58222566461595449 ) ) ;
#7219=CARTESIAN_POINT ( 'NONE',  ( 1.833750490713697223, 45.09517546033827529, -137.9248034078892999 ) ) ;
#7221=ORIENTED_EDGE ( 'NONE', *, *, #9105, .T. ) ;
#7224=CARTESIAN_POINT ( 'NONE',  ( 16.05277956358199631, 139.1285124304124565, -34.34928806929293188 ) ) ;
#7226=DIRECTION ( 'NONE',  ( -0.5946245182733608248, -0.7858154137795730909, 0.1700465163848173811 ) ) ;
#7227=CARTESIAN_POINT ( 'NONE',  ( 26.11404676487259024, 102.9690087468808031, -47.08215554553414961 ) ) ;
#7228=DIRECTION ( 'NONE',  ( 0.000000000000000000, 0.000000000000000000, 1.000000000000000000 ) ) ;
#7233=CARTESIAN_POINT ( 'NONE',  ( 13.36082413113061307, 151.2941478187907478, 22.28175172543611637 ) ) ;
#7235=EDGE_CURVE ( 'NONE', #5719, #5626, #10090, .T. ) ;
#7236=EDGE_CURVE ( 'NONE', #26082, #26014, #10151, .T. ) ;
#7238=CARTESIAN_POINT ( 'NONE',  ( 25.98552792386796995, 24.57669147553985312, 110.4352299692910435 ) ) ;
#7239=ORIENTED_EDGE ( 'NONE', *, *, #17893, .T. ) ;
#7241=ORIENTED_EDGE ( 'NONE', *, *, #6235, .F. ) ;
#7242=ORIENTED_EDGE ( 'NONE', *, *, #8529, .F. ) ;
#7245=CARTESIAN_POINT ( 'NONE',  ( 16.05277956358202829, 53.98852998724762386, -132.7473359121860028 ) ) ;
#7246=CARTESIAN_POINT ( 'NONE',  ( 10.93730112725990011, -150.7858122213662000, -10.89264110825150489 ) ) ;
#7247=B_SPLINE_CURVE_WITH_KNOTS ( 'NONE', 3,
 ( #25898, #6189, #14934, #23757, #13192, #13624, #21983, #9325, #247, #26864 ),
 .UNSPECIFIED., .F., .F.,
 ( 4, 3, 3, 4 ),
 ( 1.962615573354718958E-17, 0.0002669560319015750198, 0.0005492286108966149992, 0.0008315040496093386094 ),
 .UNSPECIFIED. ) ;
#7249=B_SPLINE_CURVE_WITH_KNOTS ( 'NONE', 3,
 ( #11423, #24694, #22816, #20487, #9553, #18473, #5083 ),
 .UNSPECIFIED., .F., .F.,
 ( 4, 3, 4 ),
 ( 4.037696989527316386E-16, 0.02816610861753247180, 0.04000277880656257640 ),
 .UNSPECIFIED. ) ;
#7250=CARTESIAN_POINT ( 'NONE',  ( 30.59138290137886429, -107.2355347544030479, -44.78723476287411387 ) ) ;
#7252=CARTESIAN_POINT ( 'NONE',  ( 26.11404676487257603, 113.2169081140373947, 1.130420376097532653 ) ) ;
#7253=CARTESIAN_POINT ( 'NONE',  ( 10.93730112725971715, 4.928439153520177030, 151.0983828010091372 ) ) ;
#7256=DIRECTION ( 'NONE',  ( 0.5914120900931444380, -0.7398809652418049110, 0.3206367055789364762 ) ) ;
#7259=CARTESIAN_POINT ( 'NONE',  ( 10.93730112725936898, 142.1801301103782578, 51.37919228020297879 ) ) ;
#7260=CARTESIAN_POINT ( 'NONE',  ( 26.11404676487257603, 33.91085499298377925, 108.0249973236468577 ) ) ;
#7261=CARTESIAN_POINT ( 'NONE',  ( 32.73300124599732186, 0.000000000000000000, 0.000000000000000000 ) ) ;
#7263=CARTESIAN_POINT ( 'NONE',  ( 55.49584447822657296, -72.18163437663946524, 7.317474139115394571 ) ) ;
#7264=ADVANCED_FACE ( 'NONE', ( #6752 ), #20429, .F. ) ;
#7265=VERTEX_POINT ( 'NONE', #24038 ) ;
#7267=CARTESIAN_POINT ( 'NONE',  ( 1.833838850093465034, -30.17001281793454126, 141.9387673160884447 ) ) ;
#7268=VERTEX_POINT ( 'NONE', #13494 ) ;
#7269=B_SPLINE_CURVE_WITH_KNOTS ( 'NONE', 3,
 ( #5281, #3272, #16506, #22866 ),
 .UNSPECIFIED., .F., .F.,
 ( 4, 4 ),
 ( 5.928593550334433897E-17, 0.008383748772659517859 ),
 .UNSPECIFIED. ) ;
#7271=ORIENTED_EDGE ( 'NONE', *, *, #27628, .T. ) ;
#7272=EDGE_LOOP ( 'NONE', ( #9874, #16611, #2153, #21456 ) ) ;
#7273=VERTEX_POINT ( 'NONE', #259 ) ;
#7274=CARTESIAN_POINT ( 'NONE',  ( 13.84597867724977505, -145.3211459389823403, -20.08297016719535222 ) ) ;
#7275=CARTESIAN_POINT ( 'NONE',  ( 10.93730112726003156, 125.1380233598492140, -84.82621002473311478 ) ) ;
#7276=CARTESIAN_POINT ( 'NONE',  ( 109.1586900883932856, -0.004277182003227263107, -0.005715190711481709686 ) ) ;
#7278=CARTESIAN_POINT ( 'NONE',  ( 26.11404676487257603, -76.59696442953135431, -83.38016054979861735 ) ) ;
#7281=VERTEX_POINT ( 'NONE', #2404 ) ;
#7284=EDGE_CURVE ( 'NONE', #25711, #5567, #26312, .T. ) ;
#7285=CARTESIAN_POINT ( 'NONE',  ( 1.833603222531955401, 84.93295186324861845, 117.6571262511681653 ) ) ;
#7287=CARTESIAN_POINT ( 'NONE',  ( 2.433796855181233454, 1.451562450949631211, 145.5024947199069913 ) ) ;
#7288=CARTESIAN_POINT ( 'NONE',  ( 2.108393763691193801, 138.5721856399489695, -43.67806918958995510 ) ) ;
#7292=EDGE_CURVE ( 'NONE', #6704, #13141, #1577, .T. ) ;
#7293=CARTESIAN_POINT ( 'NONE',  ( 28.43349137099832546, -115.0977416143053205, -46.80919715693011796 ) ) ;
#7294=DIRECTION ( 'NONE',  ( -1.000000000000000000, -0.000000000000000000, -0.000000000000000000 ) ) ;
#7296=FACE_OUTER_BOUND ( 'NONE', #576, .T. ) ;
#7297=ORIENTED_EDGE ( 'NONE', *, *, #21591, .F. ) ;
#7298=CARTESIAN_POINT ( 'NONE',  ( 25.70243777736190438, -112.4037002646848435, 11.07690056740829476 ) ) ;
#7303=ORIENTED_EDGE ( 'NONE', *, *, #2099, .T. ) ;
#7304=FACE_OUTER_BOUND ( 'NONE', #13470, .T. ) ;
#7306=B_SPLINE_CURVE_WITH_KNOTS ( 'NONE', 3,
 ( #12747, #6016, #19646, #10468, #23997, #19788, #10753, #4396 ),
 .UNSPECIFIED., .F., .F.,
 ( 4, 2, 2, 4 ),
 ( 0.000000000000000000, 0.0002429592666046805820, 0.0004859185332093611640, 0.0009718370664186841640 ),
 .UNSPECIFIED. ) ;
#7313=CARTESIAN_POINT ( 'NONE',  ( 1.833838850093517658, 1.769966374633376447E-14, 145.1097630783160923 ) ) ;
#7315=CARTESIAN_POINT ( 'NONE',  ( 2.430230287190572103, 46.34481016237007367, -137.9371479820457580 ) ) ;
#7321=CARTESIAN_POINT ( 'NONE',  ( 26.11404676487257603, -90.92995828888153653, -67.46175819463459788 ) ) ;
#7323=ADVANCED_FACE ( 'NONE', ( #398 ), #14151, .T. ) ;
#7324=CARTESIAN_POINT ( 'NONE',  ( 109.1586900883932856, 0.0006456433529069069291, -0.007109207791180753924 ) ) ;
#7325=CARTESIAN_POINT ( 'NONE',  ( 32.73300124599738581, -115.8010721414081985, -20.69176323058746902 ) ) ;
#7327=CARTESIAN_POINT ( 'NONE',  ( 25.64708010899967050, 45.87517365398623781, -103.1718249732469985 ) ) ;
#7328=ORIENTED_EDGE ( 'NONE', *, *, #746, .T. ) ;
#7329=CARTESIAN_POINT ( 'NONE',  ( 2.108985857320918367, 145.2876352664462729, -1.281428372376275382 ) ) ;
#7330=CARTESIAN_POINT ( 'NONE',  ( 109.1586900883932856, -0.003481399864227415798, -0.006231977675082095783 ) ) ;
#7331=CARTESIAN_POINT ( 'NONE',  ( -40.00000000000000000, 9.797174393178826052E-15, 80.00000000000000000 ) ) ;
#7333=EDGE_CURVE ( 'NONE', #13658, #17914, #14617, .T. ) ;
#7334=LINE ( 'NONE', #2163, #21193 ) ;
#7336=CARTESIAN_POINT ( 'NONE',  ( 5.340103556456532452, -28.39990973639961069, -144.6887562347052665 ) ) ;
#7337=CARTESIAN_POINT ( 'NONE',  ( 1.832998868059890096, 59.50898020732687144, -132.3466930259788228 ) ) ;
#7338=CARTESIAN_POINT ( 'NONE',  ( 25.81918753295376945, 110.3582118788980750, -24.41190151229150374 ) ) ;
#7339=CARTESIAN_POINT ( 'NONE',  ( 109.1721716018069515, 0.01467989464938422063, 0.008708654716135796198 ) ) ;
#7341=B_SPLINE_CURVE_WITH_KNOTS ( 'NONE', 3,
 ( #5447, #9782, #27318, #12078, #6831, #23833, #15436, #4089 ),
 .UNSPECIFIED., .F., .F.,
 ( 4, 2, 2, 4 ),
 ( 3.469446951953614189E-18, 0.0002429588503611278543, 0.0004859177007222522391, 0.0009718354014444975392 ),
 .UNSPECIFIED. ) ;
#7342=EDGE_LOOP ( 'NONE', ( #22878, #8894, #22257, #17790 ) ) ;
#7344=EDGE_LOOP ( 'NONE', ( #22078, #16345, #14629, #493 ) ) ;
#7345=B_SPLINE_CURVE_WITH_KNOTS ( 'NONE', 3,
 ( #997, #27324, #7639, #5455, #16395, #14214 ),
 .UNSPECIFIED., .F., .F.,
 ( 4, 2, 4 ),
 ( 1.041737195591640451E-17, 0.0006311571484585964649, 0.001262314296917183172 ),
 .UNSPECIFIED. ) ;
#7346=DIRECTION ( 'NONE',  ( 0.000000000000000000, 0.000000000000000000, 1.000000000000000000 ) ) ;
#7348=CARTESIAN_POINT ( 'NONE',  ( 32.73300124599732186, 0.000000000000000000, 0.000000000000000000 ) ) ;
#7351=CARTESIAN_POINT ( 'NONE',  ( 25.64681081121879203, -103.3177883989782657, 45.54494737132187510 ) ) ;
#7353=ORIENTED_EDGE ( 'NONE', *, *, #11400, .F. ) ;
#7354=ORIENTED_EDGE ( 'NONE', *, *, #417, .T. ) ;
#7357=EDGE_CURVE ( 'NONE', #18716, #11755, #22533, .T. ) ;
#7359=CARTESIAN_POINT ( 'NONE',  ( 26.11404676487259024, -24.64483677384768967, -110.5078194225163912 ) ) ;
#7360=CARTESIAN_POINT ( 'NONE',  ( 109.1586900883932856, -0.007088091345232584196, -0.0008465529156545617030 ) ) ;
#7362=VERTEX_POINT ( 'NONE', #9764 ) ;
#7363=CARTESIAN_POINT ( 'NONE',  ( 1.833838850855488145, 58.94016894581469757, 132.6005571022081142 ) ) ;
#7364=CARTESIAN_POINT ( 'NONE',  ( 2.108393763691193357, 16.46048390411989004, -144.3574619851890475 ) ) ;
#7365=EDGE_CURVE ( 'NONE', #9181, #11289, #2207, .T. ) ;
#7368=CARTESIAN_POINT ( 'NONE',  ( 25.98107933586719653, -76.50887835172591167, 83.34070894055847134 ) ) ;
#7369=CARTESIAN_POINT ( 'NONE',  ( 25.98552792386800903, -107.9280603639524543, -33.93357582585603183 ) ) ;
#7370=VERTEX_POINT ( 'NONE', #18097 ) ;
#7371=CARTESIAN_POINT ( 'NONE',  ( 25.98107933586701890, 22.45325949158483780, 110.8834224379717881 ) ) ;
#7372=VERTEX_POINT ( 'NONE', #973 ) ;
#7377=CIRCLE ( 'NONE', #9676, 117.6351876552689504 ) ;
#7378=CARTESIAN_POINT ( 'NONE',  ( 10.93730112725971360, 36.23586118136525158, 146.7718404940643211 ) ) ;
#7381=EDGE_CURVE ( 'NONE', #4903, #15441, #18018, .T. ) ;
#7383=VERTEX_POINT ( 'NONE', #22434 ) ;
#7384=CARTESIAN_POINT ( 'NONE',  ( 25.81918753295379076, -74.93271318951781268, 84.61657260023618221 ) ) ;
#7386=B_SPLINE_CURVE_WITH_KNOTS ( 'NONE', 3,
 ( #10955, #21893, #4331, #6643 ),
 .UNSPECIFIED., .F., .F.,
 ( 4, 4 ),
 ( 0.000000000000000000, 0.01077107196513857335 ),
 .UNSPECIFIED. ) ;
#7387=CARTESIAN_POINT ( 'NONE',  ( 2.108393763691183143, 108.8265195087761867, -96.26428731761880897 ) ) ;
#7389=ADVANCED_FACE ( 'NONE', ( #20250 ), #16040, .F. ) ;
#7391=LINE ( 'NONE', #16451, #22947 ) ;
#7392=CIRCLE ( 'NONE', #11060, 117.6351876552689504 ) ;
#7393=CARTESIAN_POINT ( 'NONE',  ( 109.1592201516379674, 0.004867031887010210903, -0.006174480289200333372 ) ) ;
#7395=CARTESIAN_POINT ( 'NONE',  ( 2.433796855181233454, 16.65276281464563723, 144.5536872373192807 ) ) ;
#7398=CARTESIAN_POINT ( 'NONE',  ( 25.64700659047693776, 84.06149911284546761, -75.38309044531806080 ) ) ;
#7399=ORIENTED_EDGE ( 'NONE', *, *, #20269, .F. ) ;
#7401=VECTOR ( 'NONE', #12641, 1000.000000000000000 ) ;
#7402=ORIENTED_EDGE ( 'NONE', *, *, #11335, .T. ) ;
#7403=CARTESIAN_POINT ( 'NONE',  ( 109.1587776205901577, -0.007280006032833112421, -0.0008489206734409592177 ) ) ;
#7404=CARTESIAN_POINT ( 'NONE',  ( 25.64660436782551756, 12.37913844083040793, 112.2303901742707950 ) ) ;
#7406=( BOUNDED_SURFACE ( )  B_SPLINE_SURFACE ( 3, 1, ( 
 ( #2597, #442 ),
 ( #26627, #4080 ),
 ( #15539, #13385 ),
 ( #20016, #22033 ) ),
 .UNSPECIFIED., .F., .F., .F. ) 
 B_SPLINE_SURFACE_WITH_KNOTS ( ( 4, 4 ),
 ( 2, 2 ),
 ( 0.000000000000000000, 1.000000000000000000 ),
 ( 0.000000000000000000, 1.000000000000000000 ),
 .UNSPECIFIED. ) 
 GEOMETRIC_REPRESENTATION_ITEM ( )  RATIONAL_B_SPLINE_SURFACE ( (
 ( 1.000000000000000000, 1.000000000000000000),
 ( 0.9956975270656954757, 0.8568959468854893125),
 ( 0.9956975270656954757, 0.8568959468854893125),
 ( 1.000000000000000000, 1.000000000000000000) ) ) 
 REPRESENTATION_ITEM ( '' )  SURFACE ( )  );
#7407=ORIENTED_EDGE ( 'NONE', *, *, #626, .T. ) ;
#7408=VERTEX_POINT ( 'NONE', #3136 ) ;
#7409=CARTESIAN_POINT ( 'NONE',  ( 10.93730112726003156, 115.5857507957718440, -97.44200844886164248 ) ) ;
#7410=EDGE_CURVE ( 'NONE', #7268, #12091, #10504, .T. ) ;
#7411=CARTESIAN_POINT ( 'NONE',  ( 55.79472521941426777, 15.83764557006368534, -71.00924468211141516 ) ) ;
#7414=CARTESIAN_POINT ( 'NONE',  ( 26.11404676487259024, -1.130420376096339385, -113.2169081140374232 ) ) ;
#7416=CARTESIAN_POINT ( 'NONE',  ( 1.833603222531969834, 144.3605362014090474, -14.72553080638845913 ) ) ;
#7417=CARTESIAN_POINT ( 'NONE',  ( 1.833485406944043827, 29.64752363041542083, 142.0485807715646729 ) ) ;
#7418=VECTOR ( 'NONE', #13034, 1000.000000000000000 ) ;
#7421=FACE_OUTER_BOUND ( 'NONE', #20355, .T. ) ;
#7423=CARTESIAN_POINT ( 'NONE',  ( 109.1586059443104944, -0.002447596125914214184, -0.006637156007970144468 ) ) ;
#7425=CARTESIAN_POINT ( 'NONE',  ( 1.834118845439484335, -96.96525081349928143, -107.9567937753803193 ) ) ;
#7426=ORIENTED_EDGE ( 'NONE', *, *, #9267, .F. ) ;
#7427=VERTEX_POINT ( 'NONE', #13774 ) ;
#7428=CARTESIAN_POINT ( 'NONE',  ( 10.93730112725990367, -133.3192575531795399, -71.28103789255078482 ) ) ;
#7429=CARTESIAN_POINT ( 'NONE',  ( 1.833809397773885630, 85.14934054436471911, 117.5007887865410936 ) ) ;
#7430=CARTESIAN_POINT ( 'NONE',  ( 26.11404676487257603, 76.59696442953305962, -83.38016054979703995 ) ) ;
#7432=CARTESIAN_POINT ( 'NONE',  ( 32.73300124599738581, 28.19767303745763698, -114.2056417606545153 ) ) ;
#7434=CARTESIAN_POINT ( 'NONE',  ( 25.64681081121879203, -112.9102952884414606, 0.4157506337723927414 ) ) ;
#7435=EDGE_LOOP ( 'NONE', ( #28099, #8912 ) ) ;
#7436=CARTESIAN_POINT ( 'NONE',  ( 109.1587776205901861, -0.004842060007769426189, 0.005502145856762287804 ) ) ;
#7437=VECTOR ( 'NONE', #11772, 1000.000000000000000 ) ;
#7438=CARTESIAN_POINT ( 'NONE',  ( 13.84597867724974840, -55.26821062125468842, -135.8932891738222963 ) ) ;
#7440=CARTESIAN_POINT ( 'NONE',  ( 21.16825799904903249, -97.63815233965115681, 93.85612807858974804 ) ) ;
#7441=VERTEX_POINT ( 'NONE', #2847 ) ;
#7442=B_SPLINE_CURVE_WITH_KNOTS ( 'NONE', 3,
 ( #1003, #3449, #23047, #18997, #9798, #27778 ),
 .UNSPECIFIED., .F., .F.,
 ( 4, 2, 4 ),
 ( 2.289900696569189619E-17, 0.0006311636237756888855, 0.001262327247551354786 ),
 .UNSPECIFIED. ) ;
#7445=EDGE_CURVE ( 'NONE', #3333, #16927, #6366, .T. ) ;
#7448=ORIENTED_EDGE ( 'NONE', *, *, #23450, .T. ) ;
#7450=EDGE_CURVE ( 'NONE', #26082, #10457, #1539, .T. ) ;
#7451=VERTEX_POINT ( 'NONE', #23586 ) ;
#7452=CARTESIAN_POINT ( 'NONE',  ( 55.49584447822657296, 14.82242356767935654, 71.02133150427260944 ) ) ;
#7456=CARTESIAN_POINT ( 'NONE',  ( 0.000000000000000000, 0.000000000000000000, -80.00000000000000000 ) ) ;
#7459=CARTESIAN_POINT ( 'NONE',  ( 1.833838848569414592, -125.5797553397075035, 72.70900949568731164 ) ) ;
#7460=ORIENTED_EDGE ( 'NONE', *, *, #17862, .F. ) ;
#7461=ADVANCED_FACE ( 'NONE', ( #8449 ), #16394, .F. ) ;
#7462=CARTESIAN_POINT ( 'NONE',  ( 6.224689322667630975, 48.18553814190214979, -139.9988794244327437 ) ) ;
#7464=CARTESIAN_POINT ( 'NONE',  ( 19.66333377628726353, -18.85786579350040526, 136.4524620437341298 ) ) ;
#7465=ORIENTED_EDGE ( 'NONE', *, *, #24384, .T. ) ;
#7466=AXIS2_PLACEMENT_3D ( 'NONE', #23896, #26037, #15359 ) ;
#7467=ORIENTED_EDGE ( 'NONE', *, *, #5666, .F. ) ;
#7470=DIRECTION ( 'NONE',  ( 0.000000000000000000, 0.000000000000000000, 1.000000000000000000 ) ) ;
#7471=CARTESIAN_POINT ( 'NONE',  ( 1.833603222531957400, 108.1346772638459441, -96.76619886578220076 ) ) ;
#7472=CARTESIAN_POINT ( 'NONE',  ( 32.73300124599737160, -108.9684813982492244, 44.31599526637918274 ) ) ;
#7473=CARTESIAN_POINT ( 'NONE',  ( 55.49584447822657296, 29.75369869230953768, 66.16986612640785381 ) ) ;
#7474=CARTESIAN_POINT ( 'NONE',  ( 109.1592201516379674, 0.003661068210037295243, 0.006957642258146931775 ) ) ;
#7476=DIRECTION ( 'NONE',  ( -1.000000000000000000, -0.000000000000000000, -0.000000000000000000 ) ) ;
#7477=ORIENTED_EDGE ( 'NONE', *, *, #15000, .T. ) ;
#7480=CARTESIAN_POINT ( 'NONE',  ( 26.11404676487257603, -67.46175819463425682, 90.92995828888176391 ) ) ;
#7481=DIRECTION ( 'NONE',  ( -0.000000000000000000, 0.000000000000000000, 1.000000000000000000 ) ) ;
#7482=DIRECTION ( 'NONE',  ( 0.000000000000000000, -1.000000000000000000, 0.000000000000000000 ) ) ;
#7483=CARTESIAN_POINT ( 'NONE',  ( -90.83090735639699176, 0.000000000000000000, -20.00000000000000000 ) ) ;
#7485=B_SPLINE_CURVE_WITH_KNOTS ( 'NONE', 3,
 ( #22289, #20542, #26724, #9339, #11625, #825, #15633, #7182 ),
 .UNSPECIFIED., .F., .F.,
 ( 4, 2, 2, 4 ),
 ( 6.938893903907228378E-18, 0.0002429592666046657284, 0.0004859185332093245179, 0.0009718370664186789598 ),
 .UNSPECIFIED. ) ;
#7486=CARTESIAN_POINT ( 'NONE',  ( 109.1586059443104944, -0.003294606663354695663, 0.006260042619943039129 ) ) ;
#7488=CARTESIAN_POINT ( 'NONE',  ( 109.1778270068192853, 0.004349865064712402606, 0.008236503545664826745 ) ) ;
#7494=ADVANCED_FACE ( 'NONE', ( #8175 ), #14760, .T. ) ;
#7498=DIRECTION ( 'NONE',  ( -1.000000000000000000, 0.000000000000000000, 0.000000000000000000 ) ) ;
#7500=B_SPLINE_CURVE_WITH_KNOTS ( 'NONE', 3,
 ( #14765, #10039, #25447, #14179 ),
 .UNSPECIFIED., .F., .F.,
 ( 4, 4 ),
 ( 2.302416593912983762E-16, 0.008383748772659694801 ),
 .UNSPECIFIED. ) ;
#7505=CARTESIAN_POINT ( 'NONE',  ( 25.64681081121879203, 83.63051021306002042, -75.86069728268907397 ) ) ;
#7506=CARTESIAN_POINT ( 'NONE',  ( 26.11404676487259024, -33.91085499298451822, 108.0249973236466445 ) ) ;
#7507=CARTESIAN_POINT ( 'NONE',  ( 1.831572820252009626, -132.9644823688591373, -58.11906524360610860 ) ) ;
#7511=CARTESIAN_POINT ( 'NONE',  ( 8.186469777910748036, 3.468244369821841477, 149.3111477498017621 ) ) ;
#7512=CARTESIAN_POINT ( 'NONE',  ( 16.05277956358205316, -19.61822947415880591, -141.9568301782831554 ) ) ;
#7513=CARTESIAN_POINT ( 'NONE',  ( 55.49584447822657296, -70.91003759562325115, 15.34602024131264386 ) ) ;
#7514=CARTESIAN_POINT ( 'NONE',  ( 1.833206310202332823, 107.3376456496894065, -97.64934828276996370 ) ) ;
#7516=CARTESIAN_POINT ( 'NONE',  ( 1.832998868059858122, 142.0492247521722788, 29.64765804470121324 ) ) ;
#7518=CARTESIAN_POINT ( 'NONE',  ( 26.11404676487257603, 84.89295829319590325, -74.91683232330889552 ) ) ;
#7519=FACE_OUTER_BOUND ( 'NONE', #6774, .T. ) ;
#7521=CARTESIAN_POINT ( 'NONE',  ( 109.1587776205901577, 0.0006832286435102477183, 0.007297420966928598596 ) ) ;
#7522=CARTESIAN_POINT ( 'NONE',  ( 109.1721716018069657, 0.0002019688922675414973, 0.01706748904932341160 ) ) ;
#7523=CARTESIAN_POINT ( 'NONE',  ( 25.64660436782554953, -0.5800540083543996861, -112.9095526718340636 ) ) ;
#7524=VERTEX_POINT ( 'NONE', #10471 ) ;
#7525=CARTESIAN_POINT ( 'NONE',  ( 25.64703792032469565, -75.44170528134947062, 84.00887408969030901 ) ) ;
#7526=ORIENTED_EDGE ( 'NONE', *, *, #6283, .F. ) ;
#7529=ORIENTED_EDGE ( 'NONE', *, *, #2628, .F. ) ;
#7531=AXIS2_PLACEMENT_3D ( 'NONE', #12296, #18492, #21068 ) ;
#7532=CARTESIAN_POINT ( 'NONE',  ( 2.063896406836605024, -108.8509294491471593, 96.20114399516360493 ) ) ;
#7534=VECTOR ( 'NONE', #25877, 1000.000000000000114 ) ;
#7535=EDGE_CURVE ( 'NONE', #20165, #10583, #16142, .T. ) ;
#7536=CARTESIAN_POINT ( 'NONE',  ( 13.36082413113063083, -109.3026516754239736, 106.9547846563632021 ) ) ;
#7538=B_SPLINE_CURVE_WITH_KNOTS ( 'NONE', 3,
 ( #16855, #25640, #5919, #8359 ),
 .UNSPECIFIED., .F., .F.,
 ( 4, 4 ),
 ( 8.355534721610419059E-17, 0.008383748772659540410 ),
 .UNSPECIFIED. ) ;
#7539=CARTESIAN_POINT ( 'NONE',  ( 2.433796855181233454, -126.7346379669250780, -71.49415740225209959 ) ) ;
#7541=DIRECTION ( 'NONE',  ( -1.000000000000000000, -0.000000000000000000, -0.000000000000000000 ) ) ;
#7542=CARTESIAN_POINT ( 'NONE',  ( 25.64681081121879203, -97.99105938547964456, 56.09509703373309719 ) ) ;
#7543=CARTESIAN_POINT ( 'NONE',  ( 1.831572820252009626, 137.7011124121623311, -45.77972211429671745 ) ) ;
#7544=CARTESIAN_POINT ( 'NONE',  ( 2.108393763691203571, -31.45977531353388201, 141.8460676169243015 ) ) ;
#7545=CARTESIAN_POINT ( 'NONE',  ( 10.93730112726006176, 146.7718404940648611, -36.23586118136403655 ) ) ;
#7550=CARTESIAN_POINT ( 'NONE',  ( 25.73574536432415272, 112.2643803187785494, 12.61003673871928399 ) ) ;
#7551=FACE_OUTER_BOUND ( 'NONE', #7344, .T. ) ;
#7552=CARTESIAN_POINT ( 'NONE',  ( 16.05277956358202118, -139.1285124304122007, 34.34928806929384137 ) ) ;
#7554=ORIENTED_EDGE ( 'NONE', *, *, #20710, .T. ) ;
#7555=CARTESIAN_POINT ( 'NONE',  ( 2.433796855181233454, -96.28145139437756939, 109.1007109081222666 ) ) ;
#7557=CARTESIAN_POINT ( 'NONE',  ( 1.833485406944057594, -15.69895494453287021, -144.2578170162064737 ) ) ;
#7558=CARTESIAN_POINT ( 'NONE',  ( 55.49584447822657296, -69.08290406177594889, 22.16497542184382397 ) ) ;
#7559=B_SPLINE_CURVE_WITH_KNOTS ( 'NONE', 3,
 ( #12648, #19140, #25764, #6056 ),
 .UNSPECIFIED., .F., .F.,
 ( 4, 4 ),
 ( 0.000000000000000000, 0.01077107196513847794 ),
 .UNSPECIFIED. ) ;
#7560=VERTEX_POINT ( 'NONE', #3976 ) ;
#7561=EDGE_CURVE ( 'NONE', #26729, #10772, #2521, .T. ) ;
#7563=ORIENTED_EDGE ( 'NONE', *, *, #5165, .T. ) ;
#7565=ORIENTED_EDGE ( 'NONE', *, *, #7641, .F. ) ;
#7566=CARTESIAN_POINT ( 'NONE',  ( 2.430230287190592531, 86.70145658344658557, 116.8646894862415166 ) ) ;
#7567=CARTESIAN_POINT ( 'NONE',  ( 26.11404676487257603, 92.25884714080498838, -65.63269960453146723 ) ) ;
#7569=CARTESIAN_POINT ( 'NONE',  ( 25.64681081121879203, -66.70335573067929147, 91.10197563707923507 ) ) ;
#7571=SHAPE_REPRESENTATION ( 'bevel straight', ( #27263 ), #16248 ) ;
#7572=CARTESIAN_POINT ( 'NONE',  ( 2.263178607246672858, 71.48082837426177605, -126.6115608827429782 ) ) ;
#7573=CARTESIAN_POINT ( 'NONE',  ( 1.832998868059858122, 14.63705790014008379, 144.3700883710217795 ) ) ;
#7574=CARTESIAN_POINT ( 'NONE',  ( 109.1587776205901861, 0.004375189885423106176, 0.005880209827414138897 ) ) ;
#7576=CARTESIAN_POINT ( 'NONE',  ( 2.433796855181205476, 60.50726454508082952, -132.3327394885224919 ) ) ;
#7577=FACE_OUTER_BOUND ( 'NONE', #14116, .T. ) ;
#7580=ORIENTED_EDGE ( 'NONE', *, *, #1051, .T. ) ;
#7582=DIRECTION ( 'NONE',  ( -1.000000000000000000, -0.000000000000000000, -0.000000000000000000 ) ) ;
#7583=CARTESIAN_POINT ( 'NONE',  ( 25.70243777736189728, 57.10783651465103361, -97.44734253939026303 ) ) ;
#7584=CARTESIAN_POINT ( 'NONE',  ( 1.833809397773816574, -85.43729755723236963, 117.2915757704554949 ) ) ;
#7585=DIRECTION ( 'NONE',  ( -0.000000000000000000, 1.000000000000000000, -0.000000000000000000 ) ) ;
#7587=( BOUNDED_SURFACE ( )  B_SPLINE_SURFACE ( 3, 1, ( 
 ( #27192, #20874 ),
 ( #22913, #9953 ),
 ( #18263, #7507 ),
 ( #24921, #25066 ) ),
 .UNSPECIFIED., .F., .F., .F. ) 
 B_SPLINE_SURFACE_WITH_KNOTS ( ( 4, 4 ),
 ( 2, 2 ),
 ( 0.000000000000000000, 1.000000000000000000 ),
 ( 0.000000000000000000, 1.000000000000000000 ),
 .UNSPECIFIED. ) 
 GEOMETRIC_REPRESENTATION_ITEM ( )  RATIONAL_B_SPLINE_SURFACE ( (
 ( 1.000000000000000000, 1.000000000000000000),
 ( 0.9956975270656954757, 0.8568959468854893125),
 ( 0.9956975270656954757, 0.8568959468854893125),
 ( 1.000000000000000000, 1.000000000000000000) ) ) 
 REPRESENTATION_ITEM ( '' )  SURFACE ( )  );
#7588=VERTEX_POINT ( 'NONE', #23865 ) ;
#7589=CARTESIAN_POINT ( 'NONE',  ( 1.833485406944043827, 44.33323125129927433, 138.1714136985309835 ) ) ;
#7590=CARTESIAN_POINT ( 'NONE',  ( 109.1778270068192853, -0.005186985107090082321, 0.007736698406808958234 ) ) ;
#7591=CARTESIAN_POINT ( 'NONE',  ( 1.833809397773858541, -15.34508223002545968, 144.2961330457379461 ) ) ;
#7592=ORIENTED_EDGE ( 'NONE', *, *, #21932, .T. ) ;
#7594=CARTESIAN_POINT ( 'NONE',  ( 2.108985857320907709, 116.7869613039531771, -86.43462668039018126 ) ) ;
#7596=EDGE_CURVE ( 'NONE', #27156, #14400, #1432, .T. ) ;
#7597=EDGE_CURVE ( 'NONE', #246, #15408, #20064, .T. ) ;
#7598=ORIENTED_EDGE ( 'NONE', *, *, #27973, .F. ) ;
#7600=VECTOR ( 'NONE', #16846, 1000.000000000000227 ) ;
#7601=EDGE_LOOP ( 'NONE', ( #10857, #3947, #23968, #26900 ) ) ;
#7603=CARTESIAN_POINT ( 'NONE',  ( 8.186469829614463123, 137.8131829164344708, -57.56191610809234760 ) ) ;
#7604=ORIENTED_EDGE ( 'NONE', *, *, #1562, .F. ) ;
#7606=FACE_OUTER_BOUND ( 'NONE', #11780, .T. ) ;
#7608=DIRECTION ( 'NONE',  ( 0.000000000000000000, -6.938893903907228378E-16, -1.000000000000000000 ) ) ;
#7610=EDGE_LOOP ( 'NONE', ( #4, #14931 ) ) ;
#7612=ADVANCED_FACE ( 'NONE', ( #12886 ), #19790, .F. ) ;
#7617=VERTEX_POINT ( 'NONE', #28284 ) ;
#7618=ORIENTED_EDGE ( 'NONE', *, *, #3005, .F. ) ;
#7620=CARTESIAN_POINT ( 'NONE',  ( 25.73574536432415272, -90.91878692681981988, -67.05280231777601330 ) ) ;
#7621=DIRECTION ( 'NONE',  ( -0.5946245182733608248, -0.3297108033645170799, -0.7332888028688958615 ) ) ;
#7622=CARTESIAN_POINT ( 'NONE',  ( 32.73300124599732186, 0.000000000000000000, 0.000000000000000000 ) ) ;
#7623=CARTESIAN_POINT ( 'NONE',  ( 1.832998868059858122, -141.8272129421606564, -30.69214149074159792 ) ) ;
#7626=CARTESIAN_POINT ( 'NONE',  ( 1.833691583653522361, 107.5990239011827043, 97.36155720551511195 ) ) ;
#7628=VERTEX_POINT ( 'NONE', #2367 ) ;
#7629=CARTESIAN_POINT ( 'NONE',  ( 9.884929003653626367, 135.7578851563895057, -65.04493172071342144 ) ) ;
#7632=CARTESIAN_POINT ( 'NONE',  ( 119.2224693531408803, 90.00000000000005684, 19.99999999999997513 ) ) ;
#7633=EDGE_CURVE ( 'NONE', #16816, #9521, #22118, .T. ) ;
#7634=CARTESIAN_POINT ( 'NONE',  ( 25.64660436782550335, -66.83584345385848735, -91.00479974714311027 ) ) ;
#7635=CARTESIAN_POINT ( 'NONE',  ( 25.65782528836479415, 75.12678957786506828, 84.30028114518196958 ) ) ;
#7638=ORIENTED_EDGE ( 'NONE', *, *, #2483, .F. ) ;
#7639=CARTESIAN_POINT ( 'NONE',  ( 1.894214914920992365, 29.24491455759132208, -142.1734439042093925 ) ) ;
#7640=CARTESIAN_POINT ( 'NONE',  ( 32.73300124599732186, 0.000000000000000000, 0.000000000000000000 ) ) ;
#7641=EDGE_CURVE ( 'NONE', #5555, #8700, #6673, .T. ) ;
#7642=CARTESIAN_POINT ( 'NONE',  ( 109.1624594426973260, 0.01582142368018301520, 0.002129375066970686133 ) ) ;
#7644=ORIENTED_EDGE ( 'NONE', *, *, #24913, .T. ) ;
#7646=VERTEX_POINT ( 'NONE', #4688 ) ;
#7647=CARTESIAN_POINT ( 'NONE',  ( 13.36082413113061307, 129.1512766091121307, 81.89226687792132964 ) ) ;
#7648=CARTESIAN_POINT ( 'NONE',  ( 109.1624594426973260, -0.01216903288310115100, 0.01033277910988593222 ) ) ;
#7649=CARTESIAN_POINT ( 'NONE',  ( 109.1586900883932856, -0.004277182003227263107, -0.005715190711481709686 ) ) ;
#7650=VECTOR ( 'NONE', #15834, 1000.000000000000000 ) ;
#7651=CARTESIAN_POINT ( 'NONE',  ( 32.73300124599740002, 72.21147546950675178, -92.86301839379947864 ) ) ;
#7652=CARTESIAN_POINT ( 'NONE',  ( 1.833838850093451933, 125.6687394363107728, -72.55488452980732461 ) ) ;
#7653=VERTEX_POINT ( 'NONE', #17491 ) ;
#7654=CARTESIAN_POINT ( 'NONE',  ( 10.93730112725932635, 149.7554878793145576, 20.69552240458357062 ) ) ;
#7655=CARTESIAN_POINT ( 'NONE',  ( 25.64692872815575697, 34.58541472378651349, 107.4838747185722383 ) ) ;
#7656=CARTESIAN_POINT ( 'NONE',  ( 10.93730112725971004, 51.37919228020272300, 142.1801301103785420 ) ) ;
#7657=ORIENTED_EDGE ( 'NONE', *, *, #12407, .F. ) ;
#7661=CARTESIAN_POINT ( 'NONE',  ( 1.894214914920965276, 84.54370816135735822, -117.9869255019023768 ) ) ;
#7662=CARTESIAN_POINT ( 'NONE',  ( 25.64681081121879203, -75.86069728269045243, 83.63051021305875565 ) ) ;
#7663=CARTESIAN_POINT ( 'NONE',  ( 1.833206308920057870, -84.68961866582925779, -117.8322276971144902 ) ) ;
#7665=CARTESIAN_POINT ( 'NONE',  ( 109.1587776205901577, -0.006305329297952444977, -0.003736572840486921884 ) ) ;
#7667=CARTESIAN_POINT ( 'NONE',  ( 25.64670758986457955, 84.24158725144721416, -75.18147256661973188 ) ) ;
#7668=CARTESIAN_POINT ( 'NONE',  ( 1.833485406944043827, 29.64752363041542083, 142.0485807715646729 ) ) ;
#7669=CARTESIAN_POINT ( 'NONE',  ( 1.832998868059858122, -96.70023740551195601, 108.1944082009154329 ) ) ;
#7672=CARTESIAN_POINT ( 'NONE',  ( 26.11404676487257603, -76.59696442953247697, 83.38016054979757996 ) ) ;
#7673=CARTESIAN_POINT ( 'NONE',  ( 19.66333377628723156, -135.6014041990441399, 24.23123354948793207 ) ) ;
#7674=CARTESIAN_POINT ( 'NONE',  ( 16.05277956358201763, -118.6216415718956085, -80.40847413522669740 ) ) ;
#7677=ORIENTED_EDGE ( 'NONE', *, *, #2483, .T. ) ;
#7678=( BOUNDED_SURFACE ( )  B_SPLINE_SURFACE ( 3, 1, ( 
 ( #5729, #5868 ),
 ( #10340, #968 ),
 ( #12194, #16660 ),
 ( #5425, #14188 ) ),
 .UNSPECIFIED., .F., .F., .F. ) 
 B_SPLINE_SURFACE_WITH_KNOTS ( ( 4, 4 ),
 ( 2, 2 ),
 ( 0.000000000000000000, 1.000000000000000000 ),
 ( 0.000000000000000000, 1.000000000000000000 ),
 .UNSPECIFIED. ) 
 GEOMETRIC_REPRESENTATION_ITEM ( )  RATIONAL_B_SPLINE_SURFACE ( (
 ( 1.000000000000000000, 1.000000000000000000),
 ( 0.9956975270656955868, 0.8568959468854907557),
 ( 0.9956975270656955868, 0.8568959468854907557),
 ( 1.000000000000000000, 1.000000000000000000) ) ) 
 REPRESENTATION_ITEM ( '' )  SURFACE ( )  );
#7679=EDGE_CURVE ( 'NONE', #6523, #1292, #14569, .T. ) ;
#7680=VERTEX_POINT ( 'NONE', #18058 ) ;
#7681=EDGE_LOOP ( 'NONE', ( #15101, #19007, #28071, #20572 ) ) ;
#7682=CARTESIAN_POINT ( 'NONE',  ( 25.64708228042120908, -110.4357030047556236, -23.51409906510326309 ) ) ;
#7685=CARTESIAN_POINT ( 'NONE',  ( 13.36082413113063083, 135.4964217943307290, 70.90215303572172445 ) ) ;
#7687=CARTESIAN_POINT ( 'NONE',  ( 109.1589550718175161, -0.005994046294305938397, 0.004632048724982886813 ) ) ;
#7689=CARTESIAN_POINT ( 'NONE',  ( 8.186469829614447136, 90.56875932797750295, -118.7566730983339909 ) ) ;
#7690=LINE ( 'NONE', #20181, #475 ) ;
#7692=CARTESIAN_POINT ( 'NONE',  ( 55.49584447822657296, 0.2676470673956655166, 72.55110015779771970 ) ) ;
#7693=CARTESIAN_POINT ( 'NONE',  ( 16.05277956358201763, -126.3767940428296725, -67.56865019683978346 ) ) ;
#7694=CARTESIAN_POINT ( 'NONE',  ( 9.884929003653626367, -11.54837932063133188, 150.0922431698404580 ) ) ;
#7695=EDGE_CURVE ( 'NONE', #25484, #16069, #19710, .T. ) ;
#7696=CARTESIAN_POINT ( 'NONE',  ( 1.894214914920974602, 16.12044375672287799, 144.2521558665607699 ) ) ;
#7697=CARTESIAN_POINT ( 'NONE',  ( 32.73300124599736449, -117.3295799645430435, 8.473903470905730373 ) ) ;
#7698=CARTESIAN_POINT ( 'NONE',  ( 1.831572820252009626, 132.9644823688595352, 58.11906524360522752 ) ) ;
#7699=CARTESIAN_POINT ( 'NONE',  ( 109.1778270068192853, -0.009293669915260191483, -0.0006237116683871008664 ) ) ;
#7701=ORIENTED_EDGE ( 'NONE', *, *, #6845, .F. ) ;
#7703=ORIENTED_EDGE ( 'NONE', *, *, #11438, .T. ) ;
#7704=CARTESIAN_POINT ( 'NONE',  ( 109.1586900883932856, -0.007137750914550312215, 0.0001010081143975802818 ) ) ;
#7705=EDGE_CURVE ( 'NONE', #14322, #10817, #1890, .T. ) ;
#7706=LINE ( 'NONE', #7558, #21711 ) ;
#7708=ADVANCED_FACE ( 'NONE', ( #4831 ), #1345, .F. ) ;
#7709=B_SPLINE_CURVE_WITH_KNOTS ( 'NONE', 3,
 ( #18681, #27308, #23019, #981, #16674, #9772, #12068 ),
 .UNSPECIFIED., .F., .F.,
 ( 4, 3, 4 ),
 ( 0.000000000000000000, 0.02398743853561371986, 0.04000277880656209067 ),
 .UNSPECIFIED. ) ;
#7713=DIRECTION ( 'NONE',  ( 0.5946245182733608248, -0.3243201896541589302, -0.7356888587241646738 ) ) ;
#7714=DIRECTION ( 'NONE',  ( 0.000000000000000000, 0.000000000000000000, 1.000000000000000000 ) ) ;
#7715=B_SPLINE_CURVE_WITH_KNOTS ( 'NONE', 3,
 ( #737, #27358, #9525, #5197, #5050, #24797, #7368, #7672 ),
 .UNSPECIFIED., .F., .F.,
 ( 4, 2, 2, 4 ),
 ( 0.000000000000000000, 0.0002429588503611235174, 0.0004859177007222470349, 0.0009718354014444994908 ),
 .UNSPECIFIED. ) ;
#7718=CARTESIAN_POINT ( 'NONE',  ( 25.64660436782536479, 107.5626123667561416, 34.33930645842045948 ) ) ;
#7720=CARTESIAN_POINT ( 'NONE',  ( 1.833809397773860539, -58.85883548850502933, -132.6366580004813045 ) ) ;
#7721=CARTESIAN_POINT ( 'NONE',  ( 109.1624594426973118, -0.007576898892906994316, 0.01405141589344821758 ) ) ;
#7722=CARTESIAN_POINT ( 'NONE',  ( 1.833485406944043827, 58.53321471326877656, 132.7804117027889674 ) ) ;
#7724=ORIENTED_EDGE ( 'NONE', *, *, #3803, .T. ) ;
#7725=ORIENTED_EDGE ( 'NONE', *, *, #8778, .T. ) ;
#7727=CARTESIAN_POINT ( 'NONE',  ( 1.833691583653570545, 85.00512109099250324, 117.6050685739171797 ) ) ;
#7729=EDGE_CURVE ( 'NONE', #24769, #12561, #9430, .T. ) ;
#7730=CARTESIAN_POINT ( 'NONE',  ( 1.833838850855499025, -85.36536653357421756, 117.3439621615260222 ) ) ;
#7731=CARTESIAN_POINT ( 'NONE',  ( 32.73300124599732186, 0.000000000000000000, 0.000000000000000000 ) ) ;
#7734=CARTESIAN_POINT ( 'NONE',  ( 1.831572820252008738, -45.77972211429909777, 137.7011124121615353 ) ) ;
#7735=CARTESIAN_POINT ( 'NONE',  ( 109.1592201516379674, -0.007051465909552739365, 0.003476928926134781935 ) ) ;
#7736=EDGE_CURVE ( 'NONE', #26, #24791, #23960, .T. ) ;
#7737=CARTESIAN_POINT ( 'NONE',  ( 32.73300124599740002, 116.5274707358857142, -16.10546300444702794 ) ) ;
#7740=EDGE_CURVE ( 'NONE', #26503, #21438, #933, .T. ) ;
#7744=CARTESIAN_POINT ( 'NONE',  ( 5.340103556456579526, 140.9275371673313657, -43.36842540065345730 ) ) ;
#7745=ORIENTED_EDGE ( 'NONE', *, *, #15758, .F. ) ;
#7746=CARTESIAN_POINT ( 'NONE',  ( 21.16825799904893657, -63.85626241912828505, 119.4343305756978708 ) ) ;
#7748=PRODUCT_CONTEXT ( 'NONE', #19299, 'mechanical' ) ;
#7749=CARTESIAN_POINT ( 'NONE',  ( 32.73300124599741423, 115.8010721414085822, -20.69176323058512423 ) ) ;
#7751=CARTESIAN_POINT ( 'NONE',  ( 6.224689322667630975, -89.08920297664293741, 118.2566963816767753 ) ) ;
#7753=CARTESIAN_POINT ( 'NONE',  ( 1.833485406944057594, -141.8265699653869376, 30.69200235378888308 ) ) ;
#7754=ORIENTED_EDGE ( 'NONE', *, *, #20137, .F. ) ;
#7756=EDGE_CURVE ( 'NONE', #10776, #26564, #5396, .T. ) ;
#7757=CARTESIAN_POINT ( 'NONE',  ( 28.43349137099830770, -123.9292945876798200, -8.951033805645977282 ) ) ;
#7759=ORIENTED_EDGE ( 'NONE', *, *, #27518, .T. ) ;
#7760=VERTEX_POINT ( 'NONE', #12576 ) ;
#7761=ORIENTED_EDGE ( 'NONE', *, *, #20345, .T. ) ;
#7764=CARTESIAN_POINT ( 'NONE',  ( 1.833750490713671466, 108.0159692407144121, -96.89879583303743971 ) ) ;
#7765=CARTESIAN_POINT ( 'NONE',  ( 24.01988960052047162, -121.3896480498354862, 49.36855864442090791 ) ) ;
#7768=CARTESIAN_POINT ( 'NONE',  ( 24.22246935314087324, 90.00000000000005684, -40.00000000000000711 ) ) ;
#7770=CARTESIAN_POINT ( 'NONE',  ( 10.93730112725932990, 151.0983828010088530, 4.928439153520527860 ) ) ;
#7771=VECTOR ( 'NONE', #13523, 1000.000000000000114 ) ;
#7772=EDGE_CURVE ( 'NONE', #9282, #238, #21364, .T. ) ;
#7774=ORIENTED_EDGE ( 'NONE', *, *, #8545, .T. ) ;
#7776=DIRECTION ( 'NONE',  ( 0.5914120900931444380, -0.1598001217819363939, -0.7903769105750348967 ) ) ;
#7777=LINE ( 'NONE', #5890, #20254 ) ;
#7778=CARTESIAN_POINT ( 'NONE',  ( 25.64681081121879203, -66.70335573067806934, -91.10197563708015878 ) ) ;
#7781=CARTESIAN_POINT ( 'NONE',  ( 1.831572820252008738, -144.2101521542829232, -16.14965423926357246 ) ) ;
#7783=CARTESIAN_POINT ( 'NONE',  ( 109.1587776205901577, 0.007328861771496575708, 8.330235397647321066E-05 ) ) ;
#7784=CARTESIAN_POINT ( 'NONE',  ( 1.833721034905659186, -30.51809396650913442, -141.8643653601973540 ) ) ;
#7785=CARTESIAN_POINT ( 'NONE',  ( 1.831572820252008738, -86.09108691067849861, 116.8148281295966342 ) ) ;
#7786=ORIENTED_EDGE ( 'NONE', *, *, #4747, .T. ) ;
#7789=CARTESIAN_POINT ( 'NONE',  ( 25.98552792386798771, -102.9121737515624062, 47.00040718953741248 ) ) ;
#7791=EDGE_CURVE ( 'NONE', #4553, #27587, #14455, .T. ) ;
#7792=CARTESIAN_POINT ( 'NONE',  ( 109.1586900883932856, -0.007109207791180745251, -0.0006456433529069797875 ) ) ;
#7793=LINE ( 'NONE', #27781, #7600 ) ;
#7794=CARTESIAN_POINT ( 'NONE',  ( 26.11404676487259024, 74.91683232331092768, -84.89295829319416953 ) ) ;
#7799=( BOUNDED_SURFACE ( )  B_SPLINE_SURFACE ( 3, 1, ( 
 ( #25431, #14318 ),
 ( #16920, #7734 ),
 ( #25280, #10323 ),
 ( #7878, #14890 ) ),
 .UNSPECIFIED., .F., .F., .F. ) 
 B_SPLINE_SURFACE_WITH_KNOTS ( ( 4, 4 ),
 ( 2, 2 ),
 ( 0.000000000000000000, 1.000000000000000000 ),
 ( 0.000000000000000000, 1.000000000000000000 ),
 .UNSPECIFIED. ) 
 GEOMETRIC_REPRESENTATION_ITEM ( )  RATIONAL_B_SPLINE_SURFACE ( (
 ( 1.000000000000000000, 1.000000000000000000),
 ( 0.9956975270656955868, 0.8568959468854907557),
 ( 0.9956975270656955868, 0.8568959468854907557),
 ( 1.000000000000000000, 1.000000000000000000) ) ) 
 REPRESENTATION_ITEM ( '' )  SURFACE ( )  );
#7801=ORIENTED_EDGE ( 'NONE', *, *, #21904, .T. ) ;
#7802=CARTESIAN_POINT ( 'NONE',  ( 109.1721716018069657, -0.01157047143379290842, -0.01254847260354823371 ) ) ;
#7804=DIRECTION ( 'NONE',  ( 0.5914120900931444380, -0.2567974902965192152, 0.7643865440136080602 ) ) ;
#7805=CARTESIAN_POINT ( 'NONE',  ( 28.37599760073043242, 25.60640155549320340, -111.8383885143452687 ) ) ;
#7806=FACE_OUTER_BOUND ( 'NONE', #18042, .T. ) ;
#7808=VERTEX_POINT ( 'NONE', #23542 ) ;
#7809=CARTESIAN_POINT ( 'NONE',  ( 109.1589550718174877, -0.007270618150629046088, 0.002126635388725444178 ) ) ;
#7810=DIRECTION ( 'NONE',  ( 0.000000000000000000, 0.000000000000000000, 1.000000000000000000 ) ) ;
#7811=CARTESIAN_POINT ( 'NONE',  ( 1.831572820252009626, -96.36280042116003131, 108.4969585352551746 ) ) ;
#7813=CARTESIAN_POINT ( 'NONE',  ( 2.430230287190589422, 1.451610819317738610, 145.5073573687466819 ) ) ;
#7815=CARTESIAN_POINT ( 'NONE',  ( 109.1586900883932856, 0.006960773163856032002, 0.001582822706024274422 ) ) ;
#7816=B_SPLINE_CURVE_WITH_KNOTS ( 'NONE', 3,
 ( #22948, #3205, #1052, #18609 ),
 .UNSPECIFIED., .F., .F.,
 ( 4, 4 ),
 ( 0.000000000000000000, 0.01077107196513873814 ),
 .UNSPECIFIED. ) ;
#7818=ORIENTED_EDGE ( 'NONE', *, *, #17505, .T. ) ;
#7823=EDGE_CURVE ( 'NONE', #1130, #23219, #16299, .T. ) ;
#7824=EDGE_CURVE ( 'NONE', #25988, #13553, #22108, .T. ) ;
#7825=CARTESIAN_POINT ( 'NONE',  ( 109.1778270068192853, -0.009307953841262541286, -0.0003511581237570729095 ) ) ;
#7828=ORIENTED_EDGE ( 'NONE', *, *, #8248, .F. ) ;
#7831=CARTESIAN_POINT ( 'NONE',  ( 25.64708228042119131, 83.88307475436060656, 75.58165863986067734 ) ) ;
#7832=B_SPLINE_CURVE_WITH_KNOTS ( 'NONE', 3,
 ( #8837, #17036, #26381, #24103, #4366, #25833, #21793, #6534 ),
 .UNSPECIFIED., .F., .F.,
 ( 4, 2, 2, 4 ),
 ( 6.505213034913026604E-19, 0.0002429592666046762994, 0.0004859185332093519482, 0.0009718370664186838388 ),
 .UNSPECIFIED. ) ;
#7833=CARTESIAN_POINT ( 'NONE',  ( 1.833485406944043827, 132.3460930279890704, 59.50871042846269177 ) ) ;
#7834=EDGE_CURVE ( 'NONE', #12622, #11774, #15559, .T. ) ;
#7836=CARTESIAN_POINT ( 'NONE',  ( 10.93730112726002979, 79.81734490846109509, -128.3908183996583432 ) ) ;
#7837=CARTESIAN_POINT ( 'NONE',  ( 10.93730112725932813, 146.7718404940640085, 36.23586118136551448 ) ) ;
#7838=CARTESIAN_POINT ( 'NONE',  ( 25.64704443564076186, -66.25951665433227333, -91.42548471394263743 ) ) ;
#7839=CARTESIAN_POINT ( 'NONE',  ( 25.98552792386800192, 76.50165414343565828, 83.35136888841265090 ) ) ;
#7840=FACE_OUTER_BOUND ( 'NONE', #20865, .T. ) ;
#7843=( BOUNDED_SURFACE ( )  B_SPLINE_SURFACE ( 3, 1, ( 
 ( #24448, #26580 ),
 ( #6884, #4717 ),
 ( #13491, #22286 ),
 ( #20107, #12054 ) ),
 .UNSPECIFIED., .F., .F., .F. ) 
 B_SPLINE_SURFACE_WITH_KNOTS ( ( 4, 4 ),
 ( 2, 2 ),
 ( 0.000000000000000000, 1.000000000000000000 ),
 ( 0.000000000000000000, 1.000000000000000000 ),
 .UNSPECIFIED. ) 
 GEOMETRIC_REPRESENTATION_ITEM ( )  RATIONAL_B_SPLINE_SURFACE ( (
 ( 1.000000000000000000, 1.000000000000000000),
 ( 0.9960225298536222738, 0.9999952330161893110),
 ( 0.9960225298536222738, 0.9999952330161893110),
 ( 1.000000000000000000, 1.000000000000000000) ) ) 
 REPRESENTATION_ITEM ( '' )  SURFACE ( )  );
#7844=ORIENTED_EDGE ( 'NONE', *, *, #27085, .F. ) ;
#7845=CARTESIAN_POINT ( 'NONE',  ( 55.79472521941428198, -49.22042574086388811, -53.57698701322264867 ) ) ;
#7847=CARTESIAN_POINT ( 'NONE',  ( 26.11404676487259024, -108.0249973236465308, -33.91085499298486639 ) ) ;
#7848=DIRECTION ( 'NONE',  ( 0.5946245182733608248, 0.7858154137795708705, 0.1700465163848279837 ) ) ;
#7851=ORIENTED_EDGE ( 'NONE', *, *, #21511, .F. ) ;
#7853=CARTESIAN_POINT ( 'NONE',  ( 2.433796855181233454, 138.8296532063088193, 43.58222566461690661 ) ) ;
#7856=CARTESIAN_POINT ( 'NONE',  ( 32.73300124599737870, -117.5726003567929041, -3.836798148480059734 ) ) ;
#7857=EDGE_CURVE ( 'NONE', #25030, #1343, #25897, .T. ) ;
#7858=CARTESIAN_POINT ( 'NONE',  ( 109.1778270068192853, 0.009031542838317254199, 0.002278716897421661797 ) ) ;
#7861=CARTESIAN_POINT ( 'NONE',  ( 1.832998868059858122, 85.72499093308256590, -117.0819875546686859 ) ) ;
#7864=CARTESIAN_POINT ( 'NONE',  ( 2.433796855181205476, -116.8607839509050734, -86.69855925934092511 ) ) ;
#7867=CARTESIAN_POINT ( 'NONE',  ( 1.833485406944043827, 132.7804117027896211, -58.53321471326746916 ) ) ;
#7868=CIRCLE ( 'NONE', #23506, 151.1787379149930359 ) ;
#7869=ORIENTED_EDGE ( 'NONE', *, *, #5493, .F. ) ;
#7871=CARTESIAN_POINT ( 'NONE',  ( 1.833485406944043827, 108.1939177044938560, -96.69979900902059455 ) ) ;
#7872=CARTESIAN_POINT ( 'NONE',  ( 1.833206308920110050, 132.8652726225759864, -58.34024961171099477 ) ) ;
#7875=CARTESIAN_POINT ( 'NONE',  ( 25.64681081121879203, 75.86069728268988399, 83.63051021305928145 ) ) ;
#7876=EDGE_LOOP ( 'NONE', ( #260, #11669, #5776, #24977 ) ) ;
#7877=VERTEX_POINT ( 'NONE', #11243 ) ;
#7878=CARTESIAN_POINT ( 'NONE',  ( 109.1592201516379674, -0.001934867487021774525, -0.007620268632971101234 ) ) ;
#7880=CARTESIAN_POINT ( 'NONE',  ( 13.36082413113061307, 41.18148072373615776, 147.2768864064169350 ) ) ;
#7881=CARTESIAN_POINT ( 'NONE',  ( 13.84597867724968268, -142.4258194868991723, -35.16314962059988858 ) ) ;
#7882=ORIENTED_EDGE ( 'NONE', *, *, #14620, .T. ) ;
#7883=CARTESIAN_POINT ( 'NONE',  ( 109.1592201516379674, 0.005631912476303814301, -0.005485778713202952607 ) ) ;
#7885=ORIENTED_EDGE ( 'NONE', *, *, #7381, .F. ) ;
#7886=ORIENTED_EDGE ( 'NONE', *, *, #15924, .F. ) ;
#7889=LINE ( 'NONE', #14475, #13324 ) ;
#7890=VECTOR ( 'NONE', #14877, 1000.000000000000000 ) ;
#7891=ORIENTED_EDGE ( 'NONE', *, *, #748, .T. ) ;
#7894=EDGE_CURVE ( 'NONE', #5142, #4901, #163, .T. ) ;
#7895=CARTESIAN_POINT ( 'NONE',  ( 1.831572820252009626, 58.11906524360657755, -132.9644823688589668 ) ) ;
#7896=EDGE_CURVE ( 'NONE', #5184, #17451, #2451, .T. ) ;
#7898=CARTESIAN_POINT ( 'NONE',  ( 109.1592201516379674, 0.007845213074654433863, -0.0005146241775983094154 ) ) ;
#7899=CARTESIAN_POINT ( 'NONE',  ( 10.93730112725932990, 151.0983828010088530, 4.928439153520527860 ) ) ;
#7900=CARTESIAN_POINT ( 'NONE',  ( 109.1587776205901577, 0.0008489206734408877688, -0.007280006032833121095 ) ) ;
#7902=ORIENTED_EDGE ( 'NONE', *, *, #24311, .T. ) ;
#7903=CARTESIAN_POINT ( 'NONE',  ( 16.05277956358206737, -4.672229451526818345, -143.2298391883442150 ) ) ;
#7904=CARTESIAN_POINT ( 'NONE',  ( 28.43349137099852086, 94.99961975860237828, 80.08535015163919013 ) ) ;
#7905=CARTESIAN_POINT ( 'NONE',  ( 9.884929003653626367, -141.8132360130361178, 50.49804566712076337 ) ) ;
#7908=AXIS2_PLACEMENT_3D ( 'NONE', #7640, #14370, #18699 ) ;
#7909=ORIENTED_EDGE ( 'NONE', *, *, #16448, .T. ) ;
#7910=ORIENTED_EDGE ( 'NONE', *, *, #16347, .F. ) ;
#7912=DIRECTION ( 'NONE',  ( -1.000000000000000000, -0.000000000000000000, -0.000000000000000000 ) ) ;
#7913=CARTESIAN_POINT ( 'NONE',  ( 32.73300124599735028, 8.473903470906103408, 117.3295799645430151 ) ) ;
#7918=CARTESIAN_POINT ( 'NONE',  ( 26.11404676487257603, 47.08215554553518700, 102.9690087468803341 ) ) ;
#7920=VERTEX_POINT ( 'NONE', #15847 ) ;
#7921=CARTESIAN_POINT ( 'NONE',  ( 109.1721716018069657, 0.008708654716139420035, 0.01467989464939313364 ) ) ;
#7924=CARTESIAN_POINT ( 'NONE',  ( 30.59141879584315760, 38.47120193631630514, -109.6600586137411995 ) ) ;
#7925=CARTESIAN_POINT ( 'NONE',  ( 26.11404676487257603, 84.89295829319590325, -74.91683232330889552 ) ) ;
#7926=DIRECTION ( 'NONE',  ( 0.000000000000000000, 0.000000000000000000, 1.000000000000000000 ) ) ;
#7928=CARTESIAN_POINT ( 'NONE',  ( 2.430230287190581429, -144.5585181921884725, -16.65331920325886728 ) ) ;
#7929=ORIENTED_EDGE ( 'NONE', *, *, #19681, .T. ) ;
#7930=CARTESIAN_POINT ( 'NONE',  ( 19.66333377628711432, 60.10102584214535426, -123.9466021833765268 ) ) ;
#7931=CARTESIAN_POINT ( 'NONE',  ( 109.1624594426973260, 0.01595733256931100227, 0.0004639210235576350151 ) ) ;
#7932=CARTESIAN_POINT ( 'NONE',  ( 9.884929003653626367, 119.2676479132386191, -91.84919534721818479 ) ) ;
#7933=ORIENTED_EDGE ( 'NONE', *, *, #7235, .T. ) ;
#7934=ADVANCED_FACE ( 'NONE', ( #9387 ), #7406, .F. ) ;
#7936=VERTEX_POINT ( 'NONE', #11382 ) ;
#7937=EDGE_CURVE ( 'NONE', #25105, #15925, #25236, .T. ) ;
#7942=CIRCLE ( 'NONE', #27209, 151.1787379149930359 ) ;
#7943=CARTESIAN_POINT ( 'NONE',  ( 109.1586059443104944, -0.006971743774738792081, 0.001198897580748315740 ) ) ;
#7944=CARTESIAN_POINT ( 'NONE',  ( 1.832998868059890096, 30.69214149074013420, 141.8272129421609691 ) ) ;
#7945=CARTESIAN_POINT ( 'NONE',  ( 109.1586900883932856, -0.007002774699553650055, 0.001385221016536923372 ) ) ;
#7946=DIRECTION ( 'NONE',  ( -0.5946245182733607137, -0.7655593692108988435, -0.2456431038754887941 ) ) ;
#7948=DIRECTION ( 'NONE',  ( 0.5914120900931444380, -0.3206367055789438592, -0.7398809652418016913 ) ) ;
#7949=ORIENTED_EDGE ( 'NONE', *, *, #6840, .F. ) ;
#7951=CARTESIAN_POINT ( 'NONE',  ( 2.263178113027037863, 107.1074314657344644, 98.32595894905868761 ) ) ;
#7952=DIRECTION ( 'NONE',  ( -1.000000000000000000, -0.000000000000000000, -0.000000000000000000 ) ) ;
#7954=B_SPLINE_CURVE_WITH_KNOTS ( 'NONE', 3,
 ( #27872, #8170, #16934, #12879, #8444, #16808, #14904, #18807 ),
 .UNSPECIFIED., .F., .F.,
 ( 4, 2, 2, 4 ),
 ( 3.469446951953614189E-18, 0.0002429592666046796875, 0.0004859185332093559056, 0.0009718370664186904524 ),
 .UNSPECIFIED. ) ;
#7955=CARTESIAN_POINT ( 'NONE',  ( 2.263178607246671969, 107.1074316126230883, -98.32595927618747567 ) ) ;
#7957=CARTESIAN_POINT ( 'NONE',  ( 55.49584447822657296, -48.34726110740022875, 54.09506550945609149 ) ) ;
#7958=ORIENTED_EDGE ( 'NONE', *, *, #17862, .T. ) ;
#7961=CARTESIAN_POINT ( 'NONE',  ( 26.11404676487257603, 1.130420376097130086, 113.2169081140374090 ) ) ;
#7962=AXIS2_PLACEMENT_3D ( 'NONE', #3542, #12464, #25585 ) ;
#7963=CARTESIAN_POINT ( 'NONE',  ( 1.831572820252009626, 0.9871191512914618826, 145.1082523917587253 ) ) ;
#7967=CARTESIAN_POINT ( 'NONE',  ( 28.37644542392836655, 109.6517504963498340, -58.62516076109932328 ) ) ;
#7969=VERTEX_POINT ( 'NONE', #8417 ) ;
#7970=EDGE_CURVE ( 'NONE', #3139, #142, #26916, .T. ) ;
#7971=ORIENTED_EDGE ( 'NONE', *, *, #6778, .F. ) ;
#7973=ADVANCED_FACE ( 'NONE', ( #24790 ), #20239, .F. ) ;
#7974=CARTESIAN_POINT ( 'NONE',  ( 109.1586059443104944, -0.0004635842312796545654, 0.007058870754606100771 ) ) ;
#7977=FACE_OUTER_BOUND ( 'NONE', #16191, .T. ) ;
#7978=VECTOR ( 'NONE', #21538, 1000.000000000000227 ) ;
#7980=CARTESIAN_POINT ( 'NONE',  ( 109.1586900883932856, -0.006561743627143347760, 0.002810909342011576936 ) ) ;
#7981=ORIENTED_EDGE ( 'NONE', *, *, #24702, .T. ) ;
#7982=DIRECTION ( 'NONE',  ( -1.000000000000000000, -0.000000000000000000, -0.000000000000000000 ) ) ;
#7983=CARTESIAN_POINT ( 'NONE',  ( 13.36082413113061307, -109.3026516754225099, -106.9547846563646800 ) ) ;
#7986=CARTESIAN_POINT ( 'NONE',  ( 1.833750490713684345, -85.07723081767805695, -117.5529286802296411 ) ) ;
#7987=CARTESIAN_POINT ( 'NONE',  ( 28.43349137099838941, 42.22940898499208373, 116.8557575815928971 ) ) ;
#7988=CARTESIAN_POINT ( 'NONE',  ( 2.430230287190572103, 126.7388733285354760, -71.49654683843375835 ) ) ;
#7990=CARTESIAN_POINT ( 'NONE',  ( 25.64707127832795663, -0.04959866882938956945, -112.9112343549835487 ) ) ;
#7992=CARTESIAN_POINT ( 'NONE',  ( 32.73300124599735028, 110.6325518752274206, 39.98094346392350218 ) ) ;
#7993=CARTESIAN_POINT ( 'NONE',  ( 30.58324630866339433, -119.0579156359857507, -21.27395054437367605 ) ) ;
#7994=ORIENTED_EDGE ( 'NONE', *, *, #4213, .F. ) ;
#7996=EDGE_CURVE ( 'NONE', #24633, #14412, #6318, .T. ) ;
#7997=ORIENTED_EDGE ( 'NONE', *, *, #12451, .F. ) ;
#8000=VERTEX_POINT ( 'NONE', #16422 ) ;
#8001=ADVANCED_FACE ( 'NONE', ( #7806 ), #23975, .F. ) ;
#8002=ORIENTED_EDGE ( 'NONE', *, *, #23885, .F. ) ;
#8004=VERTEX_POINT ( 'NONE', #11821 ) ;
#8007=B_SPLINE_CURVE_WITH_KNOTS ( 'NONE', 3,
 ( #11647, #20421, #13792, #4737, #18112, #22157 ),
 .UNSPECIFIED., .F., .F.,
 ( 4, 2, 4 ),
 ( 1.389302603484999005E-17, 0.0006311571484586076322, 0.001262314296917201603 ),
 .UNSPECIFIED. ) ;
#8008=CARTESIAN_POINT ( 'NONE',  ( 1.833750490713684345, -141.9939712933757221, 29.90883416717569787 ) ) ;
#8011=( BOUNDED_SURFACE ( )  B_SPLINE_SURFACE ( 3, 1, ( 
 ( #13123, #14865 ),
 ( #10425, #25687 ),
 ( #23944, #19315 ),
 ( #21772, #2035 ) ),
 .UNSPECIFIED., .F., .F., .F. ) 
 B_SPLINE_SURFACE_WITH_KNOTS ( ( 4, 4 ),
 ( 2, 2 ),
 ( 0.000000000000000000, 1.000000000000000000 ),
 ( 0.000000000000000000, 1.000000000000000000 ),
 .UNSPECIFIED. ) 
 GEOMETRIC_REPRESENTATION_ITEM ( )  RATIONAL_B_SPLINE_SURFACE ( (
 ( 1.000000000000000000, 1.000000000000000000),
 ( 0.9960225298536222738, 0.9999952330161893110),
 ( 0.9960225298536222738, 0.9999952330161893110),
 ( 1.000000000000000000, 1.000000000000000000) ) ) 
 REPRESENTATION_ITEM ( '' )  SURFACE ( )  );
#8012=LINE ( 'NONE', #9721, #26344 ) ;
#8013=CARTESIAN_POINT ( 'NONE',  ( 25.64699802086726166, 56.66140964017734660, 97.66487797954027883 ) ) ;
#8015=ORIENTED_EDGE ( 'NONE', *, *, #16587, .T. ) ;
#8016=CARTESIAN_POINT ( 'NONE',  ( 109.1592201516379674, 0.004194960840990064228, 0.006649399203953477652 ) ) ;
#8020=CARTESIAN_POINT ( 'NONE',  ( 10.93730112725990367, -84.82621002473354110, -125.1380233598488019 ) ) ;
#8022=ORIENTED_EDGE ( 'NONE', *, *, #25018, .F. ) ;
#8024=EDGE_CURVE ( 'NONE', #26828, #6495, #15751, .T. ) ;
#8025=CARTESIAN_POINT ( 'NONE',  ( 109.1592201516379674, -0.006044422199831509662, -0.005027640251764362717 ) ) ;
#8026=CARTESIAN_POINT ( 'NONE',  ( 5.340103579038210313, -117.9209211655063569, 88.52145169228927557 ) ) ;
#8028=ORIENTED_EDGE ( 'NONE', *, *, #10523, .T. ) ;
#8029=EDGE_CURVE ( 'NONE', #28095, #26828, #12649, .T. ) ;
#8031=VERTEX_POINT ( 'NONE', #2897 ) ;
#8032=EDGE_LOOP ( 'NONE', ( #17671, #19164, #15774, #8813 ) ) ;
#8033=ADVANCED_FACE ( 'NONE', ( #731 ), #10191, .F. ) ;
#8034=CARTESIAN_POINT ( 'NONE',  ( 1.833691583653538792, 96.83253123394209183, 108.0753610255256376 ) ) ;
#8035=ORIENTED_EDGE ( 'NONE', *, *, #4777, .T. ) ;
#8036=CARTESIAN_POINT ( 'NONE',  ( 25.98552792386799126, 112.6247604222998859, 10.75254026142839336 ) ) ;
#8037=CARTESIAN_POINT ( 'NONE',  ( 30.59138290137876481, 79.74792615266136409, 84.53179630244015641 ) ) ;
#8039=B_SPLINE_CURVE_WITH_KNOTS ( 'NONE', 3,
 ( #2845, #11337, #15936, #9177, #20110, #27003, #13920 ),
 .UNSPECIFIED., .F., .F.,
 ( 4, 3, 4 ),
 ( 8.998878031629686802E-18, 0.0002669560319015653704, 0.0004157520161273759373 ),
 .UNSPECIFIED. ) ;
#8040=CARTESIAN_POINT ( 'NONE',  ( 2.430230287190572103, -86.70145658344738138, 116.8646894862409056 ) ) ;
#8041=CARTESIAN_POINT ( 'NONE',  ( 21.16825799904930605, 119.4343305756974871, 63.85626241912757450 ) ) ;
#8042=DIRECTION ( 'NONE',  ( -1.000000000000000000, -0.000000000000000000, -0.000000000000000000 ) ) ;
#8046=CARTESIAN_POINT ( 'NONE',  ( 32.73300124599738581, 8.473903470907664826, -117.3295799645428588 ) ) ;
#8048=DIRECTION ( 'NONE',  ( 0.5914120900931444380, 0.09226095020378470568, -0.8010740644654233966 ) ) ;
#8049=ORIENTED_EDGE ( 'NONE', *, *, #24124, .F. ) ;
#8051=CARTESIAN_POINT ( 'NONE',  ( 1.833485406944043827, -141.8265699653865113, -30.69200235379080510 ) ) ;
#8052=CARTESIAN_POINT ( 'NONE',  ( 119.2224693531408803, 70.00000000000000000, -19.99999999999998934 ) ) ;
#8054=CARTESIAN_POINT ( 'NONE',  ( 10.93730112725969938, 56.95489579269752767, 140.0398180619111770 ) ) ;
#8055=CARTESIAN_POINT ( 'NONE',  ( 109.1589550718174877, 0.004269295012386558133, 0.006257602293694224452 ) ) ;
#8059=CARTESIAN_POINT ( 'NONE',  ( 32.73300124599732186, 0.000000000000000000, 0.000000000000000000 ) ) ;
#8062=CARTESIAN_POINT ( 'NONE',  ( 119.2224693531408803, 90.00000000000005684, -40.00000000000000711 ) ) ;
#8063=CARTESIAN_POINT ( 'NONE',  ( 25.64699802086723679, 107.4581924007665350, 34.66526531169679259 ) ) ;
#8064=CARTESIAN_POINT ( 'NONE',  ( 1.833206308920097172, -108.3342547309371469, 96.54250175814081558 ) ) ;
#8067=ORIENTED_EDGE ( 'NONE', *, *, #14398, .F. ) ;
#8068=FACE_OUTER_BOUND ( 'NONE', #285, .T. ) ;
#8069=CARTESIAN_POINT ( 'NONE',  ( 109.1586900883932856, -0.006479576224403809682, -0.002995460350180784680 ) ) ;
#8070=EDGE_CURVE ( 'NONE', #17840, #17905, #15030, .T. ) ;
#8071=CARTESIAN_POINT ( 'NONE',  ( 2.430230287190592531, -57.85706160874235593, 133.5180086894989415 ) ) ;
#8072=ADVANCED_FACE ( 'NONE', ( #27793 ), #22588, .T. ) ;
#8073=B_SPLINE_CURVE_WITH_KNOTS ( 'NONE', 3,
 ( #19647, #26000, #23998, #23863 ),
 .UNSPECIFIED., .F., .F.,
 ( 4, 4 ),
 ( 0.0005339083821118883934, 0.001067817517169162515 ),
 .UNSPECIFIED. ) ;
#8075=CARTESIAN_POINT ( 'NONE',  ( 32.73300124599741423, -75.82012867748416340, -89.94078864464141532 ) ) ;
#8076=ORIENTED_EDGE ( 'NONE', *, *, #12634, .F. ) ;
#8081=CARTESIAN_POINT ( 'NONE',  ( 24.01988960052068123, 129.8107982898200987, 17.94039809062665114 ) ) ;
#8082=LINE ( 'NONE', #1159, #23095 ) ;
#8083=CARTESIAN_POINT ( 'NONE',  ( 25.64681081121879203, 112.3352186517032294, -11.38886654529559017 ) ) ;
#8085=ORIENTED_EDGE ( 'NONE', *, *, #14943, .F. ) ;
#8087=CARTESIAN_POINT ( 'NONE',  ( 1.834118845439484335, -15.34511559672585435, -144.2964192726483645 ) ) ;
#8089=CARTESIAN_POINT ( 'NONE',  ( 2.433796855181233454, 84.34988187691088513, -118.5671979538048504 ) ) ;
#8092=CARTESIAN_POINT ( 'NONE',  ( 2.063896406836605024, 133.2511741302128314, -57.85593781835284233 ) ) ;
#8095=CARTESIAN_POINT ( 'NONE',  ( 19.66333377628718182, 105.3186440504706951, -88.78556591841191903 ) ) ;
#8098=EDGE_CURVE ( 'NONE', #21365, #675, #17142, .T. ) ;
#8100=CARTESIAN_POINT ( 'NONE',  ( 24.01988960052070610, -129.0012934948647114, 23.05141021591238371 ) ) ;
#8102=CARTESIAN_POINT ( 'NONE',  ( 109.1586900883932856, -0.0008465529156635612316, -0.007088091345229652514 ) ) ;
#8103=LINE ( 'NONE', #14555, #12087 ) ;
#8104=ORIENTED_EDGE ( 'NONE', *, *, #2356, .T. ) ;
#8105=VERTEX_POINT ( 'NONE', #19424 ) ;
#8107=CARTESIAN_POINT ( 'NONE',  ( 21.16825799904906802, -32.46271504707843292, -131.4851843440079620 ) ) ;
#8110=ORIENTED_EDGE ( 'NONE', *, *, #27428, .F. ) ;
#8111=CARTESIAN_POINT ( 'NONE',  ( 1.833485406944057594, 58.53321471327059555, -132.7804117027882285 ) ) ;
#8114=CARTESIAN_POINT ( 'NONE',  ( 2.108393763691186695, -138.5721856399487706, 43.67806918959093565 ) ) ;
#8115=CARTESIAN_POINT ( 'NONE',  ( 25.64704443564076186, -75.45310550990100751, -83.99864088993849975 ) ) ;
#8117=CARTESIAN_POINT ( 'NONE',  ( 25.64699802086725811, -11.56593161917390411, 112.3172869996024730 ) ) ;
#8119=CARTESIAN_POINT ( 'NONE',  ( 25.86096068574579832, -113.0494979885903746, -0.9975172952970271512 ) ) ;
#8121=CARTESIAN_POINT ( 'NONE',  ( 21.16825799904935224, 112.1052598354960992, 75.99073816868315134 ) ) ;
#8122=CARTESIAN_POINT ( 'NONE',  ( 25.70243777736187951, 112.2504268534934084, 12.53519966262519603 ) ) ;
#8124=CARTESIAN_POINT ( 'NONE',  ( 28.43349137099833612, -98.08682467580831599, 76.27296957774096597 ) ) ;
#8125=CARTESIAN_POINT ( 'NONE',  ( 99.22246935314079508, 69.99999999999998579, -40.00000000000000711 ) ) ;
#8127=EDGE_LOOP ( 'NONE', ( #21203, #9977, #12863, #2011 ) ) ;
#8129=DIRECTION ( 'NONE',  ( 0.5946245182733607137, 0.7655593692109022852, -0.2456431038754784968 ) ) ;
#8130=ORIENTED_EDGE ( 'NONE', *, *, #2431, .F. ) ;
#8131=ORIENTED_EDGE ( 'NONE', *, *, #20837, .T. ) ;
#8137=ADVANCED_FACE ( 'NONE', ( #8628 ), #28089, .T. ) ;
#8138=CARTESIAN_POINT ( 'NONE',  ( 1.833485406944043827, 137.8414413349085521, 45.34878176254281357 ) ) ;
#8143=EDGE_CURVE ( 'NONE', #6339, #24736, #22296, .T. ) ;
#8144=VERTEX_POINT ( 'NONE', #6620 ) ;
#8145=ORIENTED_EDGE ( 'NONE', *, *, #619, .T. ) ;
#8146=FACE_OUTER_BOUND ( 'NONE', #25958, .T. ) ;
#8149=CARTESIAN_POINT ( 'NONE',  ( 25.64699802086720837, -103.2460182674614941, -45.70780507840543549 ) ) ;
#8151=CARTESIAN_POINT ( 'NONE',  ( 26.11404676487257603, 90.92995828888199128, 67.46175819463394419 ) ) ;
#8152=ORIENTED_EDGE ( 'NONE', *, *, #15361, .F. ) ;
#8154=CARTESIAN_POINT ( 'NONE',  ( 109.1624594426973118, -0.01595733256932007141, 0.0004639210235604286246 ) ) ;
#8156=VERTEX_POINT ( 'NONE', #8922 ) ;
#8160=B_SPLINE_CURVE_WITH_KNOTS ( 'NONE', 3,
 ( #21178, #18885, #12679, #16877, #1736, #7682, #23365, #23084, #25377, #16581 ),
 .UNSPECIFIED., .F., .F.,
 ( 4, 3, 3, 4 ),
 ( 3.469446951953614189E-18, 0.0002669560319015691651, 0.0005492286108966379842, 0.0008315040496093522703 ),
 .UNSPECIFIED. ) ;
#8161=B_SPLINE_CURVE_WITH_KNOTS ( 'NONE', 3,
 ( #22739, #20688, #3142, #3558 ),
 .UNSPECIFIED., .F., .F.,
 ( 4, 4 ),
 ( 0.000000000000000000, 0.01077107196513907815 ),
 .UNSPECIFIED. ) ;
#8162=CARTESIAN_POINT ( 'NONE',  ( 109.1624594426973260, -0.01476644236456055130, 0.006066618937909619945 ) ) ;
#8164=CARTESIAN_POINT ( 'NONE',  ( 55.79472521941426777, -62.63970324008236190, -37.00555938668325950 ) ) ;
#8165=( BOUNDED_SURFACE ( )  B_SPLINE_SURFACE ( 3, 1, ( 
 ( #2232, #11037 ),
 ( #21693, #8597 ),
 ( #17360, #19800 ),
 ( #6440, #15194 ) ),
 .UNSPECIFIED., .F., .F., .F. ) 
 B_SPLINE_SURFACE_WITH_KNOTS ( ( 4, 4 ),
 ( 2, 2 ),
 ( 0.000000000000000000, 1.000000000000000000 ),
 ( 0.000000000000000000, 1.000000000000000000 ),
 .UNSPECIFIED. ) 
 GEOMETRIC_REPRESENTATION_ITEM ( )  RATIONAL_B_SPLINE_SURFACE ( (
 ( 1.000000000000000000, 1.000000000000000000),
 ( 0.9956975270656955868, 0.8568959468854907557),
 ( 0.9956975270656955868, 0.8568959468854907557),
 ( 1.000000000000000000, 1.000000000000000000) ) ) 
 REPRESENTATION_ITEM ( '' )  SURFACE ( )  );
#8166=CARTESIAN_POINT ( 'NONE',  ( 28.37599760073042532, 112.5845136272808418, -22.09615888373845038 ) ) ;
#8168=B_SPLINE_CURVE_WITH_KNOTS ( 'NONE', 3,
 ( #6632, #13362, #7065, #28475, #13226, #421, #26194, #22161, #6773, #26609 ),
 .UNSPECIFIED., .F., .F.,
 ( 4, 3, 3, 4 ),
 ( 1.962615573354718958E-17, 0.0002669559177086296099, 0.0005339118354151037174, 0.001067817517169159913 ),
 .UNSPECIFIED. ) ;
#8170=CARTESIAN_POINT ( 'NONE',  ( 26.04756280548352265, -107.2904246402797384, 36.02883009343602083 ) ) ;
#8173=CARTESIAN_POINT ( 'NONE',  ( 32.73300124599739291, -3.836798148478013371, -117.5726003567929610 ) ) ;
#8175=FACE_OUTER_BOUND ( 'NONE', #19205, .T. ) ;
#8176=ADVANCED_FACE ( 'NONE', ( #22150 ), #6969, .T. ) ;
#8178=ORIENTED_EDGE ( 'NONE', *, *, #1648, .T. ) ;
#8180=CARTESIAN_POINT ( 'NONE',  ( 109.1586900883932856, 0.002109621908814802386, -0.006819617742893407421 ) ) ;
#8182=CARTESIAN_POINT ( 'NONE',  ( 26.28373643307398666, 17.46364395087465482, 126.3595147275199935 ) ) ;
#8183=CARTESIAN_POINT ( 'NONE',  ( 28.37603512858357035, -112.5845402829047401, -22.09615328858562933 ) ) ;
#8184=CARTESIAN_POINT ( 'NONE',  ( 28.43349137099838941, -8.951033805645545627, 123.9292945876798910 ) ) ;
#8187=ADVANCED_FACE ( 'NONE', ( #13351 ), #5563, .T. ) ;
#8188=ORIENTED_EDGE ( 'NONE', *, *, #24327, .F. ) ;
#8189=DIRECTION ( 'NONE',  ( -0.000000000000000000, 1.000000000000000000, 0.000000000000000000 ) ) ;
#8190=DIRECTION ( 'NONE',  ( -0.5914120900931443270, 0.7903769105750344526, 0.1598001217819390862 ) ) ;
#8191=CARTESIAN_POINT ( 'NONE',  ( 109.1589550718175161, 0.006257602293702357703, 0.004269295012381938564 ) ) ;
#8193=CARTESIAN_POINT ( 'NONE',  ( 2.433796855181205476, -46.34326152018838485, 137.9325382748283744 ) ) ;
#8194=VERTEX_POINT ( 'NONE', #15505 ) ;
#8195=CARTESIAN_POINT ( 'NONE',  ( 109.1592201516379674, -0.005485778713202971689, -0.005631912476303796086 ) ) ;
#8196=CARTESIAN_POINT ( 'NONE',  ( 9.884929003653608603, -150.4771565009630194, -4.203795436553942722 ) ) ;
#8197=ORIENTED_EDGE ( 'NONE', *, *, #9006, .F. ) ;
#8198=CARTESIAN_POINT ( 'NONE',  ( 109.1592201516379674, 0.006536841731962000392, 0.004368284148525281539 ) ) ;
#8199=CARTESIAN_POINT ( 'NONE',  ( 25.64681081121879203, 97.57530875170606066, 56.81519825470789442 ) ) ;
#8203=CARTESIAN_POINT ( 'NONE',  ( 10.93730112726005821, 140.0398180619120865, -56.95489579269602842 ) ) ;
#8204=CARTESIAN_POINT ( 'NONE',  ( 1.833838850855462388, 141.9202662332488387, 30.25705358194902672 ) ) ;
#8207=CARTESIAN_POINT ( 'NONE',  ( 25.86096068574580187, -35.88291140783994138, 107.2082119295151585 ) ) ;
#8208=CARTESIAN_POINT ( 'NONE',  ( 25.64708228042118421, 34.92896069507428081, -107.3728320282185251 ) ) ;
#8209=EDGE_LOOP ( 'NONE', ( #6663, #7745, #21243, #18991 ) ) ;
#8210=EDGE_CURVE ( 'NONE', #22199, #4319, #11349, .T. ) ;
#8211=VERTEX_POINT ( 'NONE', #4307 ) ;
#8213=B_SPLINE_CURVE_WITH_KNOTS ( 'NONE', 3,
 ( #7753, #14769, #1387, #14487, #11908, #20676 ),
 .UNSPECIFIED., .F., .F.,
 ( 4, 2, 4 ),
 ( 1.736890526760486189E-17, 0.0006311571484586111017, 0.001262314296917205507 ),
 .UNSPECIFIED. ) ;
#8214=CARTESIAN_POINT ( 'NONE',  ( 28.43349137099830415, -111.8014342888390047, 54.21282462801730873 ) ) ;
#8215=FACE_OUTER_BOUND ( 'NONE', #28163, .T. ) ;
#8216=B_SPLINE_CURVE_WITH_KNOTS ( 'NONE', 3,
 ( #3355, #20481, #24961, #2932, #20619, #27235, #12143, #9844 ),
 .UNSPECIFIED., .F., .F.,
 ( 4, 2, 2, 4 ),
 ( 6.938893903907228378E-18, 0.0002429592666046700381, 0.0004859185332093331373, 0.0009718370664186709368 ),
 .UNSPECIFIED. ) ;
#8217=CARTESIAN_POINT ( 'NONE',  ( 25.64681081121879203, -84.18689316039996129, -75.24277141833577787 ) ) ;
#8218=CARTESIAN_POINT ( 'NONE',  ( 26.28373643307412166, 126.3595147275199935, -17.46364395087335808 ) ) ;
#8220=B_SPLINE_CURVE_WITH_KNOTS ( 'NONE', 3,
 ( #12429, #1769, #15007, #5835 ),
 .UNSPECIFIED., .F., .F.,
 ( 4, 4 ),
 ( 2.221529986854170653E-16, 0.008383748772659682658 ),
 .UNSPECIFIED. ) ;
#8222=VERTEX_POINT ( 'NONE', #8767 ) ;
#8223=CARTESIAN_POINT ( 'NONE',  ( 55.79472521941428198, -66.75682020267511518, -28.92526238350541945 ) ) ;
#8224=CARTESIAN_POINT ( 'NONE',  ( 109.1624594426973260, -0.007576898892904785146, -0.01405141589343901314 ) ) ;
#8226=FACE_OUTER_BOUND ( 'NONE', #22065, .T. ) ;
#8228=ORIENTED_EDGE ( 'NONE', *, *, #15237, .T. ) ;
#8229=CARTESIAN_POINT ( 'NONE',  ( 1.833485406944043827, 44.33323125129927433, 138.1714136985309835 ) ) ;
#8230=CARTESIAN_POINT ( 'NONE',  ( 26.04756280548353686, -97.45505646068872352, 57.54844730865634261 ) ) ;
#8231=ORIENTED_EDGE ( 'NONE', *, *, #1806, .F. ) ;
#8235=ORIENTED_EDGE ( 'NONE', *, *, #6352, .T. ) ;
#8236=B_SPLINE_CURVE_WITH_KNOTS ( 'NONE', 3,
 ( #6431, #13310, #21962, #4399 ),
 .UNSPECIFIED., .F., .F.,
 ( 4, 4 ),
 ( 3.021408270392383890E-16, 0.008383748772659765924 ),
 .UNSPECIFIED. ) ;
#8238=CARTESIAN_POINT ( 'NONE',  ( 32.73300124599737160, -113.0038235389604466, 32.68291970228198551 ) ) ;
#8239=DIRECTION ( 'NONE',  ( 0.000000000000000000, 0.000000000000000000, 1.000000000000000000 ) ) ;
#8240=EDGE_CURVE ( 'NONE', #16841, #13900, #21924, .T. ) ;
#8243=DIRECTION ( 'NONE',  ( 1.000000000000000000, -0.000000000000000000, 0.000000000000000000 ) ) ;
#8244=EDGE_CURVE ( 'NONE', #19470, #8537, #6848, .T. ) ;
#8245=ORIENTED_EDGE ( 'NONE', *, *, #13520, .F. ) ;
#8246=CARTESIAN_POINT ( 'NONE',  ( 2.433796855181205476, 1.451562450951669803, -145.5024947199069345 ) ) ;
#8248=EDGE_CURVE ( 'NONE', #11422, #20246, #22974, .T. ) ;
#8250=CARTESIAN_POINT ( 'NONE',  ( 1.833206308920083183, -138.2356393957898888, 44.13245285122219030 ) ) ;
#8251=CARTESIAN_POINT ( 'NONE',  ( 119.2224693531408803, 90.00000000000005684, 39.99999999999999289 ) ) ;
#8252=CARTESIAN_POINT ( 'NONE',  ( 13.36082413113063083, 84.67697637120581078, -127.3428651193239602 ) ) ;
#8256=EDGE_LOOP ( 'NONE', ( #18878, #24575, #6089, #20570 ) ) ;
#8257=EDGE_LOOP ( 'NONE', ( #3573, #23533, #17926, #21410 ) ) ;
#8263=B_SPLINE_CURVE_WITH_KNOTS ( 'NONE', 3,
 ( #6747, #24302, #13336, #22135, #23763, #4009, #4992, #22576, #13918, #390 ),
 .UNSPECIFIED., .F., .F.,
 ( 4, 3, 3, 4 ),
 ( 6.938893903907228378E-18, 0.0002669560319015686230, 0.0005492286108966328885, 0.0008315040496093396936 ),
 .UNSPECIFIED. ) ;
#8269=CARTESIAN_POINT ( 'NONE',  ( 25.64681081121880624, -46.30456157731397582, 102.9795863647027119 ) ) ;
#8270=CARTESIAN_POINT ( 'NONE',  ( 30.59141879584279522, 55.75104644134894016, 101.9665761624291775 ) ) ;
#8271=CARTESIAN_POINT ( 'NONE',  ( 26.11404676487259024, 102.9690087468808031, -47.08215554553414961 ) ) ;
#8273=CARTESIAN_POINT ( 'NONE',  ( 25.64660436782564190, -112.3516544824817203, -11.22538561722002548 ) ) ;
#8274=ORIENTED_EDGE ( 'NONE', *, *, #6104, .T. ) ;
#8275=ORIENTED_EDGE ( 'NONE', *, *, #4081, .T. ) ;
#8276=CARTESIAN_POINT ( 'NONE',  ( 109.1586059443104944, 0.001921075557427549818, 0.006808232911144248591 ) ) ;
#8277=CARTESIAN_POINT ( 'NONE',  ( 6.224689322667647851, -126.9212313063849820, 76.23997225729220872 ) ) ;
#8279=B_SPLINE_CURVE_WITH_KNOTS ( 'NONE', 3,
 ( #12548, #7689, #5809, #20904 ),
 .UNSPECIFIED., .F., .F.,
 ( 4, 4 ),
 ( 0.000000000000000000, 0.01077107196513889600 ),
 .UNSPECIFIED. ) ;
#8280=FACE_OUTER_BOUND ( 'NONE', #9487, .T. ) ;
#8281=CARTESIAN_POINT ( 'NONE',  ( 25.86096068574578766, 90.87263912324419834, 67.25583614083872419 ) ) ;
#8282=ORIENTED_EDGE ( 'NONE', *, *, #8645, .T. ) ;
#8283=CARTESIAN_POINT ( 'NONE',  ( 2.108985857320932578, 137.7807691131293950, -46.11505917359297513 ) ) ;
#8287=CARTESIAN_POINT ( 'NONE',  ( 2.063896406836605024, -28.88716984836217350, -142.3682421260910473 ) ) ;
#8288=VERTEX_POINT ( 'NONE', #7770 ) ;
#8290=CARTESIAN_POINT ( 'NONE',  ( 2.263178113027048077, -13.80342493153413130, -144.7392881653025825 ) ) ;
#8291=EDGE_CURVE ( 'NONE', #25686, #1993, #20911, .T. ) ;
#8292=EDGE_CURVE ( 'NONE', #1116, #17852, #28091, .T. ) ;
#8293=ORIENTED_EDGE ( 'NONE', *, *, #23171, .F. ) ;
#8294=AXIS2_PLACEMENT_3D ( 'NONE', #18866, #20881, #5922 ) ;
#8295=LINE ( 'NONE', #23151, #13323 ) ;
#8297=VECTOR ( 'NONE', #13692, 999.9999999999998863 ) ;
#8299=VECTOR ( 'NONE', #23578, 1000.000000000000114 ) ;
#8300=CARTESIAN_POINT ( 'NONE',  ( 26.11404676487257603, -110.9778746459745520, -22.43340081644882389 ) ) ;
#8301=CARTESIAN_POINT ( 'NONE',  ( 30.58324630866349025, 106.6567942264195494, 57.02364853894509622 ) ) ;
#8302=LINE ( 'NONE', #2078, #8299 ) ;
#8303=CARTESIAN_POINT ( 'NONE',  ( 19.66333377628710366, -4.491394265033200384, 137.6761449113043341 ) ) ;
#8304=ORIENTED_EDGE ( 'NONE', *, *, #16257, .F. ) ;
#8305=CARTESIAN_POINT ( 'NONE',  ( 1.833603222531970722, 125.4455769441942863, 72.93978951866027671 ) ) ;
#8311=DIRECTION ( 'NONE',  ( -0.5946245182733607137, 0.6487139525627779735, -0.4749651461092186389 ) ) ;
#8312=LINE ( 'NONE', #12753, #3777 ) ;
#8313=CARTESIAN_POINT ( 'NONE',  ( 1.833485406944057594, -137.8414413349088932, 45.34878176254188276 ) ) ;
#8314=CARTESIAN_POINT ( 'NONE',  ( 28.43349137099826862, 17.01091693849741304, 123.0821667346709063 ) ) ;
#8315=CARTESIAN_POINT ( 'NONE',  ( 1.894214914920982595, 125.2241265685480869, -73.39939580274808861 ) ) ;
#8318=VERTEX_POINT ( 'NONE', #1131 ) ;
#8320=ORIENTED_EDGE ( 'NONE', *, *, #27548, .T. ) ;
#8323=VECTOR ( 'NONE', #7482, 1000.000000000000000 ) ;
#8324=CARTESIAN_POINT ( 'NONE',  ( 1.832998868059890096, 145.1092030902949830, -0.5339089137752986991 ) ) ;
#8325=CARTESIAN_POINT ( 'NONE',  ( 25.86096068574580542, -110.7864907291860561, 22.52859312382151558 ) ) ;
#8326=CARTESIAN_POINT ( 'NONE',  ( 1.833838850855473490, 117.3439621615263917, 85.36536653357383386 ) ) ;
#8327=VECTOR ( 'NONE', #8482, 1000.000000000000000 ) ;
#8330=VECTOR ( 'NONE', #2705, 1000.000000000000114 ) ;
#8333=EDGE_CURVE ( 'NONE', #8318, #7281, #2708, .T. ) ;
#8334=B_SPLINE_CURVE_WITH_KNOTS ( 'NONE', 3,
 ( #8835, #13000, #2328, #22216, #8414, #17445, #23824, #8546 ),
 .UNSPECIFIED., .F., .F.,
 ( 4, 2, 2, 4 ),
 ( 3.469446951953614189E-18, 0.0002429588503611210509, 0.0004859177007222386323, 0.0009718354014444772647 ),
 .UNSPECIFIED. ) ;
#8335=( BOUNDED_SURFACE ( )  B_SPLINE_SURFACE ( 3, 1, ( 
 ( #1510, #10446 ),
 ( #14745, #5705 ),
 ( #14605, #17043 ),
 ( #10170, #12173 ) ),
 .UNSPECIFIED., .F., .F., .F. ) 
 B_SPLINE_SURFACE_WITH_KNOTS ( ( 4, 4 ),
 ( 2, 2 ),
 ( 0.000000000000000000, 1.000000000000000000 ),
 ( 0.000000000000000000, 1.000000000000000000 ),
 .UNSPECIFIED. ) 
 GEOMETRIC_REPRESENTATION_ITEM ( )  RATIONAL_B_SPLINE_SURFACE ( (
 ( 1.000000000000000000, 1.000000000000000000),
 ( 0.9956975270656955868, 0.8568959468854907557),
 ( 0.9956975270656955868, 0.8568959468854907557),
 ( 1.000000000000000000, 1.000000000000000000) ) ) 
 REPRESENTATION_ITEM ( '' )  SURFACE ( )  );
#8336=VERTEX_POINT ( 'NONE', #27167 ) ;
#8337=DIRECTION ( 'NONE',  ( 0.000000000000000000, 0.000000000000000000, 1.000000000000000000 ) ) ;
#8340=CARTESIAN_POINT ( 'NONE',  ( 9.884929003653608603, -57.36421526887068012, -139.1775604444709700 ) ) ;
#8342=FACE_OUTER_BOUND ( 'NONE', #21607, .T. ) ;
#8343=EDGE_CURVE ( 'NONE', #10583, #20165, #2352, .T. ) ;
#8345=VECTOR ( 'NONE', #13768, 1000.000000000000000 ) ;
#8346=FACE_OUTER_BOUND ( 'NONE', #706, .T. ) ;
#8347=CARTESIAN_POINT ( 'NONE',  ( 1.834118845439484335, 29.99597360113071787, 141.9759513273465643 ) ) ;
#8351=CARTESIAN_POINT ( 'NONE',  ( 32.73300124599732186, 0.000000000000000000, 0.000000000000000000 ) ) ;
#8352=CARTESIAN_POINT ( 'NONE',  ( 26.04756280548354042, -47.04636360340759182, -102.9366382251197507 ) ) ;
#8353=CARTESIAN_POINT ( 'NONE',  ( 5.340103556456459621, -146.8647350107031002, 13.12023871801074293 ) ) ;
#8354=ORIENTED_EDGE ( 'NONE', *, *, #17942, .T. ) ;
#8357=EDGE_LOOP ( 'NONE', ( #18129, #21226, #21513, #6144 ) ) ;
#8359=CARTESIAN_POINT ( 'NONE',  ( 26.11404676487257603, 84.89295829319495112, 74.91683232331003239 ) ) ;
#8362=CARTESIAN_POINT ( 'NONE',  ( 1.893872463202028511, -141.7768406633802840, -31.10971550360730120 ) ) ;
#8363=EDGE_CURVE ( 'NONE', #2427, #23708, #28018, .T. ) ;
#8365=CARTESIAN_POINT ( 'NONE',  ( 28.37644542392842695, -124.0168596762486999, 8.957364412599812198 ) ) ;
#8366=ORIENTED_EDGE ( 'NONE', *, *, #17857, .F. ) ;
#8368=CARTESIAN_POINT ( 'NONE',  ( 1.832998868059858122, -0.5339089137758143977, 145.1092030902949830 ) ) ;
#8369=B_SPLINE_CURVE_WITH_KNOTS ( 'NONE', 3,
 ( #28468, #6216, #10664, #24185, #26188, #23783, #1724, #23642, #26054, #17541 ),
 .UNSPECIFIED., .F., .F.,
 ( 4, 3, 3, 4 ),
 ( 5.003707553108401214E-17, 0.0002669559177086323746, 0.0005339118354151100058, 0.001067817517169148203 ),
 .UNSPECIFIED. ) ;
#8370=CARTESIAN_POINT ( 'NONE',  ( 32.73300124599741423, 113.0038235389606314, -32.68291970228113996 ) ) ;
#8371=ORIENTED_EDGE ( 'NONE', *, *, #8710, .T. ) ;
#8373=B_SPLINE_CURVE_WITH_KNOTS ( 'NONE', 3,
 ( #22342, #303, #4341, #17850, #22040, #13120 ),
 .UNSPECIFIED., .F., .F.,
 ( 4, 2, 4 ),
 ( 1.389302603484999005E-17, 0.0006311571484586052470, 0.001262314296917187292 ),
 .UNSPECIFIED. ) ;
#8374=CARTESIAN_POINT ( 'NONE',  ( 25.69398547355840989, -97.43788956976189297, 57.11291030433619653 ) ) ;
#8375=ORIENTED_EDGE ( 'NONE', *, *, #1465, .T. ) ;
#8378=VERTEX_POINT ( 'NONE', #28157 ) ;
#8379=ORIENTED_EDGE ( 'NONE', *, *, #9859, .F. ) ;
#8380=( BOUNDED_SURFACE ( )  B_SPLINE_SURFACE ( 3, 1, ( 
 ( #22867, #15792 ),
 ( #20536, #24877 ),
 ( #27148, #16072 ),
 ( #24601, #17796 ) ),
 .UNSPECIFIED., .F., .F., .F. ) 
 B_SPLINE_SURFACE_WITH_KNOTS ( ( 4, 4 ),
 ( 2, 2 ),
 ( 0.000000000000000000, 1.000000000000000000 ),
 ( 0.000000000000000000, 1.000000000000000000 ),
 .UNSPECIFIED. ) 
 GEOMETRIC_REPRESENTATION_ITEM ( )  RATIONAL_B_SPLINE_SURFACE ( (
 ( 1.000000000000000000, 1.000000000000000000),
 ( 0.9960225298536222738, 0.9999952330161893110),
 ( 0.9960225298536222738, 0.9999952330161893110),
 ( 1.000000000000000000, 1.000000000000000000) ) ) 
 REPRESENTATION_ITEM ( '' )  SURFACE ( )  );
#8381=CIRCLE ( 'NONE', #15698, 151.1787379149930359 ) ;
#8384=CARTESIAN_POINT ( 'NONE',  ( 13.84597867724975551, -140.9259526407712713, 40.76072889493709539 ) ) ;
#8385=CARTESIAN_POINT ( 'NONE',  ( 109.1721716018069515, -0.01488186354165290347, 0.008358834333178027584 ) ) ;
#8386=CARTESIAN_POINT ( 'NONE',  ( 16.05277956358202474, 92.36732600443350805, -109.5668455727251285 ) ) ;
#8387=VERTEX_POINT ( 'NONE', #6029 ) ;
#8388=CARTESIAN_POINT ( 'NONE',  ( 1.833485406944057594, -59.50871042846138437, -132.3460930279897241 ) ) ;
#8389=ORIENTED_EDGE ( 'NONE', *, *, #295, .F. ) ;
#8390=DIRECTION ( 'NONE',  ( -1.000000000000000000, -0.000000000000000000, -0.000000000000000000 ) ) ;
#8391=B_SPLINE_CURVE_WITH_KNOTS ( 'NONE', 3,
 ( #12038, #12448, #25282, #10325, #23412, #5992, #18794 ),
 .UNSPECIFIED., .F., .F.,
 ( 4, 3, 4 ),
 ( 3.642919299551294898E-17, 0.02816610861753242323, 0.04000277880656207680 ),
 .UNSPECIFIED. ) ;
#8393=CARTESIAN_POINT ( 'NONE',  ( 1.833838850855475933, 97.16351016226039405, -107.7780290788686983 ) ) ;
#8394=CARTESIAN_POINT ( 'NONE',  ( 109.1721716018069515, 0.01673651515802103765, -0.003350975118861028619 ) ) ;
#8396=CARTESIAN_POINT ( 'NONE',  ( 109.1592201516379674, -0.006044422199822568030, 0.005027640251767196387 ) ) ;
#8397=CARTESIAN_POINT ( 'NONE',  ( -40.00000000000000000, 0.000000000000000000, 0.000000000000000000 ) ) ;
#8399=ORIENTED_EDGE ( 'NONE', *, *, #3812, .T. ) ;
#8400=CARTESIAN_POINT ( 'NONE',  ( 2.433796855181233454, 74.00833731765563073, 125.2830755159756677 ) ) ;
#8401=DIRECTION ( 'NONE',  ( 0.000000000000000000, 0.000000000000000000, 1.000000000000000000 ) ) ;
#8402=ORIENTED_EDGE ( 'NONE', *, *, #4747, .F. ) ;
#8403=ORIENTED_EDGE ( 'NONE', *, *, #13864, .T. ) ;
#8405=ORIENTED_EDGE ( 'NONE', *, *, #1960, .F. ) ;
#8411=DIRECTION ( 'NONE',  ( 0.5914120900931443270, -0.8027508043202544741, 0.07630783612999995913 ) ) ;
#8412=CARTESIAN_POINT ( 'NONE',  ( 1.831572820252008738, 116.8148281295969326, 86.09108691067808650 ) ) ;
#8413=CARTESIAN_POINT ( 'NONE',  ( -90.83090735639699176, 0.000000000000000000, 0.000000000000000000 ) ) ;
#8414=CARTESIAN_POINT ( 'NONE',  ( 25.73574536432417403, 24.27578079247314946, -110.3312765349290743 ) ) ;
#8415=FACE_OUTER_BOUND ( 'NONE', #5201, .T. ) ;
#8417=CARTESIAN_POINT ( 'NONE',  ( 26.11404676487259024, 74.91683232331092768, -84.89295829319416953 ) ) ;
#8419=ORIENTED_EDGE ( 'NONE', *, *, #22905, .T. ) ;
#8422=LINE ( 'NONE', #19209, #1429 ) ;
#8423=CARTESIAN_POINT ( 'NONE',  ( 25.64681081121879203, -110.5293738517606954, -23.06870491922435207 ) ) ;
#8425=EDGE_CURVE ( 'NONE', #15441, #16457, #1549, .T. ) ;
#8426=ORIENTED_EDGE ( 'NONE', *, *, #22772, .F. ) ;
#8427=CARTESIAN_POINT ( 'NONE',  ( 25.64681081121879203, 97.57530875170684226, -56.81519825470653018 ) ) ;
#8428=CIRCLE ( 'NONE', #15762, 111.9614997405030152 ) ;
#8429=CARTESIAN_POINT ( 'NONE',  ( 10.93730112726002979, 104.7670965581027644, -108.9902118373731241 ) ) ;
#8435=VERTEX_POINT ( 'NONE', #18828 ) ;
#8436=EDGE_LOOP ( 'NONE', ( #14458, #8076, #888, #20921 ) ) ;
#8439=VERTEX_POINT ( 'NONE', #7918 ) ;
#8442=CONICAL_SURFACE ( 'NONE', #24548, 117.6351876552689504, 0.9945805576725580410 ) ;
#8443=CARTESIAN_POINT ( 'NONE',  ( 109.1778270068192853, 0.003465086990435488432, -0.008646067828082850890 ) ) ;
#8444=CARTESIAN_POINT ( 'NONE',  ( 25.81918753295378011, -107.2019194967338365, 35.81374485821577736 ) ) ;
#8448=CARTESIAN_POINT ( 'NONE',  ( 32.73300124599734318, 114.2056417606548706, 28.19767303745648945 ) ) ;
#8449=FACE_OUTER_BOUND ( 'NONE', #12806, .T. ) ;
#8450=ORIENTED_EDGE ( 'NONE', *, *, #19202, .F. ) ;
#8451=B_SPLINE_CURVE_WITH_KNOTS ( 'NONE', 3,
 ( #13534, #9518, #13965, #15685, #729, #16126 ),
 .UNSPECIFIED., .F., .F.,
 ( 4, 2, 4 ),
 ( 3.035766082959412415E-18, 0.0006311636237756829224, 0.001262327247551362809 ),
 .UNSPECIFIED. ) ;
#8452=ORIENTED_EDGE ( 'NONE', *, *, #17546, .T. ) ;
#8453=CARTESIAN_POINT ( 'NONE',  ( 5.340103579038250281, -139.5040934216402775, 47.74933483136832990 ) ) ;
#8455=FACE_OUTER_BOUND ( 'NONE', #4484, .T. ) ;
#8457=CARTESIAN_POINT ( 'NONE',  ( 32.73300124599734318, 16.10546300444822165, 116.5274707358856290 ) ) ;
#8458=CARTESIAN_POINT ( 'NONE',  ( 2.433796855181205476, 98.43889364294005873, -107.1581411821775305 ) ) ;
#8459=CARTESIAN_POINT ( 'NONE',  ( 25.98107933586725338, 97.42660475433947909, 57.50946808479267958 ) ) ;
#8461=EDGE_CURVE ( 'NONE', #431, #21575, #3374, .T. ) ;
#8463=ORIENTED_EDGE ( 'NONE', *, *, #9667, .F. ) ;
#8464=CARTESIAN_POINT ( 'NONE',  ( 28.37599760073042177, 13.77583212279483682, -113.9023239246301529 ) ) ;
#8466=EDGE_CURVE ( 'NONE', #4937, #19738, #1403, .T. ) ;
#8467=FACE_OUTER_BOUND ( 'NONE', #21437, .T. ) ;
#8469=CARTESIAN_POINT ( 'NONE',  ( 26.04756280548354397, -55.62433096787491849, 98.56594554799102070 ) ) ;
#8470=ORIENTED_EDGE ( 'NONE', *, *, #1105, .T. ) ;
#8472=CARTESIAN_POINT ( 'NONE',  ( 55.49584447822657296, 15.34602024131385711, -70.91003759562300957 ) ) ;
#8474=CARTESIAN_POINT ( 'NONE',  ( 1.833206308920053207, 116.9567745381559973, 85.89457656603909186 ) ) ;
#8476=CARTESIAN_POINT ( 'NONE',  ( 1.833485406944043827, 44.33323125129927433, 138.1714136985309835 ) ) ;
#8477=CARTESIAN_POINT ( 'NONE',  ( 1.833206310202329492, -116.9567751109825195, 85.89457578512777047 ) ) ;
#8478=CARTESIAN_POINT ( 'NONE',  ( 1.833206308920081185, 125.2945011813205127, 73.19872517709758597 ) ) ;
#8481=CARTESIAN_POINT ( 'NONE',  ( 25.64704443564077962, 23.34498572103320058, 110.4715096490033375 ) ) ;
#8482=DIRECTION ( 'NONE',  ( -1.000000000000000000, -0.000000000000000000, -0.000000000000000000 ) ) ;
#8483=CARTESIAN_POINT ( 'NONE',  ( 1.833485406944043827, -132.7804117027891948, 58.53321471326832182 ) ) ;
#8486=CARTESIAN_POINT ( 'NONE',  ( 8.186469777910922119, -19.05650978729101652, -148.1306754055310932 ) ) ;
#8489=EDGE_CURVE ( 'NONE', #18715, #13261, #13660, .T. ) ;
#8490=ORIENTED_EDGE ( 'NONE', *, *, #19272, .F. ) ;
#8491=ORIENTED_EDGE ( 'NONE', *, *, #26214, .F. ) ;
#8494=CARTESIAN_POINT ( 'NONE',  ( 1.831572820252008738, 16.14965423926401655, -144.2101521542828664 ) ) ;
#8495=CARTESIAN_POINT ( 'NONE',  ( 1.831572820252009626, -84.49389457294216754, 117.9752562883663813 ) ) ;
#8496=B_SPLINE_CURVE_WITH_KNOTS ( 'NONE', 3,
 ( #16089, #13643, #835, #18238, #22741, #9187, #2560, #24464, #15810, #3007 ),
 .UNSPECIFIED., .F., .F.,
 ( 4, 3, 3, 4 ),
 ( 3.122502256758253386E-17, 0.0002669559177086182800, 0.0005339118354150958028, 0.001067817517169165117 ),
 .UNSPECIFIED. ) ;
#8498=CARTESIAN_POINT ( 'NONE',  ( 32.73300124599740002, 62.10906484417377271, -99.90245962373766986 ) ) ;
#8500=ORIENTED_EDGE ( 'NONE', *, *, #28280, .T. ) ;
#8503=CARTESIAN_POINT ( 'NONE',  ( 25.64700659047698750, 23.69811251893883508, -110.3963107228933183 ) ) ;
#8508=ORIENTED_EDGE ( 'NONE', *, *, #27558, .F. ) ;
#8510=DIRECTION ( 'NONE',  ( 0.5946245182733607137, -0.7655593692109038395, 0.2456431038754731122 ) ) ;
#8512=ORIENTED_EDGE ( 'NONE', *, *, #17344, .T. ) ;
#8513=ORIENTED_EDGE ( 'NONE', *, *, #17543, .T. ) ;
#8514=B_SPLINE_CURVE_WITH_KNOTS ( 'NONE', 3,
 ( #14271, #12404, #5952, #16594, #3780, #23092, #25388, #5664 ),
 .UNSPECIFIED., .F., .F.,
 ( 4, 2, 2, 4 ),
 ( 1.250926888277100303E-17, 0.0002429592666046849459, 0.0004859185332093573693, 0.0009718370664187002102 ),
 .UNSPECIFIED. ) ;
#8515=B_SPLINE_CURVE_WITH_KNOTS ( 'NONE', 3,
 ( #24816, #469, #13702, #18019, #7116, #5069, #22506, #20328 ),
 .UNSPECIFIED., .F., .F.,
 ( 4, 2, 2, 4 ),
 ( 6.938893903907228378E-18, 0.0002429588503611197770, 0.0004859177007222326150, 0.0009718354014444818183 ),
 .UNSPECIFIED. ) ;
#8516=CARTESIAN_POINT ( 'NONE',  ( 1.832998868059890096, -117.7096351258393128, 84.86110816369568965 ) ) ;
#8517=DIRECTION ( 'NONE',  ( -1.000000000000000000, -0.000000000000000000, -0.000000000000000000 ) ) ;
#8520=VERTEX_POINT ( 'NONE', #28293 ) ;
#8521=EDGE_CURVE ( 'NONE', #2978, #11691, #17909, .T. ) ;
#8522=CARTESIAN_POINT ( 'NONE',  ( 1.893872463202068923, -132.2106029832898173, -59.90695624048819212 ) ) ;
#8523=EDGE_CURVE ( 'NONE', #1087, #14920, #1691, .T. ) ;
#8525=CARTESIAN_POINT ( 'NONE',  ( 9.884929003653608603, 4.203795436554465859, -150.4771565009629910 ) ) ;
#8526=CARTESIAN_POINT ( 'NONE',  ( 10.93730112725939030, 140.0398180619108075, 56.95489579269806057 ) ) ;
#8529=EDGE_CURVE ( 'NONE', #25504, #5185, #12952, .T. ) ;
#8530=CARTESIAN_POINT ( 'NONE',  ( 13.84597867724970754, 146.3210145202070009, -10.56985607909651925 ) ) ;
#8531=EDGE_CURVE ( 'NONE', #9075, #21777, #15692, .T. ) ;
#8535=CARTESIAN_POINT ( 'NONE',  ( 25.87036335909426654, -24.47383578007052662, -110.3794299719623098 ) ) ;
#8537=VERTEX_POINT ( 'NONE', #17782 ) ;
#8540=CARTESIAN_POINT ( 'NONE',  ( 2.433796855181219243, -145.5024947199069913, 1.451562450949123395 ) ) ;
#8541=CARTESIAN_POINT ( 'NONE',  ( 1.832998868059890096, 44.33343224355417789, -138.1720401012262585 ) ) ;
#8542=CARTESIAN_POINT ( 'NONE',  ( 2.433796855181233454, 16.65276281464563723, 144.5536872373192807 ) ) ;
#8543=CARTESIAN_POINT ( 'NONE',  ( 2.433796855181233454, 145.5024947199069913, -1.451562450950139249 ) ) ;
#8545=EDGE_CURVE ( 'NONE', #1646, #11749, #13298, .T. ) ;
#8546=CARTESIAN_POINT ( 'NONE',  ( 26.11404676487259024, 24.64483677385001315, -110.5078194225158654 ) ) ;
#8547=CARTESIAN_POINT ( 'NONE',  ( 109.1624594426973118, 0.009004164758064552368, -0.01318243916934998781 ) ) ;
#8548=CARTESIAN_POINT ( 'NONE',  ( 109.1778270068192853, -0.002278716897421693890, 0.009031542838317245525 ) ) ;
#8551=ORIENTED_EDGE ( 'NONE', *, *, #7365, .F. ) ;
#8552=CARTESIAN_POINT ( 'NONE',  ( 25.73574536432414561, -57.18187897120868968, 97.42965068311210075 ) ) ;
#8555=CARTESIAN_POINT ( 'NONE',  ( 2.263178607246686624, -1.401567185705457463, -145.3892423243864584 ) ) ;
#8556=CARTESIAN_POINT ( 'NONE',  ( 1.833485406944043827, 96.69979900902318093, -108.1939177044916107 ) ) ;
#8557=ORIENTED_EDGE ( 'NONE', *, *, #26796, .T. ) ;
#8559=CARTESIAN_POINT ( 'NONE',  ( 1.893872463202031398, -144.2520230501565095, -16.11957794552919054 ) ) ;
#8564=ORIENTED_EDGE ( 'NONE', *, *, #22967, .T. ) ;
#8565=CARTESIAN_POINT ( 'NONE',  ( 109.1592201516379674, 0.006044422199822535938, -0.005027640251767235419 ) ) ;
#8566=ORIENTED_EDGE ( 'NONE', *, *, #22772, .T. ) ;
#8567=B_SPLINE_CURVE_WITH_KNOTS ( 'NONE', 3,
 ( #23323, #13158, #16692, #14517 ),
 .UNSPECIFIED., .F., .F.,
 ( 4, 4 ),
 ( 3.539284956047283840E-16, 0.01077107486149763566 ),
 .UNSPECIFIED. ) ;
#8569=CARTESIAN_POINT ( 'NONE',  ( -90.83090735639699176, 0.000000000000000000, -20.00000000000000000 ) ) ;
#8571=CARTESIAN_POINT ( 'NONE',  ( 109.1587776205901577, -0.002904816147418966092, -0.006729130500857893188 ) ) ;
#8574=CARTESIAN_POINT ( 'NONE',  ( 25.64681081121879203, -12.21581276189731469, -112.2483031020014579 ) ) ;
#8576=CARTESIAN_POINT ( 'NONE',  ( 2.063896406836609909, -116.7302989755743141, 86.47093297168963488 ) ) ;
#8580=CARTESIAN_POINT ( 'NONE',  ( 1.833838850855474600, 125.6242502389386431, 72.63194208529516516 ) ) ;
#8581=CARTESIAN_POINT ( 'NONE',  ( 109.1587776205901861, 0.003057017121600544719, 0.006661366261223563776 ) ) ;
#8583=CARTESIAN_POINT ( 'NONE',  ( 25.98552792386801968, -112.3992180166319343, 12.89843290883488969 ) ) ;
#8584=EDGE_CURVE ( 'NONE', #17077, #1421, #20651, .T. ) ;
#8585=ORIENTED_EDGE ( 'NONE', *, *, #4453, .T. ) ;
#8587=CARTESIAN_POINT ( 'NONE',  ( 30.58324630866353644, 116.1819705588612663, 33.60235057864013442 ) ) ;
#8588=CARTESIAN_POINT ( 'NONE',  ( 1.833485406944043827, -73.01664920993054864, 125.4007332306543105 ) ) ;
#8590=EDGE_CURVE ( 'NONE', #4923, #5555, #7162, .T. ) ;
#8591=CARTESIAN_POINT ( 'NONE',  ( 13.84597867724988518, 69.17016226639039189, 129.3717503931851240 ) ) ;
#8592=CARTESIAN_POINT ( 'NONE',  ( 5.340103579038085968, 100.3626145943033663, 108.0219267094749114 ) ) ;
#8593=CARTESIAN_POINT ( 'NONE',  ( 26.04756280548353686, 90.90573670389328242, -67.42001818240375144 ) ) ;
#8595=CARTESIAN_POINT ( 'NONE',  ( 2.108393763691192913, -107.1124103264142775, -98.16799842733358616 ) ) ;
#8596=CARTESIAN_POINT ( 'NONE',  ( 109.1586900883932856, -0.0001010081143884683351, 0.007137750914552287197 ) ) ;
#8597=CARTESIAN_POINT ( 'NONE',  ( 1.831572820252008738, -59.92262167723526289, 132.1614873090347260 ) ) ;
#8598=CARTESIAN_POINT ( 'NONE',  ( 5.340103556456493372, -147.4316330165020190, -2.303180381359786644 ) ) ;
#8599=CARTESIAN_POINT ( 'NONE',  ( 1.833838848569431468, 117.5008734796311529, 85.14939661881604138 ) ) ;
#8601=LINE ( 'NONE', #6731, #5718 ) ;
#8602=CARTESIAN_POINT ( 'NONE',  ( 1.833750490713681458, 15.43355859895851445, -144.2866297127912105 ) ) ;
#8604=CARTESIAN_POINT ( 'NONE',  ( 2.263178113027036531, 116.7985471375932036, 86.59154384226214063 ) ) ;
#8606=CARTESIAN_POINT ( 'NONE',  ( 25.64681081121879203, 66.03065707439057519, -91.59071981940505225 ) ) ;
#8607=DIRECTION ( 'NONE',  ( 0.000000000000000000, 0.000000000000000000, 1.000000000000000000 ) ) ;
#8608=CARTESIAN_POINT ( 'NONE',  ( 25.64704443564077607, 97.71717520928676493, 56.57116289738639381 ) ) ;
#8609=CARTESIAN_POINT ( 'NONE',  ( 2.263178113027023652, 125.2099934853450947, 73.90841366068426055 ) ) ;
#8611=CARTESIAN_POINT ( 'NONE',  ( 25.87036335909426299, 55.67065048714147935, -98.40409479825380856 ) ) ;
#8612=CARTESIAN_POINT ( 'NONE',  ( 119.2224693531408803, -90.00000000000005684, 39.99999999999997158 ) ) ;
#8616=ADVANCED_FACE ( 'NONE', ( #5258 ), #5405, .F. ) ;
#8617=CARTESIAN_POINT ( 'NONE',  ( 2.063896406836609909, 46.16709813092625581, 137.7380992975104164 ) ) ;
#8618=EDGE_CURVE ( 'NONE', #14205, #12120, #17428, .T. ) ;
#8619=CARTESIAN_POINT ( 'NONE',  ( 9.884929003653608603, 97.56484214660623877, 114.6392083957121315 ) ) ;
#8620=DIRECTION ( 'NONE',  ( 0.000000000000000000, -3.469446951953603342E-16, 1.000000000000000000 ) ) ;
#8621=CARTESIAN_POINT ( 'NONE',  ( 6.224689322667630975, 62.55544044765430556, -134.1951906609232594 ) ) ;
#8623=VERTEX_POINT ( 'NONE', #512 ) ;
#8626=CARTESIAN_POINT ( 'NONE',  ( 26.11404676487259024, 108.0249973236467582, 33.91085499298413453 ) ) ;
#8627=FACE_OUTER_BOUND ( 'NONE', #8127, .T. ) ;
#8628=FACE_OUTER_BOUND ( 'NONE', #15894, .T. ) ;
#8629=CARTESIAN_POINT ( 'NONE',  ( 55.79472521941428198, -53.57698701322248525, 49.22042574086407996 ) ) ;
#8631=EDGE_LOOP ( 'NONE', ( #1713, #12980, #25503, #16720 ) ) ;
#8632=CARTESIAN_POINT ( 'NONE',  ( 2.108393763691198242, 132.2055356348361670, 60.26375949664234355 ) ) ;
#8637=CARTESIAN_POINT ( 'NONE',  ( 30.58324630866343696, -100.1119227962715996, -67.85993782330868385 ) ) ;
#8639=ORIENTED_EDGE ( 'NONE', *, *, #4847, .F. ) ;
#8641=ORIENTED_EDGE ( 'NONE', *, *, #22090, .T. ) ;
#8642=ADVANCED_FACE ( 'NONE', ( #9308 ), #27181, .T. ) ;
#8643=CARTESIAN_POINT ( 'NONE',  ( 26.28373643307413232, -35.44121223574943258, 122.5382646256986590 ) ) ;
#8644=CARTESIAN_POINT ( 'NONE',  ( 1.833485406944043827, 144.3694338680884925, 14.63699153649408480 ) ) ;
#8645=EDGE_CURVE ( 'NONE', #17323, #16951, #6798, .T. ) ;
#8646=CARTESIAN_POINT ( 'NONE',  ( 26.11404676487257603, 65.63269960453364149, -92.25884714080342519 ) ) ;
#8647=EDGE_CURVE ( 'NONE', #15393, #27833, #25674, .T. ) ;
#8648=B_SPLINE_CURVE_WITH_KNOTS ( 'NONE', 3,
 ( #28449, #28316, #13334, #19822, #8754, #26168 ),
 .UNSPECIFIED., .F., .F.,
 ( 4, 2, 4 ),
 ( 6.942281208919283290E-18, 0.0006311571484586111017, 0.001262314296917215264 ),
 .UNSPECIFIED. ) ;
#8649=CARTESIAN_POINT ( 'NONE',  ( 1.833809397773874084, 72.40070666294590751, 125.7576368866145629 ) ) ;
#8651=ORIENTED_EDGE ( 'NONE', *, *, #13617, .T. ) ;
#8653=ORIENTED_EDGE ( 'NONE', *, *, #25532, .T. ) ;
#8654=CARTESIAN_POINT ( 'NONE',  ( 1.833206310202325051, 126.0392056382542165, 71.90885922990194956 ) ) ;
#8657=DIRECTION ( 'NONE',  ( -1.000000000000000000, -0.000000000000000000, -0.000000000000000000 ) ) ;
#8660=CARTESIAN_POINT ( 'NONE',  ( 2.433796855181219243, -28.83182736670634583, 142.6247129145647534 ) ) ;
#8664=ORIENTED_EDGE ( 'NONE', *, *, #16799, .T. ) ;
#8665=VECTOR ( 'NONE', #237, 1000.000000000000000 ) ;
#8666=ORIENTED_EDGE ( 'NONE', *, *, #1278, .F. ) ;
#8667=CARTESIAN_POINT ( 'NONE',  ( 1.894214914920957948, -108.5033568857718649, -96.41356089048393585 ) ) ;
#8668=CARTESIAN_POINT ( 'NONE',  ( 55.49584447822657296, -48.34726110739950400, -54.09506550945674519 ) ) ;
#8670=ORIENTED_EDGE ( 'NONE', *, *, #5865, .F. ) ;
#8671=VERTEX_POINT ( 'NONE', #9447 ) ;
#8672=ADVANCED_FACE ( 'NONE', ( #3249 ), #3765, .T. ) ;
#8673=MANIFOLD_SOLID_BREP ( 'Chamfer1', #3167 ) ;
#8674=EDGE_CURVE ( 'NONE', #24455, #25128, #17080, .T. ) ;
#8675=B_SPLINE_CURVE_WITH_KNOTS ( 'NONE', 3,
 ( #20728, #1017, #14676, #25641, #25203, #10386, #16558 ),
 .UNSPECIFIED., .F., .F.,
 ( 4, 3, 4 ),
 ( 5.239467995070050734E-16, 0.02816610861753244405, 0.04000277880656272211 ),
 .UNSPECIFIED. ) ;
#8676=CARTESIAN_POINT ( 'NONE',  ( 55.79472521941428198, 28.92526238350565393, -66.75682020267501571 ) ) ;
#8678=CARTESIAN_POINT ( 'NONE',  ( 109.1778270068192853, 0.008960903982060982112, -0.002542344697958619920 ) ) ;
#8679=ADVANCED_FACE ( 'NONE', ( #8280 ), #8335, .F. ) ;
#8680=FACE_OUTER_BOUND ( 'NONE', #17201, .T. ) ;
#8681=CARTESIAN_POINT ( 'NONE',  ( 1.831572820252008738, 117.9752562883678308, -84.49389457294016381 ) ) ;
#8683=CARTESIAN_POINT ( 'NONE',  ( 25.64681081121879203, -110.5293738517610080, 23.06870491922286348 ) ) ;
#8684=CARTESIAN_POINT ( 'NONE',  ( 32.73300124599732186, 0.000000000000000000, 0.000000000000000000 ) ) ;
#8687=( BOUNDED_SURFACE ( )  B_SPLINE_SURFACE ( 3, 1, ( 
 ( #5536, #7573 ),
 ( #12017, #20789 ),
 ( #9719, #18774 ),
 ( #9868, #1352 ) ),
 .UNSPECIFIED., .F., .F., .F. ) 
 B_SPLINE_SURFACE_WITH_KNOTS ( ( 4, 4 ),
 ( 2, 2 ),
 ( 0.000000000000000000, 1.000000000000000000 ),
 ( 0.000000000000000000, 1.000000000000000000 ),
 .UNSPECIFIED. ) 
 GEOMETRIC_REPRESENTATION_ITEM ( )  RATIONAL_B_SPLINE_SURFACE ( (
 ( 1.000000000000000000, 1.000000000000000000),
 ( 0.9956975270656955868, 0.8568959468854907557),
 ( 0.9956975270656955868, 0.8568959468854907557),
 ( 1.000000000000000000, 1.000000000000000000) ) ) 
 REPRESENTATION_ITEM ( '' )  SURFACE ( )  );
#8688=ORIENTED_EDGE ( 'NONE', *, *, #26871, .T. ) ;
#8689=VERTEX_POINT ( 'NONE', #27560 ) ;
#8690=B_SPLINE_CURVE_WITH_KNOTS ( 'NONE', 3,
 ( #9102, #13265, #1906, #17729, #19474, #8540 ),
 .UNSPECIFIED., .F., .F.,
 ( 4, 2, 4 ),
 ( 9.659140056172959483E-18, 0.0006311571484586074154, 0.001262314296917205940 ),
 .UNSPECIFIED. ) ;
#8693=CARTESIAN_POINT ( 'NONE',  ( 10.93730112725932635, 0.000000000000000000, 0.000000000000000000 ) ) ;
#8696=VERTEX_POINT ( 'NONE', #8020 ) ;
#8697=CARTESIAN_POINT ( 'NONE',  ( 25.64692232868534560, 97.62014907493959015, -56.73833653200140503 ) ) ;
#8700=VERTEX_POINT ( 'NONE', #1780 ) ;
#8702=B_SPLINE_CURVE_WITH_KNOTS ( 'NONE', 3,
 ( #9627, #10221, #7924, #20854 ),
 .UNSPECIFIED., .F., .F.,
 ( 4, 4 ),
 ( 2.081668171172168513E-17, 0.008383560773332729421 ),
 .UNSPECIFIED. ) ;
#8705=CARTESIAN_POINT ( 'NONE',  ( 25.98107933586719298, 107.2544904356373223, 35.99661810150902852 ) ) ;
#8708=CARTESIAN_POINT ( 'NONE',  ( 25.81918753295379432, 67.18811037444432088, 90.88802830331984239 ) ) ;
#8709=VERTEX_POINT ( 'NONE', #23133 ) ;
#8710=EDGE_CURVE ( 'NONE', #26014, #21864, #21507, .T. ) ;
#8711=CARTESIAN_POINT ( 'NONE',  ( 2.430230287190589422, 98.44218333480770866, 107.1617224697467634 ) ) ;
#8713=CARTESIAN_POINT ( 'NONE',  ( 25.64681081121879203, -66.03065707438999254, 91.59071981940550700 ) ) ;
#8714=CARTESIAN_POINT ( 'NONE',  ( 2.430230287190572103, -71.49654683843419889, -126.7388733285352345 ) ) ;
#8716=CARTESIAN_POINT ( 'NONE',  ( 2.108985857320894386, 144.3577886602087403, -16.46110181986536602 ) ) ;
#8717=CARTESIAN_POINT ( 'NONE',  ( 32.73300124599735739, -3.836798148479648507, 117.5726003567929610 ) ) ;
#8718=CARTESIAN_POINT ( 'NONE',  ( 25.69398547355839568, 103.4778695380289548, 45.25878216557469358 ) ) ;
#8719=CARTESIAN_POINT ( 'NONE',  ( 1.832998868059858122, -14.63705790013910502, -144.3700883710218648 ) ) ;
#8724=CARTESIAN_POINT ( 'NONE',  ( 25.69398547355838502, 83.43419615433096226, -76.12333255527431675 ) ) ;
#8725=CARTESIAN_POINT ( 'NONE',  ( 1.834118845439484335, -14.99112450600344104, 144.3336252355296381 ) ) ;
#8727=CARTESIAN_POINT ( 'NONE',  ( 55.49584447822657296, -15.34602024131336151, 70.91003759562310904 ) ) ;
#8728=CARTESIAN_POINT ( 'NONE',  ( 10.93730112726002979, 104.7670965581027644, -108.9902118373731241 ) ) ;
#8730=CARTESIAN_POINT ( 'NONE',  ( 19.66333377628728840, 135.6014041990442820, -24.23123354948703323 ) ) ;
#8732=ORIENTED_EDGE ( 'NONE', *, *, #25751, .T. ) ;
#8734=CARTESIAN_POINT ( 'NONE',  ( -90.83090735639699176, 0.000000000000000000, 0.000000000000000000 ) ) ;
#8735=CARTESIAN_POINT ( 'NONE',  ( 25.64692872815576763, 112.2585610031153038, 12.12228186621096704 ) ) ;
#8736=CARTESIAN_POINT ( 'NONE',  ( 25.64681081121879203, 75.24277141833607629, -84.18689316039970549 ) ) ;
#8739=( BOUNDED_SURFACE ( )  B_SPLINE_SURFACE ( 3, 1, ( 
 ( #573, #9370 ),
 ( #18125, #9506 ),
 ( #26903, #7214 ),
 ( #24776, #5024 ) ),
 .UNSPECIFIED., .F., .F., .F. ) 
 B_SPLINE_SURFACE_WITH_KNOTS ( ( 4, 4 ),
 ( 2, 2 ),
 ( 0.000000000000000000, 1.000000000000000000 ),
 ( 0.000000000000000000, 1.000000000000000000 ),
 .UNSPECIFIED. ) 
 GEOMETRIC_REPRESENTATION_ITEM ( )  RATIONAL_B_SPLINE_SURFACE ( (
 ( 1.000000000000000000, 1.000000000000000000),
 ( 0.9956975270656955868, 0.8568959468854907557),
 ( 0.9956975270656955868, 0.8568959468854907557),
 ( 1.000000000000000000, 1.000000000000000000) ) ) 
 REPRESENTATION_ITEM ( '' )  SURFACE ( )  );
#8745=ORIENTED_EDGE ( 'NONE', *, *, #6646, .T. ) ;
#8747=CARTESIAN_POINT ( 'NONE',  ( 2.433796855181233454, 116.8607839509068498, -86.69855925933855190 ) ) ;
#8749=EDGE_LOOP ( 'NONE', ( #23808, #16100, #11715, #3424 ) ) ;
#8750=EDGE_CURVE ( 'NONE', #182, #4802, #13972, .T. ) ;
#8751=CARTESIAN_POINT ( 'NONE',  ( 2.108985857320947677, -71.53406810961571693, 126.4634971826981484 ) ) ;
#8752=CARTESIAN_POINT ( 'NONE',  ( 32.73300124599736449, -66.00340565729409548, 97.37344512919831629 ) ) ;
#8753=LINE ( 'NONE', #17521, #19874 ) ;
#8754=CARTESIAN_POINT ( 'NONE',  ( 2.263178607246697727, -138.7064943909642238, -43.59477707254173851 ) ) ;
#8755=CARTESIAN_POINT ( 'NONE',  ( 109.1721716018069515, 0.001583175916617806213, 0.01699510305643761598 ) ) ;
#8756=CARTESIAN_POINT ( 'NONE',  ( 109.1592201516379674, 0.001331853079208314200, 0.007748443302128560708 ) ) ;
#8757=FACE_OUTER_BOUND ( 'NONE', #20646, .T. ) ;
#8758=DIRECTION ( 'NONE',  ( -1.000000000000000000, -0.000000000000000000, -0.000000000000000000 ) ) ;
#8759=CARTESIAN_POINT ( 'NONE',  ( 9.884929003653608603, 65.04493172071660467, -135.7578851563879425 ) ) ;
#8760=VERTEX_POINT ( 'NONE', #7875 ) ;
#8761=ORIENTED_EDGE ( 'NONE', *, *, #27775, .T. ) ;
#8763=CARTESIAN_POINT ( 'NONE',  ( 55.49584447822657296, 54.09506550945689440, -48.34726110739932636 ) ) ;
#8764=CARTESIAN_POINT ( 'NONE',  ( 1.832998868059890096, -84.86110816369685494, 117.7096351258384885 ) ) ;
#8765=VECTOR ( 'NONE', #25380, 1000.000000000000227 ) ;
#8766=CARTESIAN_POINT ( 'NONE',  ( 109.1592201516379674, 0.005027640251767214602, 0.006044422199822552418 ) ) ;
#8767=CARTESIAN_POINT ( 'NONE',  ( 1.833485406944057594, 0.5339064996884692604, 145.1085452359073429 ) ) ;
#8768=EDGE_CURVE ( 'NONE', #4319, #9399, #3952, .T. ) ;
#8769=CARTESIAN_POINT ( 'NONE',  ( 55.79472521941428198, -72.42790650415570042, -6.880567342320453861 ) ) ;
#8770=ORIENTED_EDGE ( 'NONE', *, *, #13408, .T. ) ;
#8771=CARTESIAN_POINT ( 'NONE',  ( 28.37603512858459709, 37.15644006762219220, 108.5491486026792387 ) ) ;
#8772=CARTESIAN_POINT ( 'NONE',  ( 2.063896406836609909, 132.1577797566314416, -60.31174178979677691 ) ) ;
#8773=CIRCLE ( 'NONE', #17925, 151.1787379149930359 ) ;
#8774=CARTESIAN_POINT ( 'NONE',  ( 25.64703792032470986, 23.32999623362277219, -110.4746717456747263 ) ) ;
#8776=CARTESIAN_POINT ( 'NONE',  ( 25.98107933586735641, 12.91054317625263437, -112.3948402207510497 ) ) ;
#8778=EDGE_CURVE ( 'NONE', #1993, #28403, #15331, .T. ) ;
#8779=( BOUNDED_SURFACE ( )  B_SPLINE_SURFACE ( 3, 1, ( 
 ( #19010, #1166 ),
 ( #9959, #25356 ),
 ( #16858, #5921 ),
 ( #14395, #12245 ) ),
 .UNSPECIFIED., .F., .F., .F. ) 
 B_SPLINE_SURFACE_WITH_KNOTS ( ( 4, 4 ),
 ( 2, 2 ),
 ( 0.000000000000000000, 1.000000000000000000 ),
 ( 0.000000000000000000, 1.000000000000000000 ),
 .UNSPECIFIED. ) 
 GEOMETRIC_REPRESENTATION_ITEM ( )  RATIONAL_B_SPLINE_SURFACE ( (
 ( 1.000000000000000000, 1.000000000000000000),
 ( 0.6386103224230302855, 0.9954351624131538845),
 ( 0.6386103224230302855, 0.9954351624131538845),
 ( 1.000000000000000000, 1.000000000000000000) ) ) 
 REPRESENTATION_ITEM ( '' )  SURFACE ( )  );
#8781=CARTESIAN_POINT ( 'NONE',  ( 2.108393763691170264, 142.3786741588524194, -28.95405853987377398 ) ) ;
#8782=CARTESIAN_POINT ( 'NONE',  ( 109.1589550718174877, -0.005233222325298260598, 0.005477029346537757269 ) ) ;
#8783=EDGE_LOOP ( 'NONE', ( #26482, #24369, #25399, #21017 ) ) ;
#8784=ADVANCED_FACE ( 'NONE', ( #25428 ), #590, .F. ) ;
#8785=EDGE_CURVE ( 'NONE', #11951, #9428, #24657, .T. ) ;
#8787=ORIENTED_EDGE ( 'NONE', *, *, #1885, .F. ) ;
#8788=AXIS2_PLACEMENT_3D ( 'NONE', #16687, #27895, #7926 ) ;
#8789=AXIS2_PLACEMENT_3D ( 'NONE', #24272, #11305, #21960 ) ;
#8790=CARTESIAN_POINT ( 'NONE',  ( 32.73300124599732186, 0.000000000000000000, 0.000000000000000000 ) ) ;
#8791=LINE ( 'NONE', #1875, #18865 ) ;
#8793=VECTOR ( 'NONE', #15367, 1000.000000000000000 ) ;
#8800=CARTESIAN_POINT ( 'NONE',  ( 2.433796855181233454, 57.85512797798071460, -133.5135467655512400 ) ) ;
#8805=DIRECTION ( 'NONE',  ( 0.000000000000000000, 0.000000000000000000, 1.000000000000000000 ) ) ;
#8806=AXIS2_PLACEMENT_3D ( 'NONE', #26308, #6196, #1839 ) ;
#8809=FACE_OUTER_BOUND ( 'NONE', #14169, .T. ) ;
#8810=CARTESIAN_POINT ( 'NONE',  ( 109.1586900883932856, -0.003656351050331892692, -0.006130969560687349849 ) ) ;
#8812=EDGE_CURVE ( 'NONE', #19237, #13619, #2651, .T. ) ;
#8813=ORIENTED_EDGE ( 'NONE', *, *, #24634, .F. ) ;
#8814=AXIS2_PLACEMENT_3D ( 'NONE', #10966, #12, #8805 ) ;
#8815=EDGE_CURVE ( 'NONE', #6918, #16636, #18824, .T. ) ;
#8816=ORIENTED_EDGE ( 'NONE', *, *, #27395, .F. ) ;
#8817=CARTESIAN_POINT ( 'NONE',  ( 32.73300124599739291, -20.69176323058542621, -115.8010721414085538 ) ) ;
#8818=CARTESIAN_POINT ( 'NONE',  ( 10.93730112725993919, -42.00474393596157086, -145.2260730187406352 ) ) ;
#8819=ORIENTED_EDGE ( 'NONE', *, *, #9241, .F. ) ;
#8821=ORIENTED_EDGE ( 'NONE', *, *, #561, .T. ) ;
#8822=ORIENTED_EDGE ( 'NONE', *, *, #26478, .T. ) ;
#8823=CARTESIAN_POINT ( 'NONE',  ( 109.1586059443104944, 0.004524147648833166946, 0.005438258427225630375 ) ) ;
#8826=CARTESIAN_POINT ( 'NONE',  ( 2.430230287190589422, -107.1617224697470903, 98.44218333480735339 ) ) ;
#8827=CARTESIAN_POINT ( 'NONE',  ( 109.1586900883932856, -0.006757191295060859491, -0.002301750759599753733 ) ) ;
#8830=( BOUNDED_SURFACE ( )  B_SPLINE_SURFACE ( 3, 1, ( 
 ( #8596, #17359 ),
 ( #6304, #28296 ),
 ( #6033, #26150 ),
 ( #4407, #19253 ) ),
 .UNSPECIFIED., .F., .F., .F. ) 
 B_SPLINE_SURFACE_WITH_KNOTS ( ( 4, 4 ),
 ( 2, 2 ),
 ( 0.000000000000000000, 1.000000000000000000 ),
 ( 0.000000000000000000, 1.000000000000000000 ),
 .UNSPECIFIED. ) 
 GEOMETRIC_REPRESENTATION_ITEM ( )  RATIONAL_B_SPLINE_SURFACE ( (
 ( 1.000000000000000000, 1.000000000000000000),
 ( 0.9956975270656955868, 0.8568959468854907557),
 ( 0.9956975270656955868, 0.8568959468854907557),
 ( 1.000000000000000000, 1.000000000000000000) ) ) 
 REPRESENTATION_ITEM ( '' )  SURFACE ( )  );
#8833=CARTESIAN_POINT ( 'NONE',  ( 2.063896406836605024, 118.3103904147693157, -84.29612368209032525 ) ) ;
#8834=CARTESIAN_POINT ( 'NONE',  ( 28.37603512858455801, -91.75440368549980974, 68.88140609180166507 ) ) ;
#8835=CARTESIAN_POINT ( 'NONE',  ( 25.64681081121880624, 23.88203588908233499, -110.3564950173079353 ) ) ;
#8836=CARTESIAN_POINT ( 'NONE',  ( 10.93730112725977932, -128.3908183996597074, 79.81734490845860819 ) ) ;
#8837=CARTESIAN_POINT ( 'NONE',  ( 26.11404676487259024, 113.2169081140373947, -1.130420376097525326 ) ) ;
#8838=CARTESIAN_POINT ( 'NONE',  ( 1.833838850855474378, -117.4485666028824085, 85.22139087169041716 ) ) ;
#8839=EDGE_CURVE ( 'NONE', #6575, #27642, #10801, .T. ) ;
#8840=ORIENTED_EDGE ( 'NONE', *, *, #24348, .T. ) ;
#8841=ORIENTED_EDGE ( 'NONE', *, *, #13704, .F. ) ;
#8843=CARTESIAN_POINT ( 'NONE',  ( 28.37599760073042887, 58.91309773266286953, -98.45181492308057614 ) ) ;
#8844=DIRECTION ( 'NONE',  ( -0.5946245182733608248, 0.3243201896541688112, -0.7356888587241603439 ) ) ;
#8846=CARTESIAN_POINT ( 'NONE',  ( 2.433796855181205476, -16.65276281464661423, 144.5536872373191102 ) ) ;
#8847=CARTESIAN_POINT ( 'NONE',  ( 32.73300124599732186, 0.000000000000000000, 0.000000000000000000 ) ) ;
#8849=CARTESIAN_POINT ( 'NONE',  ( 2.433796855181205476, 145.5024947199069629, 1.451562450950146133 ) ) ;
#8854=ORIENTED_EDGE ( 'NONE', *, *, #295, .T. ) ;
#8858=ORIENTED_EDGE ( 'NONE', *, *, #13408, .F. ) ;
#8859=CARTESIAN_POINT ( 'NONE',  ( 109.1778270068192853, 0.005186985107080939461, 0.007736698406806046500 ) ) ;
#8860=AXIS2_PLACEMENT_3D ( 'NONE', #19684, #8758, #15363 ) ;
#8861=EDGE_LOOP ( 'NONE', ( #25353, #6138, #8551, #22527 ) ) ;
#8863=EDGE_LOOP ( 'NONE', ( #2738, #1313, #2141, #19764 ) ) ;
#8864=B_SPLINE_CURVE_WITH_KNOTS ( 'NONE', 3,
 ( #20186, #20047, #19911, #13569 ),
 .UNSPECIFIED., .F., .F.,
 ( 4, 4 ),
 ( 0.000000000000000000, 0.008383560773332717278 ),
 .UNSPECIFIED. ) ;
#8865=CARTESIAN_POINT ( 'NONE',  ( 2.433796855181205476, 126.7346379669265843, -71.49415740224942795 ) ) ;
#8866=CARTESIAN_POINT ( 'NONE',  ( 109.1721716018069657, -0.01019541462303503142, -0.01368917435591430511 ) ) ;
#8867=( BOUNDED_SURFACE ( )  B_SPLINE_SURFACE ( 3, 1, ( 
 ( #10013, #1217 ),
 ( #18490, #27547 ),
 ( #18637, #10155 ),
 ( #928, #20929 ) ),
 .UNSPECIFIED., .F., .F., .F. ) 
 B_SPLINE_SURFACE_WITH_KNOTS ( ( 4, 4 ),
 ( 2, 2 ),
 ( 0.000000000000000000, 1.000000000000000000 ),
 ( 0.000000000000000000, 1.000000000000000000 ),
 .UNSPECIFIED. ) 
 GEOMETRIC_REPRESENTATION_ITEM ( )  RATIONAL_B_SPLINE_SURFACE ( (
 ( 1.000000000000000000, 1.000000000000000000),
 ( 0.9960225298536222738, 0.9999952330161893110),
 ( 0.9960225298536222738, 0.9999952330161893110),
 ( 1.000000000000000000, 1.000000000000000000) ) ) 
 REPRESENTATION_ITEM ( '' )  SURFACE ( )  );
#8868=CARTESIAN_POINT ( 'NONE',  ( 109.1592201516379674, -0.004867031887010251669, 0.006174480289200302147 ) ) ;
#8871=CARTESIAN_POINT ( 'NONE',  ( 2.430230287190581429, -132.3371620660946917, -60.50928654924886274 ) ) ;
#8872=AXIS2_PLACEMENT_3D ( 'NONE', #18380, #18542, #25039 ) ;
#8873=CARTESIAN_POINT ( 'NONE',  ( 2.430230287190572103, -138.8342928068223046, 43.58368230469342564 ) ) ;
#8874=CARTESIAN_POINT ( 'NONE',  ( 109.1589550718175161, -0.001793588804100445990, -0.007359857714025717923 ) ) ;
#8875=CARTESIAN_POINT ( 'NONE',  ( 25.64692232868535982, -56.17236075412014173, 97.94691534265413679 ) ) ;
#8876=CIRCLE ( 'NONE', #19433, 151.1787379149930359 ) ;
#8878=ORIENTED_EDGE ( 'NONE', *, *, #852, .T. ) ;
#8879=CARTESIAN_POINT ( 'NONE',  ( 26.11404676487259024, 83.38016054979885894, -76.59696442953111273 ) ) ;
#8882=CARTESIAN_POINT ( 'NONE',  ( 2.108985857320942348, 125.1820688103232015, -73.75356715682956121 ) ) ;
#8883=CARTESIAN_POINT ( 'NONE',  ( 2.433796855181205476, -109.1007109081232471, 96.28145139437646094 ) ) ;
#8885=CARTESIAN_POINT ( 'NONE',  ( 109.1589550718175161, -0.005777059646713217020, -0.004900004919101213011 ) ) ;
#8886=ADVANCED_FACE ( 'NONE', ( #19881 ), #3369, .F. ) ;
#8887=CARTESIAN_POINT ( 'NONE',  ( 1.832998868059858122, 138.1720401012266848, 44.33343224355280654 ) ) ;
#8889=CARTESIAN_POINT ( 'NONE',  ( 1.832998868059890096, 96.70023740551270919, -108.1944082009147365 ) ) ;
#8892=CARTESIAN_POINT ( 'NONE',  ( 2.263178607246631113, -60.41552769843737991, -132.2496131833836159 ) ) ;
#8893=AXIS2_PLACEMENT_3D ( 'NONE', #17488, #25728, #21822 ) ;
#8894=ORIENTED_EDGE ( 'NONE', *, *, #3536, .T. ) ;
#8895=CARTESIAN_POINT ( 'NONE',  ( 25.64700659047694487, -112.9110011064639565, -0.2275682798798776274 ) ) ;
#8896=VECTOR ( 'NONE', #19985, 1000.000000000000000 ) ;
#8898=CARTESIAN_POINT ( 'NONE',  ( 8.186469777910488688, 148.8557359139590517, 12.15801985874036539 ) ) ;
#8899=VECTOR ( 'NONE', #15677, 1000.000000000000000 ) ;
#8900=VERTEX_POINT ( 'NONE', #24796 ) ;
#8901=CARTESIAN_POINT ( 'NONE',  ( 32.73300124599732186, 0.000000000000000000, 0.000000000000000000 ) ) ;
#8904=CARTESIAN_POINT ( 'NONE',  ( 32.73300124599732186, 0.000000000000000000, 0.000000000000000000 ) ) ;
#8906=CARTESIAN_POINT ( 'NONE',  ( 55.49584447822657296, 42.86099773636541244, 58.53775398922272188 ) ) ;
#8909=CARTESIAN_POINT ( 'NONE',  ( 10.93730112725953596, 92.80059208661681680, 119.3442956573276206 ) ) ;
#8910=CARTESIAN_POINT ( 'NONE',  ( 10.93730112725991432, -71.28103789254845424, -133.3192575531807620 ) ) ;
#8911=CARTESIAN_POINT ( 'NONE',  ( 25.98552792386801613, -98.51438617140701126, -55.63155129533035392 ) ) ;
#8912=ORIENTED_EDGE ( 'NONE', *, *, #1105, .F. ) ;
#8915=VERTEX_POINT ( 'NONE', #15544 ) ;
#8917=CARTESIAN_POINT ( 'NONE',  ( 26.11404676487257603, -33.91085499298301897, -108.0249973236470993 ) ) ;
#8919=CARTESIAN_POINT ( 'NONE',  ( 2.263178607246686180, 98.32595927618852727, 107.1074316126221362 ) ) ;
#8920=CARTESIAN_POINT ( 'NONE',  ( 25.64703792032470631, 75.66285916808298850, 83.80974623566321213 ) ) ;
#8921=FACE_BOUND ( 'NONE', #19918, .T. ) ;
#8922=CARTESIAN_POINT ( 'NONE',  ( 26.11404676487257603, 112.4785329405483765, -12.95861723607337979 ) ) ;
#8924=CARTESIAN_POINT ( 'NONE',  ( 109.1586900883932856, -0.004701023939953891985, -0.005371970278523950648 ) ) ;
#8925=ORIENTED_EDGE ( 'NONE', *, *, #1314, .F. ) ;
#8928=CARTESIAN_POINT ( 'NONE',  ( 25.64692872815576408, 11.48248630407279336, 112.3258062264002746 ) ) ;
#8929=CARTESIAN_POINT ( 'NONE',  ( 10.93730112726002979, 79.81734490846109509, -128.3908183996583432 ) ) ;
#8931=B_SPLINE_CURVE_WITH_KNOTS ( 'NONE', 3,
 ( #21146, #3735, #8081, #1431, #27482, #16973, #7654 ),
 .UNSPECIFIED., .F., .F.,
 ( 4, 3, 4 ),
 ( 0.000000000000000000, 0.02398743853561324108, 0.04000277880656206986 ),
 .UNSPECIFIED. ) ;
#8932=CARTESIAN_POINT ( 'NONE',  ( 109.1721716018069657, 0.01567407524362079974, 0.006757465437538844391 ) ) ;
#8936=CARTESIAN_POINT ( 'NONE',  ( 25.64681081121879203, -56.09509703373275613, -97.99105938547980088 ) ) ;
#8937=ORIENTED_EDGE ( 'NONE', *, *, #25016, .T. ) ;
#8940=ORIENTED_EDGE ( 'NONE', *, *, #26411, .T. ) ;
#8942=DIRECTION ( 'NONE',  ( 0.000000000000000000, 0.000000000000000000, 1.000000000000000000 ) ) ;
#8944=EDGE_LOOP ( 'NONE', ( #27715, #19323, #4507, #10314 ) ) ;
#8947=ORIENTED_EDGE ( 'NONE', *, *, #20466, .T. ) ;
#8949=EDGE_LOOP ( 'NONE', ( #2438, #12654, #156, #9787 ) ) ;
#8951=EDGE_CURVE ( 'NONE', #22982, #12673, #21214, .T. ) ;
#8953=LINE ( 'NONE', #9386, #21260 ) ;
#8954=CARTESIAN_POINT ( 'NONE',  ( 1.833838850093452599, 132.5643635152042634, -59.02146106674950232 ) ) ;
#8964=VERTEX_POINT ( 'NONE', #17715 ) ;
#8965=EDGE_LOOP ( 'NONE', ( #8085, #11186, #17162, #17348 ) ) ;
#8967=CARTESIAN_POINT ( 'NONE',  ( 55.49584447822657296, 70.91003759562315167, 15.34602024131312170 ) ) ;
#8968=CARTESIAN_POINT ( 'NONE',  ( 1.831572820252009626, -107.1759352627512811, 97.82994539998347250 ) ) ;
#8969=ORIENTED_EDGE ( 'NONE', *, *, #27996, .F. ) ;
#8970=CARTESIAN_POINT ( 'NONE',  ( 13.36082413113063083, 127.3428651193248271, 84.67697637120454601 ) ) ;
#8973=CARTESIAN_POINT ( 'NONE',  ( 2.063896406836605024, -142.3682421260909337, 28.88716984836274193 ) ) ;
#8976=CARTESIAN_POINT ( 'NONE',  ( 13.84597867724978038, 4.782757490007880641, -146.6243035057531756 ) ) ;
#8977=CARTESIAN_POINT ( 'NONE',  ( 2.430230287190592531, -144.5585181921887283, 16.65331920325692039 ) ) ;
#8978=ADVANCED_FACE ( 'NONE', ( #16281 ), #13263, .F. ) ;
#8979=CARTESIAN_POINT ( 'NONE',  ( 25.69398547355841345, -65.78402800526225747, 91.80679989327114754 ) ) ;
#8980=VECTOR ( 'NONE', #14300, 999.9999999999998863 ) ;
#8981=CARTESIAN_POINT ( 'NONE',  ( 109.1586059443104944, 0.001014167950280784247, -0.007001002073871750823 ) ) ;
#8984=ORIENTED_EDGE ( 'NONE', *, *, #9132, .F. ) ;
#8987=CARTESIAN_POINT ( 'NONE',  ( 10.93730112725986281, -149.7554878793150408, 20.69552240458288850 ) ) ;
#8989=CARTESIAN_POINT ( 'NONE',  ( 2.430230287190589422, -71.49654683843598946, 126.7388733285342823 ) ) ;
#8992=ORIENTED_EDGE ( 'NONE', *, *, #9532, .T. ) ;
#8994=CARTESIAN_POINT ( 'NONE',  ( 1.833485406944057594, -29.64752363041639782, 142.0485807715645024 ) ) ;
#8995=ORIENTED_EDGE ( 'NONE', *, *, #12407, .T. ) ;
#8996=VERTEX_POINT ( 'NONE', #17181 ) ;
#8997=CARTESIAN_POINT ( 'NONE',  ( 1.833485406944043827, -58.53321471326791681, -132.7804117027893938 ) ) ;
#8998=B_SPLINE_CURVE_WITH_KNOTS ( 'NONE', 3,
 ( #20381, #9024, #17786, #15611 ),
 .UNSPECIFIED., .F., .F.,
 ( 4, 4 ),
 ( 0.000000000000000000, 0.008383560773332706870 ),
 .UNSPECIFIED. ) ;
#8999=ORIENTED_EDGE ( 'NONE', *, *, #21640, .F. ) ;
#9000=CARTESIAN_POINT ( 'NONE',  ( 109.1589550718175161, 0.007008495014555480088, 0.002874971999837445946 ) ) ;
#9001=ORIENTED_EDGE ( 'NONE', *, *, #7705, .F. ) ;
#9002=CARTESIAN_POINT ( 'NONE',  ( 25.64660436782533282, 66.83584345385925474, 91.00479974714288289 ) ) ;
#9003=EDGE_CURVE ( 'NONE', #12622, #25271, #28386, .T. ) ;
#9004=CARTESIAN_POINT ( 'NONE',  ( 10.93730112725932813, 146.7718404940640085, 36.23586118136551448 ) ) ;
#9006=EDGE_CURVE ( 'NONE', #9151, #26384, #7832, .T. ) ;
#9007=CARTESIAN_POINT ( 'NONE',  ( 1.832998868059890096, -132.7810136645742034, 58.53348008137602676 ) ) ;
#9008=CARTESIAN_POINT ( 'NONE',  ( 25.64681081121879203, 75.86069728269103507, -83.63051021305824406 ) ) ;
#9010=CARTESIAN_POINT ( 'NONE',  ( 1.832998868059890096, -97.49378069860867413, 107.4798986104856908 ) ) ;
#9012=CARTESIAN_POINT ( 'NONE',  ( 109.1586059443104944, -0.005555961672780091939, -0.004378796245583014765 ) ) ;
#9013=DIRECTION ( 'NONE',  ( 0.000000000000000000, 0.000000000000000000, -1.000000000000000000 ) ) ;
#9015=CARTESIAN_POINT ( 'NONE',  ( 25.64708228042120908, -56.48974615488991446, 97.76433875577625088 ) ) ;
#9016=VERTEX_POINT ( 'NONE', #25967 ) ;
#9017=CARTESIAN_POINT ( 'NONE',  ( 10.93730112725996229, -10.89264110824889364, -150.7858122213663989 ) ) ;
#9020=CARTESIAN_POINT ( 'NONE',  ( 25.64660436782560637, 91.00479974714322395, -66.83584345385810366 ) ) ;
#9021=CARTESIAN_POINT ( 'NONE',  ( 25.64699802086722968, -35.11755197949763385, -107.3112355540544769 ) ) ;
#9023=DIRECTION ( 'NONE',  ( -1.000000000000000000, -0.000000000000000000, -0.000000000000000000 ) ) ;
#9024=CARTESIAN_POINT ( 'NONE',  ( 28.37599760073042532, -37.15642189426477415, 108.5491283158100657 ) ) ;
#9026=CARTESIAN_POINT ( 'NONE',  ( 109.1592201516379674, 0.004368284148525261590, -0.006536841731962014269 ) ) ;
#9027=CARTESIAN_POINT ( 'NONE',  ( 1.833721034905616776, -96.83259691102576028, 108.0754384393931673 ) ) ;
#9028=ORIENTED_EDGE ( 'NONE', *, *, #8210, .F. ) ;
#9031=EDGE_LOOP ( 'NONE', ( #11342, #19564, #5917, #23886 ) ) ;
#9032=B_SPLINE_CURVE_WITH_KNOTS ( 'NONE', 3,
 ( #22730, #11777, #824, #17938 ),
 .UNSPECIFIED., .F., .F.,
 ( 4, 4 ),
 ( 0.000000000000000000, 0.01077107196513850222 ),
 .UNSPECIFIED. ) ;
#9033=CARTESIAN_POINT ( 'NONE',  ( 55.79472521941426777, -53.57698701322181023, -49.22042574086480471 ) ) ;
#9037=ADVANCED_FACE ( 'NONE', ( #1772 ), #11265, .F. ) ;
#9038=CARTESIAN_POINT ( 'NONE',  ( 25.64681081121879203, -34.49579773461859133, 107.5125461021401492 ) ) ;
#9039=CARTESIAN_POINT ( 'NONE',  ( 25.64700659047696263, 23.25292178500362894, 110.4909389345859694 ) ) ;
#9041=FACE_OUTER_BOUND ( 'NONE', #10898, .T. ) ;
#9044=EDGE_CURVE ( 'NONE', #9116, #8689, #5047, .T. ) ;
#9048=ORIENTED_EDGE ( 'NONE', *, *, #26196, .F. ) ;
#9049=VERTEX_POINT ( 'NONE', #18751 ) ;
#9050=ORIENTED_EDGE ( 'NONE', *, *, #21119, .F. ) ;
#9053=CARTESIAN_POINT ( 'NONE',  ( 25.64681081121880624, -23.88203588908156760, 110.3564950173080916 ) ) ;
#9055=DIRECTION ( 'NONE',  ( 0.000000000000000000, 0.000000000000000000, 1.000000000000000000 ) ) ;
#9057=ORIENTED_EDGE ( 'NONE', *, *, #18420, .T. ) ;
#9060=CARTESIAN_POINT ( 'NONE',  ( 109.1592201516379674, -0.006649399203953420406, -0.004194960840980667231 ) ) ;
#9061=CARTESIAN_POINT ( 'NONE',  ( 13.36082413113061307, 152.6206443696329984, -9.660980093453126472 ) ) ;
#9064=CARTESIAN_POINT ( 'NONE',  ( 2.430230287190572103, -74.01081053031188617, 125.2872625092160064 ) ) ;
#9066=CARTESIAN_POINT ( 'NONE',  ( 26.11404676487259024, -90.92995828888244603, 67.46175819463337575 ) ) ;
#9067=ORIENTED_EDGE ( 'NONE', *, *, #6446, .T. ) ;
#9069=ORIENTED_EDGE ( 'NONE', *, *, #7970, .T. ) ;
#9071=CARTESIAN_POINT ( 'NONE',  ( 109.1778270068192853, 0.009177562596833046746, 0.001591747944966680336 ) ) ;
#9072=CARTESIAN_POINT ( 'NONE',  ( 32.73300124599736449, -114.2056417606550127, 28.19767303745571496 ) ) ;
#9074=EDGE_CURVE ( 'NONE', #11142, #5234, #8514, .T. ) ;
#9075=VERTEX_POINT ( 'NONE', #14431 ) ;
#9079=ORIENTED_EDGE ( 'NONE', *, *, #6252, .F. ) ;
#9080=EDGE_LOOP ( 'NONE', ( #315, #22581, #19116, #3948 ) ) ;
#9081=CARTESIAN_POINT ( 'NONE',  ( 1.833691583653521695, 142.0122737882511785, -29.82175144857958671 ) ) ;
#9083=CARTESIAN_POINT ( 'NONE',  ( 1.833206308920112049, -145.1075835660717246, -0.7447049373426916086 ) ) ;
#9085=CARTESIAN_POINT ( 'NONE',  ( 25.64681081121879203, 56.09509703373343115, 97.99105938547943140 ) ) ;
#9087=CARTESIAN_POINT ( 'NONE',  ( 2.433796855181233454, -133.5135467655514390, -57.85512797798025275 ) ) ;
#9091=CARTESIAN_POINT ( 'NONE',  ( 1.834118845439484335, 96.96525081350000619, 107.9567937753796514 ) ) ;
#9092=CARTESIAN_POINT ( 'NONE',  ( 28.37603512858351706, -10.20681926544442319, 114.2774673387026070 ) ) ;
#9093=VERTEX_POINT ( 'NONE', #3490 ) ;
#9094=ORIENTED_EDGE ( 'NONE', *, *, #23582, .F. ) ;
#9096=CARTESIAN_POINT ( 'NONE',  ( 25.64660436782546071, 107.2041192742820783, -35.44263474731832986 ) ) ;
#9100=CARTESIAN_POINT ( 'NONE',  ( 25.64681081121880624, -75.24277141833435678, -84.18689316040122606 ) ) ;
#9102=CARTESIAN_POINT ( 'NONE',  ( 1.833485406944057594, -145.1085452359073429, 0.5339064996879626657 ) ) ;
#9104=CARTESIAN_POINT ( 'NONE',  ( 109.1587776205901861, -0.007186028091168167320, -0.001442274044995771765 ) ) ;
#9105=EDGE_CURVE ( 'NONE', #26503, #5673, #17424, .T. ) ;
#9106=B_SPLINE_CURVE_WITH_KNOTS ( 'NONE', 3,
 ( #23007, #27577, #3838, #25724 ),
 .UNSPECIFIED., .F., .F.,
 ( 4, 4 ),
 ( 3.348019117447978055E-16, 0.01077107486149846138 ),
 .UNSPECIFIED. ) ;
#9108=CARTESIAN_POINT ( 'NONE',  ( 2.433796855181233454, 43.58222566461826375, -138.8296532063083646 ) ) ;
#9111=CARTESIAN_POINT ( 'NONE',  ( 5.340103556456435641, -126.5279493230354859, -75.71042922800671704 ) ) ;
#9113=CARTESIAN_POINT ( 'NONE',  ( 2.430230287190572103, -125.2872625092157364, -74.01081053031231249 ) ) ;
#9114=CIRCLE ( 'NONE', #3591, 151.1787379149930359 ) ;
#9116=VERTEX_POINT ( 'NONE', #15259 ) ;
#9118=CARTESIAN_POINT ( 'NONE',  ( 10.93730112725939030, 136.0306644680981947, 65.95960219663135149 ) ) ;
#9119=CARTESIAN_POINT ( 'NONE',  ( 1.833721034905652081, -144.3516387774751024, -14.81406766076082171 ) ) ;
#9122=CARTESIAN_POINT ( 'NONE',  ( 26.28373643307409679, -82.21796085350716510, 97.52903534490833692 ) ) ;
#9123=EDGE_CURVE ( 'NONE', #1609, #3680, #11257, .T. ) ;
#9124=VERTEX_POINT ( 'NONE', #26209 ) ;
#9125=CARTESIAN_POINT ( 'NONE',  ( 1.833691583653536572, -14.81406002961217894, -144.3515375443196262 ) ) ;
#9129=VERTEX_POINT ( 'NONE', #6102 ) ;
#9132=EDGE_CURVE ( 'NONE', #16636, #16438, #4361, .T. ) ;
#9133=EDGE_LOOP ( 'NONE', ( #20492, #23929, #19132, #16760 ) ) ;
#9139=DIRECTION ( 'NONE',  ( -1.000000000000000000, -0.000000000000000000, -0.000000000000000000 ) ) ;
#9142=DIRECTION ( 'NONE',  ( -1.000000000000000000, -0.000000000000000000, -0.000000000000000000 ) ) ;
#9144=CARTESIAN_POINT ( 'NONE',  ( 0.000000000000000000, 9.797174393178826052E-15, 80.00000000000000000 ) ) ;
#9146=CARTESIAN_POINT ( 'NONE',  ( 1.833485406944057594, 125.4007332306555895, -73.01664920992834595 ) ) ;
#9148=CARTESIAN_POINT ( 'NONE',  ( 109.1586900883932856, 0.007002774699553659596, -0.001385221016536877401 ) ) ;
#9151=VERTEX_POINT ( 'NONE', #19309 ) ;
#9152=CARTESIAN_POINT ( 'NONE',  ( 1.833485406944043827, -45.34878176254329674, 137.8414413349084100 ) ) ;
#9153=CARTESIAN_POINT ( 'NONE',  ( 25.73574536432414206, 110.6664861019686725, -22.69874377039331392 ) ) ;
#9155=LINE ( 'NONE', #13612, #24979 ) ;
#9156=ORIENTED_EDGE ( 'NONE', *, *, #24151, .F. ) ;
#9158=CARTESIAN_POINT ( 'NONE',  ( 2.433796855181233454, -86.69855925933894980, -116.8607839509065371 ) ) ;
#9166=CARTESIAN_POINT ( 'NONE',  ( 28.37599760073042532, 93.86375353586258541, -65.97809271467041015 ) ) ;
#9167=B_SPLINE_CURVE_WITH_KNOTS ( 'NONE', 3,
 ( #19883, #26496, #6802, #24361, #2032, #738, #7523, #13830 ),
 .UNSPECIFIED., .F., .F.,
 ( 4, 2, 2, 4 ),
 ( 6.505213034913026604E-19, 0.0002429592666046745376, 0.0004859185332093484246, 0.0009718370664186767914 ),
 .UNSPECIFIED. ) ;
#9168=CARTESIAN_POINT ( 'NONE',  ( 10.93730112725972781, -71.28103789255033007, 133.3192575531796251 ) ) ;
#9169=EDGE_LOOP ( 'NONE', ( #10952, #3888, #7067, #4509 ) ) ;
#9170=( NAMED_UNIT ( * ) PLANE_ANGLE_UNIT ( ) SI_UNIT ( $, .RADIAN. ) );
#9171=CARTESIAN_POINT ( 'NONE',  ( 30.58324630866341920, -92.47020419020127235, -77.95273942827436997 ) ) ;
#9173=LINE ( 'NONE', #5832, #1622 ) ;
#9175=CARTESIAN_POINT ( 'NONE',  ( 25.64681081121879203, -112.9102952884414606, 0.4157506337723927414 ) ) ;
#9176=ORIENTED_EDGE ( 'NONE', *, *, #1401, .T. ) ;
#9177=CARTESIAN_POINT ( 'NONE',  ( 25.64703792032469565, 0.1487959541341497549, 112.9111140735909089 ) ) ;
#9178=CARTESIAN_POINT ( 'NONE',  ( 28.37603512858449761, 48.29936889363955288, 104.0705994281838258 ) ) ;
#9179=CARTESIAN_POINT ( 'NONE',  ( 32.73300124599732186, 0.000000000000000000, 0.000000000000000000 ) ) ;
#9181=VERTEX_POINT ( 'NONE', #22631 ) ;
#9182=ORIENTED_EDGE ( 'NONE', *, *, #21326, .T. ) ;
#9184=DIRECTION ( 'NONE',  ( 0.5914120900931444380, 0.6570486713847274451, -0.4674599267565326399 ) ) ;
#9187=CARTESIAN_POINT ( 'NONE',  ( 1.833838850855499691, 144.3055354793886238, 15.25659494068155375 ) ) ;
#9188=CARTESIAN_POINT ( 'NONE',  ( 25.73574536432413851, -103.5288236655399174, 45.21157800100269242 ) ) ;
#9189=CARTESIAN_POINT ( 'NONE',  ( 26.11404676487257603, 47.08215554553518700, 102.9690087468803341 ) ) ;
#9191=CARTESIAN_POINT ( 'NONE',  ( 6.224689322667647851, 134.1951906609247658, -62.55544044765115785 ) ) ;
#9192=CARTESIAN_POINT ( 'NONE',  ( 1.832998868059858122, 132.3466930259802155, -59.50898020732380189 ) ) ;
#9193=CARTESIAN_POINT ( 'NONE',  ( 1.833485406944043827, -58.53321471326791681, -132.7804117027893938 ) ) ;
#9194=ADVANCED_FACE ( 'NONE', ( #17711 ), #17148, .F. ) ;
#9197=DIRECTION ( 'NONE',  ( 0.000000000000000000, 0.000000000000000000, 1.000000000000000000 ) ) ;
#9198=CIRCLE ( 'NONE', #25293, 117.6351876552689504 ) ;
#9200=B_SPLINE_CURVE_WITH_KNOTS ( 'NONE', 3,
 ( #26785, #20312, #7099, #15859 ),
 .UNSPECIFIED., .F., .F.,
 ( 4, 4 ),
 ( 0.000000000000000000, 0.01077107196513847273 ),
 .UNSPECIFIED. ) ;
#9201=FACE_OUTER_BOUND ( 'NONE', #14347, .T. ) ;
#9202=ORIENTED_EDGE ( 'NONE', *, *, #14221, .F. ) ;
#9203=CARTESIAN_POINT ( 'NONE',  ( 1.833485406944043827, 96.69979900902167458, 108.1939177044929323 ) ) ;
#9204=EDGE_CURVE ( 'NONE', #17261, #25984, #11042, .T. ) ;
#9206=ORIENTED_EDGE ( 'NONE', *, *, #22999, .F. ) ;
#9207=EDGE_CURVE ( 'NONE', #1068, #23545, #4470, .T. ) ;
#9212=DIRECTION ( 'NONE',  ( 0.7071067811865485719, 0.000000000000000000, -0.7071067811865465735 ) ) ;
#9214=DIRECTION ( 'NONE',  ( -1.000000000000000000, -0.000000000000000000, -0.000000000000000000 ) ) ;
#9216=EDGE_LOOP ( 'NONE', ( #20684, #6243, #23224, #28029 ) ) ;
#9217=CARTESIAN_POINT ( 'NONE',  ( 1.833485406944043827, 14.63699153649552365, -144.3694338680883789 ) ) ;
#9218=B_SPLINE_CURVE_WITH_KNOTS ( 'NONE', 3,
 ( #21639, #19481, #7387, #18458, #20476, #20040 ),
 .UNSPECIFIED., .F., .F.,
 ( 4, 2, 4 ),
 ( 1.815771614269358398E-17, 0.0006311636237756957160, 0.001262327247551373434 ),
 .UNSPECIFIED. ) ;
#9226=CARTESIAN_POINT ( 'NONE',  ( 13.84597867724974130, -69.17016226638961029, -129.3717503931858062 ) ) ;
#9229=CARTESIAN_POINT ( 'NONE',  ( 32.73300124599738581, -62.10906484417165530, -99.90245962373897726 ) ) ;
#9230=CARTESIAN_POINT ( 'NONE',  ( 13.36082413113063083, -53.25066407421704895, -143.3553710183994951 ) ) ;
#9234=ADVANCED_FACE ( 'NONE', ( #10253 ), #5550, .F. ) ;
#9235=CARTESIAN_POINT ( 'NONE',  ( 10.93730112725996051, 20.69552240458543224, -149.7554878793147282 ) ) ;
#9240=FACE_OUTER_BOUND ( 'NONE', #24243, .T. ) ;
#9241=EDGE_CURVE ( 'NONE', #27092, #24861, #14715, .T. ) ;
#9242=VECTOR ( 'NONE', #17011, 1000.000000000000000 ) ;
#9244=ORIENTED_EDGE ( 'NONE', *, *, #21254, .F. ) ;
#9247=ORIENTED_EDGE ( 'NONE', *, *, #17764, .F. ) ;
#9249=LINE ( 'NONE', #24806, #14719 ) ;
#9254=CARTESIAN_POINT ( 'NONE',  ( 119.2224693531408519, 70.00000000000000000, -20.00000000000001421 ) ) ;
#9257=CONICAL_SURFACE ( 'NONE', #11106, 117.6351876552689504, 0.9945805576725580410 ) ;
#9258=CARTESIAN_POINT ( 'NONE',  ( 32.73300124599738581, 3.836798148480494497, -117.5726003567928757 ) ) ;
#9260=CARTESIAN_POINT ( 'NONE',  ( 109.1624594426973118, -0.01570508117120619426, -0.002863932759303039303 ) ) ;
#9261=DIRECTION ( 'NONE',  ( -0.5946245182733607137, -0.4701913299128818169, 0.6521823330502973803 ) ) ;
#9262=CARTESIAN_POINT ( 'NONE',  ( 8.186469829614306803, -146.7694295239426481, 27.65107825763907812 ) ) ;
#9264=CIRCLE ( 'NONE', #15673, 117.6351876552689504 ) ;
#9267=EDGE_CURVE ( 'NONE', #22024, #16670, #23210, .T. ) ;
#9268=CARTESIAN_POINT ( 'NONE',  ( 2.433796855181219243, 142.0211193075560061, -31.67151202412830813 ) ) ;
#9269=CARTESIAN_POINT ( 'NONE',  ( 109.1586059443104944, 0.005881369279880096536, 0.003930911098385099153 ) ) ;
#9272=VERTEX_POINT ( 'NONE', #14544 ) ;
#9273=CARTESIAN_POINT ( 'NONE',  ( 1.833809397773857430, -14.99109763364046799, -144.3333383260367953 ) ) ;
#9274=ORIENTED_EDGE ( 'NONE', *, *, #3506, .T. ) ;
#9275=CARTESIAN_POINT ( 'NONE',  ( 32.73300124599739291, -108.9684813982485707, -44.31599526638064646 ) ) ;
#9276=EDGE_CURVE ( 'NONE', #7372, #22961, #23349, .T. ) ;
#9277=CARTESIAN_POINT ( 'NONE',  ( 30.59141879584289470, -101.9665761624294049, 55.75104644134855647 ) ) ;
#9278=B_SPLINE_CURVE_WITH_KNOTS ( 'NONE', 3,
 ( #6641, #15107, #17417, #2019, #8649, #2, #13235, #21603, #17557, #2148 ),
 .UNSPECIFIED., .F., .F.,
 ( 4, 3, 3, 4 ),
 ( 6.206335383118182794E-17, 0.0002669559177086440840, 0.0005339118354151246425, 0.001067817517169165117 ),
 .UNSPECIFIED. ) ;
#9279=EDGE_LOOP ( 'NONE', ( #19221, #8450, #9727, #4153 ) ) ;
#9280=ADVANCED_FACE ( 'NONE', ( #1447 ), #25769, .T. ) ;
#9282=VERTEX_POINT ( 'NONE', #10632 ) ;
#9284=B_SPLINE_CURVE_WITH_KNOTS ( 'NONE', 3,
 ( #16791, #5552, #3396, #8283, #23554, #27563 ),
 .UNSPECIFIED., .F., .F.,
 ( 4, 2, 4 ),
 ( 1.389302603484999005E-17, 0.0006311571484585952723, 0.001262314296917176884 ),
 .UNSPECIFIED. ) ;
#9287=CARTESIAN_POINT ( 'NONE',  ( 30.59141879584290891, -116.1811685142589852, -2.701465575440967548 ) ) ;
#9288=( BOUNDED_SURFACE ( )  B_SPLINE_SURFACE ( 3, 1, ( 
 ( #4803, #26385 ),
 ( #19486, #15144 ),
 ( #22066, #13280 ),
 ( #10721, #17316 ) ),
 .UNSPECIFIED., .F., .F., .F. ) 
 B_SPLINE_SURFACE_WITH_KNOTS ( ( 4, 4 ),
 ( 2, 2 ),
 ( 0.000000000000000000, 1.000000000000000000 ),
 ( 0.000000000000000000, 1.000000000000000000 ),
 .UNSPECIFIED. ) 
 GEOMETRIC_REPRESENTATION_ITEM ( )  RATIONAL_B_SPLINE_SURFACE ( (
 ( 1.000000000000000000, 1.000000000000000000),
 ( 0.9956975270656955868, 0.8568959468854907557),
 ( 0.9956975270656955868, 0.8568959468854907557),
 ( 1.000000000000000000, 1.000000000000000000) ) ) 
 REPRESENTATION_ITEM ( '' )  SURFACE ( )  );
#9289=VECTOR ( 'NONE', #16605, 1000.000000000000114 ) ;
#9294=CARTESIAN_POINT ( 'NONE',  ( 1.833603222531960508, -72.16916166673654232, -125.8904991419474442 ) ) ;
#9295=CARTESIAN_POINT ( 'NONE',  ( 109.1586900883932856, -0.006130969560693691131, -0.003656351050324861858 ) ) ;
#9297=B_SPLINE_CURVE_WITH_KNOTS ( 'NONE', 3,
 ( #22814, #7552, #15883, #11853, #24967, #14002, #16309 ),
 .UNSPECIFIED., .F., .F.,
 ( 4, 3, 4 ),
 ( 6.081733682261733487E-16, 0.02816610861753244405, 0.04000277880656275681 ),
 .UNSPECIFIED. ) ;
#9298=CARTESIAN_POINT ( 'NONE',  ( 25.65782528836479770, -110.3293115225705492, -24.04194111108980181 ) ) ;
#9300=CARTESIAN_POINT ( 'NONE',  ( 109.1586059443104944, 0.005067816690893742551, 0.004935564877218420222 ) ) ;
#9301=ORIENTED_EDGE ( 'NONE', *, *, #18625, .T. ) ;
#9305=ADVANCED_FACE ( 'NONE', ( #24296 ), #26133, .F. ) ;
#9307=CARTESIAN_POINT ( 'NONE',  ( 109.1586059443104944, 0.002622205828279748022, -0.006570129623063777728 ) ) ;
#9308=FACE_OUTER_BOUND ( 'NONE', #5289, .T. ) ;
#9309=VECTOR ( 'NONE', #16938, 999.9999999999998863 ) ;
#9311=CARTESIAN_POINT ( 'NONE',  ( 2.063896406836605024, 126.4736179849657560, -71.46753739785881976 ) ) ;
#9312=VECTOR ( 'NONE', #25816, 1000.000000000000114 ) ;
#9314=CARTESIAN_POINT ( 'NONE',  ( 109.1587776205901861, 8.330235398536594530E-05, 0.007328861771499511728 ) ) ;
#9316=CARTESIAN_POINT ( 'NONE',  ( 32.73300124599734318, 92.86301839380026024, 72.21147546950587071 ) ) ;
#9317=VERTEX_POINT ( 'NONE', #4556 ) ;
#9319=DIRECTION ( 'NONE',  ( 0.000000000000000000, 0.000000000000000000, 1.000000000000000000 ) ) ;
#9321=CARTESIAN_POINT ( 'NONE',  ( 25.64703792032472052, -112.9111140735908805, 0.1487959541337554870 ) ) ;
#9323=CARTESIAN_POINT ( 'NONE',  ( 1.834118845439484335, 137.9527673765105646, 45.01070051384637338 ) ) ;
#9325=CARTESIAN_POINT ( 'NONE',  ( 25.64700659047696973, 103.2418925369179732, -45.71714758798273692 ) ) ;
#9327=ADVANCED_FACE ( 'NONE', ( #2389, #4140 ), #26573, .F. ) ;
#9328=CARTESIAN_POINT ( 'NONE',  ( 24.22246935314087324, -90.00000000000005684, 39.99999999999997158 ) ) ;
#9329=VECTOR ( 'NONE', #9184, 1000.000000000000000 ) ;
#9330=CARTESIAN_POINT ( 'NONE',  ( 32.73300124599739291, 105.8473486001057466, -51.32617430724801721 ) ) ;
#9331=DIRECTION ( 'NONE',  ( -0.5914120900931443270, 0.7643865440136140554, -0.2567974902965012296 ) ) ;
#9333=CARTESIAN_POINT ( 'NONE',  ( 25.64660436782547848, -112.9095526718342342, 0.5800540083547919279 ) ) ;
#9334=VERTEX_POINT ( 'NONE', #11048 ) ;
#9335=B_SPLINE_CURVE_WITH_KNOTS ( 'NONE', 3,
 ( #26654, #9262, #13563, #2480 ),
 .UNSPECIFIED., .F., .F.,
 ( 4, 4 ),
 ( 0.000000000000000000, 0.01077107196513865661 ),
 .UNSPECIFIED. ) ;
#9338=CARTESIAN_POINT ( 'NONE',  ( 24.01988960052051780, -57.17607523395295743, 117.9135177031536585 ) ) ;
#9339=CARTESIAN_POINT ( 'NONE',  ( 25.87036335909426654, 33.99475147239157025, -107.8283083010000212 ) ) ;
#9340=CARTESIAN_POINT ( 'NONE',  ( 19.66333377628668799, -116.9853418557808169, -72.72773398758353380 ) ) ;
#9341=VERTEX_POINT ( 'NONE', #8476 ) ;
#9343=VERTEX_POINT ( 'NONE', #6455 ) ;
#9346=CARTESIAN_POINT ( 'NONE',  ( 30.59138290137912364, 44.78723476287443361, -107.2355347544031190 ) ) ;
#9347=EDGE_CURVE ( 'NONE', #24750, #22385, #24985, .T. ) ;
#9348=CARTESIAN_POINT ( 'NONE',  ( 32.73300124599738581, 39.98094346392455378, -110.6325518752269517 ) ) ;
#9350=CARTESIAN_POINT ( 'NONE',  ( 26.28373643307406837, -43.35364178852690031, -119.9673604189461429 ) ) ;
#9352=EDGE_LOOP ( 'NONE', ( #1308, #15056, #20819, #24039 ) ) ;
#9353=CARTESIAN_POINT ( 'NONE',  ( 1.833206310202334599, 145.1075835704899930, -0.7447039688730743290 ) ) ;
#9355=CARTESIAN_POINT ( 'NONE',  ( 2.430230287190581429, -1.451610819318752688, 145.5073573687466819 ) ) ;
#9357=CARTESIAN_POINT ( 'NONE',  ( 25.73574536432414561, -74.99093179013911481, -84.49061642666552530 ) ) ;
#9359=FACE_OUTER_BOUND ( 'NONE', #15239, .T. ) ;
#9360=AXIS2_PLACEMENT_3D ( 'NONE', #20867, #1151, #10372 ) ;
#9361=AXIS2_PLACEMENT_3D ( 'NONE', #26033, #15487, #19678 ) ;
#9366=VERTEX_POINT ( 'NONE', #19673 ) ;
#9367=ORIENTED_EDGE ( 'NONE', *, *, #16752, .T. ) ;
#9368=CARTESIAN_POINT ( 'NONE',  ( 13.36082413113061307, 109.3026516754232773, 106.9547846563639126 ) ) ;
#9370=CARTESIAN_POINT ( 'NONE',  ( 1.832998868059858122, 96.70023740551121705, 108.1944082009160724 ) ) ;
#9371=EDGE_CURVE ( 'NONE', #7281, #10842, #22926, .T. ) ;
#9374=DIRECTION ( 'NONE',  ( 0.000000000000000000, 0.000000000000000000, 1.000000000000000000 ) ) ;
#9376=CARTESIAN_POINT ( 'NONE',  ( 5.340103556456504919, -140.9275371673309962, 43.36842540065445917 ) ) ;
#9377=CARTESIAN_POINT ( 'NONE',  ( 25.64681081121880624, 35.28660243342550729, 107.2555980796242494 ) ) ;
#9378=DIRECTION ( 'NONE',  ( 0.000000000000000000, 0.000000000000000000, 1.000000000000000000 ) ) ;
#9380=EDGE_CURVE ( 'NONE', #17407, #11640, #17524, .T. ) ;
#9381=ORIENTED_EDGE ( 'NONE', *, *, #27487, .T. ) ;
#9385=CARTESIAN_POINT ( 'NONE',  ( 6.224689322667647851, 146.9579047224771955, -18.02516478983991988 ) ) ;
#9386=CARTESIAN_POINT ( 'NONE',  ( 55.49584447822657296, 22.16497542184406200, 69.08290406177587784 ) ) ;
#9387=FACE_OUTER_BOUND ( 'NONE', #26313, .T. ) ;
#9388=EDGE_CURVE ( 'NONE', #20199, #4178, #11189, .T. ) ;
#9389=CARTESIAN_POINT ( 'NONE',  ( 109.1624594426973260, -0.01318243916934109389, 0.009004164758061344864 ) ) ;
#9391=CARTESIAN_POINT ( 'NONE',  ( 1.833485406944057594, 142.0485807715645876, 29.64752363041592531 ) ) ;
#9393=LINE ( 'NONE', #23217, #21770 ) ;
#9394=CARTESIAN_POINT ( 'NONE',  ( 26.11404676487259024, -108.0249973236465308, -33.91085499298486639 ) ) ;
#9396=CARTESIAN_POINT ( 'NONE',  ( 32.73300124599732186, 0.000000000000000000, 0.000000000000000000 ) ) ;
#9399=VERTEX_POINT ( 'NONE', #15621 ) ;
#9403=EDGE_CURVE ( 'NONE', #20917, #11289, #2828, .T. ) ;
#9405=FACE_OUTER_BOUND ( 'NONE', #21626, .T. ) ;
#9407=DIRECTION ( 'NONE',  ( -1.000000000000000000, -0.000000000000000000, -0.000000000000000000 ) ) ;
#9410=CARTESIAN_POINT ( 'NONE',  ( 25.64670758986457244, 112.9099239813695306, 0.4979020485381295269 ) ) ;
#9411=EDGE_CURVE ( 'NONE', #23363, #16816, #22953, .T. ) ;
#9412=CARTESIAN_POINT ( 'NONE',  ( 1.833206310202323941, 59.70089235435430197, 132.2594754479307255 ) ) ;
#9414=ORIENTED_EDGE ( 'NONE', *, *, #24663, .F. ) ;
#9416=CARTESIAN_POINT ( 'NONE',  ( 109.1592201516379674, 0.003661068210037295243, 0.006957642258146931775 ) ) ;
#9417=LINE ( 'NONE', #20621, #6596 ) ;
#9419=CARTESIAN_POINT ( 'NONE',  ( 1.833485406944043827, -107.4794113447415924, 97.49333871408656194 ) ) ;
#9421=CARTESIAN_POINT ( 'NONE',  ( 1.833838850855489255, -15.07960613928529092, -144.3241377520100173 ) ) ;
#9422=ORIENTED_EDGE ( 'NONE', *, *, #24664, .F. ) ;
#9425=ORIENTED_EDGE ( 'NONE', *, *, #4453, .F. ) ;
#9428=VERTEX_POINT ( 'NONE', #2837 ) ;
#9430=B_SPLINE_CURVE_WITH_KNOTS ( 'NONE', 3,
 ( #18197, #20644, #24715, #5108, #22694, #652, #16189, #5252 ),
 .UNSPECIFIED., .F., .F.,
 ( 4, 2, 2, 4 ),
 ( 0.000000000000000000, 0.0002429588503611278814, 0.0004859177007222557627, 0.0009718354014444947203 ),
 .UNSPECIFIED. ) ;
#9431=VERTEX_POINT ( 'NONE', #2986 ) ;
#9432=EDGE_CURVE ( 'NONE', #6115, #3474, #6123, .T. ) ;
#9433=CARTESIAN_POINT ( 'NONE',  ( 109.1586900883932856, -0.0006456433529162947105, -0.007109207791181750523 ) ) ;
#9434=CARTESIAN_POINT ( 'NONE',  ( 109.1586900883932856, 0.006960773163852190457, -0.001582822706032850245 ) ) ;
#9436=EDGE_CURVE ( 'NONE', #18370, #16400, #10901, .T. ) ;
#9438=CARTESIAN_POINT ( 'NONE',  ( 16.05277956358231961, 75.66118899150499999, 121.7045645913016898 ) ) ;
#9440=CARTESIAN_POINT ( 'NONE',  ( 25.86096068574581253, -0.9975172952966359086, 113.0494979885903888 ) ) ;
#9441=CARTESIAN_POINT ( 'NONE',  ( 28.37644542392838432, -86.16884085958004391, 89.64009552702880512 ) ) ;
#9442=ORIENTED_EDGE ( 'NONE', *, *, #28204, .F. ) ;
#9444=CARTESIAN_POINT ( 'NONE',  ( 25.64681081121879203, 91.59071981940572016, 66.03065707438965148 ) ) ;
#9446=CARTESIAN_POINT ( 'NONE',  ( 25.73574536432417403, -84.49061642666517002, 74.99093179013938482 ) ) ;
#9447=CARTESIAN_POINT ( 'NONE',  ( 25.64681081121879203, -84.18689316039996129, -75.24277141833577787 ) ) ;
#9448=ORIENTED_EDGE ( 'NONE', *, *, #12887, .T. ) ;
#9449=DIRECTION ( 'NONE',  ( -0.5914120900931443270, -0.07630783613001361487, 0.8027508043202532528 ) ) ;
#9451=CARTESIAN_POINT ( 'NONE',  ( 16.05277956358206737, -103.3141821208289031, 99.31161228512438299 ) ) ;
#9452=ORIENTED_EDGE ( 'NONE', *, *, #11086, .T. ) ;
#9453=CARTESIAN_POINT ( 'NONE',  ( 25.64681081121879203, 75.86069728269103507, -83.63051021305824406 ) ) ;
#9454=ORIENTED_EDGE ( 'NONE', *, *, #13757, .F. ) ;
#9455=B_SPLINE_CURVE_WITH_KNOTS ( 'NONE', 3,
 ( #10896, #19657, #4403, #8730, #21966, #2229, #11034 ),
 .UNSPECIFIED., .F., .F.,
 ( 4, 3, 4 ),
 ( 0.000000000000000000, 0.02398743853561323414, 0.04000277880656222251 ),
 .UNSPECIFIED. ) ;
#9457=( BOUNDED_SURFACE ( )  B_SPLINE_SURFACE ( 3, 1, ( 
 ( #17770, #26546 ),
 ( #15904, #22250 ),
 ( #22392, #2659 ),
 ( #501, #354 ) ),
 .UNSPECIFIED., .F., .F., .F. ) 
 B_SPLINE_SURFACE_WITH_KNOTS ( ( 4, 4 ),
 ( 2, 2 ),
 ( 0.000000000000000000, 1.000000000000000000 ),
 ( 0.000000000000000000, 1.000000000000000000 ),
 .UNSPECIFIED. ) 
 GEOMETRIC_REPRESENTATION_ITEM ( )  RATIONAL_B_SPLINE_SURFACE ( (
 ( 1.000000000000000000, 1.000000000000000000),
 ( 0.9960225298536222738, 0.9999952330161893110),
 ( 0.9960225298536222738, 0.9999952330161893110),
 ( 1.000000000000000000, 1.000000000000000000) ) ) 
 REPRESENTATION_ITEM ( '' )  SURFACE ( )  );
#9458=CARTESIAN_POINT ( 'NONE',  ( 28.37644542392841274, 8.957364412600206549, 124.0168596762486715 ) ) ;
#9460=ORIENTED_EDGE ( 'NONE', *, *, #7535, .F. ) ;
#9461=CARTESIAN_POINT ( 'NONE',  ( 109.1586900883932856, 0.0008465529156635116835, 0.007088091345229658585 ) ) ;
#9462=ORIENTED_EDGE ( 'NONE', *, *, #2731, .T. ) ;
#9464=EDGE_CURVE ( 'NONE', #18908, #19494, #18218, .T. ) ;
#9468=EDGE_CURVE ( 'NONE', #4669, #6221, #16405, .T. ) ;
#9469=CARTESIAN_POINT ( 'NONE',  ( 10.93730112726002979, 104.7670965581027644, -108.9902118373731241 ) ) ;
#9471=CARTESIAN_POINT ( 'NONE',  ( 1.833485406944043827, -125.4007332306540405, -73.01664920993097496 ) ) ;
#9472=ADVANCED_FACE ( 'NONE', ( #9748 ), #25231, .F. ) ;
#9473=ORIENTED_EDGE ( 'NONE', *, *, #24725, .F. ) ;
#9475=CARTESIAN_POINT ( 'NONE',  ( 10.93730112725992676, -65.95960219663038515, -136.0306644680990473 ) ) ;
#9477=ORIENTED_EDGE ( 'NONE', *, *, #19330, .T. ) ;
#9481=CARTESIAN_POINT ( 'NONE',  ( 2.433796855181233454, 98.43889364293860922, 107.1581411821788947 ) ) ;
#9482=CARTESIAN_POINT ( 'NONE',  ( 25.64670758986459376, -23.96231489924965885, 110.3390515846397477 ) ) ;
#9483=B_SPLINE_CURVE_WITH_KNOTS ( 'NONE', 3,
 ( #23767, #3885, #19276, #19143, #10382, #12787 ),
 .UNSPECIFIED., .F., .F.,
 ( 4, 2, 4 ),
 ( 6.942281208919283290E-18, 0.0006311571484585998260, 0.001262314296917192713 ),
 .UNSPECIFIED. ) ;
#9485=CARTESIAN_POINT ( 'NONE',  ( 25.64703792032471341, -83.80974623566345372, 75.66285916808271850 ) ) ;
#9486=CARTESIAN_POINT ( 'NONE',  ( 2.433796855181205476, -86.69855925934052721, 116.8607839509053434 ) ) ;
#9487=EDGE_LOOP ( 'NONE', ( #1671, #28050, #20665, #1871 ) ) ;
#9488=CARTESIAN_POINT ( 'NONE',  ( 13.84597867724968623, -137.9700459519984861, -49.85807424839893542 ) ) ;
#9490=CARTESIAN_POINT ( 'NONE',  ( 25.64704443564079384, 11.66968230815913898, 112.3065506427462310 ) ) ;
#9492=CARTESIAN_POINT ( 'NONE',  ( 1.832998868059890096, -72.09222286251173273, 125.9352106559981621 ) ) ;
#9493=CARTESIAN_POINT ( 'NONE',  ( 1.833485406944043827, 125.9346397303445286, -72.09189602597577107 ) ) ;
#9494=ORIENTED_EDGE ( 'NONE', *, *, #23752, .T. ) ;
#9495=CARTESIAN_POINT ( 'NONE',  ( 25.81918753295380498, -12.74259626488075980, -112.3053965977762800 ) ) ;
#9497=CARTESIAN_POINT ( 'NONE',  ( 25.64681081121879203, 110.3564950173084895, -23.88203588907973085 ) ) ;
#9498=CARTESIAN_POINT ( 'NONE',  ( 1.832998868059858122, 44.33343224355416368, -138.1720401012262585 ) ) ;
#9502=ORIENTED_EDGE ( 'NONE', *, *, #755, .F. ) ;
#9503=ADVANCED_FACE ( 'NONE', ( #22570 ), #3525, .F. ) ;
#9504=( BOUNDED_SURFACE ( )  B_SPLINE_SURFACE ( 3, 1, ( 
 ( #20318, #13555 ),
 ( #6960, #20606 ),
 ( #24807, #7532 ),
 ( #20464, #16292 ) ),
 .UNSPECIFIED., .F., .F., .F. ) 
 B_SPLINE_SURFACE_WITH_KNOTS ( ( 4, 4 ),
 ( 2, 2 ),
 ( 0.000000000000000000, 1.000000000000000000 ),
 ( 0.000000000000000000, 1.000000000000000000 ),
 .UNSPECIFIED. ) 
 GEOMETRIC_REPRESENTATION_ITEM ( )  RATIONAL_B_SPLINE_SURFACE ( (
 ( 1.000000000000000000, 1.000000000000000000),
 ( 0.9956975270656955868, 0.8568959468854907557),
 ( 0.9956975270656955868, 0.8568959468854907557),
 ( 1.000000000000000000, 1.000000000000000000) ) ) 
 REPRESENTATION_ITEM ( '' )  SURFACE ( )  );
#9505=DIRECTION ( 'NONE',  ( -1.000000000000000000, -0.000000000000000000, -0.000000000000000000 ) ) ;
#9506=CARTESIAN_POINT ( 'NONE',  ( 1.831572820252008738, 96.36280042115929234, 108.4969585352558141 ) ) ;
#9507=DIRECTION ( 'NONE',  ( 0.000000000000000000, 0.000000000000000000, 1.000000000000000000 ) ) ;
#9508=CARTESIAN_POINT ( 'NONE',  ( 55.49584447822657296, 54.09506550945626202, 48.34726110740004401 ) ) ;
#9509=ORIENTED_EDGE ( 'NONE', *, *, #22969, .T. ) ;
#9512=CARTESIAN_POINT ( 'NONE',  ( 109.1587776205901577, -0.001605238040359084932, 0.007151389024634731938 ) ) ;
#9514=ORIENTED_EDGE ( 'NONE', *, *, #13936, .F. ) ;
#9517=FACE_OUTER_BOUND ( 'NONE', #22822, .T. ) ;
#9518=CARTESIAN_POINT ( 'NONE',  ( 2.263178113027033866, 96.24282436106614114, 108.9830942735796953 ) ) ;
#9519=CARTESIAN_POINT ( 'NONE',  ( 1.832998868059858122, 137.8420662456170191, 45.34898734666095521 ) ) ;
#9520=B_SPLINE_CURVE_WITH_KNOTS ( 'NONE', 3,
 ( #8728, #26143, #4125, #8458 ),
 .UNSPECIFIED., .F., .F.,
 ( 4, 4 ),
 ( 0.000000000000000000, 0.01077107196513892549 ),
 .UNSPECIFIED. ) ;
#9521=VERTEX_POINT ( 'NONE', #6007 ) ;
#9523=CARTESIAN_POINT ( 'NONE',  ( 10.93730112725994275, -36.23586118136433498, -146.7718404940647190 ) ) ;
#9525=CARTESIAN_POINT ( 'NONE',  ( 25.65782528836482257, -75.98558751977830639, 83.52701600504848045 ) ) ;
#9527=ORIENTED_EDGE ( 'NONE', *, *, #26992, .F. ) ;
#9528=CARTESIAN_POINT ( 'NONE',  ( 1.833603222531972055, 145.1089511853978422, 0.4449221977524496774 ) ) ;
#9529=ORIENTED_EDGE ( 'NONE', *, *, #21053, .F. ) ;
#9530=B_SPLINE_CURVE_WITH_KNOTS ( 'NONE', 3,
 ( #5703, #16484, #20802, #13890, #18645, #25132, #18784, #7430 ),
 .UNSPECIFIED., .F., .F.,
 ( 4, 2, 2, 4 ),
 ( 0.000000000000000000, 0.0002429588503611257672, 0.0004859177007222515343, 0.0009718354014445030687 ),
 .UNSPECIFIED. ) ;
#9531=EDGE_LOOP ( 'NONE', ( #28270, #1455, #8131, #15249 ) ) ;
#9532=EDGE_CURVE ( 'NONE', #16816, #27092, #21194, .T. ) ;
#9534=DIRECTION ( 'NONE',  ( 0.5914120900931444380, -0.09226095020378993761, 0.8010740644654227305 ) ) ;
#9535=EDGE_CURVE ( 'NONE', #27686, #14763, #12050, .T. ) ;
#9538=B_SPLINE_CURVE_WITH_KNOTS ( 'NONE', 3,
 ( #16866, #1028, #25650, #23354 ),
 .UNSPECIFIED., .F., .F.,
 ( 4, 4 ),
 ( 2.031330821370476332E-16, 0.008383748772659684392 ),
 .UNSPECIFIED. ) ;
#9540=CARTESIAN_POINT ( 'NONE',  ( 1.832998868059858122, 142.0492247521726199, -29.64765804469933386 ) ) ;
#9542=CARTESIAN_POINT ( 'NONE',  ( 25.70243777736190438, 107.6443926015135304, -34.20488708977986647 ) ) ;
#9543=CARTESIAN_POINT ( 'NONE',  ( 109.1586900883932856, -0.005833932871491344374, -0.004113747440992306104 ) ) ;
#9544=CARTESIAN_POINT ( 'NONE',  ( 2.430230287190572103, 13.76600171652642857, 144.8619874886007324 ) ) ;
#9547=CARTESIAN_POINT ( 'NONE',  ( 25.64708228042118421, -66.33571787052753166, -91.37028996123333968 ) ) ;
#9551=CARTESIAN_POINT ( 'NONE',  ( 109.1778270068192853, 0.009177562596826678576, -0.001591747944959453478 ) ) ;
#9553=CARTESIAN_POINT ( 'NONE',  ( 28.43349137099836810, 29.78331910005492489, 120.6297847406436858 ) ) ;
#9555=ORIENTED_EDGE ( 'NONE', *, *, #10269, .F. ) ;
#9556=CARTESIAN_POINT ( 'NONE',  ( 25.73574536432417759, 103.5288236655401732, -45.21157800100201030 ) ) ;
#9557=CARTESIAN_POINT ( 'NONE',  ( 25.86096068574580187, -12.80894308910809976, 112.3259320600844404 ) ) ;
#9558=ORIENTED_EDGE ( 'NONE', *, *, #2658, .T. ) ;
#9559=EDGE_CURVE ( 'NONE', #2065, #23678, #22088, .T. ) ;
#9560=ORIENTED_EDGE ( 'NONE', *, *, #12599, .F. ) ;
#9562=EDGE_CURVE ( 'NONE', #17914, #1034, #1615, .T. ) ;
#9563=CARTESIAN_POINT ( 'NONE',  ( 109.1624594426973260, 0.009754804742273283369, -0.01263706729758985563 ) ) ;
#9564=ADVANCED_FACE ( 'NONE', ( #23284 ), #20075, .F. ) ;
#9565=DIRECTION ( 'NONE',  ( 0.000000000000000000, 0.000000000000000000, 1.000000000000000000 ) ) ;
#9566=CARTESIAN_POINT ( 'NONE',  ( 1.833809397773857208, 144.3333383260368805, -14.99109763363995818 ) ) ;
#9569=FACE_OUTER_BOUND ( 'NONE', #26120, .T. ) ;
#9570=CARTESIAN_POINT ( 'NONE',  ( 8.186469777910877710, -102.4860666868856924, -108.6390983781767972 ) ) ;
#9573=CARTESIAN_POINT ( 'NONE',  ( 2.430230287190572103, -132.3371620660946917, -60.50928654924886985 ) ) ;
#9574=CARTESIAN_POINT ( 'NONE',  ( 28.37603512858454735, -48.29936889363892760, -104.0705994281842095 ) ) ;
#9575=ORIENTED_EDGE ( 'NONE', *, *, #21012, .F. ) ;
#9576=ORIENTED_EDGE ( 'NONE', *, *, #6249, .F. ) ;
#9578=CARTESIAN_POINT ( 'NONE',  ( 10.93730112726002623, 65.95960219663321311, -136.0306644680977683 ) ) ;
#9580=CARTESIAN_POINT ( 'NONE',  ( 10.93730112725993919, -42.00474393596157086, -145.2260730187406352 ) ) ;
#9581=CARTESIAN_POINT ( 'NONE',  ( 28.37644542392844826, 29.80435743554116712, -120.7150203538605240 ) ) ;
#9582=CARTESIAN_POINT ( 'NONE',  ( 32.73300124599739291, -113.0038235389599635, -32.68291970228351317 ) ) ;
#9586=DIRECTION ( 'NONE',  ( -1.000000000000000000, -0.000000000000000000, -0.000000000000000000 ) ) ;
#9587=CARTESIAN_POINT ( 'NONE',  ( 10.93730112725992853, -56.95489579269655422, -140.0398180619117738 ) ) ;
#9588=CARTESIAN_POINT ( 'NONE',  ( 28.43349137099833968, -89.57679848841864612, 86.10800331998756008 ) ) ;
#9589=ORIENTED_EDGE ( 'NONE', *, *, #16621, .T. ) ;
#9593=CARTESIAN_POINT ( 'NONE',  ( 30.58324630866339433, -119.8048187378265226, 16.55818995381107683 ) ) ;
#9594=EDGE_CURVE ( 'NONE', #24974, #2917, #8295, .T. ) ;
#9596=CARTESIAN_POINT ( 'NONE',  ( 2.263178607246675078, -132.2496131833833601, 60.41552769843774939 ) ) ;
#9598=DIRECTION ( 'NONE',  ( -1.000000000000000000, -0.000000000000000000, -0.000000000000000000 ) ) ;
#9599=ORIENTED_EDGE ( 'NONE', *, *, #27252, .F. ) ;
#9601=VERTEX_POINT ( 'NONE', #21388 ) ;
#9604=CARTESIAN_POINT ( 'NONE',  ( 25.64704443564078318, 107.4261196778967502, -34.76451658509423481 ) ) ;
#9605=CARTESIAN_POINT ( 'NONE',  ( 24.01988960052056754, 130.9749633972838296, 4.273195451969105108 ) ) ;
#9607=ORIENTED_EDGE ( 'NONE', *, *, #8489, .F. ) ;
#9609=DIRECTION ( 'NONE',  ( -1.000000000000000000, -0.000000000000000000, -0.000000000000000000 ) ) ;
#9611=CARTESIAN_POINT ( 'NONE',  ( 25.69398547355838502, 98.18017599249837701, 55.82723250638802881 ) ) ;
#9614=ORIENTED_EDGE ( 'NONE', *, *, #23662, .F. ) ;
#9618=FACE_OUTER_BOUND ( 'NONE', #1133, .T. ) ;
#9621=CARTESIAN_POINT ( 'NONE',  ( 25.64704443564076897, -83.99864088993820133, 75.45310550990124909 ) ) ;
#9623=ORIENTED_EDGE ( 'NONE', *, *, #12539, .F. ) ;
#9624=CARTESIAN_POINT ( 'NONE',  ( 10.93730112726002623, 65.95960219663321311, -136.0306644680977683 ) ) ;
#9626=( BOUNDED_SURFACE ( )  B_SPLINE_SURFACE ( 3, 1, ( 
 ( #20015, #13384 ),
 ( #6936, #15257 ),
 ( #23933, #4336 ),
 ( #4193, #26208 ) ),
 .UNSPECIFIED., .F., .F., .F. ) 
 B_SPLINE_SURFACE_WITH_KNOTS ( ( 4, 4 ),
 ( 2, 2 ),
 ( 0.000000000000000000, 1.000000000000000000 ),
 ( 0.000000000000000000, 1.000000000000000000 ),
 .UNSPECIFIED. ) 
 GEOMETRIC_REPRESENTATION_ITEM ( )  RATIONAL_B_SPLINE_SURFACE ( (
 ( 1.000000000000000000, 1.000000000000000000),
 ( 0.9956975270656954757, 0.8568959468854893125),
 ( 0.9956975270656954757, 0.8568959468854893125),
 ( 1.000000000000000000, 1.000000000000000000) ) ) 
 REPRESENTATION_ITEM ( '' )  SURFACE ( )  );
#9627=CARTESIAN_POINT ( 'NONE',  ( 26.11404676487257603, 36.06104232266594067, -107.3263591096426666 ) ) ;
#9629=CARTESIAN_POINT ( 'NONE',  ( 32.73300124599741423, 114.2056417606551406, -28.19767303745493336 ) ) ;
#9632=ORIENTED_EDGE ( 'NONE', *, *, #26538, .T. ) ;
#9633=CARTESIAN_POINT ( 'NONE',  ( 25.98552792386800192, -12.89843290883451665, -112.3992180166320765 ) ) ;
#9635=EDGE_CURVE ( 'NONE', #26995, #10146, #7500, .T. ) ;
#9637=ORIENTED_EDGE ( 'NONE', *, *, #14189, .T. ) ;
#9641=ORIENTED_EDGE ( 'NONE', *, *, #4816, .T. ) ;
#9643=CARTESIAN_POINT ( 'NONE',  ( 109.1721716018069515, 0.007126480965767985690, -0.01550977894511847664 ) ) ;
#9646=CARTESIAN_POINT ( 'NONE',  ( 25.64670758986457244, 66.76959937251574217, -91.05338785329374218 ) ) ;
#9647=CARTESIAN_POINT ( 'NONE',  ( 25.64692232868534560, -103.0161468101950533, 46.22343382108700638 ) ) ;
#9649=CARTESIAN_POINT ( 'NONE',  ( 26.11404676487259024, 22.43340081644921113, -110.9778746459744667 ) ) ;
#9651=ORIENTED_EDGE ( 'NONE', *, *, #16071, .F. ) ;
#9657=CARTESIAN_POINT ( 'NONE',  ( 1.893872463202060707, -84.54426271294347828, -117.9862474593105617 ) ) ;
#9658=ADVANCED_FACE ( 'NONE', ( #10877 ), #19325, .F. ) ;
#9662=CARTESIAN_POINT ( 'NONE',  ( 25.64681081121879203, 84.18689316040146764, -75.24277141833410099 ) ) ;
#9664=ADVANCED_FACE ( 'NONE', ( #15167 ), #19013, .F. ) ;
#9665=CARTESIAN_POINT ( 'NONE',  ( 109.1589550718174877, -0.0002241941239240967485, 0.007571935245604908063 ) ) ;
#9667=EDGE_CURVE ( 'NONE', #21777, #28456, #24313, .T. ) ;
#9668=CARTESIAN_POINT ( 'NONE',  ( 1.833485406944043827, -137.8414413349082110, -45.34878176254374438 ) ) ;
#9670=CARTESIAN_POINT ( 'NONE',  ( 28.43349137099837165, -102.8504004831930843, -69.71646995966284521 ) ) ;
#9671=ORIENTED_EDGE ( 'NONE', *, *, #25112, .F. ) ;
#9673=VERTEX_POINT ( 'NONE', #6282 ) ;
#9675=AXIS2_PLACEMENT_3D ( 'NONE', #23889, #26162, #15205 ) ;
#9676=AXIS2_PLACEMENT_3D ( 'NONE', #18193, #4683, #22691 ) ;
#9677=CARTESIAN_POINT ( 'NONE',  ( 24.01988960052068833, 117.9135177031536159, 57.17607523395246716 ) ) ;
#9678=CARTESIAN_POINT ( 'NONE',  ( 109.1624594426973260, 0.003771499231549574858, -0.01551217196236920511 ) ) ;
#9679=CARTESIAN_POINT ( 'NONE',  ( 2.433796855181205476, -98.43889364293931976, 107.1581411821782268 ) ) ;
#9682=CARTESIAN_POINT ( 'NONE',  ( 2.063896406836609909, 137.7380992975108995, -46.16709813092479919 ) ) ;
#9683=DIRECTION ( 'NONE',  ( 0.000000000000000000, 0.000000000000000000, 1.000000000000000000 ) ) ;
#9685=CARTESIAN_POINT ( 'NONE',  ( 32.73300124599740002, 110.6325518752278896, -39.98094346392192477 ) ) ;
#9686=DIRECTION ( 'NONE',  ( -1.000000000000000000, -0.000000000000000000, -0.000000000000000000 ) ) ;
#9687=CARTESIAN_POINT ( 'NONE',  ( 25.73574536432413851, -55.78561308781419115, -98.23578516675019046 ) ) ;
#9688=EDGE_CURVE ( 'NONE', #10668, #26700, #9857, .T. ) ;
#9689=CARTESIAN_POINT ( 'NONE',  ( 25.64681081121879203, -66.03065707438874199, -91.59071981940638807 ) ) ;
#9690=AXIS2_PLACEMENT_3D ( 'NONE', #10786, #4008, #11055 ) ;
#9691=EDGE_CURVE ( 'NONE', #14673, #4178, #14985, .T. ) ;
#9692=CARTESIAN_POINT ( 'NONE',  ( 25.69398547355841345, 76.12333255527515519, 83.43419615433019487 ) ) ;
#9693=CARTESIAN_POINT ( 'NONE',  ( 2.433796855181205476, -71.49415740224986848, -126.7346379669263001 ) ) ;
#9694=CARTESIAN_POINT ( 'NONE',  ( 109.1624594426973260, 0.01438905500501226620, 0.006914244825461683328 ) ) ;
#9695=ORIENTED_EDGE ( 'NONE', *, *, #6002, .T. ) ;
#9696=CARTESIAN_POINT ( 'NONE',  ( 9.884929003653626367, 150.4771565009630478, -4.203795436552884013 ) ) ;
#9697=VECTOR ( 'NONE', #3228, 1000.000000000000114 ) ;
#9698=EDGE_LOOP ( 'NONE', ( #8002, #17022, #26286, #7774, #5857, #6700, #8035, #26974, #5036, #5052, #18357, #26361, #12964, #8821, #372, #19364, #305, #28405, #20382, #20376, #13465, #6467, #11389, #18496, #3194, #13978, #1551, #20954, #12371, #18641, #2259, #3725, #485, #1483, #18930, #4065, #10534, #851, #15890, #20309, #16061, #6150, #14097, #5275, #10206, #12360, #18676, #10909, #25464, #15431, #23464, #15675, #27542, #21300, #26574, #2727, #22431, #9641, #10176, #9589, #10578, #4610, #2987, #11455, #22469, #5870, #2992, #27195, #1460, #4386, #25738, #5840, #4102, #23057, #5326, #17266, #21209, #17821, #11119, #11156, #27847, #15103, #16143, #22877, #7303, #24546, #15126, #17723, #5261, #5043, #25286, #27422, #17743, #24481, #9367, #22129, #14008, #20746, #25970, #18627, #17298, #6260, #21503, #25577, #22511, #10396, #11604, #24303, #19965, #25843, #28069, #26963, #6699, #14825, #5015, #19688, #16549, #20333, #2348, #12655, #21448, #22292, #24829, #2278, #25334, #20352, #11286, #7407, #11083, #26612, #922, #24323, #21047, #12111, #23558, #22444, #8854, #20052, #20851, #20769, #23675, #16020, #15839, #7102, #3416, #2034, #17279, #5033, #23350, #11970, #13867, #14848, #263, #9494, #1631, #2476, #5203, #14651, #7818, #13157, #4575, #28239, #21459, #14440, #20591, #18761, #25166, #2172, #5231, #23168, #5994, #22194, #9637, #15783, #21279, #24800, #28423, #5492, #15635, #3317, #10333, #15600, #10673, #21683 ) ) ;
#9699=CARTESIAN_POINT ( 'NONE',  ( 1.832998868059890096, 14.63705790014200936, -144.3700883710215521 ) ) ;
#9700=CARTESIAN_POINT ( 'NONE',  ( 109.1721716018069657, -0.01629455849720094079, -0.005082060336469356072 ) ) ;
#9703=VERTEX_POINT ( 'NONE', #21492 ) ;
#9704=( BOUNDED_SURFACE ( )  B_SPLINE_SURFACE ( 3, 1, ( 
 ( #16386, #10069 ),
 ( #5304, #27601 ),
 ( #27464, #16685 ),
 ( #19121, #18982 ) ),
 .UNSPECIFIED., .F., .F., .F. ) 
 B_SPLINE_SURFACE_WITH_KNOTS ( ( 4, 4 ),
 ( 2, 2 ),
 ( 0.000000000000000000, 1.000000000000000000 ),
 ( 0.000000000000000000, 1.000000000000000000 ),
 .UNSPECIFIED. ) 
 GEOMETRIC_REPRESENTATION_ITEM ( )  RATIONAL_B_SPLINE_SURFACE ( (
 ( 1.000000000000000000, 1.000000000000000000),
 ( 0.9956975270656954757, 0.8568959468854893125),
 ( 0.9956975270656954757, 0.8568959468854893125),
 ( 1.000000000000000000, 1.000000000000000000) ) ) 
 REPRESENTATION_ITEM ( '' )  SURFACE ( )  );
#9709=CARTESIAN_POINT ( 'NONE',  ( 6.224689322667647851, 89.08920297664211319, 118.2566963816774290 ) ) ;
#9710=CARTESIAN_POINT ( 'NONE',  ( 109.1586059443104944, 0.006344953511159727791, -0.003127959656221018965 ) ) ;
#9711=VECTOR ( 'NONE', #13463, 1000.000000000000114 ) ;
#9712=AXIS2_PLACEMENT_3D ( 'NONE', #13885, #22398, #2664 ) ;
#9714=CARTESIAN_POINT ( 'NONE',  ( 25.64708010899966695, -66.32331961783448548, 91.37928813995148403 ) ) ;
#9717=CARTESIAN_POINT ( 'NONE',  ( 32.73300124599735739, -81.52272205837257957, 84.80615050150346690 ) ) ;
#9719=CARTESIAN_POINT ( 'NONE',  ( 109.1589550718175161, -0.003980125429509265116, -0.006445391216541633550 ) ) ;
#9721=CARTESIAN_POINT ( 'NONE',  ( 55.49584447822657296, 48.34726110739985927, 54.09506550945642545 ) ) ;
#9724=CARTESIAN_POINT ( 'NONE',  ( 119.2224693531408803, 90.00000000000005684, -19.99999999999998934 ) ) ;
#9727=ORIENTED_EDGE ( 'NONE', *, *, #7695, .F. ) ;
#9729=CARTESIAN_POINT ( 'NONE',  ( 25.64700659047694842, 66.55152787776250989, -91.21315746821456116 ) ) ;
#9730=CARTESIAN_POINT ( 'NONE',  ( 25.64708228042118421, -91.37028996123309810, 66.33571787052784430 ) ) ;
#9732=CARTESIAN_POINT ( 'NONE',  ( 1.833721034905632985, -85.00517831633766264, 117.6051524288280916 ) ) ;
#9733=CARTESIAN_POINT ( 'NONE',  ( 94.22246935314088034, -151.1871800109700246, -6.938893903907228378E-15 ) ) ;
#9734=CARTESIAN_POINT ( 'NONE',  ( 10.93730112726002623, 56.95489579269933955, -140.0398180619107507 ) ) ;
#9736=EDGE_LOOP ( 'NONE', ( #6166, #12418, #19257, #20877 ) ) ;
#9737=CARTESIAN_POINT ( 'NONE',  ( 25.86096068574582674, 98.40249579084591858, -55.66087367585303980 ) ) ;
#9738=CARTESIAN_POINT ( 'NONE',  ( 1.832998868059858122, 144.2584710144580242, 15.69902610990423319 ) ) ;
#9739=CARTESIAN_POINT ( 'NONE',  ( 55.49584447822657296, -29.26468316696818306, 66.38758986585106925 ) ) ;
#9740=VERTEX_POINT ( 'NONE', #8574 ) ;
#9741=CARTESIAN_POINT ( 'NONE',  ( 94.22246935314088034, -151.1871800109700246, 12.49999999999999467 ) ) ;
#9742=AXIS2_PLACEMENT_3D ( 'NONE', #4707, #1832, #8607 ) ;
#9743=DIRECTION ( 'NONE',  ( 0.7071067811865464625, -2.207942520024055603E-15, 0.7071067811865485719 ) ) ;
#9744=CONICAL_SURFACE ( 'NONE', #17530, 117.6351876552689504, 0.9945805576725580410 ) ;
#9745=ORIENTED_EDGE ( 'NONE', *, *, #23752, .F. ) ;
#9747=ORIENTED_EDGE ( 'NONE', *, *, #1276, .T. ) ;
#9748=FACE_OUTER_BOUND ( 'NONE', #22041, .T. ) ;
#9755=CARTESIAN_POINT ( 'NONE',  ( 1.833838850093517880, 0.08898415480168050951, -145.1097630783160923 ) ) ;
#9756=CARTESIAN_POINT ( 'NONE',  ( 109.1592201516379674, 0.002720803050361310545, -0.007376275279030886783 ) ) ;
#9757=ADVANCED_FACE ( 'NONE', ( #2213 ), #24906, .F. ) ;
#9758=VERTEX_POINT ( 'NONE', #24267 ) ;
#9759=B_SPLINE_CURVE_WITH_KNOTS ( 'NONE', 3,
 ( #24727, #26850, #13468, #7158, #11454, #22708, #27280 ),
 .UNSPECIFIED., .F., .F.,
 ( 4, 3, 4 ),
 ( 1.913235636441834259E-16, 0.02816610861753247180, 0.04000277880656216006 ),
 .UNSPECIFIED. ) ;
#9761=( BOUNDED_SURFACE ( )  B_SPLINE_SURFACE ( 3, 1, ( 
 ( #23600, #3859 ),
 ( #17229, #12624 ),
 ( #1684, #17088 ),
 ( #25881, #14925 ) ),
 .UNSPECIFIED., .F., .F., .F. ) 
 B_SPLINE_SURFACE_WITH_KNOTS ( ( 4, 4 ),
 ( 2, 2 ),
 ( 0.000000000000000000, 1.000000000000000000 ),
 ( 0.000000000000000000, 1.000000000000000000 ),
 .UNSPECIFIED. ) 
 GEOMETRIC_REPRESENTATION_ITEM ( )  RATIONAL_B_SPLINE_SURFACE ( (
 ( 1.000000000000000000, 1.000000000000000000),
 ( 0.9960225298536222738, 0.9999952330161893110),
 ( 0.9960225298536222738, 0.9999952330161893110),
 ( 1.000000000000000000, 1.000000000000000000) ) ) 
 REPRESENTATION_ITEM ( '' )  SURFACE ( )  );
#9763=CARTESIAN_POINT ( 'NONE',  ( 2.430230287190592531, -137.9371479820465254, 46.34481016236778572 ) ) ;
#9764=CARTESIAN_POINT ( 'NONE',  ( 10.93730112726006176, 142.1801301103792809, -51.37919228020152929 ) ) ;
#9766=AXIS2_PLACEMENT_3D ( 'NONE', #21186, #1470, #24209 ) ;
#9768=VERTEX_POINT ( 'NONE', #9008 ) ;
#9769=ORIENTED_EDGE ( 'NONE', *, *, #19441, .F. ) ;
#9771=CARTESIAN_POINT ( 'NONE',  ( 24.01988960052073452, 73.52806416354073349, 108.4726924928698679 ) ) ;
#9772=CARTESIAN_POINT ( 'NONE',  ( 13.84597867724989229, 115.8103190066271679, 90.05293531772652216 ) ) ;
#9773=CARTESIAN_POINT ( 'NONE',  ( 25.64692232868534560, 11.47740546588784483, -112.3263170481596234 ) ) ;
#9774=CARTESIAN_POINT ( 'NONE',  ( 25.64681081121879203, 56.81519825470891760, -97.57530875170544959 ) ) ;
#9775=CARTESIAN_POINT ( 'NONE',  ( 55.49584447822657296, -71.02133150427263786, 14.82242356767912561 ) ) ;
#9778=ADVANCED_FACE ( 'NONE', ( #22249 ), #21014, .F. ) ;
#9779=ORIENTED_EDGE ( 'NONE', *, *, #6002, .F. ) ;
#9780=CARTESIAN_POINT ( 'NONE',  ( 30.59141879584275969, 105.0379937202713734, 49.72305007553475775 ) ) ;
#9782=CARTESIAN_POINT ( 'NONE',  ( 25.64670758986457244, 110.3390515846398472, 23.96231489924928937 ) ) ;
#9783=CARTESIAN_POINT ( 'NONE',  ( 25.69398547355837437, -66.98507266663692405, -90.93418986874874577 ) ) ;
#9786=CARTESIAN_POINT ( 'NONE',  ( 26.28373643307438101, 118.1623717393431008, 48.05579805965559359 ) ) ;
#9787=ORIENTED_EDGE ( 'NONE', *, *, #13803, .F. ) ;
#9788=CARTESIAN_POINT ( 'NONE',  ( 1.834118845439484335, 58.85894970555094829, -132.6369225636068165 ) ) ;
#9793=VERTEX_POINT ( 'NONE', #28412 ) ;
#9795=CIRCLE ( 'NONE', #17133, 37.50000000000002132 ) ;
#9796=DIRECTION ( 'NONE',  ( 0.5946245182733607137, -0.08697490616139977315, 0.7992853357633863398 ) ) ;
#9797=LINE ( 'NONE', #17102, #11409 ) ;
#9798=CARTESIAN_POINT ( 'NONE',  ( 1.833206308920083183, 73.19872517709890758, -125.2945011813198164 ) ) ;
#9800=CARTESIAN_POINT ( 'NONE',  ( 2.263178607246687069, 57.85473702627292170, -133.3897506477015895 ) ) ;
#9801=CARTESIAN_POINT ( 'NONE',  ( 25.98552792386799482, 97.43552975939697092, -57.50018541500323721 ) ) ;
#9802=ORIENTED_EDGE ( 'NONE', *, *, #11438, .F. ) ;
#9804=EDGE_CURVE ( 'NONE', #22601, #8915, #10205, .T. ) ;
#9805=CARTESIAN_POINT ( 'NONE',  ( 1.833485406944043827, 45.34878176254417070, -137.8414413349080974 ) ) ;
#9807=ORIENTED_EDGE ( 'NONE', *, *, #8291, .F. ) ;
#9808=( BOUNDED_SURFACE ( )  B_SPLINE_SURFACE ( 3, 1, ( 
 ( #27584, #25161 ),
 ( #1249, #7905 ),
 ( #972, #23432 ),
 ( #1120, #9763 ) ),
 .UNSPECIFIED., .F., .F., .F. ) 
 B_SPLINE_SURFACE_WITH_KNOTS ( ( 4, 4 ),
 ( 2, 2 ),
 ( 0.000000000000000000, 1.000000000000000000 ),
 ( 0.000000000000000000, 1.000000000000000000 ),
 .UNSPECIFIED. ) 
 GEOMETRIC_REPRESENTATION_ITEM ( )  RATIONAL_B_SPLINE_SURFACE ( (
 ( 1.000000000000000000, 1.000000000000000000),
 ( 0.6386103224230316178, 0.9954351624131538845),
 ( 0.6386103224230316178, 0.9954351624131538845),
 ( 1.000000000000000000, 1.000000000000000000) ) ) 
 REPRESENTATION_ITEM ( '' )  SURFACE ( )  );
#9813=CARTESIAN_POINT ( 'NONE',  ( 1.834118845439484335, 132.4921483272736396, -59.18411796426921967 ) ) ;
#9815=CARTESIAN_POINT ( 'NONE',  ( 2.263178113027032978, 144.4462808674010148, 16.59120315151625746 ) ) ;
#9818=CARTESIAN_POINT ( 'NONE',  ( 25.86096068574579121, 84.67961880569399113, -74.90357932134547525 ) ) ;
#9819=CARTESIAN_POINT ( 'NONE',  ( 2.430230287190581429, -137.9371479820459570, -46.34481016236964734 ) ) ;
#9822=CARTESIAN_POINT ( 'NONE',  ( 2.430230287190589422, -57.85706160874236303, 133.5180086894989415 ) ) ;
#9824=EDGE_LOOP ( 'NONE', ( #3101, #2916, #18624, #28207 ) ) ;
#9826=ORIENTED_EDGE ( 'NONE', *, *, #10740, .T. ) ;
#9828=VECTOR ( 'NONE', #12804, 1000.000000000000000 ) ;
#9830=CARTESIAN_POINT ( 'NONE',  ( 1.831572820252009626, 125.1738732943820480, -73.40899645745874125 ) ) ;
#9831=CARTESIAN_POINT ( 'NONE',  ( 30.58324630866346183, 45.56259622822511801, -112.0331114996530459 ) ) ;
#9834=CARTESIAN_POINT ( 'NONE',  ( 109.1586059443104944, 0.005555961672780061582, 0.004378796245583053796 ) ) ;
#9835=CARTESIAN_POINT ( 'NONE',  ( 1.831572820252008738, 142.1425225354583688, -29.20415387690428233 ) ) ;
#9837=B_SPLINE_CURVE_WITH_KNOTS ( 'NONE', 3,
 ( #15401, #23801, #19725, #4335 ),
 .UNSPECIFIED., .F., .F.,
 ( 4, 4 ),
 ( 0.000000000000000000, 0.01077107196513872600 ),
 .UNSPECIFIED. ) ;
#9838=CARTESIAN_POINT ( 'NONE',  ( 25.64670758986458665, 107.5375791514047705, -34.41755235608631125 ) ) ;
#9840=CARTESIAN_POINT ( 'NONE',  ( 1.833838848569443458, -85.43736077718784827, -117.2916552720327275 ) ) ;
#9841=CARTESIAN_POINT ( 'NONE',  ( 25.64700659047693776, -75.38309044531831660, -84.06149911284524023 ) ) ;
#9842=AXIS2_PLACEMENT_3D ( 'NONE', #17758, #19355, #15585 ) ;
#9843=CARTESIAN_POINT ( 'NONE',  ( 32.73300124599732186, 0.000000000000000000, 0.000000000000000000 ) ) ;
#9844=CARTESIAN_POINT ( 'NONE',  ( 25.64681081121879203, -83.63051021305953725, 75.86069728268962820 ) ) ;
#9845=CARTESIAN_POINT ( 'NONE',  ( 25.64660436782549979, -22.90783756890928302, 110.5628080555245987 ) ) ;
#9846=CARTESIAN_POINT ( 'NONE',  ( 55.49584447822657296, -66.38758986585096977, -29.26468316696839622 ) ) ;
#9847=CARTESIAN_POINT ( 'NONE',  ( 25.64692232868534205, 83.69035111837304441, -75.79483800045692021 ) ) ;
#9848=( BOUNDED_SURFACE ( )  B_SPLINE_SURFACE ( 3, 1, ( 
 ( #20891, #20599 ),
 ( #14554, #1177 ),
 ( #18733, #27506 ),
 ( #7815, #5645 ) ),
 .UNSPECIFIED., .F., .F., .F. ) 
 B_SPLINE_SURFACE_WITH_KNOTS ( ( 4, 4 ),
 ( 2, 2 ),
 ( 0.000000000000000000, 1.000000000000000000 ),
 ( 0.000000000000000000, 1.000000000000000000 ),
 .UNSPECIFIED. ) 
 GEOMETRIC_REPRESENTATION_ITEM ( )  RATIONAL_B_SPLINE_SURFACE ( (
 ( 1.000000000000000000, 1.000000000000000000),
 ( 0.9960225298536222738, 0.9999952330161893110),
 ( 0.9960225298536222738, 0.9999952330161893110),
 ( 1.000000000000000000, 1.000000000000000000) ) ) 
 REPRESENTATION_ITEM ( '' )  SURFACE ( )  );
#9849=ORIENTED_EDGE ( 'NONE', *, *, #8778, .F. ) ;
#9851=ORIENTED_EDGE ( 'NONE', *, *, #20499, .T. ) ;
#9853=CARTESIAN_POINT ( 'NONE',  ( 2.433796855181219243, -74.00833731765649759, 125.2830755159751703 ) ) ;
#9856=ORIENTED_EDGE ( 'NONE', *, *, #24763, .T. ) ;
#9857=B_SPLINE_CURVE_WITH_KNOTS ( 'NONE', 3,
 ( #21783, #24092, #4355, #2175, #17588, #12839 ),
 .UNSPECIFIED., .F., .F.,
 ( 4, 2, 4 ),
 ( 1.041737195591640451E-17, 0.0006311571484586062228, 0.001262314296917201820 ),
 .UNSPECIFIED. ) ;
#9858=LINE ( 'NONE', #27402, #24843 ) ;
#9859=EDGE_CURVE ( 'NONE', #18908, #7560, #23254, .T. ) ;
#9860=AXIS2_PLACEMENT_3D ( 'NONE', #6701, #19928, #4098 ) ;
#9865=DIRECTION ( 'NONE',  ( 0.000000000000000000, 0.000000000000000000, -1.000000000000000000 ) ) ;
#9867=CARTESIAN_POINT ( 'NONE',  ( 30.59138290137884653, -99.26509990456052890, 60.43009393261933582 ) ) ;
#9868=CARTESIAN_POINT ( 'NONE',  ( 109.1592201516379674, -0.004867031887019586216, -0.006174480289199391417 ) ) ;
#9872=CARTESIAN_POINT ( 'NONE',  ( 109.1624594426973118, 0.01033277910989004525, -0.01216903288310966155 ) ) ;
#9874=ORIENTED_EDGE ( 'NONE', *, *, #21320, .F. ) ;
#9875=ORIENTED_EDGE ( 'NONE', *, *, #24327, .T. ) ;
#9877=CARTESIAN_POINT ( 'NONE',  ( 32.73300124599732186, 0.000000000000000000, 0.000000000000000000 ) ) ;
#9878=CARTESIAN_POINT ( 'NONE',  ( 1.832998868059858122, 125.9352106559983895, 72.09222286251124956 ) ) ;
#9879=CARTESIAN_POINT ( 'NONE',  ( 1.833838850093477690, -85.29337590730617080, 117.3962664098819886 ) ) ;
#9882=ORIENTED_EDGE ( 'NONE', *, *, #6141, .F. ) ;
#9883=CARTESIAN_POINT ( 'NONE',  ( 25.65782528836482257, 98.07785559018951460, -55.95807498711376837 ) ) ;
#9884=( BOUNDED_SURFACE ( )  B_SPLINE_SURFACE ( 3, 1, ( 
 ( #22755, #18248 ),
 ( #16101, #11493 ),
 ( #20565, #11797 ),
 ( #16247, #2719 ) ),
 .UNSPECIFIED., .F., .F., .F. ) 
 B_SPLINE_SURFACE_WITH_KNOTS ( ( 4, 4 ),
 ( 2, 2 ),
 ( 0.000000000000000000, 1.000000000000000000 ),
 ( 0.000000000000000000, 1.000000000000000000 ),
 .UNSPECIFIED. ) 
 GEOMETRIC_REPRESENTATION_ITEM ( )  RATIONAL_B_SPLINE_SURFACE ( (
 ( 1.000000000000000000, 1.000000000000000000),
 ( 0.6386103224230316178, 0.9954351624131538845),
 ( 0.6386103224230316178, 0.9954351624131538845),
 ( 1.000000000000000000, 1.000000000000000000) ) ) 
 REPRESENTATION_ITEM ( '' )  SURFACE ( )  );
#9888=CARTESIAN_POINT ( 'NONE',  ( 25.64692232868534560, -97.62014907493917804, 56.73833653200207294 ) ) ;
#9889=CARTESIAN_POINT ( 'NONE',  ( 109.1586900883932856, 0.002810909342011593849, 0.006561743627143341688 ) ) ;
#9890=EDGE_CURVE ( 'NONE', #14469, #16227, #4671, .T. ) ;
#9893=B_SPLINE_CURVE_WITH_KNOTS ( 'NONE', 3,
 ( #3629, #17686, #15235, #133, #1478, #8119, #13219, #10286 ),
 .UNSPECIFIED., .F., .F.,
 ( 4, 2, 2, 4 ),
 ( 0.000000000000000000, 0.0002429588503611232193, 0.0004859177007222464386, 0.0009718354014444878898 ),
 .UNSPECIFIED. ) ;
#9894=ORIENTED_EDGE ( 'NONE', *, *, #10805, .T. ) ;
#9896=EDGE_CURVE ( 'NONE', #27156, #1087, #6082, .T. ) ;
#9897=EDGE_CURVE ( 'NONE', #14763, #18716, #12918, .T. ) ;
#9898=ORIENTED_EDGE ( 'NONE', *, *, #9003, .T. ) ;
#9901=EDGE_LOOP ( 'NONE', ( #539, #19619 ) ) ;
#9904=CARTESIAN_POINT ( 'NONE',  ( 55.49584447822657296, -54.09506550945658887, 48.34726110739968163 ) ) ;
#9905=CARTESIAN_POINT ( 'NONE',  ( 1.833838848569429247, -107.9566558236570160, -96.96512505224337986 ) ) ;
#9907=CARTESIAN_POINT ( 'NONE',  ( 13.36082413113061307, -9.660980093453659379, -152.6206443696329700 ) ) ;
#9909=CARTESIAN_POINT ( 'NONE',  ( 10.93730112725945247, 97.44200844886275092, 115.5857507957704087 ) ) ;
#9913=ORIENTED_EDGE ( 'NONE', *, *, #74, .F. ) ;
#9915=DIRECTION ( 'NONE',  ( 0.000000000000000000, 0.000000000000000000, 1.000000000000000000 ) ) ;
#9916=CARTESIAN_POINT ( 'NONE',  ( 1.833838850855474822, 107.8971100408363100, -97.03125735562127829 ) ) ;
#9917=CARTESIAN_POINT ( 'NONE',  ( 25.64692872815575342, 12.12228186621208259, -112.2585610031152186 ) ) ;
#9918=CARTESIAN_POINT ( 'NONE',  ( 10.93730112725996051, -4.928439153519255989, -151.0983828010092793 ) ) ;
#9919=CARTESIAN_POINT ( 'NONE',  ( 55.49584447822657296, -62.69727227546376014, -36.50733923851264251 ) ) ;
#9920=VERTEX_POINT ( 'NONE', #17760 ) ;
#9922=DIRECTION ( 'NONE',  ( 0.5914120900931444380, 0.1598001217819306763, 0.7903769105750361179 ) ) ;
#9925=CARTESIAN_POINT ( 'NONE',  ( 109.1587776205901861, -0.004375189885423146942, -0.005880209827414109407 ) ) ;
#9927=CARTESIAN_POINT ( 'NONE',  ( 109.1778270068192853, -0.001591747944959357852, -0.009177562596826695923 ) ) ;
#9929=FACE_OUTER_BOUND ( 'NONE', #21969, .T. ) ;
#9930=LINE ( 'NONE', #12627, #12114 ) ;
#9931=CARTESIAN_POINT ( 'NONE',  ( 2.063896406836605024, -144.3268707900446088, -16.52087515463925627 ) ) ;
#9932=ORIENTED_EDGE ( 'NONE', *, *, #3578, .T. ) ;
#9933=DIRECTION ( 'NONE',  ( -1.000000000000000000, -0.000000000000000000, -0.000000000000000000 ) ) ;
#9934=EDGE_CURVE ( 'NONE', #12511, #21273, #7392, .T. ) ;
#9935=FACE_OUTER_BOUND ( 'NONE', #26240, .T. ) ;
#9936=LINE ( 'NONE', #11937, #28166 ) ;
#9937=ADVANCED_FACE ( 'NONE', ( #11293 ), #4448, .F. ) ;
#9938=B_SPLINE_CURVE_WITH_KNOTS ( 'NONE', 3,
 ( #5218, #22946, #20903, #16153 ),
 .UNSPECIFIED., .F., .F.,
 ( 4, 4 ),
 ( 0.000000000000000000, 0.01077107196513883008 ),
 .UNSPECIFIED. ) ;
#9939=ORIENTED_EDGE ( 'NONE', *, *, #17627, .T. ) ;
#9940=ORIENTED_EDGE ( 'NONE', *, *, #13846, .T. ) ;
#9943=( BOUNDED_SURFACE ( )  B_SPLINE_SURFACE ( 3, 1, ( 
 ( #1307, #15096 ),
 ( #21313, #14829 ),
 ( #1594, #14964 ),
 ( #10394, #23644 ) ),
 .UNSPECIFIED., .F., .F., .F. ) 
 B_SPLINE_SURFACE_WITH_KNOTS ( ( 4, 4 ),
 ( 2, 2 ),
 ( 0.000000000000000000, 1.000000000000000000 ),
 ( 0.000000000000000000, 1.000000000000000000 ),
 .UNSPECIFIED. ) 
 GEOMETRIC_REPRESENTATION_ITEM ( )  RATIONAL_B_SPLINE_SURFACE ( (
 ( 1.000000000000000000, 1.000000000000000000),
 ( 0.9960225298536222738, 0.9999952330161893110),
 ( 0.9960225298536222738, 0.9999952330161893110),
 ( 1.000000000000000000, 1.000000000000000000) ) ) 
 REPRESENTATION_ITEM ( '' )  SURFACE ( )  );
#9944=CARTESIAN_POINT ( 'NONE',  ( 2.430230287190589422, -74.01081053031012402, -125.2872625092170153 ) ) ;
#9945=EDGE_CURVE ( 'NONE', #18731, #10482, #9837, .T. ) ;
#9946=VERTEX_POINT ( 'NONE', #15743 ) ;
#9948=CARTESIAN_POINT ( 'NONE',  ( 25.64703792032472052, -23.32999623362200126, 110.4746717456748542 ) ) ;
#9951=CARTESIAN_POINT ( 'NONE',  ( 25.64681081121879203, 97.57530875170606066, 56.81519825470789442 ) ) ;
#9952=CARTESIAN_POINT ( 'NONE',  ( 1.833838850855476599, -59.10274688031942958, 132.5281727421684366 ) ) ;
#9953=CARTESIAN_POINT ( 'NONE',  ( 2.063896406836609909, -133.2511741302116945, -57.85593781835549265 ) ) ;
#9954=ORIENTED_EDGE ( 'NONE', *, *, #23489, .T. ) ;
#9955=ORIENTED_EDGE ( 'NONE', *, *, #23216, .T. ) ;
#9959=CARTESIAN_POINT ( 'NONE',  ( 109.1624594426973118, -0.01033277910988996545, 0.01216903288310973094 ) ) ;
#9960=DIRECTION ( 'NONE',  ( 0.5946245182733607137, 0.4045541647807479602, -0.6948076064830646104 ) ) ;
#9962=LINE ( 'NONE', #5481, #5682 ) ;
#9963=B_SPLINE_CURVE_WITH_KNOTS ( 'NONE', 3,
 ( #2180, #4362, #24680, #6820 ),
 .UNSPECIFIED., .F., .F.,
 ( 4, 4 ),
 ( 3.465291969645973218E-16, 0.01077107486149812138 ),
 .UNSPECIFIED. ) ;
#9966=CARTESIAN_POINT ( 'NONE',  ( 1.833721034905634095, 59.34646046113778084, 132.4192200895884355 ) ) ;
#9968=CARTESIAN_POINT ( 'NONE',  ( 25.65782528836480481, -11.22838748007539955, -112.3587790429871660 ) ) ;
#9970=CARTESIAN_POINT ( 'NONE',  ( 25.64704443564079028, 0.1334765861219636696, -112.9111375659905718 ) ) ;
#9971=ORIENTED_EDGE ( 'NONE', *, *, #2351, .F. ) ;
#9972=CARTESIAN_POINT ( 'NONE',  ( 25.64681081121879203, -56.81519825470687834, -97.57530875170664331 ) ) ;
#9975=EDGE_CURVE ( 'NONE', #16334, #13261, #28358, .T. ) ;
#9977=ORIENTED_EDGE ( 'NONE', *, *, #15891, .F. ) ;
#9979=B_SPLINE_CURVE_WITH_KNOTS ( 'NONE', 3,
 ( #9017, #19652, #2089, #1954 ),
 .UNSPECIFIED., .F., .F.,
 ( 4, 4 ),
 ( 0.000000000000000000, 0.01077107196513880927 ),
 .UNSPECIFIED. ) ;
#9980=CARTESIAN_POINT ( 'NONE',  ( 25.64681081121879203, 66.03065707439057519, -91.59071981940505225 ) ) ;
#9981=CARTESIAN_POINT ( 'NONE',  ( 10.93730112725982195, -145.2260730187404079, 42.00474393596209666 ) ) ;
#9982=( BOUNDED_SURFACE ( )  B_SPLINE_SURFACE ( 3, 1, ( 
 ( #21989, #19827 ),
 ( #256, #15492 ),
 ( #26582, #28320 ),
 ( #8756, #21859 ) ),
 .UNSPECIFIED., .F., .F., .F. ) 
 B_SPLINE_SURFACE_WITH_KNOTS ( ( 4, 4 ),
 ( 2, 2 ),
 ( 0.000000000000000000, 1.000000000000000000 ),
 ( 0.000000000000000000, 1.000000000000000000 ),
 .UNSPECIFIED. ) 
 GEOMETRIC_REPRESENTATION_ITEM ( )  RATIONAL_B_SPLINE_SURFACE ( (
 ( 1.000000000000000000, 1.000000000000000000),
 ( 0.6386103224230316178, 0.9954351624131538845),
 ( 0.6386103224230316178, 0.9954351624131538845),
 ( 1.000000000000000000, 1.000000000000000000) ) ) 
 REPRESENTATION_ITEM ( '' )  SURFACE ( )  );
#9983=CARTESIAN_POINT ( 'NONE',  ( 6.224689322667647851, -89.08920297664128896, -118.2566963816780259 ) ) ;
#9984=CARTESIAN_POINT ( 'NONE',  ( 109.1586900883932856, 0.006130969560693665978, 0.003656351050324904359 ) ) ;
#9985=CARTESIAN_POINT ( 'NONE',  ( 30.58324630866350802, 120.6294372749319734, 8.712468656081018281 ) ) ;
#9986=CARTESIAN_POINT ( 'NONE',  ( 25.70243777736190438, 112.9457924277214005, 0.7331659071599172517 ) ) ;
#9988=CARTESIAN_POINT ( 'NONE',  ( 2.433796855181205476, -137.9325382748282038, -46.34326152018883249 ) ) ;
#9989=CARTESIAN_POINT ( 'NONE',  ( 25.64681081121879203, 84.18689316040146764, -75.24277141833410099 ) ) ;
#9990=CARTESIAN_POINT ( 'NONE',  ( 1.833485406944043827, -0.5339064996894915538, 145.1085452359073145 ) ) ;
#9991=CARTESIAN_POINT ( 'NONE',  ( 10.93730112725972958, -84.82621002473526062, 125.1380233598475229 ) ) ;
#9993=CARTESIAN_POINT ( 'NONE',  ( 28.37599760073042532, -86.45296943207071649, 75.42809173301579051 ) ) ;
#9994=DIRECTION ( 'NONE',  ( -1.000000000000000000, -0.000000000000000000, -0.000000000000000000 ) ) ;
#9995=CARTESIAN_POINT ( 'NONE',  ( 10.93730112726006354, 145.2260730187408626, -42.00474393596100953 ) ) ;
#9996=ORIENTED_EDGE ( 'NONE', *, *, #10953, .T. ) ;
#9998=ORIENTED_EDGE ( 'NONE', *, *, #1624, .T. ) ;
#10000=LINE ( 'NONE', #16765, #24503 ) ;
#10001=ORIENTED_EDGE ( 'NONE', *, *, #11435, .F. ) ;
#10007=B_SPLINE_CURVE_WITH_KNOTS ( 'NONE', 3,
 ( #10129, #1053, #3206, #7986, #16747, #13853, #2928, #9840, #18610, #22661 ),
 .UNSPECIFIED., .F., .F.,
 ( 4, 3, 3, 4 ),
 ( 3.925231146709437917E-17, 0.0002669559177086094437, 0.0005339118354150799734, 0.001067817517169168152 ),
 .UNSPECIFIED. ) ;
#10008=B_SPLINE_CURVE_WITH_KNOTS ( 'NONE', 3,
 ( #17014, #25684, #28471, #5959, #27679, #25395, #8776, #14711 ),
 .UNSPECIFIED., .F., .F.,
 ( 4, 2, 2, 4 ),
 ( 0.000000000000000000, 0.0002429588503611195872, 0.0004859177007222391744, 0.0009718354014444835530 ),
 .UNSPECIFIED. ) ;
#10009=CARTESIAN_POINT ( 'NONE',  ( 32.73300124599735739, 75.82012867748483131, 89.94078864464094636 ) ) ;
#10012=CARTESIAN_POINT ( 'NONE',  ( 109.1592201516379674, -0.005027640251764426034, 0.006044422199831456753 ) ) ;
#10013=CARTESIAN_POINT ( 'NONE',  ( 109.1586900883932856, -0.006757191295056145380, 0.002301750759607874407 ) ) ;
#10014=( BOUNDED_SURFACE ( )  B_SPLINE_SURFACE ( 3, 1, ( 
 ( #21206, #23107 ),
 ( #14583, #27242 ),
 ( #7403, #27683 ),
 ( #7704, #10143 ) ),
 .UNSPECIFIED., .F., .F., .F. ) 
 B_SPLINE_SURFACE_WITH_KNOTS ( ( 4, 4 ),
 ( 2, 2 ),
 ( 0.000000000000000000, 1.000000000000000000 ),
 ( 0.000000000000000000, 1.000000000000000000 ),
 .UNSPECIFIED. ) 
 GEOMETRIC_REPRESENTATION_ITEM ( )  RATIONAL_B_SPLINE_SURFACE ( (
 ( 1.000000000000000000, 1.000000000000000000),
 ( 0.9956975270656954757, 0.8568959468854893125),
 ( 0.9956975270656954757, 0.8568959468854893125),
 ( 1.000000000000000000, 1.000000000000000000) ) ) 
 REPRESENTATION_ITEM ( '' )  SURFACE ( )  );
#10015=CARTESIAN_POINT ( 'NONE',  ( 109.1586900883932856, -0.004113747441000958037, -0.005833932871487499359 ) ) ;
#10017=CARTESIAN_POINT ( 'NONE',  ( 1.831572820252008738, -145.1082523917587253, -0.9871191512929762268 ) ) ;
#10019=EDGE_LOOP ( 'NONE', ( #19772, #10873, #20375, #3505 ) ) ;
#10021=CARTESIAN_POINT ( 'NONE',  ( 1.832998868059858122, 0.5339089137768276982, -145.1092030902949830 ) ) ;
#10023=CARTESIAN_POINT ( 'NONE',  ( 25.64681081121879203, 56.81519825470891760, -97.57530875170544959 ) ) ;
#10024=CARTESIAN_POINT ( 'NONE',  ( 2.433796855181205476, 13.76554153471693454, 144.8571464219890004 ) ) ;
#10025=CARTESIAN_POINT ( 'NONE',  ( 25.64660436782554598, 11.22538561722038253, -112.3516544824818908 ) ) ;
#10028=ORIENTED_EDGE ( 'NONE', *, *, #20710, .F. ) ;
#10029=DIRECTION ( 'NONE',  ( 0.000000000000000000, 0.000000000000000000, 1.000000000000000000 ) ) ;
#10030=CARTESIAN_POINT ( 'NONE',  ( 25.81918753295376945, -35.81374485821542208, -107.2019194967339217 ) ) ;
#10031=CARTESIAN_POINT ( 'NONE',  ( 1.833485406944043827, -15.69895494453482598, 144.2578170162062463 ) ) ;
#10032=ORIENTED_EDGE ( 'NONE', *, *, #6231, .F. ) ;
#10034=EDGE_CURVE ( 'NONE', #9343, #2712, #21493, .T. ) ;
#10035=CARTESIAN_POINT ( 'NONE',  ( 2.430230287190581429, -28.83279105684324861, -142.6294793592101087 ) ) ;
#10039=CARTESIAN_POINT ( 'NONE',  ( 30.59138290137886429, -116.1811451928593613, 2.701446546447824115 ) ) ;
#10040=B_SPLINE_CURVE_WITH_KNOTS ( 'NONE', 3,
 ( #3232, #3511, #18633, #2693 ),
 .UNSPECIFIED., .F., .F.,
 ( 4, 4 ),
 ( 1.962615573354718958E-17, 0.008383560773332699931 ),
 .UNSPECIFIED. ) ;
#10042=B_SPLINE_CURVE_WITH_KNOTS ( 'NONE', 3,
 ( #7163, #18078, #14043, #20815, #11458, #9593, #13616 ),
 .UNSPECIFIED., .F., .F.,
 ( 4, 3, 4 ),
 ( 5.645319006159137796E-16, 0.02816610861753248221, 0.04000277880656271517 ),
 .UNSPECIFIED. ) ;
#10044=CARTESIAN_POINT ( 'NONE',  ( 25.86096068574581608, -46.89265070732192697, 102.8701285401540275 ) ) ;
#10045=CARTESIAN_POINT ( 'NONE',  ( 2.063896406836609909, 31.51663808384556731, 141.8093313989361661 ) ) ;
#10049=CARTESIAN_POINT ( 'NONE',  ( 109.1592201516379674, 0.003476928926134712113, 0.007051465909552774060 ) ) ;
#10052=ORIENTED_EDGE ( 'NONE', *, *, #1276, .F. ) ;
#10053=ORIENTED_EDGE ( 'NONE', *, *, #135, .T. ) ;
#10055=CARTESIAN_POINT ( 'NONE',  ( 28.37644542392847669, 69.76573497039082383, 102.9230687709010681 ) ) ;
#10056=CARTESIAN_POINT ( 'NONE',  ( 1.833485406944057594, 107.4794113447422603, -97.49333871408586560 ) ) ;
#10057=CARTESIAN_POINT ( 'NONE',  ( 25.64699802086722968, 11.56593161917464485, -112.3172869996024446 ) ) ;
#10058=CARTESIAN_POINT ( 'NONE',  ( 2.433796855181233454, 133.5135467655518369, 57.85512797797937168 ) ) ;
#10059=CARTESIAN_POINT ( 'NONE',  ( 32.73300124599738581, 75.82012867748602503, -89.94078864463983791 ) ) ;
#10060=EDGE_LOOP ( 'NONE', ( #18146, #14973, #1953, #25637 ) ) ;
#10062=VECTOR ( 'NONE', #1331, 1000.000000000000227 ) ;
#10063=CARTESIAN_POINT ( 'NONE',  ( 8.186469829614228644, -90.56875932797659345, 118.7566730983345309 ) ) ;
#10067=VECTOR ( 'NONE', #14579, 1000.000000000000341 ) ;
#10068=CARTESIAN_POINT ( 'NONE',  ( 13.36082413113063083, 143.3553710183996941, -53.25066407421655157 ) ) ;
#10069=CARTESIAN_POINT ( 'NONE',  ( 2.430230287190589422, 116.8646894862423835, -86.70145658344540607 ) ) ;
#10071=DIRECTION ( 'NONE',  ( 0.5946245182733607137, -0.7637359336799405263, -0.2512550613902199692 ) ) ;
#10073=CARTESIAN_POINT ( 'NONE',  ( 109.1624594426973260, -0.002129375066970737307, 0.01582142368018301520 ) ) ;
#10074=ORIENTED_EDGE ( 'NONE', *, *, #347, .F. ) ;
#10075=CARTESIAN_POINT ( 'NONE',  ( 28.37644542392839853, -29.80435743554031092, 120.7150203538607940 ) ) ;
#10076=CARTESIAN_POINT ( 'NONE',  ( 1.833691583653482171, -29.82175144857997395, -142.0122737882512354 ) ) ;
#10077=FACE_OUTER_BOUND ( 'NONE', #12124, .T. ) ;
#10078=EDGE_LOOP ( 'NONE', ( #23748, #4723, #12559, #28072 ) ) ;
#10080=EDGE_LOOP ( 'NONE', ( #23501, #13320, #7043, #14445 ) ) ;
#10082=CARTESIAN_POINT ( 'NONE',  ( 25.87036335909427365, -102.8789780196092352, 46.88819766600075667 ) ) ;
#10085=CARTESIAN_POINT ( 'NONE',  ( 30.59138290137920890, 109.6600423140547633, -38.47117663195857773 ) ) ;
#10087=CARTESIAN_POINT ( 'NONE',  ( 1.833750490713684345, 141.8829662951652608, 30.43107162405918942 ) ) ;
#10088=CARTESIAN_POINT ( 'NONE',  ( 1.833838848569443458, -125.7577269771227009, -72.40075357737779882 ) ) ;
#10089=CARTESIAN_POINT ( 'NONE',  ( 25.64681081121879203, 112.2483031020015147, -12.21581276189692211 ) ) ;
#10090=LINE ( 'NONE', #27631, #6757 ) ;
#10092=EDGE_CURVE ( 'NONE', #3668, #18167, #10828, .T. ) ;
#10093=EDGE_LOOP ( 'NONE', ( #20315, #12772, #10944, #16399 ) ) ;
#10094=CARTESIAN_POINT ( 'NONE',  ( 6.224689322667647851, 57.86870174583612680, -136.2818611715185000 ) ) ;
#10097=CARTESIAN_POINT ( 'NONE',  ( 26.11404676487259024, -112.7148551500679616, -10.71016160607683432 ) ) ;
#10098=CARTESIAN_POINT ( 'NONE',  ( 1.833206308920071193, 144.2348261777516143, 15.90849808441927671 ) ) ;
#10099=CARTESIAN_POINT ( 'NONE',  ( 5.340103579038292025, 108.0219267094759630, -100.3626145943024284 ) ) ;
#10103=CARTESIAN_POINT ( 'NONE',  ( 26.11404676487259024, -112.7148551500679616, -10.71016160607683432 ) ) ;
#10105=EDGE_CURVE ( 'NONE', #5234, #9758, #13675, .T. ) ;
#10107=ADVANCED_FACE ( 'NONE', ( #13823 ), #6312, .F. ) ;
#10108=ORIENTED_EDGE ( 'NONE', *, *, #22784, .F. ) ;
#10109=ORIENTED_EDGE ( 'NONE', *, *, #14938, .T. ) ;
#10110=CARTESIAN_POINT ( 'NONE',  ( 25.64660436782535058, -56.95711784271921374, -97.49251393956843970 ) ) ;
#10111=B_SPLINE_CURVE_WITH_KNOTS ( 'NONE', 3,
 ( #7961, #12668, #16990, #14686, #21453, #23492, #12384, #19431 ),
 .UNSPECIFIED., .F., .F.,
 ( 4, 2, 2, 4 ),
 ( 7.857287273937903510E-18, 0.0002429592666046824793, 0.0004859185332093570982, 0.0009718370664186868745 ),
 .UNSPECIFIED. ) ;
#10112=CARTESIAN_POINT ( 'NONE',  ( 109.1587776205901577, 0.003736572840486944002, -0.006305329297952431099 ) ) ;
#10113=ORIENTED_EDGE ( 'NONE', *, *, #7894, .T. ) ;
#10114=ORIENTED_EDGE ( 'NONE', *, *, #20987, .T. ) ;
#10119=CARTESIAN_POINT ( 'NONE',  ( 1.833485406944043827, 30.69200235379130959, -141.8265699653863976 ) ) ;
#10120=CARTESIAN_POINT ( 'NONE',  ( 1.833485406944043827, -97.49333871408762775, 107.4794113447406119 ) ) ;
#10125=B_SPLINE_CURVE_WITH_KNOTS ( 'NONE', 3,
 ( #26106, #327, #22222, #24540, #6539, #26522, #6688, #15432, #2485, #4500 ),
 .UNSPECIFIED., .F., .F.,
 ( 4, 3, 3, 4 ),
 ( 0.000000000000000000, 0.0002669560319015632562, 0.0005492286108966289854, 0.0008315040496093541135 ),
 .UNSPECIFIED. ) ;
#10126=CARTESIAN_POINT ( 'NONE',  ( 13.36082413113063083, 6.345145185218039607, 152.7944199136427699 ) ) ;
#10128=EDGE_CURVE ( 'NONE', #15825, #2900, #26219, .T. ) ;
#10129=CARTESIAN_POINT ( 'NONE',  ( 1.833485406944043827, -84.86072343962486286, -117.7091014914958578 ) ) ;
#10130=CARTESIAN_POINT ( 'NONE',  ( 28.37599760073042532, -33.74340001061027294, -109.6580863494833409 ) ) ;
#10131=CARTESIAN_POINT ( 'NONE',  ( 25.64681081121879203, -11.38886654529750331, 112.3352186517030447 ) ) ;
#10132=EDGE_CURVE ( 'NONE', #24473, #12568, #8451, .T. ) ;
#10134=CARTESIAN_POINT ( 'NONE',  ( 25.81918753295380498, 76.32043280377813232, 83.36706424720470920 ) ) ;
#10135=CARTESIAN_POINT ( 'NONE',  ( 25.64699802086721547, -0.2377811728589946105, -112.9109702078780657 ) ) ;
#10136=CARTESIAN_POINT ( 'NONE',  ( 25.64681081121879203, -91.10197563707900770, -66.70335573067958990 ) ) ;
#10138=CARTESIAN_POINT ( 'NONE',  ( 10.93730112725978110, -119.3442956573278479, 92.80059208661636205 ) ) ;
#10139=CARTESIAN_POINT ( 'NONE',  ( 19.66333377628714985, 132.3257119126255077, -38.27269871460917017 ) ) ;
#10140=EDGE_LOOP ( 'NONE', ( #8049, #23881, #16067, #23246 ) ) ;
#10141=CARTESIAN_POINT ( 'NONE',  ( 2.430230287190592531, 31.67257033707503311, 142.0258656395022570 ) ) ;
#10142=ORIENTED_EDGE ( 'NONE', *, *, #18278, .T. ) ;
#10143=CARTESIAN_POINT ( 'NONE',  ( 1.832998868059858122, 141.8272129421612817, -30.69214149073875930 ) ) ;
#10144=CARTESIAN_POINT ( 'NONE',  ( 26.11404676487259024, 36.06104232266452669, 107.3263591096431639 ) ) ;
#10145=ORIENTED_EDGE ( 'NONE', *, *, #23686, .T. ) ;
#10146=VERTEX_POINT ( 'NONE', #3044 ) ;
#10148=VERTEX_POINT ( 'NONE', #7359 ) ;
#10149=ORIENTED_EDGE ( 'NONE', *, *, #22243, .F. ) ;
#10150=B_SPLINE_CURVE_WITH_KNOTS ( 'NONE', 3,
 ( #9679, #24953, #16444, #11982, #5064, #10120 ),
 .UNSPECIFIED., .F., .F.,
 ( 4, 2, 4 ),
 ( 6.505213034913026604E-18, 0.0006311636237756815130, 0.001262327247551356738 ),
 .UNSPECIFIED. ) ;
#10151=B_SPLINE_CURVE_WITH_KNOTS ( 'NONE', 3,
 ( #25502, #27785, #3592, #12370, #21150, #1436 ),
 .UNSPECIFIED., .F., .F.,
 ( 4, 2, 4 ),
 ( 9.745765416140531346E-18, 0.0006311636237756778267, 0.001262327247551345679 ),
 .UNSPECIFIED. ) ;
#10155=CARTESIAN_POINT ( 'NONE',  ( 1.834118845439484335, 125.7578880615055255, -72.40084790867199160 ) ) ;
#10156=EDGE_CURVE ( 'NONE', #13750, #13485, #4765, .T. ) ;
#10162=VECTOR ( 'NONE', #7608, 1000.000000000000000 ) ;
#10163=EDGE_CURVE ( 'NONE', #21210, #14489, #17918, .T. ) ;
#10165=DIRECTION ( 'NONE',  ( -1.000000000000000000, -0.000000000000000000, -0.000000000000000000 ) ) ;
#10166=CARTESIAN_POINT ( 'NONE',  ( 10.93730112725971892, -10.89264110825104837, 150.7858122213660863 ) ) ;
#10167=CARTESIAN_POINT ( 'NONE',  ( 25.64692232868534560, -91.15460455808870677, 66.63160215461235225 ) ) ;
#10169=CARTESIAN_POINT ( 'NONE',  ( 1.833485406944043827, -85.72460230293772554, 117.0814567582541201 ) ) ;
#10170=CARTESIAN_POINT ( 'NONE',  ( 109.1592201516379674, 0.007845213074660002325, 0.0005146241775907644525 ) ) ;
#10171=CARTESIAN_POINT ( 'NONE',  ( 25.86096068574579832, 92.04529103340867380, -65.64181925268235318 ) ) ;
#10172=ORIENTED_EDGE ( 'NONE', *, *, #9559, .F. ) ;
#10173=CARTESIAN_POINT ( 'NONE',  ( 32.73300124599732186, 0.000000000000000000, 0.000000000000000000 ) ) ;
#10176=ORIENTED_EDGE ( 'NONE', *, *, #25192, .T. ) ;
#10179=ORIENTED_EDGE ( 'NONE', *, *, #16257, .T. ) ;
#10180=ORIENTED_EDGE ( 'NONE', *, *, #23231, .F. ) ;
#10183=B_SPLINE_CURVE_WITH_KNOTS ( 'NONE', 3,
 ( #3440, #1557, #23453, #12352, #5603, #8325, #25884, #6181 ),
 .UNSPECIFIED., .F., .F.,
 ( 4, 2, 2, 4 ),
 ( 3.469446951953614189E-18, 0.0002429588503611278543, 0.0004859177007222522391, 0.0009718354014444750963 ),
 .UNSPECIFIED. ) ;
#10184=CARTESIAN_POINT ( 'NONE',  ( 2.263178607246654206, -86.59154415224521983, -116.7985473178711970 ) ) ;
#10186=EDGE_LOOP ( 'NONE', ( #2138, #27562, #8371, #827 ) ) ;
#10188=DIRECTION ( 'NONE',  ( -1.000000000000000000, -0.000000000000000000, -0.000000000000000000 ) ) ;
#10190=CARTESIAN_POINT ( 'NONE',  ( 32.73300124599734318, 81.52272205837205377, 84.80615050150403533 ) ) ;
#10191=( BOUNDED_SURFACE ( )  B_SPLINE_SURFACE ( 3, 1, ( 
 ( #7360, #9519 ),
 ( #18270, #5190 ),
 ( #3045, #20589 ),
 ( #25072, #3598 ) ),
 .UNSPECIFIED., .F., .F., .F. ) 
 B_SPLINE_SURFACE_WITH_KNOTS ( ( 4, 4 ),
 ( 2, 2 ),
 ( 0.000000000000000000, 1.000000000000000000 ),
 ( 0.000000000000000000, 1.000000000000000000 ),
 .UNSPECIFIED. ) 
 GEOMETRIC_REPRESENTATION_ITEM ( )  RATIONAL_B_SPLINE_SURFACE ( (
 ( 1.000000000000000000, 1.000000000000000000),
 ( 0.9956975270656955868, 0.8568959468854907557),
 ( 0.9956975270656955868, 0.8568959468854907557),
 ( 1.000000000000000000, 1.000000000000000000) ) ) 
 REPRESENTATION_ITEM ( '' )  SURFACE ( )  );
#10193=CARTESIAN_POINT ( 'NONE',  ( 25.64681081121879203, 66.70335573067866619, 91.10197563707968982 ) ) ;
#10195=CARTESIAN_POINT ( 'NONE',  ( 1.833603222531974275, -107.5392551439147582, -97.42748212378386086 ) ) ;
#10196=EDGE_CURVE ( 'NONE', #11003, #1646, #27200, .T. ) ;
#10197=ORIENTED_EDGE ( 'NONE', *, *, #22095, .F. ) ;
#10198=CARTESIAN_POINT ( 'NONE',  ( 9.884929003653608603, -11.54837932062929440, -150.0922431698406285 ) ) ;
#10200=CARTESIAN_POINT ( 'NONE',  ( 24.22246935314087324, -90.00000000000005684, -40.00000000000002842 ) ) ;
#10203=VECTOR ( 'NONE', #26618, 1000.000000000000114 ) ;
#10204=ORIENTED_EDGE ( 'NONE', *, *, #2222, .F. ) ;
#10205=B_SPLINE_CURVE_WITH_KNOTS ( 'NONE', 3,
 ( #8713, #24839, #20207, #352, #9714, #13733, #14153, #25120, #22687, #7569 ),
 .UNSPECIFIED., .F., .F.,
 ( 4, 3, 3, 4 ),
 ( 1.387778780781445676E-17, 0.0002669560319015616299, 0.0005492286108966353822, 0.0008315040496093367662 ),
 .UNSPECIFIED. ) ;
#10206=ORIENTED_EDGE ( 'NONE', *, *, #12267, .T. ) ;
#10207=CARTESIAN_POINT ( 'NONE',  ( 5.340103579038268933, -47.74933483136786805, -139.5040934216405333 ) ) ;
#10208=B_SPLINE_CURVE_WITH_KNOTS ( 'NONE', 3,
 ( #20715, #19136, #7789, #10082, #5617, #23194, #16702, #18849 ),
 .UNSPECIFIED., .F., .F.,
 ( 4, 2, 2, 4 ),
 ( 3.469446951953614189E-18, 0.0002429592666046686829, 0.0004859185332093338963, 0.0009718370664186767914 ),
 .UNSPECIFIED. ) ;
#10211=CARTESIAN_POINT ( 'NONE',  ( 25.64681081121879203, 12.21581276189956711, -112.2483031020012305 ) ) ;
#10212=STYLED_ITEM('',(#28500),#8673);
#10217=ORIENTED_EDGE ( 'NONE', *, *, #15518, .F. ) ;
#10220=AXIS2_PLACEMENT_3D ( 'NONE', #13387, #19728, #2748 ) ;
#10221=CARTESIAN_POINT ( 'NONE',  ( 28.37599760073040400, 37.15642189426546338, -108.5491283158098383 ) ) ;
#10222=CARTESIAN_POINT ( 'NONE',  ( 10.93730112725932635, 0.000000000000000000, 0.000000000000000000 ) ) ;
#10224=CARTESIAN_POINT ( 'NONE',  ( 1.831572820252008738, -126.1609924456735143, 71.69925593429763921 ) ) ;
#10225=EDGE_LOOP ( 'NONE', ( #21915, #16208, #24122, #6584 ) ) ;
#10226=CARTESIAN_POINT ( 'NONE',  ( 13.36082413113063083, 9.660980093456728923, -152.6206443696327710 ) ) ;
#10227=CARTESIAN_POINT ( 'NONE',  ( 109.1586059443104944, -0.005983234375919703821, -0.003774052605959013398 ) ) ;
#10228=CARTESIAN_POINT ( 'NONE',  ( 28.43349137099830060, 111.8014342888394594, -54.21282462801664792 ) ) ;
#10229=VERTEX_POINT ( 'NONE', #26771 ) ;
#10230=CARTESIAN_POINT ( 'NONE',  ( 32.73300124599738581, 16.10546300444979195, -116.5274707358853163 ) ) ;
#10232=CARTESIAN_POINT ( 'NONE',  ( 30.59141879584286983, -70.47510900703845493, 92.40465812955523006 ) ) ;
#10234=CARTESIAN_POINT ( 'NONE',  ( 109.1587776205901577, 0.001442274045003904149, 0.007186028091163438464 ) ) ;
#10235=EDGE_CURVE ( 'NONE', #23267, #21777, #26657, .T. ) ;
#10236=AXIS2_PLACEMENT_3D ( 'NONE', #12000, #18619, #1062 ) ;
#10237=EDGE_CURVE ( 'NONE', #20294, #14489, #19458, .T. ) ;
#10240=CARTESIAN_POINT ( 'NONE',  ( 1.833838848569415925, 141.9757689770221987, 29.99593366454804055 ) ) ;
#10242=CARTESIAN_POINT ( 'NONE',  ( 5.340103579038241399, -75.71042924122960471, -126.5279493327092837 ) ) ;
#10245=ORIENTED_EDGE ( 'NONE', *, *, #6840, .T. ) ;
#10246=ORIENTED_EDGE ( 'NONE', *, *, #25410, .T. ) ;
#10247=CARTESIAN_POINT ( 'NONE',  ( 25.98107933586735996, -97.42660475433896750, -57.50946808479330485 ) ) ;
#10249=FACE_OUTER_BOUND ( 'NONE', #24208, .T. ) ;
#10250=CARTESIAN_POINT ( 'NONE',  ( 25.64699802086724034, -84.06830990999276310, -75.37548011155811878 ) ) ;
#10251=CARTESIAN_POINT ( 'NONE',  ( 25.64660436782551756, -91.68669413043107852, -65.89729635303008592 ) ) ;
#10252=CARTESIAN_POINT ( 'NONE',  ( 25.64692232868535982, -91.53874134430752463, -66.10288322707289410 ) ) ;
#10253=FACE_OUTER_BOUND ( 'NONE', #26360, .T. ) ;
#10255=CARTESIAN_POINT ( 'NONE',  ( 1.833485406944043827, -144.3694338680886062, 14.63699153649312201 ) ) ;
#10257=CARTESIAN_POINT ( 'NONE',  ( 25.86096068574579832, -10.82483750674526668, -112.5344699600050262 ) ) ;
#10259=CARTESIAN_POINT ( 'NONE',  ( 55.49584447822657296, -15.34602024131236497, -70.91003759562332220 ) ) ;
#10260=VECTOR ( 'NONE', #12193, 1000.000000000000000 ) ;
#10261=CARTESIAN_POINT ( 'NONE',  ( 55.79472521941428198, -68.96476385670678155, 23.17337251492740080 ) ) ;
#10262=CIRCLE ( 'NONE', #20323, 151.1787379149930359 ) ;
#10266=VERTEX_POINT ( 'NONE', #23207 ) ;
#10268=VERTEX_POINT ( 'NONE', #7662 ) ;
#10269=EDGE_CURVE ( 'NONE', #6096, #2848, #6067, .T. ) ;
#10270=B_SPLINE_CURVE_WITH_KNOTS ( 'NONE', 3,
 ( #13036, #1800, #28416, #13167 ),
 .UNSPECIFIED., .F., .F.,
 ( 4, 4 ),
 ( 0.000000000000000000, 0.008383560773332715543 ),
 .UNSPECIFIED. ) ;
#10271=B_SPLINE_CURVE_WITH_KNOTS ( 'NONE', 3,
 ( #4582, #10933, #17680, #26459, #15649, #24466, #4731 ),
 .UNSPECIFIED., .F., .F.,
 ( 4, 3, 4 ),
 ( 0.000000000000000000, 0.02398743853561285944, 0.04000277880656218782 ),
 .UNSPECIFIED. ) ;
#10273=LINE ( 'NONE', #14260, #27575 ) ;
#10274=CARTESIAN_POINT ( 'NONE',  ( 25.64681081121879203, 97.99105938547923245, 56.09509703373377931 ) ) ;
#10275=EDGE_CURVE ( 'NONE', #17261, #20966, #18071, .T. ) ;
#10276=DIRECTION ( 'NONE',  ( 0.000000000000000000, 0.000000000000000000, 1.000000000000000000 ) ) ;
#10277=AXIS2_PLACEMENT_3D ( 'NONE', #21265, #10610, #25735 ) ;
#10278=AXIS2_PLACEMENT_3D ( 'NONE', #1398, #7912, #7470 ) ;
#10279=CARTESIAN_POINT ( 'NONE',  ( 109.1721716018069515, -0.01695288006056417524, -0.001984900887706834635 ) ) ;
#10280=CARTESIAN_POINT ( 'NONE',  ( 9.884929003653626367, 4.203795436552358211, 150.4771565009630763 ) ) ;
#10282=B_SPLINE_CURVE_WITH_KNOTS ( 'NONE', 3,
 ( #25053, #27326, #3019, #3157, #11935, #23188, #27611 ),
 .UNSPECIFIED., .F., .F.,
 ( 4, 3, 4 ),
 ( 0.000000000000000000, 0.02398743853561341455, 0.04000277880656216700 ),
 .UNSPECIFIED. ) ;
#10283=CARTESIAN_POINT ( 'NONE',  ( 1.833485406944043827, -138.1714136985311256, 44.33323125129879116 ) ) ;
#10284=CARTESIAN_POINT ( 'NONE',  ( 25.64692872815577473, -75.31297890941213780, -84.12425003484119657 ) ) ;
#10285=CARTESIAN_POINT ( 'NONE',  ( 109.1624594426973118, 0.003771499231554082537, 0.01551217196237752310 ) ) ;
#10286=CARTESIAN_POINT ( 'NONE',  ( 26.11404676487257603, -113.2169081140373947, -1.130420376098323576 ) ) ;
#10289=CARTESIAN_POINT ( 'NONE',  ( 25.64670758986457955, 112.2393466678478262, 12.29747533046004548 ) ) ;
#10290=CARTESIAN_POINT ( 'NONE',  ( 32.73300124599738581, -62.10906484417165530, -99.90245962373897726 ) ) ;
#10291=CARTESIAN_POINT ( 'NONE',  ( 2.433796855181233454, 31.67151202412969724, 142.0211193075556935 ) ) ;
#10292=CARTESIAN_POINT ( 'NONE',  ( 25.65782528836480481, 102.9197507294676086, 46.45532072021219960 ) ) ;
#10294=CIRCLE ( 'NONE', #24514, 117.6351876552689504 ) ;
#10295=ORIENTED_EDGE ( 'NONE', *, *, #18998, .F. ) ;
#10298=EDGE_LOOP ( 'NONE', ( #2341, #5980, #21174, #24942 ) ) ;
#10299=VECTOR ( 'NONE', #6291, 1000.000000000000114 ) ;
#10302=ORIENTED_EDGE ( 'NONE', *, *, #1078, .T. ) ;
#10303=ADVANCED_FACE ( 'NONE', ( #3321 ), #1444, .T. ) ;
#10304=EDGE_CURVE ( 'NONE', #2416, #21273, #22213, .T. ) ;
#10305=EDGE_CURVE ( 'NONE', #19603, #15408, #21304, .T. ) ;
#10306=CARTESIAN_POINT ( 'NONE',  ( 1.833603222531974719, -142.0304769734131014, 29.73464781350211084 ) ) ;
#10309=LINE ( 'NONE', #23540, #5658 ) ;
#10313=CARTESIAN_POINT ( 'NONE',  ( 55.49584447822657296, -68.91748907713603955, 22.67407039687217818 ) ) ;
#10314=ORIENTED_EDGE ( 'NONE', *, *, #22204, .T. ) ;
#10316=B_SPLINE_CURVE_WITH_KNOTS ( 'NONE', 3,
 ( #22911, #11948, #20720, #22324 ),
 .UNSPECIFIED., .F., .F.,
 ( 4, 4 ),
 ( 3.417011720166793662E-16, 0.01077107486149841975 ),
 .UNSPECIFIED. ) ;
#10317=DIRECTION ( 'NONE',  ( -1.000000000000000000, -0.000000000000000000, -0.000000000000000000 ) ) ;
#10319=FACE_OUTER_BOUND ( 'NONE', #24220, .T. ) ;
#10322=EDGE_LOOP ( 'NONE', ( #12485, #5372, #25307, #14144 ) ) ;
#10323=CARTESIAN_POINT ( 'NONE',  ( 2.063896406836605024, -46.16709813092717241, 137.7380992975101037 ) ) ;
#10324=CARTESIAN_POINT ( 'NONE',  ( 109.1589550718175161, -0.007132058561966966165, 0.002553077953681008247 ) ) ;
#10325=CARTESIAN_POINT ( 'NONE',  ( 26.28373643307440588, 125.5716026420343212, 22.43832507403690713 ) ) ;
#10328=CARTESIAN_POINT ( 'NONE',  ( 1.832998868059858122, -29.64765804469970334, -142.0492247521725631 ) ) ;
#10330=VERTEX_POINT ( 'NONE', #27349 ) ;
#10331=EDGE_CURVE ( 'NONE', #8671, #14673, #24261, .T. ) ;
#10332=CARTESIAN_POINT ( 'NONE',  ( 32.73300124599734318, 89.94078864464067635, 75.82012867748514395 ) ) ;
#10333=ORIENTED_EDGE ( 'NONE', *, *, #16970, .T. ) ;
#10334=EDGE_CURVE ( 'NONE', #7372, #4882, #26276, .T. ) ;
#10336=CARTESIAN_POINT ( 'NONE',  ( 25.69398547355839568, 112.3990349503585264, 11.06723946918797097 ) ) ;
#10337=CARTESIAN_POINT ( 'NONE',  ( 1.833206308920102057, -59.70089323729826702, 132.2594750499823704 ) ) ;
#10339=CARTESIAN_POINT ( 'NONE',  ( 25.64700659047694842, 83.75695331063735694, 75.72132282458898089 ) ) ;
#10340=CARTESIAN_POINT ( 'NONE',  ( 109.1587776205901861, -0.007280006032835099547, 0.0008489206734501343870 ) ) ;
#10346=ORIENTED_EDGE ( 'NONE', *, *, #5650, .F. ) ;
#10347=ORIENTED_EDGE ( 'NONE', *, *, #232, .F. ) ;
#10350=CARTESIAN_POINT ( 'NONE',  ( 13.36082413113061307, -25.56125765253342763, -150.7747251079864839 ) ) ;
#10351=CARTESIAN_POINT ( 'NONE',  ( 1.894214914920951287, 45.75988301372644429, 137.7482714433625972 ) ) ;
#10352=CARTESIAN_POINT ( 'NONE',  ( 1.833206310202334821, 132.8652722326998514, 58.34025049824994369 ) ) ;
#10353=CARTESIAN_POINT ( 'NONE',  ( 16.05277956358211000, -10.32496049470181454, 142.9335921074871294 ) ) ;
#10357=ORIENTED_EDGE ( 'NONE', *, *, #428, .T. ) ;
#10359=CARTESIAN_POINT ( 'NONE',  ( 1.832998868059890096, 85.72499093308253748, -117.0819875546687143 ) ) ;
#10360=CARTESIAN_POINT ( 'NONE',  ( 10.93730112725972781, -92.80059208661754155, 119.3442956573269100 ) ) ;
#10361=DIRECTION ( 'NONE',  ( 0.000000000000000000, 0.000000000000000000, -1.000000000000000000 ) ) ;
#10362=DIRECTION ( 'NONE',  ( 0.5914120900931444380, -0.7870418015781046606, -0.1754905759872871784 ) ) ;
#10365=CARTESIAN_POINT ( 'NONE',  ( 2.108985857320890389, -137.7807691131291108, 46.11505917359396278 ) ) ;
#10367=( BOUNDED_SURFACE ( )  B_SPLINE_SURFACE ( 3, 1, ( 
 ( #3439, #18694 ),
 ( #19122, #12218 ),
 ( #8191, #20983 ),
 ( #3716, #1270 ) ),
 .UNSPECIFIED., .F., .F., .F. ) 
 B_SPLINE_SURFACE_WITH_KNOTS ( ( 4, 4 ),
 ( 2, 2 ),
 ( 0.000000000000000000, 1.000000000000000000 ),
 ( 0.000000000000000000, 1.000000000000000000 ),
 .UNSPECIFIED. ) 
 GEOMETRIC_REPRESENTATION_ITEM ( )  RATIONAL_B_SPLINE_SURFACE ( (
 ( 1.000000000000000000, 1.000000000000000000),
 ( 0.9956975270656955868, 0.8568959468854907557),
 ( 0.9956975270656955868, 0.8568959468854907557),
 ( 1.000000000000000000, 1.000000000000000000) ) ) 
 REPRESENTATION_ITEM ( '' )  SURFACE ( )  );
#10369=FACE_OUTER_BOUND ( 'NONE', #11231, .T. ) ;
#10372=DIRECTION ( 'NONE',  ( 0.000000000000000000, 0.000000000000000000, 1.000000000000000000 ) ) ;
#10373=B_SPLINE_CURVE_WITH_KNOTS ( 'NONE', 3,
 ( #8271, #1771, #17035, #25832, #6390, #1638, #26101, #16907 ),
 .UNSPECIFIED., .F., .F.,
 ( 4, 2, 2, 4 ),
 ( 0.000000000000000000, 0.0002429592666046734805, 0.0004859185332093469609, 0.0009718370664186885008 ),
 .UNSPECIFIED. ) ;
#10374=B_SPLINE_CURVE_WITH_KNOTS ( 'NONE', 3,
 ( #18031, #9847, #5371, #27089, #18617, #24827, #16167, #7398, #22668, #14136 ),
 .UNSPECIFIED., .F., .F.,
 ( 4, 3, 3, 4 ),
 ( 1.962615573354718958E-17, 0.0002669560319015674304, 0.0005492286108966131560, 0.0008315040496093250568 ),
 .UNSPECIFIED. ) ;
#10375=CARTESIAN_POINT ( 'NONE',  ( 109.1721716018069515, -0.01629455849719226371, 0.005082060336465219624 ) ) ;
#10378=FACE_OUTER_BOUND ( 'NONE', #26925, .T. ) ;
#10379=EDGE_CURVE ( 'NONE', #1405, #18334, #2948, .T. ) ;
#10380=CARTESIAN_POINT ( 'NONE',  ( 26.11404676487259024, 12.95861723607453619, 112.4785329405482628 ) ) ;
#10381=CARTESIAN_POINT ( 'NONE',  ( 25.64681081121879203, -75.24277141833549365, 84.18689316040023130 ) ) ;
#10382=CARTESIAN_POINT ( 'NONE',  ( 2.263178607246690621, -57.85473702627204773, 133.3897506477020443 ) ) ;
#10383=ORIENTED_EDGE ( 'NONE', *, *, #13874, .T. ) ;
#10385=FACE_OUTER_BOUND ( 'NONE', #18563, .T. ) ;
#10386=CARTESIAN_POINT ( 'NONE',  ( 30.58324630866340854, -67.85993782330834279, 100.1119227962718128 ) ) ;
#10387=CARTESIAN_POINT ( 'NONE',  ( 25.64703792032469920, -84.00887408969001058, -75.44170528134974063 ) ) ;
#10390=CARTESIAN_POINT ( 'NONE',  ( 24.01988960052064215, -130.7041393974935204, 9.440825210282998370 ) ) ;
#10392=CARTESIAN_POINT ( 'NONE',  ( 32.73300124599737160, -117.3295799645428872, -8.473903470907334423 ) ) ;
#10394=CARTESIAN_POINT ( 'NONE',  ( 109.1586900883932856, -0.002109621908824195913, -0.006819617742892433374 ) ) ;
#10395=EDGE_CURVE ( 'NONE', #16104, #22997, #14955, .T. ) ;
#10396=ORIENTED_EDGE ( 'NONE', *, *, #15493, .T. ) ;
#10397=CARTESIAN_POINT ( 'NONE',  ( 25.64681081121880624, -46.30456157731397582, 102.9795863647027119 ) ) ;
#10398=CARTESIAN_POINT ( 'NONE',  ( 25.64703792032469920, -11.95040607427908341, -112.2770217641849371 ) ) ;
#10399=ORIENTED_EDGE ( 'NONE', *, *, #27802, .F. ) ;
#10401=ADVANCED_FACE ( 'NONE', ( #8921, #4023 ), #17258, .F. ) ;
#10402=ORIENTED_EDGE ( 'NONE', *, *, #12451, .T. ) ;
#10403=EDGE_LOOP ( 'NONE', ( #10197, #262, #9632, #21130 ) ) ;
#10404=( BOUNDED_SURFACE ( )  B_SPLINE_SURFACE ( 3, 1, ( 
 ( #7188, #16673 ),
 ( #14499, #21110 ),
 ( #27307, #5879 ),
 ( #14067, #3426 ) ),
 .UNSPECIFIED., .F., .F., .F. ) 
 B_SPLINE_SURFACE_WITH_KNOTS ( ( 4, 4 ),
 ( 2, 2 ),
 ( 0.000000000000000000, 1.000000000000000000 ),
 ( 0.000000000000000000, 1.000000000000000000 ),
 .UNSPECIFIED. ) 
 GEOMETRIC_REPRESENTATION_ITEM ( )  RATIONAL_B_SPLINE_SURFACE ( (
 ( 1.000000000000000000, 1.000000000000000000),
 ( 0.9960225298536222738, 0.9999952330161893110),
 ( 0.9960225298536222738, 0.9999952330161893110),
 ( 1.000000000000000000, 1.000000000000000000) ) ) 
 REPRESENTATION_ITEM ( '' )  SURFACE ( )  );
#10406=LINE ( 'NONE', #23227, #11980 ) ;
#10407=CARTESIAN_POINT ( 'NONE',  ( 1.833838850093440165, 30.17001281793556089, -141.9387673160883026 ) ) ;
#10408=CARTESIAN_POINT ( 'NONE',  ( 13.84597867724973064, 124.5889929031786920, 77.45414123936249950 ) ) ;
#10409=ORIENTED_EDGE ( 'NONE', *, *, #11684, .F. ) ;
#10410=CARTESIAN_POINT ( 'NONE',  ( 1.833838850093439943, -59.02146106674994996, -132.5643635152040929 ) ) ;
#10411=B_SPLINE_CURVE_WITH_KNOTS ( 'NONE', 3,
 ( #19161, #8230, #12672, #23648, #16872, #8374, #1732, #27933 ),
 .UNSPECIFIED., .F., .F.,
 ( 4, 2, 2, 4 ),
 ( 3.469446951953614189E-18, 0.0002429592666046782238, 0.0004859185332093529782, 0.0009718370664186902355 ),
 .UNSPECIFIED. ) ;
#10412=CARTESIAN_POINT ( 'NONE',  ( 10.93730112725932635, 0.000000000000000000, 0.000000000000000000 ) ) ;
#10416=CARTESIAN_POINT ( 'NONE',  ( 6.224689322667647851, 48.18553814190031659, 139.9988794244333690 ) ) ;
#10417=CARTESIAN_POINT ( 'NONE',  ( 109.1586900883932856, -0.002301750759599823989, 0.006757191295060836073 ) ) ;
#10418=CARTESIAN_POINT ( 'NONE',  ( 9.884929003653626367, 42.50195158091224101, -144.4113244745767588 ) ) ;
#10419=FACE_OUTER_BOUND ( 'NONE', #17370, .T. ) ;
#10421=EDGE_CURVE ( 'NONE', #16227, #17233, #15599, .T. ) ;
#10422=ORIENTED_EDGE ( 'NONE', *, *, #6928, .T. ) ;
#10423=ADVANCED_FACE ( 'NONE', ( #8627 ), #21181, .F. ) ;
#10424=ORIENTED_EDGE ( 'NONE', *, *, #27698, .T. ) ;
#10425=CARTESIAN_POINT ( 'NONE',  ( 109.1586059443104944, 0.007001002073869785382, -0.001014167950289997146 ) ) ;
#10427=VERTEX_POINT ( 'NONE', #28461 ) ;
#10428=ORIENTED_EDGE ( 'NONE', *, *, #24664, .T. ) ;
#10429=VERTEX_POINT ( 'NONE', #15371 ) ;
#10430=CARTESIAN_POINT ( 'NONE',  ( 19.66333377628706458, 88.78556591841305590, 105.3186440504699561 ) ) ;
#10433=( BOUNDED_SURFACE ( )  B_SPLINE_SURFACE ( 3, 1, ( 
 ( #10536, #16879 ),
 ( #7974, #14417 ),
 ( #21325, #25378 ),
 ( #21179, #14261 ) ),
 .UNSPECIFIED., .F., .F., .F. ) 
 B_SPLINE_SURFACE_WITH_KNOTS ( ( 4, 4 ),
 ( 2, 2 ),
 ( 0.000000000000000000, 1.000000000000000000 ),
 ( 0.000000000000000000, 1.000000000000000000 ),
 .UNSPECIFIED. ) 
 GEOMETRIC_REPRESENTATION_ITEM ( )  RATIONAL_B_SPLINE_SURFACE ( (
 ( 1.000000000000000000, 1.000000000000000000),
 ( 0.9960225298536222738, 0.9999952330161893110),
 ( 0.9960225298536222738, 0.9999952330161893110),
 ( 1.000000000000000000, 1.000000000000000000) ) ) 
 REPRESENTATION_ITEM ( '' )  SURFACE ( )  );
#10434=CARTESIAN_POINT ( 'NONE',  ( 109.1592201516379674, -0.005485778713193788063, 0.005631912476305676526 ) ) ;
#10435=CARTESIAN_POINT ( 'NONE',  ( 1.833485406944043827, -14.63699153649458040, 144.3694338680884641 ) ) ;
#10436=CARTESIAN_POINT ( 'NONE',  ( 2.433796855181233454, -86.69855925933894980, -116.8607839509065371 ) ) ;
#10438=CARTESIAN_POINT ( 'NONE',  ( 25.87036335909426654, -112.5399073133628463, -10.83311869338186462 ) ) ;
#10439=ADVANCED_FACE ( 'NONE', ( #10515 ), #22100, .F. ) ;
#10440=EDGE_LOOP ( 'NONE', ( #17727, #11211, #20460, #12474 ) ) ;
#10442=ADVANCED_FACE ( 'NONE', ( #19423 ), #22281, .F. ) ;
#10444=CARTESIAN_POINT ( 'NONE',  ( 2.430230287190592531, -125.2872625092167596, 74.01081053031055035 ) ) ;
#10445=CARTESIAN_POINT ( 'NONE',  ( 5.340103579038270709, 96.93942141937453982, -111.1041836885938068 ) ) ;
#10446=CARTESIAN_POINT ( 'NONE',  ( 1.832998868059858122, -117.0819875546689417, -85.72499093308222484 ) ) ;
#10447=CARTESIAN_POINT ( 'NONE',  ( 25.70243777736192570, 112.4037002646849146, -11.07690056740750073 ) ) ;
#10448=ORIENTED_EDGE ( 'NONE', *, *, #9934, .F. ) ;
#10452=CARTESIAN_POINT ( 'NONE',  ( 2.063896406836605024, 46.16709813092805348, -137.7380992975097911 ) ) ;
#10454=VERTEX_POINT ( 'NONE', #20553 ) ;
#10457=VERTEX_POINT ( 'NONE', #15809 ) ;
#10459=CARTESIAN_POINT ( 'NONE',  ( 6.224689322667647851, -18.02516478984043857, -146.9579047224771386 ) ) ;
#10461=CARTESIAN_POINT ( 'NONE',  ( 1.832998868059890096, 137.8420662456170191, 45.34898734666091968 ) ) ;
#10463=CARTESIAN_POINT ( 'NONE',  ( 26.11404676487256893, -55.62948129436175293, -98.61392875273419634 ) ) ;
#10464=CARTESIAN_POINT ( 'NONE',  ( 109.1778270068192853, -0.003465086990435428584, 0.008646067828082875176 ) ) ;
#10465=CARTESIAN_POINT ( 'NONE',  ( 2.263178607246682628, 138.7064943909645649, 43.59477707254079348 ) ) ;
#10467=CARTESIAN_POINT ( 'NONE',  ( 13.84597867724978215, -10.56985607909703617, -146.3210145202069441 ) ) ;
#10468=CARTESIAN_POINT ( 'NONE',  ( 25.87036335909428075, -103.6841944152903920, -45.07965203035023904 ) ) ;
#10470=CARTESIAN_POINT ( 'NONE',  ( 25.81918753295377300, -10.88546493098934320, 112.5005889664128489 ) ) ;
#10471=CARTESIAN_POINT ( 'NONE',  ( 10.93730112725971892, -10.89264110825104837, 150.7858122213660863 ) ) ;
#10473=ORIENTED_EDGE ( 'NONE', *, *, #25597, .T. ) ;
#10474=LINE ( 'NONE', #1124, #989 ) ;
#10475=CARTESIAN_POINT ( 'NONE',  ( 1.832998868059858122, -85.72499093308022111, -117.0819875546704054 ) ) ;
#10477=CARTESIAN_POINT ( 'NONE',  ( 109.1624594426973118, 0.01591840958353239743, 0.001206615835669516733 ) ) ;
#10478=CARTESIAN_POINT ( 'NONE',  ( 25.69398547355840634, -76.12333255527457254, -83.43419615433070646 ) ) ;
#10479=CARTESIAN_POINT ( 'NONE',  ( 2.433796855181233454, 98.43889364293860922, 107.1581411821788947 ) ) ;
#10482=VERTEX_POINT ( 'NONE', #11482 ) ;
#10484=DIRECTION ( 'NONE',  ( -1.000000000000000000, -0.000000000000000000, -0.000000000000000000 ) ) ;
#10490=EDGE_LOOP ( 'NONE', ( #23190, #233, #3857, #15304 ) ) ;
#10491=CARTESIAN_POINT ( 'NONE',  ( 16.75465622695655199, -34.09043808962508137, 138.0797984721904754 ) ) ;
#10494=CARTESIAN_POINT ( 'NONE',  ( 1.833206310202347034, -29.44113265021029591, 142.0914673790819620 ) ) ;
#10496=B_SPLINE_CURVE_WITH_KNOTS ( 'NONE', 3,
 ( #22689, #26968, #13452, #20501, #26688, #18052, #7275 ),
 .UNSPECIFIED., .F., .F.,
 ( 4, 3, 4 ),
 ( 0.000000000000000000, 0.02398743853561398701, 0.04000277880656223639 ),
 .UNSPECIFIED. ) ;
#10497=CARTESIAN_POINT ( 'NONE',  ( 25.64681081121879203, 97.99105938547923245, 56.09509703373377931 ) ) ;
#10500=CARTESIAN_POINT ( 'NONE',  ( 5.340103579038080639, 128.8311297206841459, 71.72120379026067383 ) ) ;
#10501=CARTESIAN_POINT ( 'NONE',  ( 16.05277956358202118, 67.56865019684023821, -126.3767940428294736 ) ) ;
#10502=CARTESIAN_POINT ( 'NONE',  ( 109.1592201516379674, -0.006649399203953433417, 0.004194960840990133617 ) ) ;
#10504=CIRCLE ( 'NONE', #371, 151.1787379149930359 ) ;
#10505=CARTESIAN_POINT ( 'NONE',  ( 1.833838850093452821, -59.02145475724738333, 132.5643663243755839 ) ) ;
#10506=CARTESIAN_POINT ( 'NONE',  ( 1.832998868059858122, 132.3466930259793628, 59.50898020732557114 ) ) ;
#10507=CARTESIAN_POINT ( 'NONE',  ( 55.49584447822657296, 48.34726110740061245, -54.09506550945575754 ) ) ;
#10509=EDGE_LOOP ( 'NONE', ( #24887, #25869, #15995, #24904 ) ) ;
#10511=ORIENTED_EDGE ( 'NONE', *, *, #23726, .T. ) ;
#10513=CARTESIAN_POINT ( 'NONE',  ( 25.64707127832796019, 1.378041109049876443E-14, 112.9112343549835487 ) ) ;
#10515=FACE_OUTER_BOUND ( 'NONE', #8749, .T. ) ;
#10516=CARTESIAN_POINT ( 'NONE',  ( 26.11404676487259024, -83.38016054979834735, 76.59696442953165274 ) ) ;
#10517=CARTESIAN_POINT ( 'NONE',  ( 109.1586900883932856, -0.001385221016527508594, 0.007002774699553633575 ) ) ;
#10518=ORIENTED_EDGE ( 'NONE', *, *, #13864, .F. ) ;
#10519=CARTESIAN_POINT ( 'NONE',  ( 8.186469829614219762, 57.56191610809376868, 137.8131829164336182 ) ) ;
#10521=CARTESIAN_POINT ( 'NONE',  ( 109.1624594426973118, 0.01595733256932007488, -0.0004639210235603172228 ) ) ;
#10523=EDGE_CURVE ( 'NONE', #604, #24791, #21138, .T. ) ;
#10524=B_SPLINE_CURVE_WITH_KNOTS ( 'NONE', 3,
 ( #21803, #6697, #19350, #27988, #28398, #21939, #8429 ),
 .UNSPECIFIED., .F., .F.,
 ( 4, 3, 4 ),
 ( 0.000000000000000000, 0.02398743853561394884, 0.04000277880656219476 ),
 .UNSPECIFIED. ) ;
#10528=CARTESIAN_POINT ( 'NONE',  ( 25.64692232868534560, -112.3263170481596660, -11.47740546588750199 ) ) ;
#10529=CARTESIAN_POINT ( 'NONE',  ( 10.93730112725932635, 0.000000000000000000, 0.000000000000000000 ) ) ;
#10533=VECTOR ( 'NONE', #12040, 1000.000000000000000 ) ;
#10534=ORIENTED_EDGE ( 'NONE', *, *, #7071, .T. ) ;
#10535=CARTESIAN_POINT ( 'NONE',  ( 109.1778270068192853, 0.001322180554006313971, -0.009220257877172538530 ) ) ;
#10536=CARTESIAN_POINT ( 'NONE',  ( 109.1586900883932856, -0.001385221016527508594, 0.007002774699553633575 ) ) ;
#10537=CARTESIAN_POINT ( 'NONE',  ( 1.833485406944071361, 29.64752363041738548, -142.0485807715643034 ) ) ;
#10538=EDGE_CURVE ( 'NONE', #2946, #8194, #694, .T. ) ;
#10539=CARTESIAN_POINT ( 'NONE',  ( 28.37644542392823865, 105.5967537682344926, 65.64862111872109551 ) ) ;
#10540=ORIENTED_EDGE ( 'NONE', *, *, #4844, .F. ) ;
#10543=CARTESIAN_POINT ( 'NONE',  ( 109.1586900883932856, -0.006960773163856042410, -0.001582822706024228452 ) ) ;
#10544=EDGE_CURVE ( 'NONE', #6343, #5142, #22160, .T. ) ;
#10547=CARTESIAN_POINT ( 'NONE',  ( 25.64708228042118776, -11.84161204513335619, 112.2886173090159048 ) ) ;
#10548=CARTESIAN_POINT ( 'NONE',  ( 10.93730112725971715, -20.69552240458431314, 149.7554878793147282 ) ) ;
#10549=CARTESIAN_POINT ( 'NONE',  ( 94.22246935314088034, 90.00000000000005684, 12.49999999999999467 ) ) ;
#10552=ORIENTED_EDGE ( 'NONE', *, *, #4933, .T. ) ;
#10553=CARTESIAN_POINT ( 'NONE',  ( 25.64681081121880624, -23.88203588908001507, -110.3564950173084185 ) ) ;
#10557=VERTEX_POINT ( 'NONE', #3288 ) ;
#10559=CARTESIAN_POINT ( 'NONE',  ( 10.93730112725970294, 65.95960219663110990, 136.0306644680985642 ) ) ;
#10565=EDGE_CURVE ( 'NONE', #15445, #1356, #27665, .T. ) ;
#10566=CARTESIAN_POINT ( 'NONE',  ( 1.832998868059858122, 117.0819875546695528, 85.72499093308138640 ) ) ;
#10567=LINE ( 'NONE', #19201, #6527 ) ;
#10570=CARTESIAN_POINT ( 'NONE',  ( 6.224689322667647851, -134.1951906609243110, 62.55544044765201761 ) ) ;
#10571=CARTESIAN_POINT ( 'NONE',  ( 10.93730112725991077, -79.81734490845832397, -128.3908183996600201 ) ) ;
#10572=ORIENTED_EDGE ( 'NONE', *, *, #7071, .F. ) ;
#10573=VERTEX_POINT ( 'NONE', #23306 ) ;
#10574=CARTESIAN_POINT ( 'NONE',  ( 2.433796855181219243, -13.76554153471791864, 144.8571464219888583 ) ) ;
#10577=CARTESIAN_POINT ( 'NONE',  ( 2.108985857320914370, 96.26411661813186527, -108.8271972979190423 ) ) ;
#10578=ORIENTED_EDGE ( 'NONE', *, *, #18889, .T. ) ;
#10579=CARTESIAN_POINT ( 'NONE',  ( 8.186469777911039358, 148.1306754055311501, -19.05650978729052270 ) ) ;
#10582=ORIENTED_EDGE ( 'NONE', *, *, #3353, .T. ) ;
#10583=VERTEX_POINT ( 'NONE', #21267 ) ;
#10589=EDGE_CURVE ( 'NONE', #16457, #15104, #19400, .T. ) ;
#10590=ORIENTED_EDGE ( 'NONE', *, *, #9535, .T. ) ;
#10592=B_SPLINE_CURVE_WITH_KNOTS ( 'NONE', 3,
 ( #11442, #24269, #9570, #17898 ),
 .UNSPECIFIED., .F., .F.,
 ( 4, 4 ),
 ( 3.492272924721346237E-16, 0.01077107486149825148 ),
 .UNSPECIFIED. ) ;
#10593=VECTOR ( 'NONE', #23851, 1000.000000000000114 ) ;
#10594=CARTESIAN_POINT ( 'NONE',  ( 5.340103556456440081, -75.71042922800619124, 126.5279493230356280 ) ) ;
#10597=CARTESIAN_POINT ( 'NONE',  ( 13.36082413113061307, 70.90215303572124128, 135.4964217943309563 ) ) ;
#10598=CARTESIAN_POINT ( 'NONE',  ( 28.43349137099852442, 109.5743306972603932, 58.58376153369732720 ) ) ;
#10600=CARTESIAN_POINT ( 'NONE',  ( 28.37644542392846603, -8.957364412599346792, -124.0168596762486715 ) ) ;
#10603=CARTESIAN_POINT ( 'NONE',  ( 1.831572820252009626, -144.2101521542831790, 16.14965423926163623 ) ) ;
#10605=CARTESIAN_POINT ( 'NONE',  ( 25.70243777736188662, -102.8829101922927691, -46.60897284577268351 ) ) ;
#10606=ORIENTED_EDGE ( 'NONE', *, *, #16250, .F. ) ;
#10607=ORIENTED_EDGE ( 'NONE', *, *, #18518, .F. ) ;
#10608=CARTESIAN_POINT ( 'NONE',  ( 25.64700659047695197, 56.65258046470393083, -97.67001118499042889 ) ) ;
#10610=DIRECTION ( 'NONE',  ( -1.000000000000000000, -0.000000000000000000, -0.000000000000000000 ) ) ;
#10611=CARTESIAN_POINT ( 'NONE',  ( 2.263178607246686180, 46.26071628252450552, 137.8402782326812712 ) ) ;
#10612=CARTESIAN_POINT ( 'NONE',  ( 25.81918753295379432, -76.32043280377756389, -83.36706424720522079 ) ) ;
#10613=CARTESIAN_POINT ( 'NONE',  ( 25.64670758986457955, 97.53391148296672952, 56.88615781331523635 ) ) ;
#10617=AXIS2_PLACEMENT_3D ( 'NONE', #9396, #4480, #601 ) ;
#10621=CARTESIAN_POINT ( 'NONE',  ( 26.11404676487259024, -103.8885755249566643, -45.01677474591514283 ) ) ;
#10622=AXIS2_PLACEMENT_3D ( 'NONE', #3091, #16031, #9565 ) ;
#10623=VERTEX_POINT ( 'NONE', #9774 ) ;
#10626=CARTESIAN_POINT ( 'NONE',  ( 109.1721716018069515, -0.008358834333177977277, -0.01488186354165293469 ) ) ;
#10628=CARTESIAN_POINT ( 'NONE',  ( 28.37644542392844826, -80.14194118792646293, -95.06674036596292865 ) ) ;
#10630=EDGE_CURVE ( 'NONE', #4919, #4083, #2575, .T. ) ;
#10631=CARTESIAN_POINT ( 'NONE',  ( 32.73300124599741423, -92.86301839379967760, -72.21147546950645335 ) ) ;
#10632=CARTESIAN_POINT ( 'NONE',  ( 2.433796855181205476, 137.9325382748285165, 46.34326152018790168 ) ) ;
#10637=CARTESIAN_POINT ( 'NONE',  ( 26.04756280548352976, 55.62433096787562192, -98.56594554799059438 ) ) ;
#10640=DIRECTION ( 'NONE',  ( -0.5914120900931443270, 0.7023121577978127528, 0.3962188444547265487 ) ) ;
#10641=CARTESIAN_POINT ( 'NONE',  ( 1.833603222531960730, -137.8693250773474688, -45.26427810763046011 ) ) ;
#10644=AXIS2_PLACEMENT_3D ( 'NONE', #24320, #19840, #9055 ) ;
#10645=CARTESIAN_POINT ( 'NONE',  ( 26.11404676487259024, -57.58742681967517285, 97.48350837663589630 ) ) ;
#10646=ADVANCED_FACE ( 'NONE', ( #25873 ), #15332, .F. ) ;
#10647=CARTESIAN_POINT ( 'NONE',  ( 28.43349137099851021, 86.10800331998767376, 89.57679848841816295 ) ) ;
#10648=PLANE ( 'NONE',  #11155 ) ;
#10650=ORIENTED_EDGE ( 'NONE', *, *, #8070, .F. ) ;
#10653=ORIENTED_EDGE ( 'NONE', *, *, #16479, .T. ) ;
#10656=CARTESIAN_POINT ( 'NONE',  ( 2.430230287190581429, 16.65331920325930781, -144.5585181921884157 ) ) ;
#10658=CARTESIAN_POINT ( 'NONE',  ( 10.93730112726006354, 149.7554878793152966, -20.69552240458195413 ) ) ;
#10659=CARTESIAN_POINT ( 'NONE',  ( 55.79472521941426777, -68.96476385670649734, -23.17337251492834227 ) ) ;
#10661=VERTEX_POINT ( 'NONE', #21830 ) ;
#10662=CARTESIAN_POINT ( 'NONE',  ( 1.831572820252009626, 107.1759352627519206, -97.82994539998277617 ) ) ;
#10664=CARTESIAN_POINT ( 'NONE',  ( 1.833691583653552115, 117.6050685739180182, -85.00512109099132374 ) ) ;
#10665=B_SPLINE_CURVE_WITH_KNOTS ( 'NONE', 3,
 ( #14855, #25677, #8114, #1887, #8250, #10283 ),
 .UNSPECIFIED., .F., .F.,
 ( 4, 2, 4 ),
 ( 1.127570259384924611E-17, 0.0006311636237756805372, 0.001262327247551349799 ),
 .UNSPECIFIED. ) ;
#10666=CARTESIAN_POINT ( 'NONE',  ( 30.59141879584288048, -60.43012207291027238, 99.26511058698874024 ) ) ;
#10668=VERTEX_POINT ( 'NONE', #23872 ) ;
#10670=CARTESIAN_POINT ( 'NONE',  ( 25.64708010899964208, -11.85684669924894585, -112.2870082086267587 ) ) ;
#10673=ORIENTED_EDGE ( 'NONE', *, *, #10034, .T. ) ;
#10674=VECTOR ( 'NONE', #1499, 1000.000000000000000 ) ;
#10678=EDGE_CURVE ( 'NONE', #24940, #24442, #19744, .T. ) ;
#10679=DIRECTION ( 'NONE',  ( 0.5946245182733607137, -0.4701913299128774315, -0.6521823330503007110 ) ) ;
#10681=B_SPLINE_CURVE_WITH_KNOTS ( 'NONE', 3,
 ( #23512, #3920, #1471, #27667 ),
 .UNSPECIFIED., .F., .F.,
 ( 4, 4 ),
 ( 1.097135458930219133E-17, 0.008383560773332686053 ),
 .UNSPECIFIED. ) ;
#10683=CARTESIAN_POINT ( 'NONE',  ( 30.59138290137869731, 114.2039707400270458, 21.51300488027170843 ) ) ;
#10684=ORIENTED_EDGE ( 'NONE', *, *, #27325, .F. ) ;
#10685=FACE_OUTER_BOUND ( 'NONE', #24668, .T. ) ;
#10687=CARTESIAN_POINT ( 'NONE',  ( 10.93730112725977932, -128.3908183996597074, 79.81734490845860819 ) ) ;
#10688=AXIS2_PLACEMENT_3D ( 'NONE', #24446, #678, #2841 ) ;
#10689=( BOUNDED_SURFACE ( )  B_SPLINE_SURFACE ( 3, 1, ( 
 ( #2113, #4146 ),
 ( #22133, #10917 ),
 ( #15356, #11194 ),
 ( #6324, #24165 ) ),
 .UNSPECIFIED., .F., .F., .F. ) 
 B_SPLINE_SURFACE_WITH_KNOTS ( ( 4, 4 ),
 ( 2, 2 ),
 ( 0.000000000000000000, 1.000000000000000000 ),
 ( 0.000000000000000000, 1.000000000000000000 ),
 .UNSPECIFIED. ) 
 GEOMETRIC_REPRESENTATION_ITEM ( )  RATIONAL_B_SPLINE_SURFACE ( (
 ( 1.000000000000000000, 1.000000000000000000),
 ( 0.6386103224230316178, 0.9954351624131538845),
 ( 0.6386103224230316178, 0.9954351624131538845),
 ( 1.000000000000000000, 1.000000000000000000) ) ) 
 REPRESENTATION_ITEM ( '' )  SURFACE ( )  );
#10693=VECTOR ( 'NONE', #27094, 1000.000000000000114 ) ;
#10694=CARTESIAN_POINT ( 'NONE',  ( 26.11404676487257603, 107.3263591096430218, 36.06104232266487486 ) ) ;
#10695=CARTESIAN_POINT ( 'NONE',  ( 109.1721716018069515, -0.01281875973823909734, 0.01127028715939367397 ) ) ;
#10696=CARTESIAN_POINT ( 'NONE',  ( 1.831572820252009626, 73.40899645746004865, 125.1738732943812664 ) ) ;
#10697=ORIENTED_EDGE ( 'NONE', *, *, #7169, .F. ) ;
#10698=ORIENTED_EDGE ( 'NONE', *, *, #27421, .T. ) ;
#10699=CARTESIAN_POINT ( 'NONE',  ( 109.1586059443104944, -0.001198897580739041041, 0.006971743774739755720 ) ) ;
#10701=ORIENTED_EDGE ( 'NONE', *, *, #24753, .T. ) ;
#10703=VERTEX_POINT ( 'NONE', #19795 ) ;
#10704=EDGE_CURVE ( 'NONE', #17963, #25814, #1567, .T. ) ;
#10706=EDGE_CURVE ( 'NONE', #25074, #6918, #9520, .T. ) ;
#10708=CARTESIAN_POINT ( 'NONE',  ( 1.833485406944043827, -73.01664920993054864, 125.4007332306543105 ) ) ;
#10715=VECTOR ( 'NONE', #15134, 1000.000000000000114 ) ;
#10716=CARTESIAN_POINT ( 'NONE',  ( 109.1721716018069657, -0.001583175916619938188, 0.01699510305644696614 ) ) ;
#10720=ORIENTED_EDGE ( 'NONE', *, *, #26031, .F. ) ;
#10721=CARTESIAN_POINT ( 'NONE',  ( 109.1592201516379674, -0.002134489919768192863, 0.007566779963325561721 ) ) ;
#10722=CARTESIAN_POINT ( 'NONE',  ( 25.64670758986459376, -56.88615781331557741, 97.53391148296655899 ) ) ;
#10724=CARTESIAN_POINT ( 'NONE',  ( 2.430230287190572103, 31.67257033707700131, -142.0258656395018591 ) ) ;
#10727=AXIS2_PLACEMENT_3D ( 'NONE', #16041, #26415, #9013 ) ;
#10728=ORIENTED_EDGE ( 'NONE', *, *, #21782, .T. ) ;
#10729=CARTESIAN_POINT ( 'NONE',  ( 1.893872463202064260, 145.1467500857187929, 0.9528309182402651123 ) ) ;
#10730=CIRCLE ( 'NONE', #19855, 151.1787379149930359 ) ;
#10735=CARTESIAN_POINT ( 'NONE',  ( 10.93730112725990367, -133.3192575531795399, -71.28103789255078482 ) ) ;
#10738=CARTESIAN_POINT ( 'NONE',  ( 109.1592201516379674, -0.002913740842108687636, -0.007302213399779916743 ) ) ;
#10739=ORIENTED_EDGE ( 'NONE', *, *, #9594, .F. ) ;
#10740=EDGE_CURVE ( 'NONE', #21908, #3673, #23612, .T. ) ;
#10742=CARTESIAN_POINT ( 'NONE',  ( 10.93730112725995873, 4.928439153522441885, -151.0983828010091656 ) ) ;
#10745=ORIENTED_EDGE ( 'NONE', *, *, #4039, .T. ) ;
#10748=CARTESIAN_POINT ( 'NONE',  ( 13.36082413113061307, -135.4964217943312121, 70.90215303572075811 ) ) ;
#10751=FACE_OUTER_BOUND ( 'NONE', #3977, .T. ) ;
#10752=CARTESIAN_POINT ( 'NONE',  ( 55.79472521941426777, -15.83764557006318796, 71.00924468211151463 ) ) ;
#10753=CARTESIAN_POINT ( 'NONE',  ( 25.64660436782555308, -103.3839381879728876, -45.39454672041220107 ) ) ;
#10754=CARTESIAN_POINT ( 'NONE',  ( 1.832998868059858122, -144.2584710144581663, 15.69902610990328640 ) ) ;
#10757=EDGE_LOOP ( 'NONE', ( #20893, #20719, #2345, #28130 ) ) ;
#10758=VERTEX_POINT ( 'NONE', #26556 ) ;
#10759=CARTESIAN_POINT ( 'NONE',  ( 10.93730112725982373, -142.1801301103788262, 51.37919228020236773 ) ) ;
#10760=LINE ( 'NONE', #17495, #25452 ) ;
#10766=ORIENTED_EDGE ( 'NONE', *, *, #5397, .F. ) ;
#10768=EDGE_CURVE ( 'NONE', #15152, #14205, #24629, .T. ) ;
#10769=CARTESIAN_POINT ( 'NONE',  ( 1.833485406944043827, -29.64752363041439764, -142.0485807715649003 ) ) ;
#10770=CARTESIAN_POINT ( 'NONE',  ( 8.186469829614351212, -149.3111477833938636, -3.468244397268659629 ) ) ;
#10771=CARTESIAN_POINT ( 'NONE',  ( 55.79472521941426777, 71.00924468211157148, 15.83764557006294993 ) ) ;
#10772=VERTEX_POINT ( 'NONE', #15468 ) ;
#10773=( BOUNDED_SURFACE ( )  B_SPLINE_SURFACE ( 3, 1, ( 
 ( #11025, #17487 ),
 ( #12745, #6289 ),
 ( #17071, #25862 ),
 ( #17343, #8871 ) ),
 .UNSPECIFIED., .F., .F., .F. ) 
 B_SPLINE_SURFACE_WITH_KNOTS ( ( 4, 4 ),
 ( 2, 2 ),
 ( 0.000000000000000000, 1.000000000000000000 ),
 ( 0.000000000000000000, 1.000000000000000000 ),
 .UNSPECIFIED. ) 
 GEOMETRIC_REPRESENTATION_ITEM ( )  RATIONAL_B_SPLINE_SURFACE ( (
 ( 1.000000000000000000, 1.000000000000000000),
 ( 0.9956975270656955868, 0.8568959468854907557),
 ( 0.9956975270656955868, 0.8568959468854907557),
 ( 1.000000000000000000, 1.000000000000000000) ) ) 
 REPRESENTATION_ITEM ( '' )  SURFACE ( )  );
#10774=EDGE_CURVE ( 'NONE', #17852, #14882, #13625, .T. ) ;
#10775=EDGE_CURVE ( 'NONE', #17914, #24750, #13891, .T. ) ;
#10776=VERTEX_POINT ( 'NONE', #364 ) ;
#10780=CARTESIAN_POINT ( 'NONE',  ( 32.73300124599732186, 0.000000000000000000, 0.000000000000000000 ) ) ;
#10781=CARTESIAN_POINT ( 'NONE',  ( 2.433796855181219243, -71.49415740225165905, 126.7346379669253622 ) ) ;
#10782=DIRECTION ( 'NONE',  ( -1.000000000000000000, -0.000000000000000000, -0.000000000000000000 ) ) ;
#10784=CARTESIAN_POINT ( 'NONE',  ( 25.64681081121879203, -110.3564950173080206, -23.88203588908195130 ) ) ;
#10785=CARTESIAN_POINT ( 'NONE',  ( 25.64708228042120197, 23.43704872438759423, 110.4520805602535916 ) ) ;
#10786=CARTESIAN_POINT ( 'NONE',  ( 24.22246935314087324, 0.000000000000000000, 0.000000000000000000 ) ) ;
#10788=CARTESIAN_POINT ( 'NONE',  ( 28.37603512858451538, -93.86378016273927472, -65.97809844506220145 ) ) ;
#10790=CARTESIAN_POINT ( 'NONE',  ( 55.79472521941426777, -63.36760613016249977, 35.74479459808824799 ) ) ;
#10792=ORIENTED_EDGE ( 'NONE', *, *, #13412, .F. ) ;
#10797=CARTESIAN_POINT ( 'NONE',  ( 109.1586900883932856, 0.0006456433529162480898, 0.007109207791181754860 ) ) ;
#10798=CARTESIAN_POINT ( 'NONE',  ( 2.433796855181233454, -98.43889364293788447, -107.1581411821795626 ) ) ;
#10800=CARTESIAN_POINT ( 'NONE',  ( 55.79472521941428198, 43.35047097963449403, 58.42842213658343553 ) ) ;
#10801=LINE ( 'NONE', #19152, #19380 ) ;
#10803=CARTESIAN_POINT ( 'NONE',  ( 26.11404676487257603, -65.63269960453305885, 92.25884714080386573 ) ) ;
#10804=CARTESIAN_POINT ( 'NONE',  ( 109.1589550718175161, -0.003284595046935084688, -0.006826119083824118937 ) ) ;
#10805=EDGE_CURVE ( 'NONE', #8222, #10266, #12910, .T. ) ;
#10807=B_SPLINE_CURVE_WITH_KNOTS ( 'NONE', 3,
 ( #5577, #14344, #18963, #23162, #7904, #27742, #25594 ),
 .UNSPECIFIED., .F., .F.,
 ( 4, 3, 4 ),
 ( 5.204170427930421283E-18, 0.02816610861753244405, 0.04000277880656212537 ),
 .UNSPECIFIED. ) ;
#10810=ORIENTED_EDGE ( 'NONE', *, *, #7834, .F. ) ;
#10811=CARTESIAN_POINT ( 'NONE',  ( 99.22246935314079508, -90.00000000000005684, -40.00000000000002842 ) ) ;
#10812=ADVANCED_FACE ( 'NONE', ( #2371 ), #18221, .F. ) ;
#10813=CARTESIAN_POINT ( 'NONE',  ( 25.64681081121879203, -11.38886654529598275, -112.3352186517031726 ) ) ;
#10814=ORIENTED_EDGE ( 'NONE', *, *, #21290, .T. ) ;
#10817=VERTEX_POINT ( 'NONE', #9580 ) ;
#10825=EDGE_LOOP ( 'NONE', ( #11183, #21888, #8670, #6409 ) ) ;
#10828=LINE ( 'NONE', #15256, #27137 ) ;
#10829=CARTESIAN_POINT ( 'NONE',  ( 6.224689322667630975, 2.565137105445823185, -148.0369967195762513 ) ) ;
#10832=CARTESIAN_POINT ( 'NONE',  ( 1.893872463202077805, -29.24569695044139905, -142.1730500379301532 ) ) ;
#10833=EDGE_CURVE ( 'NONE', #27728, #25430, #22206, .T. ) ;
#10835=B_SPLINE_CURVE_WITH_KNOTS ( 'NONE', 3,
 ( #17571, #6660, #17849, #15406, #26493, #24358, #11526, #11110, #17992, #18554 ),
 .UNSPECIFIED., .F., .F.,
 ( 4, 3, 3, 4 ),
 ( 3.642919299551294898E-17, 0.0002669559177086183342, 0.0005339118354150966701, 0.001067817517169159913 ),
 .UNSPECIFIED. ) ;
#10837=ORIENTED_EDGE ( 'NONE', *, *, #24362, .F. ) ;
#10838=VERTEX_POINT ( 'NONE', #4836 ) ;
#10839=EDGE_CURVE ( 'NONE', #1176, #21489, #24978, .T. ) ;
#10840=CARTESIAN_POINT ( 'NONE',  ( 13.84597867724977505, -40.76072889493656248, -140.9259526407712713 ) ) ;
#10841=ORIENTED_EDGE ( 'NONE', *, *, #21886, .F. ) ;
#10842=VERTEX_POINT ( 'NONE', #3390 ) ;
#10843=ORIENTED_EDGE ( 'NONE', *, *, #26899, .F. ) ;
#10844=CARTESIAN_POINT ( 'NONE',  ( 1.831572820252009626, 86.09108691067770280, 116.8148281295972168 ) ) ;
#10846=LINE ( 'NONE', #8676, #2787 ) ;
#10848=CARTESIAN_POINT ( 'NONE',  ( 1.832998868059890096, 45.34898734666227682, -137.8420662456165644 ) ) ;
#10849=( BOUNDED_SURFACE ( )  B_SPLINE_SURFACE ( 3, 1, ( 
 ( #15053, #15119 ),
 ( #4342, #2304 ),
 ( #21617, #28231 ),
 ( #11252, #2458 ) ),
 .UNSPECIFIED., .F., .F., .F. ) 
 B_SPLINE_SURFACE_WITH_KNOTS ( ( 4, 4 ),
 ( 2, 2 ),
 ( 0.000000000000000000, 1.000000000000000000 ),
 ( 0.000000000000000000, 1.000000000000000000 ),
 .UNSPECIFIED. ) 
 GEOMETRIC_REPRESENTATION_ITEM ( )  RATIONAL_B_SPLINE_SURFACE ( (
 ( 1.000000000000000000, 1.000000000000000000),
 ( 0.6386103224230302855, 0.9954351624131538845),
 ( 0.6386103224230302855, 0.9954351624131538845),
 ( 1.000000000000000000, 1.000000000000000000) ) ) 
 REPRESENTATION_ITEM ( '' )  SURFACE ( )  );
#10850=CARTESIAN_POINT ( 'NONE',  ( 109.1778270068192853, -0.005967275455169835166, -0.007152128381194115120 ) ) ;
#10852=DIRECTION ( 'NONE',  ( -0.5946245182733607137, -0.5401723099040838250, -0.5955128528260831278 ) ) ;
#10853=CARTESIAN_POINT ( 'NONE',  ( 55.79472521941426777, -66.16469064668278577, -30.25520714117973142 ) ) ;
#10856=VERTEX_POINT ( 'NONE', #22845 ) ;
#10857=ORIENTED_EDGE ( 'NONE', *, *, #22833, .T. ) ;
#10859=EDGE_CURVE ( 'NONE', #2880, #20917, #4352, .T. ) ;
#10867=EDGE_CURVE ( 'NONE', #28052, #13932, #14658, .T. ) ;
#10868=LINE ( 'NONE', #26253, #6139 ) ;
#10869=VERTEX_POINT ( 'NONE', #5404 ) ;
#10870=ORIENTED_EDGE ( 'NONE', *, *, #10775, .F. ) ;
#10873=ORIENTED_EDGE ( 'NONE', *, *, #10706, .F. ) ;
#10876=CARTESIAN_POINT ( 'NONE',  ( 109.1587776205901861, 0.005880209827414124152, -0.004375189885423126993 ) ) ;
#10877=FACE_OUTER_BOUND ( 'NONE', #17645, .T. ) ;
#10879=CARTESIAN_POINT ( 'NONE',  ( 9.884929003653608603, -19.90991253123348059, 149.2134106160915508 ) ) ;
#10880=CARTESIAN_POINT ( 'NONE',  ( 2.430230287190572103, -46.34481016236920681, 137.9371479820460991 ) ) ;
#10881=( BOUNDED_SURFACE ( )  B_SPLINE_SURFACE ( 3, 1, ( 
 ( #27346, #13671 ),
 ( #20878, #25069 ),
 ( #7802, #16122 ),
 ( #18135, #20585 ) ),
 .UNSPECIFIED., .F., .F., .F. ) 
 B_SPLINE_SURFACE_WITH_KNOTS ( ( 4, 4 ),
 ( 2, 2 ),
 ( 0.000000000000000000, 1.000000000000000000 ),
 ( 0.000000000000000000, 1.000000000000000000 ),
 .UNSPECIFIED. ) 
 GEOMETRIC_REPRESENTATION_ITEM ( )  RATIONAL_B_SPLINE_SURFACE ( (
 ( 1.000000000000000000, 1.000000000000000000),
 ( 0.6386103224230302855, 0.9954351624131538845),
 ( 0.6386103224230302855, 0.9954351624131538845),
 ( 1.000000000000000000, 1.000000000000000000) ) ) 
 REPRESENTATION_ITEM ( '' )  SURFACE ( )  );
#10883=CARTESIAN_POINT ( 'NONE',  ( 1.833485406944043827, -97.49333871408619245, -107.4794113447419477 ) ) ;
#10884=CARTESIAN_POINT ( 'NONE',  ( 25.73574536432414206, -112.2643803187784641, -12.61003673872005137 ) ) ;
#10886=CARTESIAN_POINT ( 'NONE',  ( 25.87036335909426299, 103.6841944152907047, 45.07965203034955692 ) ) ;
#10887=CARTESIAN_POINT ( 'NONE',  ( 2.430230287190581429, -13.76600171652546045, -144.8619874886008176 ) ) ;
#10888=FACE_OUTER_BOUND ( 'NONE', #23462, .T. ) ;
#10890=VERTEX_POINT ( 'NONE', #14314 ) ;
#10891=CARTESIAN_POINT ( 'NONE',  ( 32.73300124599732186, 0.000000000000000000, 0.000000000000000000 ) ) ;
#10892=FACE_OUTER_BOUND ( 'NONE', #10186, .T. ) ;
#10896=CARTESIAN_POINT ( 'NONE',  ( 32.73300124599741423, 115.8010721414085822, -20.69176323058512423 ) ) ;
#10898=EDGE_LOOP ( 'NONE', ( #8564, #22879, #15128, #7997 ) ) ;
#10899=CARTESIAN_POINT ( 'NONE',  ( 1.833721034905632541, -44.50273803002032480, 138.1171912769429468 ) ) ;
#10900=DIRECTION ( 'NONE',  ( 1.000000000000000000, -0.000000000000000000, -0.000000000000000000 ) ) ;
#10901=B_SPLINE_CURVE_WITH_KNOTS ( 'NONE', 3,
 ( #25023, #22862, #11328, #3122 ),
 .UNSPECIFIED., .F., .F.,
 ( 4, 4 ),
 ( 0.000000000000000000, 0.008383560773332727686 ),
 .UNSPECIFIED. ) ;
#10902=CARTESIAN_POINT ( 'NONE',  ( 25.64699802086725811, 112.3172869996024730, 11.56593161917351864 ) ) ;
#10907=CARTESIAN_POINT ( 'NONE',  ( 1.833603222531972055, 15.61050054119223063, -144.2675221341992540 ) ) ;
#10908=CARTESIAN_POINT ( 'NONE',  ( 32.73300124599739291, 89.94078864464164269, -75.82012867748392182 ) ) ;
#10909=ORIENTED_EDGE ( 'NONE', *, *, #13971, .T. ) ;
#10910=CARTESIAN_POINT ( 'NONE',  ( 28.37603512858454380, 93.86378016273968683, 65.97809844506153354 ) ) ;
#10911=CARTESIAN_POINT ( 'NONE',  ( 1.833485406944057594, 108.1939177044926055, 96.69979900902202985 ) ) ;
#10914=LINE ( 'NONE', #1983, #17957 ) ;
#10916=CARTESIAN_POINT ( 'NONE',  ( 25.86096068574581253, 46.89265070732260199, -102.8701285401536865 ) ) ;
#10917=CARTESIAN_POINT ( 'NONE',  ( 9.884929003653626367, 139.1775604444703731, 57.36421526887207989 ) ) ;
#10918=CARTESIAN_POINT ( 'NONE',  ( 19.66333377628716050, -99.30798531455278066, -95.46107873288976009 ) ) ;
#10920=CARTESIAN_POINT ( 'NONE',  ( 26.11404676487257603, 110.9778746459746941, 22.43340081644806006 ) ) ;
#10921=EDGE_CURVE ( 'NONE', #8760, #11237, #25568, .T. ) ;
#10922=CARTESIAN_POINT ( 'NONE',  ( 2.430230287190572103, 96.28466919684099423, 109.1043569252017562 ) ) ;
#10923=CARTESIAN_POINT ( 'NONE',  ( 1.832998868059890096, -117.0819875546689701, -85.72499093308219642 ) ) ;
#10924=CARTESIAN_POINT ( 'NONE',  ( 26.11404676487257603, 112.7148551500680469, 10.71016160607605627 ) ) ;
#10925=EDGE_LOOP ( 'NONE', ( #2469, #23969, #23358, #1488 ) ) ;
#10926=EDGE_CURVE ( 'NONE', #8537, #21319, #2616, .T. ) ;
#10927=VERTEX_POINT ( 'NONE', #14462 ) ;
#10930=CARTESIAN_POINT ( 'NONE',  ( 2.263178607246667973, -98.32595927618783094, -107.1074316126228183 ) ) ;
#10932=( BOUNDED_SURFACE ( )  B_SPLINE_SURFACE ( 3, 1, ( 
 ( #2252, #28451 ),
 ( #8755, #17523 ),
 ( #19824, #6605 ),
 ( #4148, #15358 ) ),
 .UNSPECIFIED., .F., .F., .F. ) 
 B_SPLINE_SURFACE_WITH_KNOTS ( ( 4, 4 ),
 ( 2, 2 ),
 ( 0.000000000000000000, 1.000000000000000000 ),
 ( 0.000000000000000000, 1.000000000000000000 ),
 .UNSPECIFIED. ) 
 GEOMETRIC_REPRESENTATION_ITEM ( )  RATIONAL_B_SPLINE_SURFACE ( (
 ( 1.000000000000000000, 1.000000000000000000),
 ( 0.6386103224230316178, 0.9954351624131538845),
 ( 0.6386103224230316178, 0.9954351624131538845),
 ( 1.000000000000000000, 1.000000000000000000) ) ) 
 REPRESENTATION_ITEM ( '' )  SURFACE ( )  );
#10933=CARTESIAN_POINT ( 'NONE',  ( 28.37644542392854063, -102.9230687709012244, 69.76573497039046856 ) ) ;
#10935=ORIENTED_EDGE ( 'NONE', *, *, #8343, .F. ) ;
#10936=CARTESIAN_POINT ( 'NONE',  ( 1.833485406944057594, 30.69200235378934849, 141.8265699653868523 ) ) ;
#10938=CARTESIAN_POINT ( 'NONE',  ( 109.1778270068192853, 0.005186985107090136965, -0.007736698406808922672 ) ) ;
#10940=CARTESIAN_POINT ( 'NONE',  ( 109.1721716018069515, 0.005466227998627255259, -0.01616973485710007305 ) ) ;
#10941=ORIENTED_EDGE ( 'NONE', *, *, #25483, .T. ) ;
#10943=CARTESIAN_POINT ( 'NONE',  ( 109.1592201516379674, -0.006044422199822568030, 0.005027640251767196387 ) ) ;
#10944=ORIENTED_EDGE ( 'NONE', *, *, #6909, .T. ) ;
#10946=ORIENTED_EDGE ( 'NONE', *, *, #1932, .T. ) ;
#10952=ORIENTED_EDGE ( 'NONE', *, *, #18728, .T. ) ;
#10953=EDGE_CURVE ( 'NONE', #335, #20657, #24886, .T. ) ;
#10955=CARTESIAN_POINT ( 'NONE',  ( 10.93730112725977932, -115.5857507957709913, 97.44200844886238144 ) ) ;
#10956=ORIENTED_EDGE ( 'NONE', *, *, #5392, .T. ) ;
#10958=CARTESIAN_POINT ( 'NONE',  ( 1.833603222531960952, 85.65285110156294479, -117.1340888386541224 ) ) ;
#10959=CARTESIAN_POINT ( 'NONE',  ( 1.833485406944043827, 142.0485807715649571, -29.64752363041402816 ) ) ;
#10960=DIRECTION ( 'NONE',  ( -1.000000000000000000, -0.000000000000000000, -0.000000000000000000 ) ) ;
#10963=EDGE_CURVE ( 'NONE', #28334, #26729, #21848, .T. ) ;
#10965=CARTESIAN_POINT ( 'NONE',  ( 8.186469829614372529, -57.56191610809284498, -137.8131829164341582 ) ) ;
#10966=CARTESIAN_POINT ( 'NONE',  ( 32.73300124599732186, 0.000000000000000000, 0.000000000000000000 ) ) ;
#10967=B_SPLINE_CURVE_WITH_KNOTS ( 'NONE', 3,
 ( #27472, #20425, #10076, #25185, #5310, #18398, #707, #20566, #7784, #16538 ),
 .UNSPECIFIED., .F., .F.,
 ( 4, 3, 3, 4 ),
 ( 3.816391647148975608E-17, 0.0002669559177086078174, 0.0005339118354150857197, 0.001067817517169160780 ),
 .UNSPECIFIED. ) ;
#10968=CARTESIAN_POINT ( 'NONE',  ( 5.340103556456443634, -2.303180381359250628, 147.4316330165019622 ) ) ;
#10969=DIRECTION ( 'NONE',  ( 0.000000000000000000, -1.000000000000000000, 0.000000000000000000 ) ) ;
#10972=CARTESIAN_POINT ( 'NONE',  ( 9.884929003653608603, 124.2095058357589039, -85.04731144912386753 ) ) ;
#10974=VECTOR ( 'NONE', #7804, 1000.000000000000000 ) ;
#10977=CARTESIAN_POINT ( 'NONE',  ( 25.69398547355838858, 35.60637981494853221, 107.1830796521255422 ) ) ;
#10980=ORIENTED_EDGE ( 'NONE', *, *, #2905, .T. ) ;
#10981=CARTESIAN_POINT ( 'NONE',  ( 109.1586900883932856, 0.002995460350188396646, 0.006479576224398257700 ) ) ;
#10982=CARTESIAN_POINT ( 'NONE',  ( 1.833750490713684345, 137.9248034078897547, 45.09517546033693947 ) ) ;
#10985=FACE_OUTER_BOUND ( 'NONE', #16488, .T. ) ;
#10988=EDGE_CURVE ( 'NONE', #27119, #3338, #495, .T. ) ;
#10992=CARTESIAN_POINT ( 'NONE',  ( 32.73300124599740002, 110.6325518752278896, -39.98094346392192477 ) ) ;
#10996=ORIENTED_EDGE ( 'NONE', *, *, #21504, .T. ) ;
#10997=CARTESIAN_POINT ( 'NONE',  ( 32.73300124599732186, 0.000000000000000000, 0.000000000000000000 ) ) ;
#10999=CARTESIAN_POINT ( 'NONE',  ( 1.833485406944043827, 15.69895494453577101, -144.2578170162061326 ) ) ;
#11000=CARTESIAN_POINT ( 'NONE',  ( 32.73300124599735028, 8.473903470906103408, 117.3295799645430151 ) ) ;
#11001=CARTESIAN_POINT ( 'NONE',  ( 8.186469829614225091, -19.05650981809914057, 148.1306754360700211 ) ) ;
#11002=CARTESIAN_POINT ( 'NONE',  ( 1.831572820252009626, -71.69925593429898925, 126.1609924456727754 ) ) ;
#11003=VERTEX_POINT ( 'NONE', #14744 ) ;
#11004=CARTESIAN_POINT ( 'NONE',  ( 25.64700659047697684, 97.89757946487087281, -56.25842064175987645 ) ) ;
#11005=ORIENTED_EDGE ( 'NONE', *, *, #19908, .F. ) ;
#11009=ORIENTED_EDGE ( 'NONE', *, *, #11022, .T. ) ;
#11012=CARTESIAN_POINT ( 'NONE',  ( 2.430230287190592531, -43.58368230469486804, 138.8342928068218498 ) ) ;
#11013=B_SPLINE_CURVE_WITH_KNOTS ( 'NONE', 3,
 ( #16761, #14231, #2887, #26762, #7077, #27040, #24645, #26908 ),
 .UNSPECIFIED., .F., .F.,
 ( 4, 2, 2, 4 ),
 ( 1.962615573354718958E-17, 0.0002429592666046852441, 0.0004859185332093508640, 0.0009718370664186700694 ),
 .UNSPECIFIED. ) ;
#11015=CARTESIAN_POINT ( 'NONE',  ( 1.833206308920042105, -125.2945011813201006, -73.19872517709852389 ) ) ;
#11019=EDGE_CURVE ( 'NONE', #8336, #7588, #11543, .T. ) ;
#11021=CARTESIAN_POINT ( 'NONE',  ( 9.884929003653608603, -132.4189379373575548, 71.59798461011283166 ) ) ;
#11022=EDGE_CURVE ( 'NONE', #17054, #26729, #8422, .T. ) ;
#11023=FACE_OUTER_BOUND ( 'NONE', #2405, .T. ) ;
#11025=CARTESIAN_POINT ( 'NONE',  ( 109.1586900883932856, 0.006960773163856030267, 0.001582822706024277024 ) ) ;
#11026=EDGE_CURVE ( 'NONE', #5021, #7441, #28352, .T. ) ;
#11028=CARTESIAN_POINT ( 'NONE',  ( 1.833838850093453043, 125.6687428896159417, 72.55487854850731821 ) ) ;
#11029=CARTESIAN_POINT ( 'NONE',  ( 109.1592201516379674, -0.002720803050370518023, -0.007376275279032888654 ) ) ;
#11030=CARTESIAN_POINT ( 'NONE',  ( 25.64700659047696263, -56.65258046470324871, 97.67001118499082679 ) ) ;
#11031=ORIENTED_EDGE ( 'NONE', *, *, #22681, .F. ) ;
#11034=CARTESIAN_POINT ( 'NONE',  ( 10.93730112726006354, 148.8212007290666747, -26.59437931460595905 ) ) ;
#11036=CARTESIAN_POINT ( 'NONE',  ( 25.64681081121879203, -35.28660243342475411, -107.2555980796244910 ) ) ;
#11037=CARTESIAN_POINT ( 'NONE',  ( 1.832998868059858122, -59.50898020732601879, 132.3466930259791923 ) ) ;
#11038=LINE ( 'NONE', #26152, #594 ) ;
#11039=CARTESIAN_POINT ( 'NONE',  ( 16.05277956358201408, 80.40847413522703846, -118.6216415718953527 ) ) ;
#11042=CIRCLE ( 'NONE', #6085, 117.6351876552689504 ) ;
#11044=AXIS2_PLACEMENT_3D ( 'NONE', #6097, #8243, #27944 ) ;
#11045=ORIENTED_EDGE ( 'NONE', *, *, #22391, .T. ) ;
#11046=CARTESIAN_POINT ( 'NONE',  ( 109.1624594426973118, -0.01503296564241274336, 0.005372302061316216668 ) ) ;
#11047=CARTESIAN_POINT ( 'NONE',  ( -90.83090735639699176, 4.592425496802575156E-15, 37.50000000000001421 ) ) ;
#11048=CARTESIAN_POINT ( 'NONE',  ( 26.11404676487257603, 57.58742681967585497, -97.48350837663548418 ) ) ;
#11051=DIRECTION ( 'NONE',  ( 1.000000000000000000, 0.000000000000000000, 0.000000000000000000 ) ) ;
#11053=CARTESIAN_POINT ( 'NONE',  ( 32.73300124599740002, -8.473903470905288060, -117.3295799645430151 ) ) ;
#11054=CARTESIAN_POINT ( 'NONE',  ( 55.79472521941426777, -71.00924468211145779, -15.83764557006343487 ) ) ;
#11055=DIRECTION ( 'NONE',  ( -0.000000000000000000, 0.000000000000000000, 1.000000000000000000 ) ) ;
#11056=CARTESIAN_POINT ( 'NONE',  ( 1.833838850093452599, -132.5643635152038655, 59.02146106675034787 ) ) ;
#11059=ORIENTED_EDGE ( 'NONE', *, *, #27157, .F. ) ;
#11060=AXIS2_PLACEMENT_3D ( 'NONE', #212, #22525, #489 ) ;
#11063=CONICAL_SURFACE ( 'NONE', #1849, 117.6351876552689504, 0.9945805576725580410 ) ;
#11068=CARTESIAN_POINT ( 'NONE',  ( 2.108985857320933466, -98.16869034643225689, -107.1123114102938274 ) ) ;
#11069=CARTESIAN_POINT ( 'NONE',  ( 1.833838850093452821, 72.55487854850862561, -125.6687428896151886 ) ) ;
#11071=ORIENTED_EDGE ( 'NONE', *, *, #19329, .F. ) ;
#11075=CARTESIAN_POINT ( 'NONE',  ( 25.64708228042123395, 23.51409906510363612, -110.4357030047554531 ) ) ;
#11080=CARTESIAN_POINT ( 'NONE',  ( 1.833809397773861649, -107.9565774559017797, 96.96506043213419446 ) ) ;
#11082=VERTEX_POINT ( 'NONE', #13146 ) ;
#11083=ORIENTED_EDGE ( 'NONE', *, *, #21712, .T. ) ;
#11084=ADVANCED_FACE ( 'NONE', ( #10319 ), #6486, .F. ) ;
#11086=EDGE_CURVE ( 'NONE', #10842, #20262, #26970, .T. ) ;
#11087=VECTOR ( 'NONE', #22955, 1000.000000000000114 ) ;
#11088=AXIS2_PLACEMENT_3D ( 'NONE', #4536, #19649, #4116 ) ;
#11089=EDGE_CURVE ( 'NONE', #15583, #3658, #16015, .T. ) ;
#11091=CARTESIAN_POINT ( 'NONE',  ( 6.224689322667647851, 126.9212313063855362, -76.23997225729135607 ) ) ;
#11092=CARTESIAN_POINT ( 'NONE',  ( 10.93730112725932635, 0.000000000000000000, 0.000000000000000000 ) ) ;
#11093=ORIENTED_EDGE ( 'NONE', *, *, #13841, .F. ) ;
#11097=ORIENTED_EDGE ( 'NONE', *, *, #16965, .T. ) ;
#11098=VERTEX_POINT ( 'NONE', #10999 ) ;
#11099=CARTESIAN_POINT ( 'NONE',  ( 2.108393763691202683, 31.45977531353488033, -141.8460676169241026 ) ) ;
#11100=CARTESIAN_POINT ( 'NONE',  ( 1.833485406944057594, -45.34878176254139248, -137.8414413349090637 ) ) ;
#11103=CARTESIAN_POINT ( 'NONE',  ( 55.79472521941428198, -71.31192372336666097, -14.41365263906626915 ) ) ;
#11106=AXIS2_PLACEMENT_3D ( 'NONE', #7064, #15662, #4883 ) ;
#11107=B_SPLINE_CURVE_WITH_KNOTS ( 'NONE', 3,
 ( #12222, #1417, #23606, #7930, #5606, #3995, #3574 ),
 .UNSPECIFIED., .F., .F.,
 ( 4, 3, 4 ),
 ( 0.000000000000000000, 0.02398743853561344230, 0.04000277880656222251 ),
 .UNSPECIFIED. ) ;
#11108=VECTOR ( 'NONE', #4127, 1000.000000000000114 ) ;
#11109=CARTESIAN_POINT ( 'NONE',  ( 109.1586900883932856, -0.006130969560687385411, 0.003656351050331833278 ) ) ;
#11110=CARTESIAN_POINT ( 'NONE',  ( 1.833838848569424806, 15.34509722932533649, 144.2962335061012027 ) ) ;
#11111=CARTESIAN_POINT ( 'NONE',  ( 109.1586059443104944, -0.004378796245590049069, -0.005555961672773755862 ) ) ;
#11112=DIRECTION ( 'NONE',  ( -0.5914120900931443270, -0.2567974902965039496, -0.7643865440136131673 ) ) ;
#11114=VECTOR ( 'NONE', #7776, 1000.000000000000114 ) ;
#11116=ORIENTED_EDGE ( 'NONE', *, *, #8521, .T. ) ;
#11117=CARTESIAN_POINT ( 'NONE',  ( 1.833485406944043827, -96.69979900902094982, -108.1939177044935860 ) ) ;
#11118=EDGE_LOOP ( 'NONE', ( #28249, #12181, #5851, #21308 ) ) ;
#11119=ORIENTED_EDGE ( 'NONE', *, *, #17059, .T. ) ;
#11120=EDGE_CURVE ( 'NONE', #2861, #24693, #3643, .T. ) ;
#11121=ORIENTED_EDGE ( 'NONE', *, *, #15719, .T. ) ;
#11122=EDGE_CURVE ( 'NONE', #24160, #11589, #14325, .T. ) ;
#11123=CARTESIAN_POINT ( 'NONE',  ( 1.833691583653523249, 137.8971124741068195, 45.17974255430862485 ) ) ;
#11124=CARTESIAN_POINT ( 'NONE',  ( 26.11404676487259024, 10.71016160607567080, 112.7148551500680753 ) ) ;
#11125=B_SPLINE_CURVE_WITH_KNOTS ( 'NONE', 3,
 ( #18268, #7224, #13672, #22478, #24925, #13820, #5038 ),
 .UNSPECIFIED., .F., .F.,
 ( 4, 3, 4 ),
 ( 6.534015072584227389E-16, 0.02816610861753247874, 0.04000277880656289559 ),
 .UNSPECIFIED. ) ;
#11127=AXIS2_PLACEMENT_3D ( 'NONE', #9877, #7582, #25131 ) ;
#11128=CARTESIAN_POINT ( 'NONE',  ( 2.263178607246687069, 43.59477707254215062, -138.7064943909641102 ) ) ;
#11130=CARTESIAN_POINT ( 'NONE',  ( 19.66333377628691181, -46.81583828063168085, 129.5498775999586485 ) ) ;
#11131=CARTESIAN_POINT ( 'NONE',  ( 9.884929003653626367, -149.2134106160917497, 19.90991253123197779 ) ) ;
#11132=CARTESIAN_POINT ( 'NONE',  ( 21.16825799904896144, 127.3716170292830725, -46.02882515936357066 ) ) ;
#11134=CARTESIAN_POINT ( 'NONE',  ( 1.833485406944043827, -117.7091014914955309, 84.86072343962528919 ) ) ;
#11139=CARTESIAN_POINT ( 'NONE',  ( 5.340103556456273104, 139.5040934094290606, 47.74933482044414745 ) ) ;
#11142=VERTEX_POINT ( 'NONE', #15434 ) ;
#11144=EDGE_CURVE ( 'NONE', #14537, #18454, #25337, .T. ) ;
#11145=ORIENTED_EDGE ( 'NONE', *, *, #15351, .T. ) ;
#11146=CARTESIAN_POINT ( 'NONE',  ( 25.70243777736190438, 103.4793210720854262, -45.26941207740190976 ) ) ;
#11148=VERTEX_POINT ( 'NONE', #9268 ) ;
#11150=EDGE_LOOP ( 'NONE', ( #18374, #27990, #8841, #12009 ) ) ;
#11151=ADVANCED_FACE ( 'NONE', ( #18028 ), #12455, .T. ) ;
#11152=CARTESIAN_POINT ( 'NONE',  ( 1.832998868059890096, -0.5339089137757804249, 145.1092030902949830 ) ) ;
#11154=CARTESIAN_POINT ( 'NONE',  ( 1.832998868059890096, 117.7096351258387870, 84.86110816369641441 ) ) ;
#11155=AXIS2_PLACEMENT_3D ( 'NONE', #23766, #8620, #4570 ) ;
#11156=ORIENTED_EDGE ( 'NONE', *, *, #27504, .T. ) ;
#11157=EDGE_CURVE ( 'NONE', #14392, #9282, #17402, .T. ) ;
#11158=FACE_OUTER_BOUND ( 'NONE', #16800, .T. ) ;
#11160=EDGE_LOOP ( 'NONE', ( #23035, #13810, #21084, #5575 ) ) ;
#11161=CARTESIAN_POINT ( 'NONE',  ( 109.1778270068192853, -0.008960903982060999459, 0.002542344697958557470 ) ) ;
#11163=CARTESIAN_POINT ( 'NONE',  ( 1.834118845439484335, -97.22976650547497002, 107.7186227765451321 ) ) ;
#11165=CARTESIAN_POINT ( 'NONE',  ( 8.186469829614047455, 84.95702201190542269, 122.8338389144547307 ) ) ;
#11168=CARTESIAN_POINT ( 'NONE',  ( 2.063896406836609909, -144.3268707900448646, 16.52087515463731648 ) ) ;
#11169=CARTESIAN_POINT ( 'NONE',  ( 109.1624594426973260, 0.01591840958352308891, -0.001206615835671232158 ) ) ;
#11170=CARTESIAN_POINT ( 'NONE',  ( 26.11404676487259024, -112.4785329405482912, 12.95861723607416671 ) ) ;
#11171=VECTOR ( 'NONE', #18508, 1000.000000000000000 ) ;
#11173=CARTESIAN_POINT ( 'NONE',  ( 5.340103579038173010, 17.70136536264663008, 146.3832392131351980 ) ) ;
#11180=LINE ( 'NONE', #94, #3371 ) ;
#11181=LINE ( 'NONE', #19957, #8665 ) ;
#11182=EDGE_CURVE ( 'NONE', #27431, #9334, #14436, .T. ) ;
#11183=ORIENTED_EDGE ( 'NONE', *, *, #3090, .T. ) ;
#11185=CARTESIAN_POINT ( 'NONE',  ( 1.833603222531958288, -97.42748212378351980, 107.5392551439151276 ) ) ;
#11186=ORIENTED_EDGE ( 'NONE', *, *, #18952, .F. ) ;
#11187=CARTESIAN_POINT ( 'NONE',  ( 28.37603512858451182, 33.74339723237929434, -109.6581134439363723 ) ) ;
#11188=VECTOR ( 'NONE', #2182, 1000.000000000000114 ) ;
#11189=LINE ( 'NONE', #9033, #22136 ) ;
#11190=ORIENTED_EDGE ( 'NONE', *, *, #2594, .F. ) ;
#11193=CARTESIAN_POINT ( 'NONE',  ( 25.70243777736189728, 46.60897284577303878, -102.8829101922925986 ) ) ;
#11194=CARTESIAN_POINT ( 'NONE',  ( 6.224689322667647851, 136.2818611715190400, 57.86870174583473414 ) ) ;
#11199=CARTESIAN_POINT ( 'NONE',  ( 2.430230287190592531, 144.8619874886006471, 13.76600171652691706 ) ) ;
#11204=ORIENTED_EDGE ( 'NONE', *, *, #11233, .T. ) ;
#11209=DIRECTION ( 'NONE',  ( 0.000000000000000000, 0.000000000000000000, 1.000000000000000000 ) ) ;
#11210=CARTESIAN_POINT ( 'NONE',  ( 25.64700659047695908, -91.21315746821477433, -66.55152787776225409 ) ) ;
#11211=ORIENTED_EDGE ( 'NONE', *, *, #3353, .F. ) ;
#11212=CARTESIAN_POINT ( 'NONE',  ( 30.59141879584272061, 115.2623358717303006, 14.83090566979459979 ) ) ;
#11213=CARTESIAN_POINT ( 'NONE',  ( 30.59141879584274193, 92.40465812955542901, 70.47510900703801440 ) ) ;
#11216=CARTESIAN_POINT ( 'NONE',  ( 2.430230287190572103, 86.70145658344814876, -116.8646894862403514 ) ) ;
#11218=ORIENTED_EDGE ( 'NONE', *, *, #20872, .T. ) ;
#11221=EDGE_CURVE ( 'NONE', #23477, #12482, #1282, .T. ) ;
#11224=EDGE_CURVE ( 'NONE', #17719, #6423, #2972, .T. ) ;
#11225=B_SPLINE_CURVE_WITH_KNOTS ( 'NONE', 3,
 ( #11453, #13898, #368, #517, #9153, #26982, #18070, #6865 ),
 .UNSPECIFIED., .F., .F.,
 ( 4, 2, 2, 4 ),
 ( 3.469446951953614189E-18, 0.0002429588503611264990, 0.0004859177007222495286, 0.0009718354014444822520 ),
 .UNSPECIFIED. ) ;
#11226=EDGE_LOOP ( 'NONE', ( #11116, #13184, #8641, #5801 ) ) ;
#11227=EDGE_LOOP ( 'NONE', ( #12596, #9576, #10792, #19534 ) ) ;
#11229=CARTESIAN_POINT ( 'NONE',  ( 10.93730112725990367, -145.2260730187398678, -42.00474393596407197 ) ) ;
#11231=EDGE_LOOP ( 'NONE', ( #19471, #18186, #919, #7902 ) ) ;
#11232=B_SPLINE_CURVE_WITH_KNOTS ( 'NONE', 3,
 ( #18814, #27877, #14059, #14345 ),
 .UNSPECIFIED., .F., .F.,
 ( 4, 4 ),
 ( 3.283912181224055105E-16, 0.01077107486149822199 ),
 .UNSPECIFIED. ) ;
#11233=EDGE_CURVE ( 'NONE', #5939, #10890, #3676, .T. ) ;
#11235=ORIENTED_EDGE ( 'NONE', *, *, #25756, .T. ) ;
#11236=CARTESIAN_POINT ( 'NONE',  ( 32.73300124599738581, 108.9684813982494092, -44.31599526637845798 ) ) ;
#11237=VERTEX_POINT ( 'NONE', #5669 ) ;
#11239=CARTESIAN_POINT ( 'NONE',  ( 25.64703792032469920, -46.06101937225536602, -103.0889146124069953 ) ) ;
#11240=CARTESIAN_POINT ( 'NONE',  ( 1.893872463202051826, -145.1467500857188213, -0.9528309182412637579 ) ) ;
#11241=DIRECTION ( 'NONE',  ( -0.5946245182733607137, 0.4045541647807432417, 0.6948076064830672749 ) ) ;
#11243=CARTESIAN_POINT ( 'NONE',  ( 25.64681081121879203, 66.70335573067988832, -91.10197563707880875 ) ) ;
#11245=CARTESIAN_POINT ( 'NONE',  ( 109.1721716018069657, 0.01254847260354827708, -0.01157047143379286505 ) ) ;
#11247=EDGE_CURVE ( 'NONE', #15244, #8760, #4693, .T. ) ;
#11249=CARTESIAN_POINT ( 'NONE',  ( 25.65782528836480481, -65.90345832277411375, -91.69136324939171345 ) ) ;
#11251=ADVANCED_FACE ( 'NONE', ( #22811 ), #27050, .F. ) ;
#11252=CARTESIAN_POINT ( 'NONE',  ( 109.1778270068192853, -0.004106684808170070998, -0.008360410075196058124 ) ) ;
#11254=ORIENTED_EDGE ( 'NONE', *, *, #4618, .T. ) ;
#11257=B_SPLINE_CURVE_WITH_KNOTS ( 'NONE', 3,
 ( #4052, #25804, #6507, #24079 ),
 .UNSPECIFIED., .F., .F.,
 ( 4, 4 ),
 ( 0.000000000000000000, 0.01077107196513816915 ),
 .UNSPECIFIED. ) ;
#11259=B_SPLINE_CURVE_WITH_KNOTS ( 'NONE', 3,
 ( #16128, #18583, #22922, #25359, #1446, #24929, #11958, #18271, #23064, #5632 ),
 .UNSPECIFIED., .F., .F.,
 ( 4, 3, 3, 4 ),
 ( 2.775557561562891351E-17, 0.0002669559177086170331, 0.0005339118354151071869, 0.001067817517169159479 ),
 .UNSPECIFIED. ) ;
#11260=B_SPLINE_CURVE_WITH_KNOTS ( 'NONE', 3,
 ( #24638, #15829, #22020, #8643, #17414, #26199, #15670 ),
 .UNSPECIFIED., .F., .F.,
 ( 4, 3, 4 ),
 ( 4.109830475680215708E-16, 0.02816610861753246833, 0.04000277880656254170 ),
 .UNSPECIFIED. ) ;
#11262=ORIENTED_EDGE ( 'NONE', *, *, #15143, .F. ) ;
#11263=CARTESIAN_POINT ( 'NONE',  ( 1.832998868059858122, 85.72499093308101692, 117.0819875546698512 ) ) ;
#11265=( BOUNDED_SURFACE ( )  B_SPLINE_SURFACE ( 3, 1, ( 
 ( #8548, #15287 ),
 ( #23694, #3945 ),
 ( #12713, #10570 ),
 ( #19337, #28113 ) ),
 .UNSPECIFIED., .F., .F., .F. ) 
 B_SPLINE_SURFACE_WITH_KNOTS ( ( 4, 4 ),
 ( 2, 2 ),
 ( 0.000000000000000000, 1.000000000000000000 ),
 ( 0.000000000000000000, 1.000000000000000000 ),
 .UNSPECIFIED. ) 
 GEOMETRIC_REPRESENTATION_ITEM ( )  RATIONAL_B_SPLINE_SURFACE ( (
 ( 1.000000000000000000, 1.000000000000000000),
 ( 0.6386103224230316178, 0.9954351624131538845),
 ( 0.6386103224230316178, 0.9954351624131538845),
 ( 1.000000000000000000, 1.000000000000000000) ) ) 
 REPRESENTATION_ITEM ( '' )  SURFACE ( )  );
#11266=CARTESIAN_POINT ( 'NONE',  ( 1.832998868059858122, -138.1720401012263721, -44.33343224355373735 ) ) ;
#11267=CARTESIAN_POINT ( 'NONE',  ( 109.1592201516379674, -0.002913740842108687636, -0.007302213399779916743 ) ) ;
#11268=CARTESIAN_POINT ( 'NONE',  ( 109.1586900883932856, 0.007002774699553638779, 0.001385221016527484091 ) ) ;
#11271=CARTESIAN_POINT ( 'NONE',  ( 16.75465622695658041, 4.637075857203486251, -142.1502242093125403 ) ) ;
#11272=CARTESIAN_POINT ( 'NONE',  ( 109.1721716018069515, -0.0002019688922686823762, 0.01706748904931388797 ) ) ;
#11275=DIRECTION ( 'NONE',  ( -1.000000000000000000, 0.000000000000000000, 0.000000000000000000 ) ) ;
#11276=ADVANCED_FACE ( 'NONE', ( #12554 ), #17302, .F. ) ;
#11277=ORIENTED_EDGE ( 'NONE', *, *, #12967, .F. ) ;
#11278=CARTESIAN_POINT ( 'NONE',  ( 26.11404676487257603, 112.7148551500681890, -10.71016160607451262 ) ) ;
#11280=CARTESIAN_POINT ( 'NONE',  ( 25.70243777736188662, -22.76560620136980617, -110.6300896395619162 ) ) ;
#11281=CARTESIAN_POINT ( 'NONE',  ( 24.01988960052065281, 80.44223964539966687, -103.4492499592074779 ) ) ;
#11282=CARTESIAN_POINT ( 'NONE',  ( 9.884929003653608603, 35.39789245780532667, -146.3148513795963481 ) ) ;
#11284=ORIENTED_EDGE ( 'NONE', *, *, #21718, .T. ) ;
#11285=CARTESIAN_POINT ( 'NONE',  ( 1.833603222531956289, -14.72553080638897249, -144.3605362014089906 ) ) ;
#11286=ORIENTED_EDGE ( 'NONE', *, *, #14854, .T. ) ;
#11287=CARTESIAN_POINT ( 'NONE',  ( 1.894214914920948845, -84.54370816135659084, 117.9869255019029879 ) ) ;
#11288=CARTESIAN_POINT ( 'NONE',  ( 1.833206308920066530, 0.7447049373431984254, -145.1075835660718099 ) ) ;
#11289=VERTEX_POINT ( 'NONE', #10548 ) ;
#11290=EDGE_LOOP ( 'NONE', ( #23789, #8491, #21055, #18175 ) ) ;
#11293=FACE_OUTER_BOUND ( 'NONE', #16738, .T. ) ;
#11296=( BOUNDED_SURFACE ( )  B_SPLINE_SURFACE ( 3, 1, ( 
 ( #1384, #8040 ),
 ( #23428, #7751 ),
 ( #25453, #20674 ),
 ( #6011, #3413 ) ),
 .UNSPECIFIED., .F., .F., .F. ) 
 B_SPLINE_SURFACE_WITH_KNOTS ( ( 4, 4 ),
 ( 2, 2 ),
 ( 0.000000000000000000, 1.000000000000000000 ),
 ( 0.000000000000000000, 1.000000000000000000 ),
 .UNSPECIFIED. ) 
 GEOMETRIC_REPRESENTATION_ITEM ( )  RATIONAL_B_SPLINE_SURFACE ( (
 ( 1.000000000000000000, 1.000000000000000000),
 ( 0.6386103224230302855, 0.9954351624131538845),
 ( 0.6386103224230302855, 0.9954351624131538845),
 ( 1.000000000000000000, 1.000000000000000000) ) ) 
 REPRESENTATION_ITEM ( '' )  SURFACE ( )  );
#11299=CARTESIAN_POINT ( 'NONE',  ( 1.833485406944057594, 30.69200235378934849, 141.8265699653868523 ) ) ;
#11300=EDGE_CURVE ( 'NONE', #10427, #9946, #14990, .T. ) ;
#11301=CARTESIAN_POINT ( 'NONE',  ( 1.833838850093465922, -72.55488452980776515, -125.6687394363104886 ) ) ;
#11302=EDGE_CURVE ( 'NONE', #9049, #8004, #16140, .T. ) ;
#11303=B_SPLINE_CURVE_WITH_KNOTS ( 'NONE', 3,
 ( #9377, #13813, #3171, #5182, #15973, #11949, #5471, #22621, #7655, #862 ),
 .UNSPECIFIED., .F., .F.,
 ( 4, 3, 3, 4 ),
 ( 6.938893903907228378E-18, 0.0002669560319015572389, 0.0005492286108966272506, 0.0008315040496093409946 ),
 .UNSPECIFIED. ) ;
#11304=CARTESIAN_POINT ( 'NONE',  ( 9.884929003653608603, -144.4113244745774693, 42.50195158090983938 ) ) ;
#11305=DIRECTION ( 'NONE',  ( -1.000000000000000000, -0.000000000000000000, -0.000000000000000000 ) ) ;
#11307=VERTEX_POINT ( 'NONE', #5955 ) ;
#11308=CARTESIAN_POINT ( 'NONE',  ( 1.834118845439484335, -145.1099497418795750, 0.1779704863065216525 ) ) ;
#11309=CARTESIAN_POINT ( 'NONE',  ( 28.37603512858450117, -33.74339723237861932, 109.6581134439366281 ) ) ;
#11310=CARTESIAN_POINT ( 'NONE',  ( 2.108985857320909929, -31.46042399111138010, -141.8463279126004295 ) ) ;
#11312=CARTESIAN_POINT ( 'NONE',  ( 2.433796855181233454, -125.2830755159759519, 74.00833731765517598 ) ) ;
#11313=EDGE_CURVE ( 'NONE', #238, #5932, #19135, .T. ) ;
#11314=CARTESIAN_POINT ( 'NONE',  ( 109.1592201516379674, -0.006536841731962029015, -0.004368284148525239038 ) ) ;
#11316=CARTESIAN_POINT ( 'NONE',  ( 10.93730112725977932, -108.9902118373748863, 104.7670965581006755 ) ) ;
#11318=CARTESIAN_POINT ( 'NONE',  ( 1.832998868059858122, -117.7096351258393270, 84.86110816369566123 ) ) ;
#11319=ORIENTED_EDGE ( 'NONE', *, *, #11684, .T. ) ;
#11322=CARTESIAN_POINT ( 'NONE',  ( 1.833206310202323719, -59.70089235435347064, -132.2594754479310950 ) ) ;
#11323=B_SPLINE_CURVE_WITH_KNOTS ( 'NONE', 3,
 ( #1673, #10207, #3700, #16672 ),
 .UNSPECIFIED., .F., .F.,
 ( 4, 4 ),
 ( 3.798054144356080256E-16, 0.01077107486149828271 ),
 .UNSPECIFIED. ) ;
#11324=ORIENTED_EDGE ( 'NONE', *, *, #21129, .F. ) ;
#11325=CARTESIAN_POINT ( 'NONE',  ( 2.430230287190572103, 84.35270093935255886, 118.5711603495684443 ) ) ;
#11327=LINE ( 'NONE', #7411, #27610 ) ;
#11328=CARTESIAN_POINT ( 'NONE',  ( 30.59141879584313628, 2.701465575441479139, -116.1811685142591557 ) ) ;
#11329=EDGE_LOOP ( 'NONE', ( #20919, #15028, #25000, #19712 ) ) ;
#11334=CARTESIAN_POINT ( 'NONE',  ( 25.98552792386799126, -113.1317367103340388, 1.078856412010440247 ) ) ;
#11335=EDGE_CURVE ( 'NONE', #6178, #213, #28037, .T. ) ;
#11337=CARTESIAN_POINT ( 'NONE',  ( 25.64692232868534560, 0.3267662677151492723, 112.9106972861223426 ) ) ;
#11341=EDGE_CURVE ( 'NONE', #27159, #9343, #20134, .T. ) ;
#11342=ORIENTED_EDGE ( 'NONE', *, *, #13844, .T. ) ;
#11346=CARTESIAN_POINT ( 'NONE',  ( 25.64708010899964918, 75.59303792846624503, 83.87281825978644179 ) ) ;
#11348=DIRECTION ( 'NONE',  ( 0.000000000000000000, 0.000000000000000000, -1.000000000000000000 ) ) ;
#11349=LINE ( 'NONE', #26320, #5589 ) ;
#11351=ORIENTED_EDGE ( 'NONE', *, *, #18310, .F. ) ;
#11352=CARTESIAN_POINT ( 'NONE',  ( 25.70243777736187951, -34.20488708978023595, -107.6443926015133457 ) ) ;
#11354=CARTESIAN_POINT ( 'NONE',  ( 25.64708010899965629, 11.85684669924970969, 112.2870082086266876 ) ) ;
#11355=CARTESIAN_POINT ( 'NONE',  ( 25.64670758986456889, -75.18147256661998767, -84.24158725144702942 ) ) ;
#11356=ORIENTED_EDGE ( 'NONE', *, *, #14655, .T. ) ;
#11358=CARTESIAN_POINT ( 'NONE',  ( 1.834118845439484335, 44.67218053242396536, 138.0627591860431380 ) ) ;
#11359=CARTESIAN_POINT ( 'NONE',  ( 1.833206310202330602, -142.0914673790818483, -29.44113265021077197 ) ) ;
#11360=ORIENTED_EDGE ( 'NONE', *, *, #7896, .F. ) ;
#11361=B_SPLINE_CURVE_WITH_KNOTS ( 'NONE', 3,
 ( #21202, #1482, #10292, #2421, #703, #4878, #20129, #15657 ),
 .UNSPECIFIED., .F., .F.,
 ( 4, 2, 2, 4 ),
 ( 6.938893903907228378E-18, 0.0002429588503611281253, 0.0004859177007222493117, 0.0009718354014444792162 ),
 .UNSPECIFIED. ) ;
#11362=ORIENTED_EDGE ( 'NONE', *, *, #24563, .F. ) ;
#11363=B_SPLINE_CURVE_WITH_KNOTS ( 'NONE', 3,
 ( #14361, #1818, #5889, #14646, #16952, #3988, #23448, #25880, #14924, #6179 ),
 .UNSPECIFIED., .F., .F.,
 ( 4, 3, 3, 4 ),
 ( 1.040834085586084257E-17, 0.0002669560319015712793, 0.0005492286108966347316, 0.0008315040496093422957 ),
 .UNSPECIFIED. ) ;
#11365=CARTESIAN_POINT ( 'NONE',  ( 55.79472521941428198, 53.57698701322279788, -49.22042574086372468 ) ) ;
#11369=CARTESIAN_POINT ( 'NONE',  ( 25.86096068574578766, 67.25583614083966211, -90.87263912324351622 ) ) ;
#11371=DIRECTION ( 'NONE',  ( -0.5914120900931443270, -0.4804373588864723210, -0.6476200150380233556 ) ) ;
#11372=VERTEX_POINT ( 'NONE', #22751 ) ;
#11374=EDGE_CURVE ( 'NONE', #21438, #378, #13937, .T. ) ;
#11377=CARTESIAN_POINT ( 'NONE',  ( 2.108393763691207123, 13.91282116576980421, 144.6252321290181442 ) ) ;
#11378=CARTESIAN_POINT ( 'NONE',  ( 2.430230287190589422, -142.0258656395023991, 31.67257033707456770 ) ) ;
#11380=CARTESIAN_POINT ( 'NONE',  ( 10.93730112725971360, 26.59437931460756488, 148.8212007290661916 ) ) ;
#11382=CARTESIAN_POINT ( 'NONE',  ( 2.433796855181205476, 86.69855925934130880, -116.8607839509047892 ) ) ;
#11385=CARTESIAN_POINT ( 'NONE',  ( 25.64681081121879203, -66.03065707438999254, 91.59071981940550700 ) ) ;
#11389=ORIENTED_EDGE ( 'NONE', *, *, #12539, .T. ) ;
#11390=CARTESIAN_POINT ( 'NONE',  ( 25.81918753295378721, 24.41190151229255534, 110.3582118788977766 ) ) ;
#11391=CARTESIAN_POINT ( 'NONE',  ( 109.1586059443104944, 0.005438258427231131183, 0.004524147648825582735 ) ) ;
#11394=ORIENTED_EDGE ( 'NONE', *, *, #15584, .F. ) ;
#11395=ORIENTED_EDGE ( 'NONE', *, *, #26036, .F. ) ;
#11396=CARTESIAN_POINT ( 'NONE',  ( 26.11404676487257603, 83.38016054979783576, 76.59696442953219275 ) ) ;
#11397=CARTESIAN_POINT ( 'NONE',  ( 25.64681081121879203, -110.5293738517610080, 23.06870491922286348 ) ) ;
#11400=EDGE_CURVE ( 'NONE', #19738, #24861, #16365, .T. ) ;
#11405=DIRECTION ( 'NONE',  ( 0.000000000000000000, 0.000000000000000000, 1.000000000000000000 ) ) ;
#11407=CARTESIAN_POINT ( 'NONE',  ( 1.833206310202334821, -132.8652722326994535, -58.34025049825082476 ) ) ;
#11408=CARTESIAN_POINT ( 'NONE',  ( 1.832998868059858122, -117.7096351258382043, -84.86110816369723864 ) ) ;
#11409=VECTOR ( 'NONE', #22122, 1000.000000000000000 ) ;
#11410=CARTESIAN_POINT ( 'NONE',  ( 28.43349137099831836, 116.8557575815934655, -42.22940898499091844 ) ) ;
#11413=CARTESIAN_POINT ( 'NONE',  ( 1.833809397773815686, -117.5007887865414489, 85.14934054436442068 ) ) ;
#11414=ORIENTED_EDGE ( 'NONE', *, *, #7633, .F. ) ;
#11417=CARTESIAN_POINT ( 'NONE',  ( 8.186469777910582835, 113.2805152945354195, 97.33125097303739892 ) ) ;
#11418=CARTESIAN_POINT ( 'NONE',  ( 25.64700659047694842, 45.71714758798376010, 103.2418925369174758 ) ) ;
#11419=CARTESIAN_POINT ( 'NONE',  ( 26.11404676487257603, 98.61392875273440950, -55.62948129436141897 ) ) ;
#11420=FACE_OUTER_BOUND ( 'NONE', #9279, .T. ) ;
#11421=DIRECTION ( 'NONE',  ( 0.5914120900931444380, -0.6045864222316781333, 0.5335794202785162366 ) ) ;
#11422=VERTEX_POINT ( 'NONE', #20420 ) ;
#11423=CARTESIAN_POINT ( 'NONE',  ( 10.93730112725971360, 36.23586118136525158, 146.7718404940643211 ) ) ;
#11425=CARTESIAN_POINT ( 'NONE',  ( 25.98107933586711482, 103.7920584735901599, -45.01656174308481440 ) ) ;
#11426=CARTESIAN_POINT ( 'NONE',  ( 25.69398547355842766, 12.54367966928045064, 112.2438548322122926 ) ) ;
#11427=ORIENTED_EDGE ( 'NONE', *, *, #14912, .F. ) ;
#11431=CARTESIAN_POINT ( 'NONE',  ( 26.11404676487257603, -97.48350837663569735, -57.58742681967552102 ) ) ;
#11432=ORIENTED_EDGE ( 'NONE', *, *, #25822, .F. ) ;
#11434=CARTESIAN_POINT ( 'NONE',  ( 5.340103579038268933, 13.12023871299920330, -146.8647350263016733 ) ) ;
#11435=EDGE_CURVE ( 'NONE', #7273, #21979, #27692, .T. ) ;
#11436=ADVANCED_FACE ( 'NONE', ( #4340 ), #12359, .F. ) ;
#11437=CARTESIAN_POINT ( 'NONE',  ( 109.1586900883932856, -0.002810909342002450555, 0.006561743627145253353 ) ) ;
#11438=EDGE_CURVE ( 'NONE', #17576, #11749, #7334, .T. ) ;
#11441=CARTESIAN_POINT ( 'NONE',  ( 109.1586900883932856, 0.003656351050324883108, -0.006130969560693678121 ) ) ;
#11442=CARTESIAN_POINT ( 'NONE',  ( 2.433796855181233454, -98.43889364293788447, -107.1581411821795626 ) ) ;
#11443=FACE_OUTER_BOUND ( 'NONE', #7876, .T. ) ;
#11444=CARTESIAN_POINT ( 'NONE',  ( 25.87036335909427009, -33.99475147239086681, 107.8283083010002912 ) ) ;
#11446=LINE ( 'NONE', #18336, #75 ) ;
#11448=B_SPLINE_CURVE_WITH_KNOTS ( 'NONE', 3,
 ( #23028, #3712, #3149, #18551, #25613, #16684, #11929, #7480 ),
 .UNSPECIFIED., .F., .F.,
 ( 4, 2, 2, 4 ),
 ( 0.000000000000000000, 0.0002429588503611160636, 0.0004859177007222321271, 0.0009718354014444642542 ),
 .UNSPECIFIED. ) ;
#11449=CARTESIAN_POINT ( 'NONE',  ( 26.28373643307402219, -122.5382646256987158, -35.44121223574987312 ) ) ;
#11452=CARTESIAN_POINT ( 'NONE',  ( 10.93730112725994097, -51.37919228020192008, -142.1801301103790536 ) ) ;
#11453=CARTESIAN_POINT ( 'NONE',  ( 25.64681081121879203, 110.5293738517611501, -23.06870491922213873 ) ) ;
#11454=CARTESIAN_POINT ( 'NONE',  ( 28.43349137099851021, 76.27296957774109387, 98.08682467580786124 ) ) ;
#11455=ORIENTED_EDGE ( 'NONE', *, *, #20041, .T. ) ;
#11456=CARTESIAN_POINT ( 'NONE',  ( 32.73300124599732186, 0.000000000000000000, 0.000000000000000000 ) ) ;
#11457=ORIENTED_EDGE ( 'NONE', *, *, #22501, .F. ) ;
#11458=CARTESIAN_POINT ( 'NONE',  ( 28.43349137099828638, -123.0821667346708068, 17.01091693849698672 ) ) ;
#11459=( BOUNDED_SURFACE ( )  B_SPLINE_SURFACE ( 3, 1, ( 
 ( #7474, #23175 ),
 ( #8055, #25737 ),
 ( #23307, #16525 ),
 ( #12618, #27311 ) ),
 .UNSPECIFIED., .F., .F., .F. ) 
 B_SPLINE_SURFACE_WITH_KNOTS ( ( 4, 4 ),
 ( 2, 2 ),
 ( 0.000000000000000000, 1.000000000000000000 ),
 ( 0.000000000000000000, 1.000000000000000000 ),
 .UNSPECIFIED. ) 
 GEOMETRIC_REPRESENTATION_ITEM ( )  RATIONAL_B_SPLINE_SURFACE ( (
 ( 1.000000000000000000, 1.000000000000000000),
 ( 0.9956975270656954757, 0.8568959468854893125),
 ( 0.9956975270656954757, 0.8568959468854893125),
 ( 1.000000000000000000, 1.000000000000000000) ) ) 
 REPRESENTATION_ITEM ( '' )  SURFACE ( )  );
#11461=CARTESIAN_POINT ( 'NONE',  ( 1.833691583653564328, -97.36155720551542458, 107.5990239011822922 ) ) ;
#11463=CARTESIAN_POINT ( 'NONE',  ( 25.64708010899966339, -112.9112661935489683, 0.05470523945829951218 ) ) ;
#11464=ADVANCED_FACE ( 'NONE', ( #6513 ), #15274, .F. ) ;
#11465=ORIENTED_EDGE ( 'NONE', *, *, #6145, .T. ) ;
#11466=CARTESIAN_POINT ( 'NONE',  ( 9.884929003653608603, -119.2676479132367433, -91.84919534722065748 ) ) ;
#11467=ORIENTED_EDGE ( 'NONE', *, *, #20635, .T. ) ;
#11469=CARTESIAN_POINT ( 'NONE',  ( 28.37644542392837010, -109.6517504963493650, 58.62516076110009777 ) ) ;
#11470=CARTESIAN_POINT ( 'NONE',  ( 25.64681081121879203, 107.2555980796245905, -35.28660243342437752 ) ) ;
#11471=CARTESIAN_POINT ( 'NONE',  ( 32.73300124599738581, -115.8010721414081985, -20.69176323058746902 ) ) ;
#11472=CARTESIAN_POINT ( 'NONE',  ( 26.04756280548353686, -113.1727782765313890, 1.110889087302109113 ) ) ;
#11473=ORIENTED_EDGE ( 'NONE', *, *, #26871, .F. ) ;
#11474=CARTESIAN_POINT ( 'NONE',  ( 10.93730112725932635, 0.000000000000000000, 0.000000000000000000 ) ) ;
#11475=CARTESIAN_POINT ( 'NONE',  ( 2.433796855181233454, -96.28145139437756939, 109.1007109081222666 ) ) ;
#11477=ORIENTED_EDGE ( 'NONE', *, *, #13997, .F. ) ;
#11479=DIRECTION ( 'NONE',  ( 0.5914120900931444380, 0.008020494143001851220, -0.8063295922669342364 ) ) ;
#11481=CARTESIAN_POINT ( 'NONE',  ( 25.64700659047696973, 75.38309044531882819, 84.06149911284467180 ) ) ;
#11482=CARTESIAN_POINT ( 'NONE',  ( 2.433796855181205476, -96.28145139437610567, -109.1007109081235882 ) ) ;
#11486=CARTESIAN_POINT ( 'NONE',  ( 109.1592201516379674, -0.007780772729118872952, -0.001127733110579658832 ) ) ;
#11487=CARTESIAN_POINT ( 'NONE',  ( 2.430230287190581429, 43.58368230469393723, 138.8342928068221624 ) ) ;
#11488=CARTESIAN_POINT ( 'NONE',  ( 2.108393763691185807, -57.92353377304199569, -133.2474712570800364 ) ) ;
#11490=LINE ( 'NONE', #4588, #20164 ) ;
#11491=AXIS2_PLACEMENT_3D ( 'NONE', #5059, #11696, #3198 ) ;
#11492=ORIENTED_EDGE ( 'NONE', *, *, #26407, .F. ) ;
#11493=CARTESIAN_POINT ( 'NONE',  ( 9.884929003653626367, -35.39789245780224292, -146.3148513795970587 ) ) ;
#11494=EDGE_CURVE ( 'NONE', #6343, #17039, #16596, .T. ) ;
#11497=CARTESIAN_POINT ( 'NONE',  ( 1.833485406944043827, 144.2578170162062747, 15.69895494453433393 ) ) ;
#11499=EDGE_CURVE ( 'NONE', #13959, #27119, #17734, .T. ) ;
#11500=B_SPLINE_CURVE_WITH_KNOTS ( 'NONE', 3,
 ( #8300, #17628, #17069, #6157, #15036, #26412, #25994, #12603 ),
 .UNSPECIFIED., .F., .F.,
 ( 4, 2, 2, 4 ),
 ( 3.469446951953614189E-18, 0.0002429592666046667042, 0.0004859185332093299389, 0.0009718370664186788514 ),
 .UNSPECIFIED. ) ;
#11501=ORIENTED_EDGE ( 'NONE', *, *, #26774, .T. ) ;
#11507=CARTESIAN_POINT ( 'NONE',  ( 119.2224693531408803, 90.00000000000005684, 19.99999999999997513 ) ) ;
#11509=B_SPLINE_CURVE_WITH_KNOTS ( 'NONE', 3,
 ( #20558, #23026, #13787, #5445, #26887, #9488, #18242 ),
 .UNSPECIFIED., .F., .F.,
 ( 4, 3, 4 ),
 ( 0.000000000000000000, 0.02398743853561337985, 0.04000277880656215312 ),
 .UNSPECIFIED. ) ;
#11510=CARTESIAN_POINT ( 'NONE',  ( 10.93730112725932635, 0.000000000000000000, 0.000000000000000000 ) ) ;
#11513=CARTESIAN_POINT ( 'NONE',  ( 25.73574536432412074, 67.05280231777622646, -90.91878692681962093 ) ) ;
#11516=CARTESIAN_POINT ( 'NONE',  ( 2.433796855181205476, -142.6247129145649808, 28.83182736670489987 ) ) ;
#11519=ORIENTED_EDGE ( 'NONE', *, *, #6490, .T. ) ;
#11521=CARTESIAN_POINT ( 'NONE',  ( 1.893872463202068923, 14.22435552398011005, 144.4512189534318054 ) ) ;
#11523=CARTESIAN_POINT ( 'NONE',  ( 109.1592201516379674, -0.007051465909551689858, -0.003476928926125464302 ) ) ;
#11524=CARTESIAN_POINT ( 'NONE',  ( 26.28373643307409679, -67.34887744616709426, -108.3320567927997047 ) ) ;
#11526=CARTESIAN_POINT ( 'NONE',  ( 1.833838850093451933, 15.16810397409781253, 144.3148362521193064 ) ) ;
#11527=FACE_OUTER_BOUND ( 'NONE', #11227, .T. ) ;
#11528=CARTESIAN_POINT ( 'NONE',  ( 109.1778270068192853, -0.0006237116683805482738, -0.009293669915253103403 ) ) ;
#11529=ORIENTED_EDGE ( 'NONE', *, *, #8098, .F. ) ;
#11532=CARTESIAN_POINT ( 'NONE',  ( 109.1586900883932856, 0.006479576224403787998, 0.002995460350180830216 ) ) ;
#11533=ORIENTED_EDGE ( 'NONE', *, *, #18488, .F. ) ;
#11534=ADVANCED_FACE ( 'NONE', ( #9929 ), #10367, .F. ) ;
#11535=AXIS2_PLACEMENT_3D ( 'NONE', #28008, #14911, #21105 ) ;
#11536=VERTEX_POINT ( 'NONE', #10360 ) ;
#11541=EDGE_CURVE ( 'NONE', #26952, #15878, #21277, .T. ) ;
#11542=FACE_OUTER_BOUND ( 'NONE', #15451, .T. ) ;
#11543=B_SPLINE_CURVE_WITH_KNOTS ( 'NONE', 3,
 ( #6541, #10445, #23700, #3951 ),
 .UNSPECIFIED., .F., .F.,
 ( 4, 4 ),
 ( 3.419165934695819025E-16, 0.01077107486149840761 ),
 .UNSPECIFIED. ) ;
#11545=( BOUNDED_SURFACE ( )  B_SPLINE_SURFACE ( 3, 1, ( 
 ( #27316, #2713 ),
 ( #16093, #7629 ),
 ( #16383, #9191 ),
 ( #11486, #2862 ) ),
 .UNSPECIFIED., .F., .F., .F. ) 
 B_SPLINE_SURFACE_WITH_KNOTS ( ( 4, 4 ),
 ( 2, 2 ),
 ( 0.000000000000000000, 1.000000000000000000 ),
 ( 0.000000000000000000, 1.000000000000000000 ),
 .UNSPECIFIED. ) 
 GEOMETRIC_REPRESENTATION_ITEM ( )  RATIONAL_B_SPLINE_SURFACE ( (
 ( 1.000000000000000000, 1.000000000000000000),
 ( 0.6386103224230316178, 0.9954351624131538845),
 ( 0.6386103224230316178, 0.9954351624131538845),
 ( 1.000000000000000000, 1.000000000000000000) ) ) 
 REPRESENTATION_ITEM ( '' )  SURFACE ( )  );
#11547=DIRECTION ( 'NONE',  ( 0.000000000000000000, 0.000000000000000000, 1.000000000000000000 ) ) ;
#11550=AXIS2_PLACEMENT_3D ( 'NONE', #12086, #11653, #1144 ) ;
#11551=CARTESIAN_POINT ( 'NONE',  ( 16.75465622695641343, -48.33695624543422298, 133.7599617830026943 ) ) ;
#11557=ORIENTED_EDGE ( 'NONE', *, *, #555, .T. ) ;
#11562=CARTESIAN_POINT ( 'NONE',  ( 30.59141879584279167, 66.10404588653790370, 95.58042137919471770 ) ) ;
#11565=CARTESIAN_POINT ( 'NONE',  ( 13.36082413113063083, 152.7944199136427414, -6.345145185218573403 ) ) ;
#11568=CARTESIAN_POINT ( 'NONE',  ( 26.04756280548354397, 12.93458011762476012, 112.4366864265127930 ) ) ;
#11569=ORIENTED_EDGE ( 'NONE', *, *, #3997, .T. ) ;
#11570=EDGE_CURVE ( 'NONE', #14056, #19926, #13605, .T. ) ;
#11572=ORIENTED_EDGE ( 'NONE', *, *, #13183, .F. ) ;
#11574=EDGE_CURVE ( 'NONE', #24022, #15878, #5048, .T. ) ;
#11575=ADVANCED_FACE ( 'NONE', ( #13051 ), #19169, .F. ) ;
#11579=DIRECTION ( 'NONE',  ( -1.000000000000000000, -0.000000000000000000, -0.000000000000000000 ) ) ;
#11581=DIRECTION ( 'NONE',  ( 0.000000000000000000, 0.000000000000000000, 1.000000000000000000 ) ) ;
#11582=( BOUNDED_SURFACE ( )  B_SPLINE_SURFACE ( 3, 1, ( 
 ( #13780, #20971 ),
 ( #16375, #16522 ),
 ( #16232, #25169 ),
 ( #20842, #20687 ) ),
 .UNSPECIFIED., .F., .F., .F. ) 
 B_SPLINE_SURFACE_WITH_KNOTS ( ( 4, 4 ),
 ( 2, 2 ),
 ( 0.000000000000000000, 1.000000000000000000 ),
 ( 0.000000000000000000, 1.000000000000000000 ),
 .UNSPECIFIED. ) 
 GEOMETRIC_REPRESENTATION_ITEM ( )  RATIONAL_B_SPLINE_SURFACE ( (
 ( 1.000000000000000000, 1.000000000000000000),
 ( 0.6386103224230316178, 0.9954351624131538845),
 ( 0.6386103224230316178, 0.9954351624131538845),
 ( 1.000000000000000000, 1.000000000000000000) ) ) 
 REPRESENTATION_ITEM ( '' )  SURFACE ( )  );
#11583=CARTESIAN_POINT ( 'NONE',  ( 1.832998868059890096, -96.70023740551195601, 108.1944082009154187 ) ) ;
#11585=B_SPLINE_CURVE_WITH_KNOTS ( 'NONE', 3,
 ( #10144, #6112, #19318, #19467, #28236, #10977, #15411, #26220 ),
 .UNSPECIFIED., .F., .F.,
 ( 4, 2, 2, 4 ),
 ( 9.813077866773594792E-18, 0.0002429592666046790912, 0.0004859185332093483704, 0.0009718370664186869829 ),
 .UNSPECIFIED. ) ;
#11588=CARTESIAN_POINT ( 'NONE',  ( 10.93730112725977932, -104.7670965581018123, 108.9902118373738062 ) ) ;
#11589=VERTEX_POINT ( 'NONE', #19531 ) ;
#11590=CARTESIAN_POINT ( 'NONE',  ( 109.1586059443104944, 0.007058870754606109445, -0.0004635842312890220179 ) ) ;
#11592=CARTESIAN_POINT ( 'NONE',  ( 25.73574536432417759, 45.21157800100309032, 103.5288236655397185 ) ) ;
#11593=CARTESIAN_POINT ( 'NONE',  ( 25.98107933586712903, -84.80123094405263373, 74.88680433646213430 ) ) ;
#11594=CARTESIAN_POINT ( 'NONE',  ( 1.833206310202332379, 85.89457578512813996, 116.9567751109822069 ) ) ;
#11595=ORIENTED_EDGE ( 'NONE', *, *, #11499, .T. ) ;
#11596=CIRCLE ( 'NONE', #26301, 117.6351876552689504 ) ;
#11597=( BOUNDED_SURFACE ( )  B_SPLINE_SURFACE ( 3, 1, ( 
 ( #2005, #15234 ),
 ( #10521, #21876 ),
 ( #15377, #22008 ),
 ( #10938, #16989 ) ),
 .UNSPECIFIED., .F., .F., .F. ) 
 B_SPLINE_SURFACE_WITH_KNOTS ( ( 4, 4 ),
 ( 2, 2 ),
 ( 0.000000000000000000, 1.000000000000000000 ),
 ( 0.000000000000000000, 1.000000000000000000 ),
 .UNSPECIFIED. ) 
 GEOMETRIC_REPRESENTATION_ITEM ( )  RATIONAL_B_SPLINE_SURFACE ( (
 ( 1.000000000000000000, 1.000000000000000000),
 ( 0.6386103224230302855, 0.9954351624131538845),
 ( 0.6386103224230302855, 0.9954351624131538845),
 ( 1.000000000000000000, 1.000000000000000000) ) ) 
 REPRESENTATION_ITEM ( '' )  SURFACE ( )  );
#11598=ADVANCED_FACE ( 'NONE', ( #1964 ), #19388, .T. ) ;
#11599=VERTEX_POINT ( 'NONE', #25883 ) ;
#11600=CARTESIAN_POINT ( 'NONE',  ( 1.831572820252008738, 126.1609924456739975, -71.69925593429677235 ) ) ;
#11602=CARTESIAN_POINT ( 'NONE',  ( 16.75465622695654133, -53.58152542127593421, -131.7467602971414919 ) ) ;
#11604=ORIENTED_EDGE ( 'NONE', *, *, #13757, .T. ) ;
#11605=CARTESIAN_POINT ( 'NONE',  ( 10.93730112726003156, 84.82621002473607064, -125.1380233598471960 ) ) ;
#11607=VERTEX_POINT ( 'NONE', #6180 ) ;
#11609=B_SPLINE_CURVE_WITH_KNOTS ( 'NONE', 3,
 ( #13085, #10252, #19014, #22151, #2266, #20122, #22300, #11210, #4438, #26738 ),
 .UNSPECIFIED., .F., .F.,
 ( 4, 3, 3, 4 ),
 ( 1.387778780781445676E-17, 0.0002669560319015615215, 0.0005492286108966200949, 0.0008315040496093287431 ),
 .UNSPECIFIED. ) ;
#11610=B_SPLINE_CURVE_WITH_KNOTS ( 'NONE', 3,
 ( #21276, #18835, #20982, #14511 ),
 .UNSPECIFIED., .F., .F.,
 ( 4, 4 ),
 ( 3.314527865495573890E-16, 0.01077107486149804158 ),
 .UNSPECIFIED. ) ;
#11615=CARTESIAN_POINT ( 'NONE',  ( 1.832998868059890096, 138.1720401012266848, 44.33343224355281365 ) ) ;
#11616=ORIENTED_EDGE ( 'NONE', *, *, #21968, .F. ) ;
#11618=VECTOR ( 'NONE', #23737, 1000.000000000000227 ) ;
#11621=CARTESIAN_POINT ( 'NONE',  ( 26.11404676487259024, 108.0249973236467582, 33.91085499298413453 ) ) ;
#11622=CARTESIAN_POINT ( 'NONE',  ( 1.833838850855463498, -125.7132320915354029, 72.47782099564605574 ) ) ;
#11624=CARTESIAN_POINT ( 'NONE',  ( 109.1624594426973118, 0.01318243916934995832, 0.009004164758064592267 ) ) ;
#11625=CARTESIAN_POINT ( 'NONE',  ( 25.81918753295378011, 34.03777907512061773, -107.7789657594971402 ) ) ;
#11626=CARTESIAN_POINT ( 'NONE',  ( 10.93730112725990011, -128.3908183996585990, -79.81734490846054086 ) ) ;
#11628=EDGE_CURVE ( 'NONE', #17548, #9151, #25675, .T. ) ;
#11629=ORIENTED_EDGE ( 'NONE', *, *, #12768, .T. ) ;
#11630=VERTEX_POINT ( 'NONE', #10769 ) ;
#11632=CARTESIAN_POINT ( 'NONE',  ( 55.79472521941426777, -59.28412330436329825, 42.17269936297619637 ) ) ;
#11637=CARTESIAN_POINT ( 'NONE',  ( 25.64681081121879203, -84.18689316040098447, 75.24277141833462679 ) ) ;
#11640=VERTEX_POINT ( 'NONE', #15339 ) ;
#11643=( BOUNDED_SURFACE ( )  B_SPLINE_SURFACE ( 3, 1, ( 
 ( #18413, #27191 ),
 ( #22769, #20439 ),
 ( #9512, #15837 ),
 ( #16116, #4898 ) ),
 .UNSPECIFIED., .F., .F., .F. ) 
 B_SPLINE_SURFACE_WITH_KNOTS ( ( 4, 4 ),
 ( 2, 2 ),
 ( 0.000000000000000000, 1.000000000000000000 ),
 ( 0.000000000000000000, 1.000000000000000000 ),
 .UNSPECIFIED. ) 
 GEOMETRIC_REPRESENTATION_ITEM ( )  RATIONAL_B_SPLINE_SURFACE ( (
 ( 1.000000000000000000, 1.000000000000000000),
 ( 0.9956975270656954757, 0.8568959468854893125),
 ( 0.9956975270656954757, 0.8568959468854893125),
 ( 1.000000000000000000, 1.000000000000000000) ) ) 
 REPRESENTATION_ITEM ( '' )  SURFACE ( )  );
#11645=ADVANCED_FACE ( 'NONE', ( #19254 ), #8165, .F. ) ;
#11646=CARTESIAN_POINT ( 'NONE',  ( 109.1586900883932856, 0.004701023939945712764, -0.005371970278528660422 ) ) ;
#11647=CARTESIAN_POINT ( 'NONE',  ( 1.833485406944057594, 142.0485807715645876, 29.64752363041592531 ) ) ;
#11649=CARTESIAN_POINT ( 'NONE',  ( 2.063896406836609909, -137.7380992975105301, 46.16709813092576553 ) ) ;
#11653=DIRECTION ( 'NONE',  ( 1.000000000000000000, -0.000000000000000000, -0.000000000000000000 ) ) ;
#11654=CARTESIAN_POINT ( 'NONE',  ( 109.1592201516379674, 0.006536841731953405704, -0.004368284148529032879 ) ) ;
#11655=ORIENTED_EDGE ( 'NONE', *, *, #6235, .T. ) ;
#11656=B_SPLINE_CURVE_WITH_KNOTS ( 'NONE', 3,
 ( #18894, #19037, #21036, #8522, #21332, #21472 ),
 .UNSPECIFIED., .F., .F.,
 ( 4, 2, 4 ),
 ( 1.110764993427085326E-17, 0.0006311636237756819466, 0.001262327247551352834 ),
 .UNSPECIFIED. ) ;
#11659=CARTESIAN_POINT ( 'NONE',  ( 109.1592201516379674, -0.007748443302134891582, -0.001331853079201365982 ) ) ;
#11661=CARTESIAN_POINT ( 'NONE',  ( 109.1586900883932856, 0.004277182003227222341, 0.005715190711481739176 ) ) ;
#11662=CARTESIAN_POINT ( 'NONE',  ( 16.75465622695645962, 19.47041796022427462, -140.8868039942615553 ) ) ;
#11664=CARTESIAN_POINT ( 'NONE',  ( 25.64692872815577473, -103.2799065540887256, 45.63107645358293496 ) ) ;
#11667=ORIENTED_EDGE ( 'NONE', *, *, #22307, .T. ) ;
#11668=ADVANCED_FACE ( 'NONE', ( #8467 ), #5031, .F. ) ;
#11669=ORIENTED_EDGE ( 'NONE', *, *, #13326, .F. ) ;
#11671=EDGE_CURVE ( 'NONE', #2917, #12674, #11225, .T. ) ;
#11672=CARTESIAN_POINT ( 'NONE',  ( 25.64699802086724389, -46.14225289916239348, -103.0525896353906319 ) ) ;
#11673=CARTESIAN_POINT ( 'NONE',  ( 109.1586059443104944, 0.007068659269322301146, 0.0002768082440195569175 ) ) ;
#11674=CARTESIAN_POINT ( 'NONE',  ( 2.430230287190592531, 144.5585181921888420, -16.65331920325590787 ) ) ;
#11676=B_SPLINE_CURVE_WITH_KNOTS ( 'NONE', 3,
 ( #8849, #17610, #6695, #10729, #4508, #13287 ),
 .UNSPECIFIED., .F., .F.,
 ( 4, 2, 4 ),
 ( 9.263427422397553349E-18, 0.0006311636237756821635, 0.001262327247551355220 ),
 .UNSPECIFIED. ) ;
#11680=EDGE_CURVE ( 'NONE', #7646, #10229, #13973, .T. ) ;
#11682=CARTESIAN_POINT ( 'NONE',  ( 6.224689322667630975, 146.9579047224769397, 18.02516478984192716 ) ) ;
#11684=EDGE_CURVE ( 'NONE', #16498, #12003, #23931, .T. ) ;
#11685=ORIENTED_EDGE ( 'NONE', *, *, #3257, .F. ) ;
#11686=ORIENTED_EDGE ( 'NONE', *, *, #492, .T. ) ;
#11687=FACE_OUTER_BOUND ( 'NONE', #18910, .T. ) ;
#11689=B_SPLINE_CURVE_WITH_KNOTS ( 'NONE', 3,
 ( #6110, #12833, #4345, #8535, #1757, #17433, #14714, #10553 ),
 .UNSPECIFIED., .F., .F.,
 ( 4, 2, 2, 4 ),
 ( 1.250926888277100303E-17, 0.0002429592666046839430, 0.0004859185332093553635, 0.0009718370664186946808 ),
 .UNSPECIFIED. ) ;
#11691=VERTEX_POINT ( 'NONE', #4975 ) ;
#11693=CARTESIAN_POINT ( 'NONE',  ( 26.11404676487257603, -113.2169081140373947, -1.130420376098323576 ) ) ;
#11694=B_SPLINE_CURVE_WITH_KNOTS ( 'NONE', 3,
 ( #17067, #3836, #24128, #17481, #17206, #1795, #26267 ),
 .UNSPECIFIED., .F., .F.,
 ( 4, 3, 4 ),
 ( 0.000000000000000000, 0.02398743853561358108, 0.04000277880656216700 ),
 .UNSPECIFIED. ) ;
#11696=DIRECTION ( 'NONE',  ( -1.000000000000000000, -0.000000000000000000, -0.000000000000000000 ) ) ;
#11698=PRODUCT_DEFINITION_CONTEXT ( 'detailed design', #28110, 'design' ) ;
#11699=CARTESIAN_POINT ( 'NONE',  ( 109.1587776205901861, 0.006661366261223553367, -0.003057017121600569438 ) ) ;
#11700=CARTESIAN_POINT ( 'NONE',  ( 25.64681081121879203, 107.2555980796241215, 35.28660243342585545 ) ) ;
#11702=CARTESIAN_POINT ( 'NONE',  ( 25.70243777736189728, -35.59945151684150488, 107.1912711514953713 ) ) ;
#11703=CARTESIAN_POINT ( 'NONE',  ( 25.73574536432413851, 112.9674920590232858, 0.8061344836373177669 ) ) ;
#11704=CARTESIAN_POINT ( 'NONE',  ( 28.43349137099834323, 4.052139611198435354, 124.1860347533534963 ) ) ;
#11707=CARTESIAN_POINT ( 'NONE',  ( 5.340103556456496925, -117.9209211572679976, -88.52145167812714988 ) ) ;
#11711=CARTESIAN_POINT ( 'NONE',  ( 26.11404676487259024, 76.59696442953192275, 83.38016054979810576 ) ) ;
#11713=CARTESIAN_POINT ( 'NONE',  ( 109.1721716018069657, -0.003746085893652680628, -0.01665253177026228618 ) ) ;
#11715=ORIENTED_EDGE ( 'NONE', *, *, #10538, .F. ) ;
#11716=LINE ( 'NONE', #7263, #3782 ) ;
#11717=ORIENTED_EDGE ( 'NONE', *, *, #19743, .F. ) ;
#11720=ORIENTED_EDGE ( 'NONE', *, *, #15901, .F. ) ;
#11721=ORIENTED_EDGE ( 'NONE', *, *, #18532, .F. ) ;
#11723=ORIENTED_EDGE ( 'NONE', *, *, #12677, .T. ) ;
#11724=B_SPLINE_CURVE_WITH_KNOTS ( 'NONE', 3,
 ( #2962, #22396, #9298, #24844, #26691, #4685, #15906, #22254 ),
 .UNSPECIFIED., .F., .F.,
 ( 4, 2, 2, 4 ),
 ( 6.938893903907228378E-18, 0.0002429588503611240595, 0.0004859177007222411802, 0.0009718354014444684826 ),
 .UNSPECIFIED. ) ;
#11726=CARTESIAN_POINT ( 'NONE',  ( 28.37644542392841984, -123.1691345231581494, -17.02293047611490096 ) ) ;
#11727=CARTESIAN_POINT ( 'NONE',  ( 109.1586900883932856, 0.005833932871487514972, -0.004113747441000937220 ) ) ;
#11730=DIRECTION ( 'NONE',  ( 0.000000000000000000, 0.000000000000000000, 1.000000000000000000 ) ) ;
#11731=CARTESIAN_POINT ( 'NONE',  ( 109.1586900883932856, -0.002995460350180851900, 0.006479576224403776723 ) ) ;
#11732=CARTESIAN_POINT ( 'NONE',  ( 5.340103556456367251, 84.79482753886546220, 120.6284720803327986 ) ) ;
#11733=ADVANCED_FACE ( 'NONE', ( #2976 ), #16840, .F. ) ;
#11734=DIRECTION ( 'NONE',  ( 0.5946245182733607137, 0.6977579871484563823, -0.3994439555666204344 ) ) ;
#11735=CARTESIAN_POINT ( 'NONE',  ( 1.833485406944043827, 84.86072343962567288, 117.7091014914953320 ) ) ;
#11736=CARTESIAN_POINT ( 'NONE',  ( 13.36082413113063083, -25.56125765253554860, 150.7747251079861428 ) ) ;
#11742=DIRECTION ( 'NONE',  ( -0.5914120900931443270, 0.07630783613001886068, -0.8027508043202528087 ) ) ;
#11743=CARTESIAN_POINT ( 'NONE',  ( 109.1587776205901577, -0.004842060007774085656, -0.005502145856754143277 ) ) ;
#11744=ADVANCED_FACE ( 'NONE', ( #23411 ), #14021, .F. ) ;
#11746=CARTESIAN_POINT ( 'NONE',  ( 1.832998868059890096, -45.34898734666140285, 137.8420662456168770 ) ) ;
#11747=CARTESIAN_POINT ( 'NONE',  ( 2.263178113027038307, 138.7064940342184514, -43.59477710889581914 ) ) ;
#11749=VERTEX_POINT ( 'NONE', #27279 ) ;
#11750=CARTESIAN_POINT ( 'NONE',  ( 30.58324630866347604, 120.8793175557613324, -3.944468862008090326 ) ) ;
#11751=CARTESIAN_POINT ( 'NONE',  ( 109.1592201516379674, 0.007856029051018016685, 0.0003082430541935266563 ) ) ;
#11752=CARTESIAN_POINT ( 'NONE',  ( 13.36082413113063083, -84.67697637120498655, 127.3428651193245287 ) ) ;
#11755=VERTEX_POINT ( 'NONE', #18940 ) ;
#11756=CARTESIAN_POINT ( 'NONE',  ( 32.73300124599732186, 0.000000000000000000, 0.000000000000000000 ) ) ;
#11757=B_SPLINE_CURVE_WITH_KNOTS ( 'NONE', 3,
 ( #28481, #6499, #20002, #13370 ),
 .UNSPECIFIED., .F., .F.,
 ( 4, 4 ),
 ( 3.511136132061045056E-16, 0.01077107486149755586 ),
 .UNSPECIFIED. ) ;
#11758=LINE ( 'NONE', #18512, #17948 ) ;
#11761=ADVANCED_FACE ( 'NONE', ( #14609 ), #14799, .F. ) ;
#11763=( BOUNDED_SURFACE ( )  B_SPLINE_SURFACE ( 3, 1, ( 
 ( #11875, #3655 ),
 ( #18775, #12164 ),
 ( #931, #3381 ),
 ( #14305, #20930 ) ),
 .UNSPECIFIED., .F., .F., .F. ) 
 B_SPLINE_SURFACE_WITH_KNOTS ( ( 4, 4 ),
 ( 2, 2 ),
 ( 0.000000000000000000, 1.000000000000000000 ),
 ( 0.000000000000000000, 1.000000000000000000 ),
 .UNSPECIFIED. ) 
 GEOMETRIC_REPRESENTATION_ITEM ( )  RATIONAL_B_SPLINE_SURFACE ( (
 ( 1.000000000000000000, 1.000000000000000000),
 ( 0.9956975270656954757, 0.8568959468854893125),
 ( 0.9956975270656954757, 0.8568959468854893125),
 ( 1.000000000000000000, 1.000000000000000000) ) ) 
 REPRESENTATION_ITEM ( '' )  SURFACE ( )  );
#11764=CARTESIAN_POINT ( 'NONE',  ( 8.186469777910781787, -71.65198614410293487, 131.0413692044509162 ) ) ;
#11766=ORIENTED_EDGE ( 'NONE', *, *, #290, .T. ) ;
#11769=LINE ( 'NONE', #13764, #6958 ) ;
#11772=DIRECTION ( 'NONE',  ( -1.000000000000000000, -0.000000000000000000, -0.000000000000000000 ) ) ;
#11773=EDGE_CURVE ( 'NONE', #21319, #2536, #6741, .T. ) ;
#11774=VERTEX_POINT ( 'NONE', #12037 ) ;
#11775=( BOUNDED_SURFACE ( )  B_SPLINE_SURFACE ( 3, 1, ( 
 ( #9889, #10328 ),
 ( #21087, #5996 ),
 ( #18653, #8287 ),
 ( #12312, #10035 ) ),
 .UNSPECIFIED., .F., .F., .F. ) 
 B_SPLINE_SURFACE_WITH_KNOTS ( ( 4, 4 ),
 ( 2, 2 ),
 ( 0.000000000000000000, 1.000000000000000000 ),
 ( 0.000000000000000000, 1.000000000000000000 ),
 .UNSPECIFIED. ) 
 GEOMETRIC_REPRESENTATION_ITEM ( )  RATIONAL_B_SPLINE_SURFACE ( (
 ( 1.000000000000000000, 1.000000000000000000),
 ( 0.9956975270656955868, 0.8568959468854907557),
 ( 0.9956975270656955868, 0.8568959468854907557),
 ( 1.000000000000000000, 1.000000000000000000) ) ) 
 REPRESENTATION_ITEM ( '' )  SURFACE ( )  );
#11777=CARTESIAN_POINT ( 'NONE',  ( 8.186469829614228644, -34.43598812953204202, 145.3272524103320222 ) ) ;
#11778=CARTESIAN_POINT ( 'NONE',  ( 1.833485406944043827, 72.09189602597706426, 125.9346397303438039 ) ) ;
#11779=CARTESIAN_POINT ( 'NONE',  ( 25.81918753295377300, 98.34688456803397116, 55.70247894228205610 ) ) ;
#11780=EDGE_LOOP ( 'NONE', ( #17183, #2688, #27864, #22916 ) ) ;
#11781=ORIENTED_EDGE ( 'NONE', *, *, #25291, .F. ) ;
#11782=ORIENTED_EDGE ( 'NONE', *, *, #20539, .T. ) ;
#11786=CARTESIAN_POINT ( 'NONE',  ( 109.1586900883932856, 0.005236795036860546551, -0.004851151255037378096 ) ) ;
#11787=CARTESIAN_POINT ( 'NONE',  ( 2.433796855181233454, 145.5024947199069913, -1.451562450950139249 ) ) ;
#11790=VERTEX_POINT ( 'NONE', #12177 ) ;
#11794=CARTESIAN_POINT ( 'NONE',  ( 109.1778270068192853, 0.009293669915260186279, 0.0006237116683871661354 ) ) ;
#11796=CARTESIAN_POINT ( 'NONE',  ( 25.87036335909425588, -84.67915015758804032, -74.91347493818344105 ) ) ;
#11797=CARTESIAN_POINT ( 'NONE',  ( 6.224689322667647851, -33.28770499679229999, -144.2687111683198964 ) ) ;
#11799=CARTESIAN_POINT ( 'NONE',  ( 109.1586900883932856, -0.003481399864218472865, 0.006231977675084978893 ) ) ;
#11802=EDGE_LOOP ( 'NONE', ( #17420, #22523, #19733, #4513 ) ) ;
#11804=CARTESIAN_POINT ( 'NONE',  ( 25.64692232868535626, -23.79507962493545747, -110.3753891203788982 ) ) ;
#11811=CARTESIAN_POINT ( 'NONE',  ( 26.28373643307403995, 108.3320567928000173, -67.34887744616673899 ) ) ;
#11812=CARTESIAN_POINT ( 'NONE',  ( 25.64699802086724745, -103.0525896353904898, 46.14225289916271322 ) ) ;
#11814=ORIENTED_EDGE ( 'NONE', *, *, #25016, .F. ) ;
#11815=( BOUNDED_SURFACE ( )  B_SPLINE_SURFACE ( 3, 1, ( 
 ( #11731, #7861 ),
 ( #2959, #27261 ),
 ( #5390, #18926 ),
 ( #22831, #13881 ) ),
 .UNSPECIFIED., .F., .F., .F. ) 
 B_SPLINE_SURFACE_WITH_KNOTS ( ( 4, 4 ),
 ( 2, 2 ),
 ( 0.000000000000000000, 1.000000000000000000 ),
 ( 0.000000000000000000, 1.000000000000000000 ),
 .UNSPECIFIED. ) 
 GEOMETRIC_REPRESENTATION_ITEM ( )  RATIONAL_B_SPLINE_SURFACE ( (
 ( 1.000000000000000000, 1.000000000000000000),
 ( 0.9956975270656955868, 0.8568959468854907557),
 ( 0.9956975270656955868, 0.8568959468854907557),
 ( 1.000000000000000000, 1.000000000000000000) ) ) 
 REPRESENTATION_ITEM ( '' )  SURFACE ( )  );
#11817=FACE_OUTER_BOUND ( 'NONE', #10925, .T. ) ;
#11820=CARTESIAN_POINT ( 'NONE',  ( 9.884929003653626367, 149.2134106160918634, -19.90991253123092974 ) ) ;
#11821=CARTESIAN_POINT ( 'NONE',  ( 32.73300124599737160, -113.0038235389604466, 32.68291970228198551 ) ) ;
#11822=PLANE ( 'NONE',  #26345 ) ;
#11823=CARTESIAN_POINT ( 'NONE',  ( 2.430230287190589422, 142.6294793592097960, 28.83279105684476207 ) ) ;
#11827=CARTESIAN_POINT ( 'NONE',  ( 25.70243777736189728, -65.79472741891204635, -91.80600962488466621 ) ) ;
#11828=CARTESIAN_POINT ( 'NONE',  ( 109.1778270068192853, 0.004958088776549099581, 0.007885345421917318992 ) ) ;
#11831=CARTESIAN_POINT ( 'NONE',  ( 21.16825799904903604, -112.1052598354960281, -75.99073816868427400 ) ) ;
#11832=ORIENTED_EDGE ( 'NONE', *, *, #27399, .F. ) ;
#11833=ORIENTED_EDGE ( 'NONE', *, *, #15361, .T. ) ;
#11836=CARTESIAN_POINT ( 'NONE',  ( 5.340103579038184556, 32.90561047415598495, 143.7310399932977987 ) ) ;
#11837=EDGE_CURVE ( 'NONE', #18454, #25074, #10524, .T. ) ;
#11838=CARTESIAN_POINT ( 'NONE',  ( 1.832998868059858122, -144.3700883710218363, 14.63705790013961305 ) ) ;
#11839=CARTESIAN_POINT ( 'NONE',  ( 5.340103579038260051, -140.9275371836308750, -43.36842539899515714 ) ) ;
#11840=ADVANCED_FACE ( 'NONE', ( #15301 ), #3732, .T. ) ;
#11842=CARTESIAN_POINT ( 'NONE',  ( 10.93730112726003156, 119.3442956573285443, -92.80059208661575099 ) ) ;
#11843=CARTESIAN_POINT ( 'NONE',  ( 25.65782528836482257, 112.9169519833626509, 0.5778133093781777641 ) ) ;
#11846=DIRECTION ( 'NONE',  ( -0.5914120900931443270, 0.7398809652418005811, 0.3206367055789464127 ) ) ;
#11847=CARTESIAN_POINT ( 'NONE',  ( 25.64670758986457955, -56.02376616805354814, -98.03181353150543487 ) ) ;
#11849=CARTESIAN_POINT ( 'NONE',  ( 13.36082413113061307, 150.7747251079865123, -25.56125765253303328 ) ) ;
#11850=CARTESIAN_POINT ( 'NONE',  ( 2.433796855181205476, -144.5536872373190818, -16.65276281464712582 ) ) ;
#11851=CARTESIAN_POINT ( 'NONE',  ( 25.64681081121879203, 45.54494737132223747, 103.3177883989780952 ) ) ;
#11853=CARTESIAN_POINT ( 'NONE',  ( 26.28373643307407548, -123.8418562193900812, 30.57614217577425464 ) ) ;
#11854=( BOUNDED_SURFACE ( )  B_SPLINE_SURFACE ( 3, 1, ( 
 ( #21784, #8541 ),
 ( #17305, #23953 ),
 ( #4212, #12994 ),
 ( #2045, #10848 ) ),
 .UNSPECIFIED., .F., .F., .F. ) 
 B_SPLINE_SURFACE_WITH_KNOTS ( ( 4, 4 ),
 ( 2, 2 ),
 ( 0.000000000000000000, 1.000000000000000000 ),
 ( 0.000000000000000000, 1.000000000000000000 ),
 .UNSPECIFIED. ) 
 GEOMETRIC_REPRESENTATION_ITEM ( )  RATIONAL_B_SPLINE_SURFACE ( (
 ( 1.000000000000000000, 1.000000000000000000),
 ( 0.9960225298536222738, 0.9999952330161893110),
 ( 0.9960225298536222738, 0.9999952330161893110),
 ( 1.000000000000000000, 1.000000000000000000) ) ) 
 REPRESENTATION_ITEM ( '' )  SURFACE ( )  );
#11856=CARTESIAN_POINT ( 'NONE',  ( 109.1778270068192853, 0.005755170886745426644, -0.007323887274071915615 ) ) ;
#11858=CARTESIAN_POINT ( 'NONE',  ( 109.1586900883932856, -0.002109621908814847055, 0.006819617742893393543 ) ) ;
#11860=ORIENTED_EDGE ( 'NONE', *, *, #3506, .F. ) ;
#11862=ORIENTED_EDGE ( 'NONE', *, *, #24968, .F. ) ;
#11869=CARTESIAN_POINT ( 'NONE',  ( 1.833485406944043827, 144.2578170162065021, -15.69895494453236395 ) ) ;
#11871=B_SPLINE_CURVE_WITH_KNOTS ( 'NONE', 3,
 ( #11134, #6825, #18023, #13708, #11413, #8838, #2332, #19754, #17742, #192 ),
 .UNSPECIFIED., .F., .F.,
 ( 4, 3, 3, 4 ),
 ( 1.962615573354718958E-17, 0.0002669559177086076006, 0.0005339118354150894060, 0.001067817517169171188 ),
 .UNSPECIFIED. ) ;
#11872=CARTESIAN_POINT ( 'NONE',  ( 5.340103579038161463, 62.06990748397846858, 133.7487108093465906 ) ) ;
#11873=CARTESIAN_POINT ( 'NONE',  ( 55.79472521941426777, -35.74479459808802773, -63.36760613016260635 ) ) ;
#11874=CARTESIAN_POINT ( 'NONE',  ( 109.1592201516379674, -0.001331853079208366458, -0.007748443302128551168 ) ) ;
#11875=CARTESIAN_POINT ( 'NONE',  ( 109.1592201516379674, -0.002720803050361364321, 0.007376275279030867701 ) ) ;
#11876=CARTESIAN_POINT ( 'NONE',  ( 26.11404676487259024, -47.08215554553450488, -102.9690087468806325 ) ) ;
#11878=ORIENTED_EDGE ( 'NONE', *, *, #8618, .T. ) ;
#11879=FACE_OUTER_BOUND ( 'NONE', #3642, .T. ) ;
#11880=CARTESIAN_POINT ( 'NONE',  ( 1.833485406944043827, 85.72460230293692973, 117.0814567582547596 ) ) ;
#11881=CARTESIAN_POINT ( 'NONE',  ( 25.64703792032467078, -91.25955007190263757, 66.48786612795848328 ) ) ;
#11882=DIRECTION ( 'NONE',  ( -1.000000000000000000, -0.000000000000000000, -0.000000000000000000 ) ) ;
#11883=CARTESIAN_POINT ( 'NONE',  ( 32.73300124599736449, -116.5274707358856574, 16.10546300444784507 ) ) ;
#11885=VERTEX_POINT ( 'NONE', #4094 ) ;
#11886=CARTESIAN_POINT ( 'NONE',  ( 25.64670758986457599, 98.03181353150564803, -56.02376616805318577 ) ) ;
#11889=EDGE_LOOP ( 'NONE', ( #15622, #5707, #20653, #22165 ) ) ;
#11891=CARTESIAN_POINT ( 'NONE',  ( 10.93730112725932635, 0.000000000000000000, 0.000000000000000000 ) ) ;
#11893=VECTOR ( 'NONE', #20814, 1000.000000000000000 ) ;
#11898=ORIENTED_EDGE ( 'NONE', *, *, #26411, .F. ) ;
#11899=CARTESIAN_POINT ( 'NONE',  ( 1.834118845439484335, -45.01070051384498072, -137.9527673765110194 ) ) ;
#11900=EDGE_LOOP ( 'NONE', ( #14219, #3954, #18914, #10841 ) ) ;
#11901=EDGE_CURVE ( 'NONE', #12482, #24160, #3973, .T. ) ;
#11902=CARTESIAN_POINT ( 'NONE',  ( 10.93730112725990722, -136.0306644680979389, -65.95960219663263047 ) ) ;
#11904=EDGE_CURVE ( 'NONE', #17689, #18738, #17325, .T. ) ;
#11906=CARTESIAN_POINT ( 'NONE',  ( 25.64700659047696263, 107.4550658295756023, -34.67498789830337103 ) ) ;
#11907=CARTESIAN_POINT ( 'NONE',  ( 1.833750490713743853, 0.2669522761665648058, -145.1094586213657180 ) ) ;
#11908=CARTESIAN_POINT ( 'NONE',  ( 2.263178607246673746, -141.9207363487296618, 31.59906277834177146 ) ) ;
#11909=ORIENTED_EDGE ( 'NONE', *, *, #3674, .F. ) ;
#11912=DIRECTION ( 'NONE',  ( 0.000000000000000000, 0.000000000000000000, 1.000000000000000000 ) ) ;
#11913=VERTEX_POINT ( 'NONE', #21512 ) ;
#11914=EDGE_LOOP ( 'NONE', ( #11717, #28354, #1928, #25551 ) ) ;
#11916=ORIENTED_EDGE ( 'NONE', *, *, #17768, .T. ) ;
#11919=CARTESIAN_POINT ( 'NONE',  ( 1.833721034905660074, 107.5990973104336064, -97.36162733017604864 ) ) ;
#11921=B_SPLINE_CURVE_WITH_KNOTS ( 'NONE', 3,
 ( #22515, #24963, #11281, #18170, #630, #20049, #20338 ),
 .UNSPECIFIED., .F., .F.,
 ( 4, 3, 4 ),
 ( 0.000000000000000000, 0.02398743853561332434, 0.04000277880656220170 ),
 .UNSPECIFIED. ) ;
#11928=LINE ( 'NONE', #20416, #11114 ) ;
#11929=CARTESIAN_POINT ( 'NONE',  ( 25.98107933586698692, -67.37827847766595823, 90.88151529733785594 ) ) ;
#11930=CARTESIAN_POINT ( 'NONE',  ( 26.04756280548354752, -67.42001818240403566, -90.90573670389308347 ) ) ;
#11932=CARTESIAN_POINT ( 'NONE',  ( 5.340103556456475609, -120.6284720803331680, 84.79482753886512114 ) ) ;
#11933=ORIENTED_EDGE ( 'NONE', *, *, #26093, .F. ) ;
#11934=CARTESIAN_POINT ( 'NONE',  ( 55.79472521941428198, -71.00924468211167095, 15.83764557006246676 ) ) ;
#11935=CARTESIAN_POINT ( 'NONE',  ( 16.75465622695653067, -108.7410129416641098, 91.67104679059862349 ) ) ;
#11936=B_SPLINE_CURVE_WITH_KNOTS ( 'NONE', 3,
 ( #18872, #5929, #9968, #27645, #1451, #10257, #25212, #14245 ),
 .UNSPECIFIED., .F., .F.,
 ( 4, 2, 2, 4 ),
 ( 1.734723475976807094E-18, 0.0002429588503611233819, 0.0004859177007222450291, 0.0009718354014444937445 ),
 .UNSPECIFIED. ) ;
#11937=CARTESIAN_POINT ( 'NONE',  ( 55.79472521941428198, -72.27573336313959373, 8.328398066091525109 ) ) ;
#11938=EDGE_CURVE ( 'NONE', #4019, #20744, #21321, .T. ) ;
#11940=EDGE_LOOP ( 'NONE', ( #3475, #12497, #18478, #14533 ) ) ;
#11945=CARTESIAN_POINT ( 'NONE',  ( 19.66333377628712853, -77.29039328249547225, -114.0223162644910673 ) ) ;
#11946=CARTESIAN_POINT ( 'NONE',  ( 1.833750490713699666, 125.8019536335930297, -72.32354185792426904 ) ) ;
#11947=ORIENTED_EDGE ( 'NONE', *, *, #16551, .F. ) ;
#11948=CARTESIAN_POINT ( 'NONE',  ( 5.340103579038300907, 84.79482754232432740, -120.6284720963478065 ) ) ;
#11949=CARTESIAN_POINT ( 'NONE',  ( 25.64708228042118776, 34.85404436489494628, 107.3971738194632906 ) ) ;
#11950=CARTESIAN_POINT ( 'NONE',  ( 109.1586900883932856, -0.004701023939945749193, 0.005371970278528625728 ) ) ;
#11951=VERTEX_POINT ( 'NONE', #24550 ) ;
#11952=ORIENTED_EDGE ( 'NONE', *, *, #886, .T. ) ;
#11954=CARTESIAN_POINT ( 'NONE',  ( 109.1586059443104944, -0.006637156007970172224, 0.002447596125914148699 ) ) ;
#11956=B_SPLINE_CURVE_WITH_KNOTS ( 'NONE', 3,
 ( #24667, #17722, #2465, #308, #2309, #24511, #9096, #26641 ),
 .UNSPECIFIED., .F., .F.,
 ( 4, 2, 2, 4 ),
 ( 9.813077866773594792E-18, 0.0002429592666046763807, 0.0004859185332093429494, 0.0009718370664186761409 ),
 .UNSPECIFIED. ) ;
#11957=CARTESIAN_POINT ( 'NONE',  ( 2.433796855181205476, -84.34988187690851191, -118.5671979538065273 ) ) ;
#11958=CARTESIAN_POINT ( 'NONE',  ( 1.833838850093453043, -138.0075846865483982, 44.84138612521046241 ) ) ;
#11959=ORIENTED_EDGE ( 'NONE', *, *, #25943, .F. ) ;
#11960=CARTESIAN_POINT ( 'NONE',  ( 25.70243777736187951, 84.42566495012547989, -75.03063812271970789 ) ) ;
#11961=CARTESIAN_POINT ( 'NONE',  ( 1.832998868059858122, -137.8420662456167065, -45.34898734666188602 ) ) ;
#11962=CARTESIAN_POINT ( 'NONE',  ( 55.79472521941426777, -72.75035398477136539, -0.7279028900801322033 ) ) ;
#11963=CARTESIAN_POINT ( 'NONE',  ( 109.1592201516379674, -0.001127733110579631293, 0.007780772729118876421 ) ) ;
#11964=FACE_OUTER_BOUND ( 'NONE', #6274, .T. ) ;
#11966=EDGE_CURVE ( 'NONE', #13932, #21238, #17178, .T. ) ;
#11968=ORIENTED_EDGE ( 'NONE', *, *, #11671, .T. ) ;
#11969=CARTESIAN_POINT ( 'NONE',  ( 25.73574536432415627, 22.69874377039439395, 110.6664861019684878 ) ) ;
#11970=ORIENTED_EDGE ( 'NONE', *, *, #22999, .T. ) ;
#11973=ORIENTED_EDGE ( 'NONE', *, *, #19307, .T. ) ;
#11974=EDGE_LOOP ( 'NONE', ( #10113, #8639, #5749, #11781 ) ) ;
#11978=DIRECTION ( 'NONE',  ( -1.000000000000000000, -0.000000000000000000, -0.000000000000000000 ) ) ;
#11980=VECTOR ( 'NONE', #3910, 1000.000000000000114 ) ;
#11981=CARTESIAN_POINT ( 'NONE',  ( 109.1592201516379674, -0.003661068210037343815, -0.006957642258146904887 ) ) ;
#11982=CARTESIAN_POINT ( 'NONE',  ( 1.893872463202051604, -97.83022426232032842, 107.2274879309823632 ) ) ;
#11983=CARTESIAN_POINT ( 'NONE',  ( 109.1592201516379674, -0.005631912476303850730, 0.005485778713202916178 ) ) ;
#11984=CARTESIAN_POINT ( 'NONE',  ( 1.833750490713671244, 132.4555075118568368, 59.26520711749913772 ) ) ;
#11985=CARTESIAN_POINT ( 'NONE',  ( 2.108985857320898827, -133.2480631238189517, -57.92316197981790538 ) ) ;
#11987=CARTESIAN_POINT ( 'NONE',  ( 30.58324630866343696, 41.10517620771203440, 113.7441547345748489 ) ) ;
#11992=VECTOR ( 'NONE', #15357, 1000.000000000000000 ) ;
#11995=B_SPLINE_CURVE_WITH_KNOTS ( 'NONE', 3,
 ( #26315, #17391, #4576, #4156, #2408, #26044, #23903, #19690, #6470, #21865 ),
 .UNSPECIFIED., .F., .F.,
 ( 4, 3, 3, 4 ),
 ( 1.387778780781445676E-17, 0.0002669560319015654788, 0.0005492286108966274675, 0.0008315040496093373083 ),
 .UNSPECIFIED. ) ;
#11996=LINE ( 'NONE', #9846, #714 ) ;
#11997=CARTESIAN_POINT ( 'NONE',  ( 10.93730112725997294, 26.59437931460951177, -148.8212007290660210 ) ) ;
#11999=ORIENTED_EDGE ( 'NONE', *, *, #13183, .T. ) ;
#12000=CARTESIAN_POINT ( 'NONE',  ( 32.73300124599732186, 0.000000000000000000, 0.000000000000000000 ) ) ;
#12002=EDGE_CURVE ( 'NONE', #25271, #2611, #5510, .T. ) ;
#12003=VERTEX_POINT ( 'NONE', #9275 ) ;
#12005=DIRECTION ( 'NONE',  ( 0.000000000000000000, 1.000000000000000000, 3.469446951953603342E-16 ) ) ;
#12008=VERTEX_POINT ( 'NONE', #13868 ) ;
#12009=ORIENTED_EDGE ( 'NONE', *, *, #11313, .F. ) ;
#12010=CARTESIAN_POINT ( 'NONE',  ( 109.1624594426973260, 0.01476644236456051487, -0.006066618937909722294 ) ) ;
#12011=AXIS2_PLACEMENT_3D ( 'NONE', #21259, #17075, #25866 ) ;
#12012=DIRECTION ( 'NONE',  ( 0.000000000000000000, 0.000000000000000000, 1.000000000000000000 ) ) ;
#12014=CARTESIAN_POINT ( 'NONE',  ( 25.69398547355839568, 107.6418378907644353, 34.19446713634620494 ) ) ;
#12016=CARTESIAN_POINT ( 'NONE',  ( 26.11404676487257603, 36.06104232266594067, -107.3263591096426666 ) ) ;
#12017=CARTESIAN_POINT ( 'NONE',  ( 109.1587776205901861, -0.003057017121600591122, -0.006661366261223543826 ) ) ;
#12019=( BOUNDED_SURFACE ( )  B_SPLINE_SURFACE ( 3, 1, ( 
 ( #20065, #28271 ),
 ( #10876, #13160 ),
 ( #15164, #23988 ),
 ( #19933, #6995 ) ),
 .UNSPECIFIED., .F., .F., .F. ) 
 B_SPLINE_SURFACE_WITH_KNOTS ( ( 4, 4 ),
 ( 2, 2 ),
 ( 0.000000000000000000, 1.000000000000000000 ),
 ( 0.000000000000000000, 1.000000000000000000 ),
 .UNSPECIFIED. ) 
 GEOMETRIC_REPRESENTATION_ITEM ( )  RATIONAL_B_SPLINE_SURFACE ( (
 ( 1.000000000000000000, 1.000000000000000000),
 ( 0.9956975270656955868, 0.8568959468854907557),
 ( 0.9956975270656955868, 0.8568959468854907557),
 ( 1.000000000000000000, 1.000000000000000000) ) ) 
 REPRESENTATION_ITEM ( '' )  SURFACE ( )  );
#12020=FACE_OUTER_BOUND ( 'NONE', #22409, .T. ) ;
#12021=CARTESIAN_POINT ( 'NONE',  ( 1.833206308920112049, 59.70089323729912678, -132.2594750499820009 ) ) ;
#12022=CARTESIAN_POINT ( 'NONE',  ( 109.1592201516379674, 0.007780772729122757865, -0.001127733110588145750 ) ) ;
#12023=CARTESIAN_POINT ( 'NONE',  ( 30.59138290137885008, -49.72302320601725967, -105.0379801549013337 ) ) ;
#12026=CARTESIAN_POINT ( 'NONE',  ( 32.73300124599732186, 0.000000000000000000, 0.000000000000000000 ) ) ;
#12027=ADVANCED_FACE ( 'NONE', ( #24396 ), #24565, .F. ) ;
#12028=CARTESIAN_POINT ( 'NONE',  ( 1.833485406944043827, 84.86072343962567288, 117.7091014914953320 ) ) ;
#12030=CARTESIAN_POINT ( 'NONE',  ( 1.833485406944057594, -84.86072343962649711, 117.7091014914947209 ) ) ;
#12031=DIRECTION ( 'NONE',  ( -1.000000000000000000, -0.000000000000000000, -0.000000000000000000 ) ) ;
#12032=CARTESIAN_POINT ( 'NONE',  ( 2.108985857320881063, 144.6256801373127701, 13.91228467251867507 ) ) ;
#12033=B_SPLINE_CURVE_WITH_KNOTS ( 'NONE', 3,
 ( #28123, #4230, #10579, #17752 ),
 .UNSPECIFIED., .F., .F.,
 ( 4, 4 ),
 ( 3.385911829997767421E-16, 0.01077107486149848914 ),
 .UNSPECIFIED. ) ;
#12035=CARTESIAN_POINT ( 'NONE',  ( 1.833750490713730974, 44.58740205676330248, 138.0897889879340710 ) ) ;
#12037=CARTESIAN_POINT ( 'NONE',  ( 1.833485406944085350, 132.3460930279899515, -59.50871042846091541 ) ) ;
#12038=CARTESIAN_POINT ( 'NONE',  ( 10.93730112725936188, 148.8212007290658505, 26.59437931460817595 ) ) ;
#12039=ORIENTED_EDGE ( 'NONE', *, *, #22610, .T. ) ;
#12040=DIRECTION ( 'NONE',  ( -0.5946245182733607137, -0.3994439555666277619, 0.6977579871484522744 ) ) ;
#12041=AXIS2_PLACEMENT_3D ( 'NONE', #20976, #16090, #24894 ) ;
#12042=CARTESIAN_POINT ( 'NONE',  ( 109.1586900883932856, 0.006757191295060844746, 0.002301750759599800571 ) ) ;
#12043=ADVANCED_FACE ( 'NONE', ( #5825 ), #10014, .F. ) ;
#12045=CARTESIAN_POINT ( 'NONE',  ( 28.37599760073042177, -65.97809271467072278, -93.86375353586234382 ) ) ;
#12046=EDGE_LOOP ( 'NONE', ( #25690, #4880, #21700, #12204 ) ) ;
#12047=CARTESIAN_POINT ( 'NONE',  ( 1.833485406944043827, -96.69979900902094982, -108.1939177044935860 ) ) ;
#12050=LINE ( 'NONE', #8164, #954 ) ;
#12051=ORIENTED_EDGE ( 'NONE', *, *, #2431, .T. ) ;
#12052=CARTESIAN_POINT ( 'NONE',  ( 2.108393763691212452, -60.26375949664278409, 132.2055356348359112 ) ) ;
#12053=CARTESIAN_POINT ( 'NONE',  ( 2.433796855181233454, -118.5671979538051062, -84.34988187691051564 ) ) ;
#12054=CARTESIAN_POINT ( 'NONE',  ( 1.832998868059890096, -59.50898020732598326, 132.3466930259791923 ) ) ;
#12056=VECTOR ( 'NONE', #10317, 1000.000000000000000 ) ;
#12058=CARTESIAN_POINT ( 'NONE',  ( 1.833838848569414148, 85.14939661881724930, -117.5008734796303429 ) ) ;
#12060=CARTESIAN_POINT ( 'NONE',  ( 16.75465622695626422, -120.7871673903172223, -75.09093759626998121 ) ) ;
#12064=ORIENTED_EDGE ( 'NONE', *, *, #11901, .F. ) ;
#12068=CARTESIAN_POINT ( 'NONE',  ( 10.93730112725943471, 119.3442956573271516, 92.80059208661684522 ) ) ;
#12071=CARTESIAN_POINT ( 'NONE',  ( 1.833750490713671244, -132.4555075118564389, -59.26520711749999748 ) ) ;
#12073=CARTESIAN_POINT ( 'NONE',  ( 1.833838850093465700, 107.8375718686139351, 97.09738119087744224 ) ) ;
#12074=CARTESIAN_POINT ( 'NONE',  ( 25.64681081121879203, 45.54494737132363724, -103.3177883989774841 ) ) ;
#12075=ORIENTED_EDGE ( 'NONE', *, *, #10774, .T. ) ;
#12076=CARTESIAN_POINT ( 'NONE',  ( 109.1778270068192853, 0.008236503545668636198, 0.004349865064721274849 ) ) ;
#12078=CARTESIAN_POINT ( 'NONE',  ( 25.70243777736190793, 110.3252221127465447, 24.19989514742760051 ) ) ;
#12079=CARTESIAN_POINT ( 'NONE',  ( 2.433796855181205476, -133.5135467655521779, 57.85512797797844087 ) ) ;
#12080=EDGE_CURVE ( 'NONE', #17967, #24477, #21974, .T. ) ;
#12081=CARTESIAN_POINT ( 'NONE',  ( 10.93730112726003156, 71.28103789255123957, -133.3192575531793693 ) ) ;
#12082=CARTESIAN_POINT ( 'NONE',  ( 2.433796855181205476, -109.1007109081232471, 96.28145139437646094 ) ) ;
#12084=ORIENTED_EDGE ( 'NONE', *, *, #23574, .F. ) ;
#12085=CARTESIAN_POINT ( 'NONE',  ( 109.1589550718174877, 0.007507020724817403678, 0.001014448720240663810 ) ) ;
#12086=CARTESIAN_POINT ( 'NONE',  ( -90.83090735639699176, 0.000000000000000000, 0.000000000000000000 ) ) ;
#12087=VECTOR ( 'NONE', #8510, 1000.000000000000341 ) ;
#12088=CARTESIAN_POINT ( 'NONE',  ( 30.58324630866349381, 52.76949945162388644, 108.8243914523531686 ) ) ;
#12089=AXIS2_PLACEMENT_3D ( 'NONE', #8351, #15362, #24036 ) ;
#12090=VERTEX_POINT ( 'NONE', #25108 ) ;
#12091=VERTEX_POINT ( 'NONE', #12151 ) ;
#12092=CIRCLE ( 'NONE', #23114, 117.6351876552689504 ) ;
#12096=CARTESIAN_POINT ( 'NONE',  ( 25.64704443564077607, -23.60610532597032218, 110.4160069635933326 ) ) ;
#12098=CARTESIAN_POINT ( 'NONE',  ( 2.108393763691201350, -144.6252321290182579, 13.91282116576931394 ) ) ;
#12100=CARTESIAN_POINT ( 'NONE',  ( 109.1587776205901577, -0.005502145856754194451, 0.004842060007774028410 ) ) ;
#12101=EDGE_LOOP ( 'NONE', ( #11414, #8992, #24773, #6404 ) ) ;
#12106=CARTESIAN_POINT ( 'NONE',  ( 55.49584447822657296, 48.74506217377955863, -53.73688382046214684 ) ) ;
#12109=CIRCLE ( 'NONE', #1067, 151.1787379149930359 ) ;
#12110=DIRECTION ( 'NONE',  ( 0.000000000000000000, 0.000000000000000000, 1.000000000000000000 ) ) ;
#12111=ORIENTED_EDGE ( 'NONE', *, *, #6974, .T. ) ;
#12114=VECTOR ( 'NONE', #27762, 999.9999999999998863 ) ;
#12115=CARTESIAN_POINT ( 'NONE',  ( 10.93730112725953596, 92.80059208661681680, 119.3442956573276206 ) ) ;
#12117=EDGE_CURVE ( 'NONE', #20493, #5939, #28133, .T. ) ;
#12119=DIRECTION ( 'NONE',  ( -0.5914120900931443270, -0.7643865440136122791, 0.2567974902965066142 ) ) ;
#12120=VERTEX_POINT ( 'NONE', #7847 ) ;
#12124=EDGE_LOOP ( 'NONE', ( #17726, #21563, #1630, #25058 ) ) ;
#12130=VECTOR ( 'NONE', #13808, 1000.000000000000114 ) ;
#12131=FACE_OUTER_BOUND ( 'NONE', #24287, .T. ) ;
#12132=CARTESIAN_POINT ( 'NONE',  ( 2.108985857320926360, -126.4634971826979211, -71.53406810961618589 ) ) ;
#12134=CARTESIAN_POINT ( 'NONE',  ( 21.16825799904930605, 135.0813719997364899, 9.757279788663185016 ) ) ;
#12137=CARTESIAN_POINT ( 'NONE',  ( 25.64681081121879203, 84.18689316040048709, 75.24277141833519522 ) ) ;
#12138=ADVANCED_FACE ( 'NONE', ( #20629 ), #1012, .F. ) ;
#12142=CARTESIAN_POINT ( 'NONE',  ( 55.49584447822657296, 22.16497542184496794, -69.08290406177557941 ) ) ;
#12143=CARTESIAN_POINT ( 'NONE',  ( 25.64660436782553887, -83.52001792470935015, 75.98230157781821958 ) ) ;
#12144=CARTESIAN_POINT ( 'NONE',  ( 25.87036335909428075, -22.53739730344121384, 110.7910326764401390 ) ) ;
#12146=FACE_OUTER_BOUND ( 'NONE', #20390, .T. ) ;
#12148=ORIENTED_EDGE ( 'NONE', *, *, #26257, .T. ) ;
#12150=ORIENTED_EDGE ( 'NONE', *, *, #19929, .T. ) ;
#12151=CARTESIAN_POINT ( 'NONE',  ( 10.93730112725990011, -151.0983828010091656, -4.928439153521871674 ) ) ;
#12152=CARTESIAN_POINT ( 'NONE',  ( 2.430230287190581429, 138.8342928068226172, -43.58368230469247351 ) ) ;
#12156=B_SPLINE_CURVE_WITH_KNOTS ( 'NONE', 3,
 ( #7737, #16491, #4232, #23840 ),
 .UNSPECIFIED., .F., .F.,
 ( 4, 4 ),
 ( 6.662151249755524083E-16, 0.008383748772660135420 ),
 .UNSPECIFIED. ) ;
#12157=CARTESIAN_POINT ( 'NONE',  ( 1.832998868059858122, -15.69902610990472880, 144.2584710144579958 ) ) ;
#12159=CARTESIAN_POINT ( 'NONE',  ( 55.79472521941428198, 68.96476385670696629, -23.17337251492691763 ) ) ;
#12160=EDGE_CURVE ( 'NONE', #10148, #12210, #11689, .T. ) ;
#12161=CARTESIAN_POINT ( 'NONE',  ( 109.1592201516379674, 0.001127733110579580769, -0.007780772729118883360 ) ) ;
#12162=CARTESIAN_POINT ( 'NONE',  ( 25.73574536432415627, 35.67555431182972825, -107.1893601970590879 ) ) ;
#12163=DIRECTION ( 'NONE',  ( 0.5914120900931444380, 0.3962188444547191657, 0.7023121577978167496 ) ) ;
#12164=CARTESIAN_POINT ( 'NONE',  ( 2.063896406836609909, -31.51663808384454768, -141.8093313989364219 ) ) ;
#12165=FACE_OUTER_BOUND ( 'NONE', #6183, .T. ) ;
#12167=EDGE_LOOP ( 'NONE', ( #21896, #28401, #1659, #10357 ) ) ;
#12168=ORIENTED_EDGE ( 'NONE', *, *, #22090, .F. ) ;
#12170=DIRECTION ( 'NONE',  ( 0.000000000000000000, 1.000000000000000000, 0.000000000000000000 ) ) ;
#12171=FACE_OUTER_BOUND ( 'NONE', #14474, .T. ) ;
#12173=CARTESIAN_POINT ( 'NONE',  ( 2.430230287190581429, -116.8646894862406214, -86.70145658344777928 ) ) ;
#12174=VERTEX_POINT ( 'NONE', #17296 ) ;
#12175=ORIENTED_EDGE ( 'NONE', *, *, #23260, .F. ) ;
#12176=DIRECTION ( 'NONE',  ( 0.000000000000000000, 0.000000000000000000, 1.000000000000000000 ) ) ;
#12177=CARTESIAN_POINT ( 'NONE',  ( 26.11404676487257603, 36.06104232266594067, -107.3263591096426666 ) ) ;
#12178=CARTESIAN_POINT ( 'NONE',  ( 5.340103579038194326, -84.79482754232353159, 120.6284720963482755 ) ) ;
#12179=CARTESIAN_POINT ( 'NONE',  ( 109.1624594426973118, 0.001206615835669453849, -0.01591840958353240090 ) ) ;
#12181=ORIENTED_EDGE ( 'NONE', *, *, #19272, .T. ) ;
#12185=ORIENTED_EDGE ( 'NONE', *, *, #939, .F. ) ;
#12186=FACE_OUTER_BOUND ( 'NONE', #9216, .T. ) ;
#12192=ADVANCED_FACE ( 'NONE', ( #4202 ), #8011, .F. ) ;
#12193=DIRECTION ( 'NONE',  ( 0.5946245182733607137, 0.3297108033645267944, -0.7332888028688915316 ) ) ;
#12194=CARTESIAN_POINT ( 'NONE',  ( 109.1589550718175161, -0.007359857714025710984, 0.001793588804100470059 ) ) ;
#12196=ORIENTED_EDGE ( 'NONE', *, *, #16820, .T. ) ;
#12197=EDGE_CURVE ( 'NONE', #9317, #26534, #23746, .T. ) ;
#12198=CARTESIAN_POINT ( 'NONE',  ( 109.1624594426973118, 0.01570508117120617345, 0.002863932759303145122 ) ) ;
#12199=CARTESIAN_POINT ( 'NONE',  ( 1.833721034905648084, 85.00517831633841581, -117.6051524288275232 ) ) ;
#12201=DIRECTION ( 'NONE',  ( 0.000000000000000000, 0.000000000000000000, -1.000000000000000000 ) ) ;
#12202=EDGE_LOOP ( 'NONE', ( #25522, #12453, #15742, #17600 ) ) ;
#12203=ORIENTED_EDGE ( 'NONE', *, *, #16617, .F. ) ;
#12204=ORIENTED_EDGE ( 'NONE', *, *, #19599, .F. ) ;
#12205=CARTESIAN_POINT ( 'NONE',  ( 19.66333377628728485, 77.29039328249602647, 114.0223162644902004 ) ) ;
#12206=CARTESIAN_POINT ( 'NONE',  ( 25.64681081121879203, 112.9102952884414464, -0.4157506337731811663 ) ) ;
#12209=CARTESIAN_POINT ( 'NONE',  ( 1.833721034905658520, -132.7087680342064004, -58.69612512971738028 ) ) ;
#12210=VERTEX_POINT ( 'NONE', #28096 ) ;
#12212=CARTESIAN_POINT ( 'NONE',  ( 25.64708228042117710, 45.96113332231483639, -103.1335618347708021 ) ) ;
#12215=LINE ( 'NONE', #1553, #21216 ) ;
#12216=CARTESIAN_POINT ( 'NONE',  ( 109.1721716018069515, -0.003350975118860853846, -0.01673651515802107581 ) ) ;
#12217=CARTESIAN_POINT ( 'NONE',  ( 30.59141879584319312, 88.14706749784174633, -75.73279557183218458 ) ) ;
#12218=CARTESIAN_POINT ( 'NONE',  ( 1.831572820252008738, -71.69925593429721289, -126.1609924456737133 ) ) ;
#12220=LINE ( 'NONE', #7483, #5938 ) ;
#12222=CARTESIAN_POINT ( 'NONE',  ( 32.73300124599738581, 51.32617430725051832, -105.8473486001045387 ) ) ;
#12223=CARTESIAN_POINT ( 'NONE',  ( 25.87036335909426654, 110.3794299719623524, -24.47383578007024241 ) ) ;
#12224=CARTESIAN_POINT ( 'NONE',  ( 109.1587776205901577, -0.004375189885414207044, 0.005880209827416975170 ) ) ;
#12225=EDGE_LOOP ( 'NONE', ( #12168, #17436, #7724, #4381 ) ) ;
#12227=ORIENTED_EDGE ( 'NONE', *, *, #8024, .F. ) ;
#12228=EDGE_CURVE ( 'NONE', #15588, #182, #19579, .T. ) ;
#12235=CARTESIAN_POINT ( 'NONE',  ( 109.1586900883932856, -0.006819617742892453323, 0.002109621908824125657 ) ) ;
#12236=CARTESIAN_POINT ( 'NONE',  ( 1.833721034905666736, 137.8972080590637290, -45.17977675814169203 ) ) ;
#12237=CARTESIAN_POINT ( 'NONE',  ( 25.69398547355841345, 75.02007992711823192, -84.42756928260500615 ) ) ;
#12239=CARTESIAN_POINT ( 'NONE',  ( 1.833838850855487257, -125.6242502389381173, -72.63194208529603202 ) ) ;
#12243=CARTESIAN_POINT ( 'NONE',  ( 109.1586059443104944, 0.001198897580748340026, 0.006971743774738788611 ) ) ;
#12245=CARTESIAN_POINT ( 'NONE',  ( 13.36082413113061307, 137.0038452127800213, 67.94366799842862292 ) ) ;
#12246=CARTESIAN_POINT ( 'NONE',  ( 25.64708228042119131, -83.88307475436008076, -75.58165863986127420 ) ) ;
#12247=CARTESIAN_POINT ( 'NONE',  ( 8.186469777910954093, 108.6390983781771098, -102.4860666868853656 ) ) ;
#12248=CARTESIAN_POINT ( 'NONE',  ( 10.93730112725970827, 42.00474393596263667, 145.2260730187401236 ) ) ;
#12249=ORIENTED_EDGE ( 'NONE', *, *, #20765, .T. ) ;
#12250=CARTESIAN_POINT ( 'NONE',  ( 1.833838850093414186, -144.3148362521194770, 15.16810397409735423 ) ) ;
#12252=CARTESIAN_POINT ( 'NONE',  ( 2.430230287190589422, -96.28466919684173320, 109.1043569252011025 ) ) ;
#12254=CARTESIAN_POINT ( 'NONE',  ( 25.64681081121879203, 0.4157506337743640534, -112.9102952884414464 ) ) ;
#12256=ORIENTED_EDGE ( 'NONE', *, *, #21326, .F. ) ;
#12257=CARTESIAN_POINT ( 'NONE',  ( 25.64708228042122329, -75.58165863986093314, 83.88307475436030813 ) ) ;
#12258=CARTESIAN_POINT ( 'NONE',  ( 32.73300124599740002, 103.7392577722183660, -55.46353551261898218 ) ) ;
#12259=EDGE_LOOP ( 'NONE', ( #5720, #17917, #18198, #27554 ) ) ;
#12260=EDGE_LOOP ( 'NONE', ( #24723, #1656, #13188, #3966 ) ) ;
#12262=EDGE_CURVE ( 'NONE', #13553, #6393, #27102, .T. ) ;
#12263=CARTESIAN_POINT ( 'NONE',  ( 2.433796855181205476, 28.83182736670536528, 142.6247129145649239 ) ) ;
#12267=EDGE_CURVE ( 'NONE', #10482, #14469, #1376, .T. ) ;
#12268=CARTESIAN_POINT ( 'NONE',  ( 1.832998868059890096, -107.4798986104853498, -97.49378069860902940 ) ) ;
#12269=CARTESIAN_POINT ( 'NONE',  ( 26.11404676487257603, -98.61392875273325842, -55.62948129436350087 ) ) ;
#12270=VERTEX_POINT ( 'NONE', #307 ) ;
#12271=CARTESIAN_POINT ( 'NONE',  ( 25.64681081121879203, 107.5125461021407318, -34.49579773461672971 ) ) ;
#12272=CARTESIAN_POINT ( 'NONE',  ( 10.93730112725971004, 51.37919228020272300, 142.1801301103785420 ) ) ;
#12273=CARTESIAN_POINT ( 'NONE',  ( 30.59138290137908101, -26.79783179610930333, -113.0806461017757272 ) ) ;
#12274=CARTESIAN_POINT ( 'NONE',  ( 25.64681081121880624, -75.86069728268932977, -83.63051021305977883 ) ) ;
#12275=CARTESIAN_POINT ( 'NONE',  ( 1.833691583653510815, -141.8642667235906174, -30.51806994139743878 ) ) ;
#12277=CARTESIAN_POINT ( 'NONE',  ( 2.263178607246686624, 16.59120332983143342, 144.4462811785176939 ) ) ;
#12278=CARTESIAN_POINT ( 'NONE',  ( 109.1592201516379674, 0.007051465909552763651, -0.003476928926134732496 ) ) ;
#12280=CARTESIAN_POINT ( 'NONE',  ( 28.37644542392846958, 119.4444529625694287, -34.54617949427969847 ) ) ;
#12281=ORIENTED_EDGE ( 'NONE', *, *, #20602, .F. ) ;
#12282=CARTESIAN_POINT ( 'NONE',  ( 6.224689322667647851, 33.28770499679335160, 144.2687111683196406 ) ) ;
#12285=CARTESIAN_POINT ( 'NONE',  ( 2.430230287190572103, -60.50928654924845063, 132.3371620660948906 ) ) ;
#12289=B_SPLINE_CURVE_WITH_KNOTS ( 'NONE', 3,
 ( #23218, #14552, #8100, #7673, #3607, #16726, #5795 ),
 .UNSPECIFIED., .F., .F.,
 ( 4, 3, 4 ),
 ( 0.000000000000000000, 0.02398743853561319250, 0.04000277880656216700 ),
 .UNSPECIFIED. ) ;
#12290=EDGE_CURVE ( 'NONE', #24693, #391, #27842, .T. ) ;
#12293=LINE ( 'NONE', #20105, #8980 ) ;
#12294=CARTESIAN_POINT ( 'NONE',  ( 9.884929003653608603, 144.4113244745777820, -42.50195158090882330 ) ) ;
#12296=CARTESIAN_POINT ( 'NONE',  ( 10.93730112725932635, 0.000000000000000000, 0.000000000000000000 ) ) ;
#12299=ORIENTED_EDGE ( 'NONE', *, *, #11671, .F. ) ;
#12302=CARTESIAN_POINT ( 'NONE',  ( 8.186469777910954093, 57.56191611950492160, -137.8131828745822247 ) ) ;
#12303=CARTESIAN_POINT ( 'NONE',  ( 32.73300124599738581, -39.98094346392232268, -110.6325518752277759 ) ) ;
#12305=CARTESIAN_POINT ( 'NONE',  ( 109.1589550718174877, -0.003284595046925705905, 0.006826119083824063426 ) ) ;
#12311=CARTESIAN_POINT ( 'NONE',  ( 9.884929003653608603, -148.0628878137282243, 27.17402761732295957 ) ) ;
#12312=CARTESIAN_POINT ( 'NONE',  ( 109.1592201516379674, 0.005485778713202931790, 0.005631912476303835985 ) ) ;
#12313=EDGE_CURVE ( 'NONE', #27728, #1601, #23048, .T. ) ;
#12315=EDGE_LOOP ( 'NONE', ( #23528, #11071, #7477, #9671 ) ) ;
#12317=EDGE_CURVE ( 'NONE', #9129, #26116, #25019, .T. ) ;
#12318=CARTESIAN_POINT ( 'NONE',  ( 1.894214914920927972, -86.08679174687999591, -116.8658096527531853 ) ) ;
#12324=CARTESIAN_POINT ( 'NONE',  ( 32.73300124599740002, 116.5274707358857142, -16.10546300444702794 ) ) ;
#12328=CARTESIAN_POINT ( 'NONE',  ( 26.11404676487257603, -74.91683232331033082, 84.89295829319468112 ) ) ;
#12329=CARTESIAN_POINT ( 'NONE',  ( 26.28373643307406127, -127.2291519022770672, -9.189598927293246788 ) ) ;
#12333=ORIENTED_EDGE ( 'NONE', *, *, #21591, .T. ) ;
#12334=ORIENTED_EDGE ( 'NONE', *, *, #3131, .T. ) ;
#12335=CARTESIAN_POINT ( 'NONE',  ( 55.79472521941426777, -69.41463258328526820, 21.78881894124680230 ) ) ;
#12336=B_SPLINE_CURVE_WITH_KNOTS ( 'NONE', 3,
 ( #1241, #22861, #3121, #25149, #5418, #3831, #12597, #21387 ),
 .UNSPECIFIED., .F., .F.,
 ( 4, 2, 2, 4 ),
 ( 0.000000000000000000, 0.0002429588503611243848, 0.0004859177007222487696, 0.0009718354014444800836 ),
 .UNSPECIFIED. ) ;
#12337=DIRECTION ( 'NONE',  ( 0.000000000000000000, 0.000000000000000000, 1.000000000000000000 ) ) ;
#12340=CARTESIAN_POINT ( 'NONE',  ( 19.66333377628707524, 51.89484018353834927, 127.6002314355559122 ) ) ;
#12346=FACE_OUTER_BOUND ( 'NONE', #11802, .T. ) ;
#12347=CARTESIAN_POINT ( 'NONE',  ( 55.49584447822657296, -0.2676470673961756641, 72.55110015779771970 ) ) ;
#12349=ADVANCED_FACE ( 'NONE', ( #9240 ), #2912, .T. ) ;
#12350=CARTESIAN_POINT ( 'NONE',  ( 2.430230287190592531, 96.28466919684248637, -109.1043569252004488 ) ) ;
#12351=CARTESIAN_POINT ( 'NONE',  ( 2.433796855181233454, 71.49415740225254012, -126.7346379669248222 ) ) ;
#12352=CARTESIAN_POINT ( 'NONE',  ( 25.70243777736187951, -110.6300896395618736, 22.76560620137025737 ) ) ;
#12353=CARTESIAN_POINT ( 'NONE',  ( 25.64681081121879203, -84.18689316039996129, -75.24277141833577787 ) ) ;
#12354=VERTEX_POINT ( 'NONE', #19734 ) ;
#12358=CARTESIAN_POINT ( 'NONE',  ( 21.16825799904895078, 121.8625396241606182, -59.09063383105223011 ) ) ;
#12359=( BOUNDED_SURFACE ( )  B_SPLINE_SURFACE ( 3, 1, ( 
 ( #11109, #19879 ),
 ( #7199, #20699 ),
 ( #5161, #13 ),
 ( #16243, #25050 ) ),
 .UNSPECIFIED., .F., .F., .F. ) 
 B_SPLINE_SURFACE_WITH_KNOTS ( ( 4, 4 ),
 ( 2, 2 ),
 ( 0.000000000000000000, 1.000000000000000000 ),
 ( 0.000000000000000000, 1.000000000000000000 ),
 .UNSPECIFIED. ) 
 GEOMETRIC_REPRESENTATION_ITEM ( )  RATIONAL_B_SPLINE_SURFACE ( (
 ( 1.000000000000000000, 1.000000000000000000),
 ( 0.9960225298536222738, 0.9999952330161893110),
 ( 0.9960225298536222738, 0.9999952330161893110),
 ( 1.000000000000000000, 1.000000000000000000) ) ) 
 REPRESENTATION_ITEM ( '' )  SURFACE ( )  );
#12360=ORIENTED_EDGE ( 'NONE', *, *, #9890, .T. ) ;
#12365=CARTESIAN_POINT ( 'NONE',  ( 25.64700659047695552, -23.69811251893808901, 110.3963107228935741 ) ) ;
#12366=CARTESIAN_POINT ( 'NONE',  ( 1.833691583653536350, 138.1170938425798056, -44.50270951807404174 ) ) ;
#12367=CARTESIAN_POINT ( 'NONE',  ( 32.73300124599735739, -55.46353551262085091, 103.7392577722174565 ) ) ;
#12369=CARTESIAN_POINT ( 'NONE',  ( 25.64703792032470275, 112.2770217641849655, -11.95040607427869261 ) ) ;
#12370=CARTESIAN_POINT ( 'NONE',  ( 1.893872463202024736, -16.11957794552867540, 144.2520230501565663 ) ) ;
#12371=ORIENTED_EDGE ( 'NONE', *, *, #15749, .T. ) ;
#12372=VERTEX_POINT ( 'NONE', #22043 ) ;
#12373=CARTESIAN_POINT ( 'NONE',  ( 109.1586900883932856, 0.002109621908824149943, 0.006819617742892446384 ) ) ;
#12374=CARTESIAN_POINT ( 'NONE',  ( 2.433796855181205476, 107.1581411821785821, 98.43889364293895028 ) ) ;
#12375=CARTESIAN_POINT ( 'NONE',  ( 25.64681081121879203, -83.63051021305953725, 75.86069728268962820 ) ) ;
#12379=CARTESIAN_POINT ( 'NONE',  ( 109.1592201516379674, -0.007748443302128564178, 0.001331853079208289697 ) ) ;
#12380=FACE_OUTER_BOUND ( 'NONE', #2490, .T. ) ;
#12383=EDGE_CURVE ( 'NONE', #22024, #10268, #16847, .T. ) ;
#12384=CARTESIAN_POINT ( 'NONE',  ( 25.64660436782551756, 0.5800540083551843917, 112.9095526718341489 ) ) ;
#12385=CARTESIAN_POINT ( 'NONE',  ( 1.832998868059858122, 0.5339089137748035396, 145.1092030902949830 ) ) ;
#12386=ORIENTED_EDGE ( 'NONE', *, *, #25940, .F. ) ;
#12387=CARTESIAN_POINT ( 'NONE',  ( 2.433796855181233454, -46.34326152018648060, -137.9325382748289996 ) ) ;
#12388=EDGE_CURVE ( 'NONE', #28027, #7211, #14066, .T. ) ;
#12391=EDGE_CURVE ( 'NONE', #19494, #13159, #3116, .T. ) ;
#12392=ORIENTED_EDGE ( 'NONE', *, *, #26251, .F. ) ;
#12394=( BOUNDED_SURFACE ( )  B_SPLINE_SURFACE ( 3, 1, ( 
 ( #15568, #2774 ),
 ( #324, #4650 ),
 ( #20183, #24536 ),
 ( #623, #5071 ) ),
 .UNSPECIFIED., .F., .F., .F. ) 
 B_SPLINE_SURFACE_WITH_KNOTS ( ( 4, 4 ),
 ( 2, 2 ),
 ( 0.000000000000000000, 1.000000000000000000 ),
 ( 0.000000000000000000, 1.000000000000000000 ),
 .UNSPECIFIED. ) 
 GEOMETRIC_REPRESENTATION_ITEM ( )  RATIONAL_B_SPLINE_SURFACE ( (
 ( 1.000000000000000000, 1.000000000000000000),
 ( 0.9956975270656955868, 0.8568959468854907557),
 ( 0.9956975270656955868, 0.8568959468854907557),
 ( 1.000000000000000000, 1.000000000000000000) ) ) 
 REPRESENTATION_ITEM ( '' )  SURFACE ( )  );
#12396=CARTESIAN_POINT ( 'NONE',  ( 24.01988960052061373, -125.8850824254503493, 36.40943914739857945 ) ) ;
#12398=CARTESIAN_POINT ( 'NONE',  ( 6.224689322667630975, 118.2566963816771022, 89.08920297664251109 ) ) ;
#12399=ORIENTED_EDGE ( 'NONE', *, *, #27725, .F. ) ;
#12401=CARTESIAN_POINT ( 'NONE',  ( 10.93730112726006354, 149.7554878793152966, -20.69552240458195413 ) ) ;
#12403=CARTESIAN_POINT ( 'NONE',  ( 25.64692232868535982, -75.79483800045719022, -83.69035111837278862 ) ) ;
#12404=CARTESIAN_POINT ( 'NONE',  ( 26.04756280548352976, -110.4687147111161636, 24.61655718144302796 ) ) ;
#12405=CARTESIAN_POINT ( 'NONE',  ( 1.833838850855461056, -141.9202662332486113, -30.25705358194998240 ) ) ;
#12406=CARTESIAN_POINT ( 'NONE',  ( 2.433796855181205476, 74.00833731765735024, -125.2830755159746445 ) ) ;
#12407=EDGE_CURVE ( 'NONE', #2427, #18428, #6895, .T. ) ;
#12408=CARTESIAN_POINT ( 'NONE',  ( 26.11404676487257603, -22.43340081644687345, -110.9778746459749499 ) ) ;
#12409=CARTESIAN_POINT ( 'NONE',  ( 109.1589550718174877, -0.004900004919105039811, -0.005777059646704573760 ) ) ;
#12410=CARTESIAN_POINT ( 'NONE',  ( 26.11404676487257603, -24.64483677384923865, 110.5078194225160360 ) ) ;
#12413=ORIENTED_EDGE ( 'NONE', *, *, #3144, .F. ) ;
#12415=ADVANCED_FACE ( 'NONE', ( #11687 ), #9848, .F. ) ;
#12417=ORIENTED_EDGE ( 'NONE', *, *, #8839, .T. ) ;
#12418=ORIENTED_EDGE ( 'NONE', *, *, #1341, .F. ) ;
#12419=B_SPLINE_CURVE_WITH_KNOTS ( 'NONE', 3,
 ( #2544, #1985, #17379, #15626, #15488, #10785, #8481, #9039, #24301, #19679 ),
 .UNSPECIFIED., .F., .F.,
 ( 4, 3, 3, 4 ),
 ( 1.387778780781445676E-17, 0.0002669560319015803866, 0.0005492286108966434053, 0.0008315040496093427293 ),
 .UNSPECIFIED. ) ;
#12420=AXIS2_PLACEMENT_3D ( 'NONE', #17971, #9505, #24484 ) ;
#12421=ORIENTED_EDGE ( 'NONE', *, *, #22315, .F. ) ;
#12424=CARTESIAN_POINT ( 'NONE',  ( 2.263178113027060956, -73.90841366068468687, 125.2099934853448389 ) ) ;
#12425=( BOUNDED_SURFACE ( )  B_SPLINE_SURFACE ( 3, 1, ( 
 ( #6711, #6421 ),
 ( #1799, #12744 ),
 ( #28278, #17486 ),
 ( #21673, #6159 ) ),
 .UNSPECIFIED., .F., .F., .F. ) 
 B_SPLINE_SURFACE_WITH_KNOTS ( ( 4, 4 ),
 ( 2, 2 ),
 ( 0.000000000000000000, 1.000000000000000000 ),
 ( 0.000000000000000000, 1.000000000000000000 ),
 .UNSPECIFIED. ) 
 GEOMETRIC_REPRESENTATION_ITEM ( )  RATIONAL_B_SPLINE_SURFACE ( (
 ( 1.000000000000000000, 1.000000000000000000),
 ( 0.6386103224230302855, 0.9954351624131538845),
 ( 0.6386103224230302855, 0.9954351624131538845),
 ( 1.000000000000000000, 1.000000000000000000) ) ) 
 REPRESENTATION_ITEM ( '' )  SURFACE ( )  );
#12426=CARTESIAN_POINT ( 'NONE',  ( 9.884929003653626367, 27.17402761732548555, -148.0628878137277979 ) ) ;
#12428=VECTOR ( 'NONE', #15981, 1000.000000000000000 ) ;
#12429=CARTESIAN_POINT ( 'NONE',  ( 32.73300124599736449, -66.00340565729409548, 97.37344512919831629 ) ) ;
#12431=CARTESIAN_POINT ( 'NONE',  ( 10.93730112725971360, 26.59437931460756488, 148.8212007290661916 ) ) ;
#12432=CARTESIAN_POINT ( 'NONE',  ( 9.884929003653608603, -135.7578851563881983, -65.04493172071613571 ) ) ;
#12434=AXIS2_PLACEMENT_3D ( 'NONE', #12957, #8517, #15248 ) ;
#12435=ORIENTED_EDGE ( 'NONE', *, *, #8291, .T. ) ;
#12436=ORIENTED_EDGE ( 'NONE', *, *, #7284, .F. ) ;
#12438=CARTESIAN_POINT ( 'NONE',  ( 1.833206308920070082, 144.3905119031281856, -14.42724735286700088 ) ) ;
#12440=EDGE_CURVE ( 'NONE', #23510, #7205, #4195, .T. ) ;
#12443=DIRECTION ( 'NONE',  ( 0.000000000000000000, 0.000000000000000000, 1.000000000000000000 ) ) ;
#12447=EDGE_CURVE ( 'NONE', #22240, #11372, #26405, .T. ) ;
#12448=CARTESIAN_POINT ( 'NONE',  ( 16.05277956358234803, 141.0713346807230266, 25.20902801311412844 ) ) ;
#12451=EDGE_CURVE ( 'NONE', #16711, #26886, #18879, .T. ) ;
#12452=DIRECTION ( 'NONE',  ( -0.5914120900931443270, -0.4674599267565393013, 0.6570486713847228932 ) ) ;
#12453=ORIENTED_EDGE ( 'NONE', *, *, #25433, .F. ) ;
#12455=CONICAL_SURFACE ( 'NONE', #24405, 117.6351876552689504, 0.9945805576725580410 ) ;
#12456=VECTOR ( 'NONE', #16627, 1000.000000000000227 ) ;
#12457=CARTESIAN_POINT ( 'NONE',  ( 109.1721716018069515, -0.01706748904931388797, -0.0002019688922687420615 ) ) ;
#12458=AXIS2_PLACEMENT_3D ( 'NONE', #14017, #20639, #3092 ) ;
#12459=EDGE_LOOP ( 'NONE', ( #27007, #22594, #3191, #26051 ) ) ;
#12460=CARTESIAN_POINT ( 'NONE',  ( 1.832998868059890096, -144.2584710144581663, 15.69902610990327574 ) ) ;
#12461=CARTESIAN_POINT ( 'NONE',  ( 16.05277956358208868, -67.56865019683935714, 126.3767940428302552 ) ) ;
#12462=B_SPLINE_CURVE_WITH_KNOTS ( 'NONE', 3,
 ( #27070, #11836, #7107, #7378 ),
 .UNSPECIFIED., .F., .F.,
 ( 4, 4 ),
 ( 3.076313952674417705E-16, 0.01077107486149805025 ),
 .UNSPECIFIED. ) ;
#12464=DIRECTION ( 'NONE',  ( -1.000000000000000000, -0.000000000000000000, -0.000000000000000000 ) ) ;
#12465=CARTESIAN_POINT ( 'NONE',  ( 25.73574536432417403, -46.68445899255561926, 102.8730547980548522 ) ) ;
#12466=CARTESIAN_POINT ( 'NONE',  ( 1.833485406944057594, -108.1939177044919376, -96.69979900902278303 ) ) ;
#12469=CARTESIAN_POINT ( 'NONE',  ( 5.340103556456481826, -143.7310399800115874, -32.90561046456862471 ) ) ;
#12470=CARTESIAN_POINT ( 'NONE',  ( 1.833838850855463720, 85.36536653357504179, -117.3439621615255675 ) ) ;
#12471=CARTESIAN_POINT ( 'NONE',  ( 1.833485406944043827, -107.4794113447402566, -97.49333871408801144 ) ) ;
#12473=ORIENTED_EDGE ( 'NONE', *, *, #8523, .T. ) ;
#12474=ORIENTED_EDGE ( 'NONE', *, *, #16511, .F. ) ;
#12476=CARTESIAN_POINT ( 'NONE',  ( 109.1586900883932856, 0.002995460350188396646, 0.006479576224398257700 ) ) ;
#12477=CARTESIAN_POINT ( 'NONE',  ( 32.73300124599734318, 16.10546300444822165, 116.5274707358856290 ) ) ;
#12478=CARTESIAN_POINT ( 'NONE',  ( 25.86096068574580897, -98.40249579084552067, 55.66087367585372903 ) ) ;
#12481=CARTESIAN_POINT ( 'NONE',  ( -40.00000000000000000, 0.000000000000000000, 0.000000000000000000 ) ) ;
#12482=VERTEX_POINT ( 'NONE', #27932 ) ;
#12485=ORIENTED_EDGE ( 'NONE', *, *, #3812, .F. ) ;
#12486=CARTESIAN_POINT ( 'NONE',  ( 10.93730112725990189, -148.8212007290660495, -26.59437931460901439 ) ) ;
#12487=DIRECTION ( 'NONE',  ( 0.5946245182733607137, 0.002950380665390443108, -0.8039981203473692828 ) ) ;
#12488=CIRCLE ( 'NONE', #21663, 117.6351876552689504 ) ;
#12490=CARTESIAN_POINT ( 'NONE',  ( 2.433796855181219243, -43.58222566461740399, 138.8296532063086772 ) ) ;
#12495=CARTESIAN_POINT ( 'NONE',  ( 109.1624594426973118, -0.01591840958353240090, -0.001206615835669402025 ) ) ;
#12496=CARTESIAN_POINT ( 'NONE',  ( 30.58324630866341209, 108.8243914523538223, -52.76949945162287037 ) ) ;
#12497=ORIENTED_EDGE ( 'NONE', *, *, #8461, .F. ) ;
#12498=CARTESIAN_POINT ( 'NONE',  ( 16.75465622695652712, -91.67104679059826822, -108.7410129416645077 ) ) ;
#12501=AXIS2_PLACEMENT_3D ( 'NONE', #23247, #1203, #25250 ) ;
#12502=CARTESIAN_POINT ( 'NONE',  ( 109.1586059443104944, -0.007068659269321313221, 0.0002768082440288505358 ) ) ;
#12504=CARTESIAN_POINT ( 'NONE',  ( 25.64660436782542163, 75.12017330820604855, -84.29628170537191068 ) ) ;
#12505=CARTESIAN_POINT ( 'NONE',  ( 2.433796855181233454, -74.00833731765476386, -125.2830755159761935 ) ) ;
#12506=EDGE_CURVE ( 'NONE', #23219, #8435, #1674, .T. ) ;
#12507=CARTESIAN_POINT ( 'NONE',  ( 32.73300124599739291, 92.86301839380121237, -72.21147546950456331 ) ) ;
#12508=CARTESIAN_POINT ( 'NONE',  ( 1.833485406944057594, 145.1085452359073429, -0.5339064996889759662 ) ) ;
#12510=EDGE_CURVE ( 'NONE', #6049, #9341, #14725, .T. ) ;
#12511=VERTEX_POINT ( 'NONE', #27804 ) ;
#12512=( BOUNDED_SURFACE ( )  B_SPLINE_SURFACE ( 3, 1, ( 
 ( #16086, #3427 ),
 ( #692, #1126 ),
 ( #25310, #18235 ),
 ( #7324, #2854 ) ),
 .UNSPECIFIED., .F., .F., .F. ) 
 B_SPLINE_SURFACE_WITH_KNOTS ( ( 4, 4 ),
 ( 2, 2 ),
 ( 0.000000000000000000, 1.000000000000000000 ),
 ( 0.000000000000000000, 1.000000000000000000 ),
 .UNSPECIFIED. ) 
 GEOMETRIC_REPRESENTATION_ITEM ( )  RATIONAL_B_SPLINE_SURFACE ( (
 ( 1.000000000000000000, 1.000000000000000000),
 ( 0.9956975270656954757, 0.8568959468854893125),
 ( 0.9956975270656954757, 0.8568959468854893125),
 ( 1.000000000000000000, 1.000000000000000000) ) ) 
 REPRESENTATION_ITEM ( '' )  SURFACE ( )  );
#12513=ORIENTED_EDGE ( 'NONE', *, *, #193, .T. ) ;
#12515=CARTESIAN_POINT ( 'NONE',  ( 109.1592201516379674, 0.002134489919768143857, -0.007566779963325576466 ) ) ;
#12516=CARTESIAN_POINT ( 'NONE',  ( 1.833206310202321498, 84.68961945193613872, -117.8322271314356016 ) ) ;
#12517=CARTESIAN_POINT ( 'NONE',  ( 30.59138290137885008, -105.0379801549012058, 49.72302320601758652 ) ) ;
#12519=CARTESIAN_POINT ( 'NONE',  ( 19.66333377628670576, 72.72773398758388907, -116.9853418557804901 ) ) ;
#12521=ORIENTED_EDGE ( 'NONE', *, *, #15179, .F. ) ;
#12522=CARTESIAN_POINT ( 'NONE',  ( 8.186469829614033245, 118.7566730983347725, 90.56875932797599660 ) ) ;
#12524=DIRECTION ( 'NONE',  ( 0.000000000000000000, 0.000000000000000000, 1.000000000000000000 ) ) ;
#12525=VECTOR ( 'NONE', #10640, 1000.000000000000114 ) ;
#12526=( BOUNDED_SURFACE ( )  B_SPLINE_SURFACE ( 3, 1, ( 
 ( #10850, #6528 ),
 ( #6385, #12426 ),
 ( #12842, #16902 ),
 ( #10434, #6251 ) ),
 .UNSPECIFIED., .F., .F., .F. ) 
 B_SPLINE_SURFACE_WITH_KNOTS ( ( 4, 4 ),
 ( 2, 2 ),
 ( 0.000000000000000000, 1.000000000000000000 ),
 ( 0.000000000000000000, 1.000000000000000000 ),
 .UNSPECIFIED. ) 
 GEOMETRIC_REPRESENTATION_ITEM ( )  RATIONAL_B_SPLINE_SURFACE ( (
 ( 1.000000000000000000, 1.000000000000000000),
 ( 0.6386103224230316178, 0.9954351624131538845),
 ( 0.6386103224230316178, 0.9954351624131538845),
 ( 1.000000000000000000, 1.000000000000000000) ) ) 
 REPRESENTATION_ITEM ( '' )  SURFACE ( )  );
#12527=CARTESIAN_POINT ( 'NONE',  ( 2.063896406836609909, 1.344106060020366256, 145.2631347824382715 ) ) ;
#12528=VECTOR ( 'NONE', #4870, 1000.000000000000114 ) ;
#12529=VERTEX_POINT ( 'NONE', #10811 ) ;
#12531=CARTESIAN_POINT ( 'NONE',  ( 25.64692872815576408, -11.48248630407202775, -112.3258062264003314 ) ) ;
#12532=ORIENTED_EDGE ( 'NONE', *, *, #5243, .F. ) ;
#12537=CARTESIAN_POINT ( 'NONE',  ( 25.98107933586705443, -107.9289867379274597, 33.92073193606549353 ) ) ;
#12538=CARTESIAN_POINT ( 'NONE',  ( 1.832998868059858122, -132.3466930259797891, 59.50898020732465454 ) ) ;
#12539=EDGE_CURVE ( 'NONE', #7054, #15966, #27057, .T. ) ;
#12540=ADVANCED_FACE ( 'NONE', ( #21171 ), #1184, .F. ) ;
#12541=CARTESIAN_POINT ( 'NONE',  ( 2.108393763691196021, -133.2474712570797806, 57.92353377304240070 ) ) ;
#12543=CARTESIAN_POINT ( 'NONE',  ( 109.1721716018069657, -0.008358834333183826765, 0.01488186354166055533 ) ) ;
#12544=ORIENTED_EDGE ( 'NONE', *, *, #12317, .T. ) ;
#12545=CARTESIAN_POINT ( 'NONE',  ( 109.1586900883932856, 0.003481399864227371996, 0.006231977675082120069 ) ) ;
#12548=CARTESIAN_POINT ( 'NONE',  ( 10.93730112726002979, 92.80059208661855052, -119.3442956573263558 ) ) ;
#12549=EDGE_CURVE ( 'NONE', #16536, #12270, #419, .T. ) ;
#12550=CARTESIAN_POINT ( 'NONE',  ( 109.1586059443104944, -0.007068659269322302013, -0.0002768082440195081284 ) ) ;
#12552=CARTESIAN_POINT ( 'NONE',  ( 9.884929003653608603, 132.4189379373580664, -71.59798461011190795 ) ) ;
#12553=FACE_OUTER_BOUND ( 'NONE', #23409, .T. ) ;
#12554=FACE_OUTER_BOUND ( 'NONE', #21023, .T. ) ;
#12555=CARTESIAN_POINT ( 'NONE',  ( 109.1778270068192853, -0.009177562596826690719, 0.001591747944959389944 ) ) ;
#12557=CARTESIAN_POINT ( 'NONE',  ( 26.28373643307407193, -100.6987277884689291, 78.30371666786361118 ) ) ;
#12559=ORIENTED_EDGE ( 'NONE', *, *, #28203, .T. ) ;
#12560=( BOUNDED_SURFACE ( )  B_SPLINE_SURFACE ( 3, 1, ( 
 ( #2409, #13779 ),
 ( #22585, #5151 ),
 ( #15944, #15808 ),
 ( #17676, #26591 ) ),
 .UNSPECIFIED., .F., .F., .F. ) 
 B_SPLINE_SURFACE_WITH_KNOTS ( ( 4, 4 ),
 ( 2, 2 ),
 ( 0.000000000000000000, 1.000000000000000000 ),
 ( 0.000000000000000000, 1.000000000000000000 ),
 .UNSPECIFIED. ) 
 GEOMETRIC_REPRESENTATION_ITEM ( )  RATIONAL_B_SPLINE_SURFACE ( (
 ( 1.000000000000000000, 1.000000000000000000),
 ( 0.9956975270656955868, 0.8568959468854907557),
 ( 0.9956975270656955868, 0.8568959468854907557),
 ( 1.000000000000000000, 1.000000000000000000) ) ) 
 REPRESENTATION_ITEM ( '' )  SURFACE ( )  );
#12561=VERTEX_POINT ( 'NONE', #22159 ) ;
#12563=CARTESIAN_POINT ( 'NONE',  ( 24.22246935314087324, 90.00000000000005684, -40.00000000000000711 ) ) ;
#12567=ORIENTED_EDGE ( 'NONE', *, *, #455, .F. ) ;
#12568=VERTEX_POINT ( 'NONE', #9203 ) ;
#12570=EDGE_CURVE ( 'NONE', #19470, #10229, #20283, .T. ) ;
#12574=ADVANCED_FACE ( 'NONE', ( #24330 ), #9257, .T. ) ;
#12575=CARTESIAN_POINT ( 'NONE',  ( 32.73300124599735739, 55.46353551262010484, 103.7392577722178260 ) ) ;
#12576=CARTESIAN_POINT ( 'NONE',  ( 32.73300124599741423, 115.8010721414085822, -20.69176323058512423 ) ) ;
#12577=ORIENTED_EDGE ( 'NONE', *, *, #7561, .F. ) ;
#12583=CARTESIAN_POINT ( 'NONE',  ( 25.98107933586699403, 90.88151529733809753, 67.37827847766564560 ) ) ;
#12585=CARTESIAN_POINT ( 'NONE',  ( 25.64703792032468499, 91.25955007190310653, -66.48786612795782958 ) ) ;
#12588=ORIENTED_EDGE ( 'NONE', *, *, #2391, .F. ) ;
#12592=AXIS2_PLACEMENT_3D ( 'NONE', #11756, #5413, #14175 ) ;
#12595=CARTESIAN_POINT ( 'NONE',  ( 2.430230287190592531, -142.6294793592095687, -28.83279105684573196 ) ) ;
#12596=ORIENTED_EDGE ( 'NONE', *, *, #9276, .F. ) ;
#12597=CARTESIAN_POINT ( 'NONE',  ( 25.98107933586740614, -45.01656174308500624, -103.7920584735896483 ) ) ;
#12599=EDGE_CURVE ( 'NONE', #18219, #25686, #22285, .T. ) ;
#12600=B_SPLINE_CURVE_WITH_KNOTS ( 'NONE', 3,
 ( #4720, #15937, #13921, #4862 ),
 .UNSPECIFIED., .F., .F.,
 ( 4, 4 ),
 ( 0.000000000000000000, 0.01077107196513801476 ),
 .UNSPECIFIED. ) ;
#12602=EDGE_CURVE ( 'NONE', #17673, #24974, #4069, .T. ) ;
#12603=CARTESIAN_POINT ( 'NONE',  ( 25.64681081121879203, -110.5293738517606954, -23.06870491922435207 ) ) ;
#12604=CARTESIAN_POINT ( 'NONE',  ( 16.05277956358233027, 126.3767940428297578, 67.56865019683868923 ) ) ;
#12606=DIRECTION ( 'NONE',  ( -0.5946245182733608248, 0.6977579871484534957, 0.3994439555666252639 ) ) ;
#12608=CARTESIAN_POINT ( 'NONE',  ( 1.833750490713697445, 125.5350013574269781, 72.78591676343999950 ) ) ;
#12609=CARTESIAN_POINT ( 'NONE',  ( 25.64692872815576052, -97.62272225320907637, -56.73392579406814207 ) ) ;
#12612=ORIENTED_EDGE ( 'NONE', *, *, #755, .T. ) ;
#12613=VERTEX_POINT ( 'NONE', #6630 ) ;
#12614=CARTESIAN_POINT ( 'NONE',  ( 25.64699802086722613, 56.24956056770159307, -97.90265915239973538 ) ) ;
#12615=CARTESIAN_POINT ( 'NONE',  ( 1.832998868059890096, -14.63705790014106789, 144.3700883710216658 ) ) ;
#12618=CARTESIAN_POINT ( 'NONE',  ( 109.1586900883932856, 0.005371970278528643075, 0.004701023939945730111 ) ) ;
#12621=CARTESIAN_POINT ( 'NONE',  ( 10.93730112725972070, -51.37919228020375328, 142.1801301103782293 ) ) ;
#12622=VERTEX_POINT ( 'NONE', #15381 ) ;
#12624=CARTESIAN_POINT ( 'NONE',  ( 1.834118845439484335, 141.9759513273464790, 29.99597360113117972 ) ) ;
#12625=DIRECTION ( 'NONE',  ( 0.000000000000000000, 0.000000000000000000, 1.000000000000000000 ) ) ;
#12627=CARTESIAN_POINT ( 'NONE',  ( 55.79472521941426777, 6.880567342319705126, 72.42790650415577147 ) ) ;
#12628=B_SPLINE_CURVE_WITH_KNOTS ( 'NONE', 3,
 ( #18187, #11434, #2951, #494 ),
 .UNSPECIFIED., .F., .F.,
 ( 4, 4 ),
 ( 3.556521592274814591E-16, 0.01077107486149831393 ),
 .UNSPECIFIED. ) ;
#12630=VERTEX_POINT ( 'NONE', #18118 ) ;
#12631=B_SPLINE_CURVE_WITH_KNOTS ( 'NONE', 3,
 ( #15229, #24048, #6476, #4308 ),
 .UNSPECIFIED., .F., .F.,
 ( 4, 4 ),
 ( 5.059210310009494697E-16, 0.008383748772659972356 ),
 .UNSPECIFIED. ) ;
#12632=B_SPLINE_CURVE_WITH_KNOTS ( 'NONE', 3,
 ( #25449, #21524, #23573, #3968, #3834, #12740 ),
 .UNSPECIFIED., .F., .F.,
 ( 4, 2, 4 ),
 ( 1.389302603484999005E-17, 0.0006311571484586087164, 0.001262314296917203555 ),
 .UNSPECIFIED. ) ;
#12633=CARTESIAN_POINT ( 'NONE',  ( 109.1592201516379674, -0.004867031887010251669, 0.006174480289200302147 ) ) ;
#12634=EDGE_CURVE ( 'NONE', #23136, #5458, #19520, .T. ) ;
#12638=CARTESIAN_POINT ( 'NONE',  ( 1.893872463202018075, 116.8661275359698664, 86.08597552418919463 ) ) ;
#12639=ORIENTED_EDGE ( 'NONE', *, *, #21359, .T. ) ;
#12640=( BOUNDED_SURFACE ( )  B_SPLINE_SURFACE ( 3, 1, ( 
 ( #25679, #7988 ),
 ( #10285, #28087 ),
 ( #27672, #12552 ),
 ( #5953, #21477 ) ),
 .UNSPECIFIED., .F., .F., .F. ) 
 B_SPLINE_SURFACE_WITH_KNOTS ( ( 4, 4 ),
 ( 2, 2 ),
 ( 0.000000000000000000, 1.000000000000000000 ),
 ( 0.000000000000000000, 1.000000000000000000 ),
 .UNSPECIFIED. ) 
 GEOMETRIC_REPRESENTATION_ITEM ( )  RATIONAL_B_SPLINE_SURFACE ( (
 ( 1.000000000000000000, 1.000000000000000000),
 ( 0.6386103224230302855, 0.9954351624131538845),
 ( 0.6386103224230302855, 0.9954351624131538845),
 ( 1.000000000000000000, 1.000000000000000000) ) ) 
 REPRESENTATION_ITEM ( '' )  SURFACE ( )  );
#12641=DIRECTION ( 'NONE',  ( 1.000000000000000000, -0.000000000000000000, -0.000000000000000000 ) ) ;
#12643=CARTESIAN_POINT ( 'NONE',  ( 2.263178607246654206, -116.7985473178708702, 86.59154415224561774 ) ) ;
#12644=CARTESIAN_POINT ( 'NONE',  ( 1.834118845439484335, 30.34413640949891189, -141.9019470378984806 ) ) ;
#12646=CARTESIAN_POINT ( 'NONE',  ( 1.833485406944085350, 132.3460930279899515, -59.50871042846091541 ) ) ;
#12648=CARTESIAN_POINT ( 'NONE',  ( 10.93730112725970827, 42.00474393596263667, 145.2260730187401236 ) ) ;
#12649=B_SPLINE_CURVE_WITH_KNOTS ( 'NONE', 3,
 ( #18867, #7514, #20448, #27639, #7955, #16717 ),
 .UNSPECIFIED., .F., .F.,
 ( 4, 2, 4 ),
 ( 1.964531255190340430E-17, 0.0006311571484586096922, 0.001262314296917200086 ),
 .UNSPECIFIED. ) ;
#12651=CARTESIAN_POINT ( 'NONE',  ( 1.831572820252008738, 132.1614873090348681, 59.92262167723481525 ) ) ;
#12652=CARTESIAN_POINT ( 'NONE',  ( 25.64699802086724389, 34.66526531169786551, -107.4581924007661939 ) ) ;
#12653=EDGE_LOOP ( 'NONE', ( #19666, #19999, #16854, #1760 ) ) ;
#12654=ORIENTED_EDGE ( 'NONE', *, *, #3039, .F. ) ;
#12655=ORIENTED_EDGE ( 'NONE', *, *, #20442, .T. ) ;
#12656=FACE_OUTER_BOUND ( 'NONE', #9080, .T. ) ;
#12657=CARTESIAN_POINT ( 'NONE',  ( 30.58324630866342630, -108.8243914523534670, 52.76949945162356670 ) ) ;
#12659=CARTESIAN_POINT ( 'NONE',  ( 32.73300124599738581, 28.19767303745763698, -114.2056417606545153 ) ) ;
#12661=DIRECTION ( 'NONE',  ( 0.000000000000000000, 0.000000000000000000, 1.000000000000000000 ) ) ;
#12662=CARTESIAN_POINT ( 'NONE',  ( 10.93730112725972781, -56.95489579269845137, 140.0398180619108359 ) ) ;
#12663=ORIENTED_EDGE ( 'NONE', *, *, #26774, .F. ) ;
#12664=CARTESIAN_POINT ( 'NONE',  ( 32.73300124599732186, 0.000000000000000000, 0.000000000000000000 ) ) ;
#12666=CARTESIAN_POINT ( 'NONE',  ( 1.833485406944043827, -107.4794113447415924, 97.49333871408656194 ) ) ;
#12667=B_SPLINE_CURVE_WITH_KNOTS ( 'NONE', 3,
 ( #20490, #13869, #26674, #5233, #11288, #22235 ),
 .UNSPECIFIED., .F., .F.,
 ( 4, 2, 4 ),
 ( 0.000000000000000000, 0.0006311636237756690446, 0.001262327247551338089 ),
 .UNSPECIFIED. ) ;
#12668=CARTESIAN_POINT ( 'NONE',  ( 26.04756280548354042, 1.110889087302504574, 113.1727782765314032 ) ) ;
#12669=CARTESIAN_POINT ( 'NONE',  ( 25.65782528836480481, 65.90345832277473903, 91.69136324939124449 ) ) ;
#12672=CARTESIAN_POINT ( 'NONE',  ( 25.98552792386799482, -97.43552975939651617, 57.50018541500390512 ) ) ;
#12673=VERTEX_POINT ( 'NONE', #998 ) ;
#12674=VERTEX_POINT ( 'NONE', #20988 ) ;
#12677=EDGE_CURVE ( 'NONE', #13373, #7646, #27427, .T. ) ;
#12678=ADVANCED_FACE ( 'NONE', ( #14215 ), #24907, .T. ) ;
#12679=CARTESIAN_POINT ( 'NONE',  ( 25.64699802086725100, -110.4930320910559089, -23.24292564406151129 ) ) ;
#12684=CARTESIAN_POINT ( 'NONE',  ( 109.1624594426973260, 0.008380433676406057533, -0.01358749486988133394 ) ) ;
#12685=DIRECTION ( 'NONE',  ( 0.000000000000000000, 0.000000000000000000, 1.000000000000000000 ) ) ;
#12688=( BOUNDED_SURFACE ( )  B_SPLINE_SURFACE ( 3, 1, ( 
 ( #11528, #598 ),
 ( #24798, #5051 ),
 ( #22637, #20454 ),
 ( #27801, #1454 ) ),
 .UNSPECIFIED., .F., .F., .F. ) 
 B_SPLINE_SURFACE_WITH_KNOTS ( ( 4, 4 ),
 ( 2, 2 ),
 ( 0.000000000000000000, 1.000000000000000000 ),
 ( 0.000000000000000000, 1.000000000000000000 ),
 .UNSPECIFIED. ) 
 GEOMETRIC_REPRESENTATION_ITEM ( )  RATIONAL_B_SPLINE_SURFACE ( (
 ( 1.000000000000000000, 1.000000000000000000),
 ( 0.6386103224230316178, 0.9954351624131538845),
 ( 0.6386103224230316178, 0.9954351624131538845),
 ( 1.000000000000000000, 1.000000000000000000) ) ) 
 REPRESENTATION_ITEM ( '' )  SURFACE ( )  );
#12689=CARTESIAN_POINT ( 'NONE',  ( 109.1586900883932856, -0.006819617742893414360, -0.002109621908814778967 ) ) ;
#12691=CARTESIAN_POINT ( 'NONE',  ( 25.64692232868535626, -11.47740546588710941, 112.3263170481597086 ) ) ;
#12692=CARTESIAN_POINT ( 'NONE',  ( 28.43349137099855284, 102.8504004831932832, 69.71646995966189309 ) ) ;
#12693=FACE_OUTER_BOUND ( 'NONE', #22208, .T. ) ;
#12695=VERTEX_POINT ( 'NONE', #16396 ) ;
#12696=EDGE_CURVE ( 'NONE', #2900, #12695, #10282, .T. ) ;
#12697=ORIENTED_EDGE ( 'NONE', *, *, #16867, .T. ) ;
#12699=CARTESIAN_POINT ( 'NONE',  ( 16.75465622695661239, -39.51671382433843860, -136.6258322711653079 ) ) ;
#12701=ORIENTED_EDGE ( 'NONE', *, *, #16903, .T. ) ;
#12704=ADVANCED_FACE ( 'NONE', ( #9935 ), #16152, .T. ) ;
#12705=EDGE_CURVE ( 'NONE', #11630, #19484, #10967, .T. ) ;
#12707=CARTESIAN_POINT ( 'NONE',  ( 26.11404676487257603, -83.38016054979729574, -76.59696442953277540 ) ) ;
#12708=CARTESIAN_POINT ( 'NONE',  ( 1.834118845439484335, -58.85894970554831218, -132.6369225636079818 ) ) ;
#12709=DIRECTION ( 'NONE',  ( -0.5914120900931443270, -0.8063295922669344584, 0.008020494142993420464 ) ) ;
#12710=CARTESIAN_POINT ( 'NONE',  ( 26.11404676487257603, -10.71016160607490875, -112.7148551500681606 ) ) ;
#12712=CARTESIAN_POINT ( 'NONE',  ( 1.834118845439484335, -72.70910183320481224, -125.5799175751977259 ) ) ;
#12713=CARTESIAN_POINT ( 'NONE',  ( 109.1624594426973260, 0.01033277910988597038, 0.01216903288310111977 ) ) ;
#12715=( BOUNDED_SURFACE ( )  B_SPLINE_SURFACE ( 3, 1, ( 
 ( #12022, #9573 ),
 ( #9872, #18640 ),
 ( #5695, #12432 ),
 ( #24996, #22836 ) ),
 .UNSPECIFIED., .F., .F., .F. ) 
 B_SPLINE_SURFACE_WITH_KNOTS ( ( 4, 4 ),
 ( 2, 2 ),
 ( 0.000000000000000000, 1.000000000000000000 ),
 ( 0.000000000000000000, 1.000000000000000000 ),
 .UNSPECIFIED. ) 
 GEOMETRIC_REPRESENTATION_ITEM ( )  RATIONAL_B_SPLINE_SURFACE ( (
 ( 1.000000000000000000, 1.000000000000000000),
 ( 0.6386103224230302855, 0.9954351624131538845),
 ( 0.6386103224230302855, 0.9954351624131538845),
 ( 1.000000000000000000, 1.000000000000000000) ) ) 
 REPRESENTATION_ITEM ( '' )  SURFACE ( )  );
#12716=EDGE_LOOP ( 'NONE', ( #28431, #2791, #3189, #7869 ) ) ;
#12717=EDGE_LOOP ( 'NONE', ( #227, #16668, #3964, #14086 ) ) ;
#12718=CARTESIAN_POINT ( 'NONE',  ( 26.11404676487257603, -10.71016160607644174, 112.7148551500680185 ) ) ;
#12721=DIRECTION ( 'NONE',  ( 0.000000000000000000, -1.000000000000000000, 0.000000000000000000 ) ) ;
#12722=CARTESIAN_POINT ( 'NONE',  ( 109.1592201516379674, 0.006957642258146918765, -0.003661068210037320397 ) ) ;
#12723=ORIENTED_EDGE ( 'NONE', *, *, #10921, .T. ) ;
#12725=EDGE_CURVE ( 'NONE', #21979, #14003, #15747, .T. ) ;
#12729=ORIENTED_EDGE ( 'NONE', *, *, #22098, .T. ) ;
#12733=ORIENTED_EDGE ( 'NONE', *, *, #19395, .T. ) ;
#12734=B_SPLINE_CURVE_WITH_KNOTS ( 'NONE', 3,
 ( #19074, #14741, #3518, #25703, #18782, #5841, #5982, #20935, #3661, #27849 ),
 .UNSPECIFIED., .F., .F.,
 ( 4, 3, 3, 4 ),
 ( 6.938893903907228378E-18, 0.0002669560319015836392, 0.0005492286108966428632, 0.0008315040496093566071 ),
 .UNSPECIFIED. ) ;
#12736=EDGE_CURVE ( 'NONE', #12813, #6178, #8567, .T. ) ;
#12737=CARTESIAN_POINT ( 'NONE',  ( 1.833485406944043827, -14.63699153649261575, -144.3694338680886347 ) ) ;
#12739=VERTEX_POINT ( 'NONE', #3576 ) ;
#12740=CARTESIAN_POINT ( 'NONE',  ( 2.433796855181233454, -74.00833731765476386, -125.2830755159761935 ) ) ;
#12741=CARTESIAN_POINT ( 'NONE',  ( 119.2224693531408803, -90.00000000000005684, 39.99999999999997158 ) ) ;
#12743=CARTESIAN_POINT ( 'NONE',  ( 9.884929003653626367, -119.2676479132379512, 91.84919534721903744 ) ) ;
#12744=CARTESIAN_POINT ( 'NONE',  ( 6.224689322667630975, 148.0369967195762797, 2.565137105444272425 ) ) ;
#12745=CARTESIAN_POINT ( 'NONE',  ( 109.1587776205901861, 0.007297420966932447080, 0.0006832286435017099514 ) ) ;
#12746=B_SPLINE_CURVE_WITH_KNOTS ( 'NONE', 3,
 ( #13054, #25746, #17092, #28434 ),
 .UNSPECIFIED., .F., .F.,
 ( 4, 4 ),
 ( 0.000000000000000000, 0.01077107196513890641 ),
 .UNSPECIFIED. ) ;
#12747=CARTESIAN_POINT ( 'NONE',  ( 26.11404676487259024, -103.8885755249566643, -45.01677474591514283 ) ) ;
#12748=CARTESIAN_POINT ( 'NONE',  ( 1.832998868059858122, -30.69214149074111475, 141.8272129421607701 ) ) ;
#12749=CARTESIAN_POINT ( 'NONE',  ( 25.64681081121880624, -102.9795863647025556, -46.30456157731431688 ) ) ;
#12750=EDGE_LOOP ( 'NONE', ( #20006, #4137, #25931, #7134 ) ) ;
#12751=ORIENTED_EDGE ( 'NONE', *, *, #20267, .F. ) ;
#12753=CARTESIAN_POINT ( 'NONE',  ( 24.22246935314087324, -90.00000000000005684, -40.00000000000002842 ) ) ;
#12754=CARTESIAN_POINT ( 'NONE',  ( 2.063896406836609909, 144.3268707900449783, -16.52087515463630751 ) ) ;
#12755=CARTESIAN_POINT ( 'NONE',  ( 19.66333377628705747, 64.94841092372186608, 121.4767361208137828 ) ) ;
#12758=CARTESIAN_POINT ( 'NONE',  ( 1.832998868059890096, 125.9352106559983895, 72.09222286251126377 ) ) ;
#12759=ORIENTED_EDGE ( 'NONE', *, *, #7010, .T. ) ;
#12760=CARTESIAN_POINT ( 'NONE',  ( 26.11404676487257603, 12.95861723607603544, -112.4785329405480780 ) ) ;
#12763=CARTESIAN_POINT ( 'NONE',  ( 25.64660436782548203, -55.95243482911462962, 98.07256794792309051 ) ) ;
#12764=ADVANCED_FACE ( 'NONE', ( #15306 ), #19737, .F. ) ;
#12765=ORIENTED_EDGE ( 'NONE', *, *, #18024, .T. ) ;
#12768=EDGE_CURVE ( 'NONE', #15878, #238, #15073, .T. ) ;
#12769=CARTESIAN_POINT ( 'NONE',  ( 2.263178607246644880, -137.8402782326814702, 46.26071628252405077 ) ) ;
#12770=B_SPLINE_CURVE_WITH_KNOTS ( 'NONE', 3,
 ( #27545, #1214, #7035, #23116, #15793, #12014, #7718, #18922 ),
 .UNSPECIFIED., .F., .F.,
 ( 4, 2, 2, 4 ),
 ( 0.000000000000000000, 0.0002429592666046702821, 0.0004859185332093405641, 0.0009718370664186944639 ),
 .UNSPECIFIED. ) ;
#12771=ADVANCED_FACE ( 'NONE', ( #17471 ), #7078, .F. ) ;
#12772=ORIENTED_EDGE ( 'NONE', *, *, #11938, .F. ) ;
#12774=CARTESIAN_POINT ( 'NONE',  ( 10.93730112725990189, -140.0398180619108075, -56.95489579269887059 ) ) ;
#12775=CARTESIAN_POINT ( 'NONE',  ( 25.64692872815575342, 97.62272225320948849, 56.73392579406745284 ) ) ;
#12776=DIRECTION ( 'NONE',  ( 0.000000000000000000, 0.000000000000000000, 1.000000000000000000 ) ) ;
#12779=CARTESIAN_POINT ( 'NONE',  ( 30.59141879584290535, -109.6600586137411284, -38.47120193631578644 ) ) ;
#12782=AXIS2_PLACEMENT_3D ( 'NONE', #9179, #17940, #24608 ) ;
#12783=CARTESIAN_POINT ( 'NONE',  ( 26.04756280548354397, 110.9306483680202859, 22.44333019059037326 ) ) ;
#12784=CONICAL_SURFACE ( 'NONE', #16469, 117.6351876552689504, 0.9945805576725580410 ) ;
#12785=CARTESIAN_POINT ( 'NONE',  ( 32.73300124599740002, 72.21147546950675178, -92.86301839379947864 ) ) ;
#12787=CARTESIAN_POINT ( 'NONE',  ( 2.433796855181233454, -57.85512797797981932, 133.5135467655516095 ) ) ;
#12788=ORIENTED_EDGE ( 'NONE', *, *, #23369, .F. ) ;
#12789=ORIENTED_EDGE ( 'NONE', *, *, #1434, .T. ) ;
#12790=EDGE_LOOP ( 'NONE', ( #14254, #18025, #26479, #13775 ) ) ;
#12791=CARTESIAN_POINT ( 'NONE',  ( 109.1586900883932856, -0.0006456433529069550677, 0.007109207791180748720 ) ) ;
#12793=FACE_OUTER_BOUND ( 'NONE', #12459, .T. ) ;
#12794=CARTESIAN_POINT ( 'NONE',  ( 1.833485406944043827, -97.49333871408619245, -107.4794113447419477 ) ) ;
#12795=CARTESIAN_POINT ( 'NONE',  ( 26.11404676487259024, -92.25884714080363835, -65.63269960453335727 ) ) ;
#12796=CARTESIAN_POINT ( 'NONE',  ( 109.1592201516379674, -0.004368284148525305825, 0.006536841731961986514 ) ) ;
#12797=CARTESIAN_POINT ( 'NONE',  ( 2.063896406836609909, -1.344106060019351734, -145.2631347824382999 ) ) ;
#12798=ORIENTED_EDGE ( 'NONE', *, *, #28203, .F. ) ;
#12799=DIRECTION ( 'NONE',  ( -1.000000000000000000, -0.000000000000000000, -0.000000000000000000 ) ) ;
#12804=DIRECTION ( 'NONE',  ( 0.5946245182733607137, -0.6977579871484591578, 0.3994439555666155495 ) ) ;
#12805=( BOUNDED_SURFACE ( )  B_SPLINE_SURFACE ( 3, 1, ( 
 ( #6208, #23774 ),
 ( #19148, #1716 ),
 ( #17534, #26318 ),
 ( #26180, #19559 ) ),
 .UNSPECIFIED., .F., .F., .F. ) 
 B_SPLINE_SURFACE_WITH_KNOTS ( ( 4, 4 ),
 ( 2, 2 ),
 ( 0.000000000000000000, 1.000000000000000000 ),
 ( 0.000000000000000000, 1.000000000000000000 ),
 .UNSPECIFIED. ) 
 GEOMETRIC_REPRESENTATION_ITEM ( )  RATIONAL_B_SPLINE_SURFACE ( (
 ( 1.000000000000000000, 1.000000000000000000),
 ( 0.9956975270656954757, 0.8568959468854893125),
 ( 0.9956975270656954757, 0.8568959468854893125),
 ( 1.000000000000000000, 1.000000000000000000) ) ) 
 REPRESENTATION_ITEM ( '' )  SURFACE ( )  );
#12806=EDGE_LOOP ( 'NONE', ( #8275, #25209, #6807, #18411, #12862, #13094, #7563, #11284, #27180, #23202, #24687, #26617, #16174, #11204, #22557, #6893, #6143, #19263, #1870, #5964, #25707, #3963, #2776, #2170, #23392, #5406, #10402, #16769, #27006, #8819, #8770, #6784, #1273, #5453, #22420, #13545, #7761, #18181, #21245, #14992, #8500, #22860, #22935, #2140, #25550, #17098, #27688, #10347, #27305, #24332, #173, #12075, #25175, #19769, #8947, #23799, #9998, #6957, #18403, #22082, #19843, #14143, #11952, #2202, #4465, #18648, #24832, #8228, #14026, #26255, #9381, #24609, #20522, #8354, #13495, #10109, #21407, #425, #3102, #25472, #2975, #2072, #24999, #6281, #7171, #5999, #1822, #3307, #10428, #1682, #16803, #5415, #15994, #21399, #6804, #20278, #1379, #27964, #2223, #6021, #22840, #24281, #22317, #20063, #2380, #16437, #8403, #4172, #11878, #12954, #1251, #6129, #20817, #6556, #8745, #8320, #6223, #2613, #8145, #26711, #20741, #17834, #24911, #10114, #13512, #1922, #3270, #16733, #4755, #19706, #10653, #13584, #7801, #27580, #3640, #13825, #8688, #10074, #16055, #2940, #27508, #14863, #1848, #408, #5265, #17667, #14011, #3530, #14140, #1882, #15704, #8995, #21598, #4498, #9939, #2850, #2311, #10996, #4977, #9448, #11723, #22310, #7136, #2014, #9477, #4607, #27368, #23828, #15896, #19930, #14607, #12852, #3679, #13919, #17659, #5229, #556, #10956, #17838, #23385, #16372, #3502, #16542, #3124 ) ) ;
#12807=CARTESIAN_POINT ( 'NONE',  ( 25.64681081121880624, -45.54494737132293380, 103.3177883989777825 ) ) ;
#12811=ADVANCED_FACE ( 'NONE', ( #22083 ), #21600, .F. ) ;
#12813=VERTEX_POINT ( 'NONE', #15027 ) ;
#12814=CIRCLE ( 'NONE', #20141, 117.6351876552689504 ) ;
#12816=CARTESIAN_POINT ( 'NONE',  ( 2.430230287190581429, 98.44218333480918659, -107.1617224697454276 ) ) ;
#12817=CARTESIAN_POINT ( 'NONE',  ( 30.59138290137910943, 66.10404757334188730, -95.58039132682482375 ) ) ;
#12818=DIRECTION ( 'NONE',  ( 0.000000000000000000, 0.000000000000000000, 1.000000000000000000 ) ) ;
#12819=CARTESIAN_POINT ( 'NONE',  ( 10.93730112726003156, 97.44200844886434254, -115.5857507957695276 ) ) ;
#12821=CARTESIAN_POINT ( 'NONE',  ( 1.833838850855476377, 59.10274688032031776, -132.5281727421680387 ) ) ;
#12822=CARTESIAN_POINT ( 'NONE',  ( 1.893872463202080692, -0.9528309182407600497, 145.1467500857187360 ) ) ;
#12824=CARTESIAN_POINT ( 'NONE',  ( 10.93730112725932635, 0.000000000000000000, 0.000000000000000000 ) ) ;
#12826=CARTESIAN_POINT ( 'NONE',  ( 1.833838848569419477, -141.9757689770219997, -29.99593366454900334 ) ) ;
#12827=ADVANCED_FACE ( 'NONE', ( #23424 ), #12917, .T. ) ;
#12829=CARTESIAN_POINT ( 'NONE',  ( 109.1624594426973260, -0.006914244825461735369, 0.01438905500501224191 ) ) ;
#12833=CARTESIAN_POINT ( 'NONE',  ( 26.04756280548355818, -24.61655718144259808, -110.4687147111162631 ) ) ;
#12835=ORIENTED_EDGE ( 'NONE', *, *, #15318, .T. ) ;
#12837=ORIENTED_EDGE ( 'NONE', *, *, #4323, .F. ) ;
#12838=CARTESIAN_POINT ( 'NONE',  ( 1.833485406944043827, 137.8414413349085521, 45.34878176254281357 ) ) ;
#12839=CARTESIAN_POINT ( 'NONE',  ( 2.433796855181219243, -144.5536872373193376, 16.65276281464516828 ) ) ;
#12841=( BOUNDED_SURFACE ( )  B_SPLINE_SURFACE ( 3, 1, ( 
 ( #10797, #13082 ),
 ( #15226, #8494 ),
 ( #24178, #21581 ),
 ( #1852, #10656 ) ),
 .UNSPECIFIED., .F., .F., .F. ) 
 B_SPLINE_SURFACE_WITH_KNOTS ( ( 4, 4 ),
 ( 2, 2 ),
 ( 0.000000000000000000, 1.000000000000000000 ),
 ( 0.000000000000000000, 1.000000000000000000 ),
 .UNSPECIFIED. ) 
 GEOMETRIC_REPRESENTATION_ITEM ( )  RATIONAL_B_SPLINE_SURFACE ( (
 ( 1.000000000000000000, 1.000000000000000000),
 ( 0.9956975270656955868, 0.8568959468854907557),
 ( 0.9956975270656955868, 0.8568959468854907557),
 ( 1.000000000000000000, 1.000000000000000000) ) ) 
 REPRESENTATION_ITEM ( '' )  SURFACE ( )  );
#12842=CARTESIAN_POINT ( 'NONE',  ( 109.1624594426973260, -0.01591840958352309932, 0.001206615835671121352 ) ) ;
#12844=LINE ( 'NONE', #28243, #6569 ) ;
#12845=CARTESIAN_POINT ( 'NONE',  ( 32.73300124599735739, 20.69176323058628597, 115.8010721414084543 ) ) ;
#12848=CARTESIAN_POINT ( 'NONE',  ( 109.1586059443104944, 0.003127959656220996847, 0.006344953511159737332 ) ) ;
#12852=ORIENTED_EDGE ( 'NONE', *, *, #11120, .T. ) ;
#12853=CARTESIAN_POINT ( 'NONE',  ( 2.263178113027065397, 133.3897502891102533, -57.85473702513737493 ) ) ;
#12854=CARTESIAN_POINT ( 'NONE',  ( 28.37644542392833813, 34.54617949428102008, 119.4444529625692581 ) ) ;
#12855=AXIS2_PLACEMENT_3D ( 'NONE', #17237, #27902, #8337 ) ;
#12856=DIRECTION ( 'NONE',  ( 0.5946245182733607137, 0.7332888028688904214, 0.3297108033645291814 ) ) ;
#12857=CARTESIAN_POINT ( 'NONE',  ( 2.433796855181233454, 96.28145139437833677, -109.1007109081216129 ) ) ;
#12858=EDGE_LOOP ( 'NONE', ( #22351, #11947, #17885, #17681 ) ) ;
#12860=DIRECTION ( 'NONE',  ( -1.000000000000000000, -0.000000000000000000, -0.000000000000000000 ) ) ;
#12862=ORIENTED_EDGE ( 'NONE', *, *, #14534, .T. ) ;
#12863=ORIENTED_EDGE ( 'NONE', *, *, #6493, .F. ) ;
#12864=B_SPLINE_CURVE_WITH_KNOTS ( 'NONE', 3,
 ( #5727, #25155, #16508, #5573, #14626, #12053 ),
 .UNSPECIFIED., .F., .F.,
 ( 4, 2, 4 ),
 ( 1.964531255190340430E-17, 0.0006311571484586177153, 0.001262314296917215915 ),
 .UNSPECIFIED. ) ;
#12867=ORIENTED_EDGE ( 'NONE', *, *, #14293, .F. ) ;
#12870=AXIS2_PLACEMENT_3D ( 'NONE', #2744, #24927, #5189 ) ;
#12875=( BOUNDED_SURFACE ( )  B_SPLINE_SURFACE ( 3, 1, ( 
 ( #3919, #10126 ),
 ( #23511, #10280 ),
 ( #25942, #27947 ),
 ( #23800, #6359 ) ),
 .UNSPECIFIED., .F., .F., .F. ) 
 B_SPLINE_SURFACE_WITH_KNOTS ( ( 4, 4 ),
 ( 2, 2 ),
 ( 0.000000000000000000, 1.000000000000000000 ),
 ( 0.000000000000000000, 1.000000000000000000 ),
 .UNSPECIFIED. ) 
 GEOMETRIC_REPRESENTATION_ITEM ( )  RATIONAL_B_SPLINE_SURFACE ( (
 ( 1.000000000000000000, 1.000000000000000000),
 ( 0.6386103224230316178, 0.9954351624131538845),
 ( 0.6386103224230316178, 0.9954351624131538845),
 ( 1.000000000000000000, 1.000000000000000000) ) ) 
 REPRESENTATION_ITEM ( '' )  SURFACE ( )  );
#12876=AXIS2_PLACEMENT_3D ( 'NONE', #3340, #21032, #1186 ) ;
#12877=ADVANCED_FACE ( 'NONE', ( #12186 ), #15702, .F. ) ;
#12878=DIRECTION ( 'NONE',  ( -1.000000000000000000, -0.000000000000000000, -0.000000000000000000 ) ) ;
#12879=CARTESIAN_POINT ( 'NONE',  ( 25.87036335909425233, -107.2165474610297196, 35.87755773825682581 ) ) ;
#12881=LINE ( 'NONE', #17210, #930 ) ;
#12884=CARTESIAN_POINT ( 'NONE',  ( 26.11404676487257603, 102.9690087468801352, 47.08215554553553517 ) ) ;
#12886=FACE_OUTER_BOUND ( 'NONE', #12858, .T. ) ;
#12887=EDGE_CURVE ( 'NONE', #27587, #13373, #12336, .T. ) ;
#12888=VERTEX_POINT ( 'NONE', #6006 ) ;
#12890=CARTESIAN_POINT ( 'NONE',  ( 10.93730112725936721, 145.2260730187397542, 42.00474393596321931 ) ) ;
#12892=CARTESIAN_POINT ( 'NONE',  ( 55.49584447822657296, 58.85239198729187393, 42.42793568432977480 ) ) ;
#12893=DIRECTION ( 'NONE',  ( 0.5946245182733607137, 0.1700465163848252637, -0.7858154137795714256 ) ) ;
#12895=CARTESIAN_POINT ( 'NONE',  ( 2.430230287190592531, 74.01081053031100510, 125.2872625092164895 ) ) ;
#12897=ADVANCED_FACE ( 'NONE', ( #14764 ), #12939, .F. ) ;
#12898=ORIENTED_EDGE ( 'NONE', *, *, #19204, .F. ) ;
#12902=DIRECTION ( 'NONE',  ( 0.000000000000000000, 0.000000000000000000, 1.000000000000000000 ) ) ;
#12906=CARTESIAN_POINT ( 'NONE',  ( 109.1586059443104944, 0.006856640434643072185, -0.001740416220259429674 ) ) ;
#12909=CARTESIAN_POINT ( 'NONE',  ( 1.894214914920961723, -29.24491455759036995, 142.1734439042097051 ) ) ;
#12910=B_SPLINE_CURVE_WITH_KNOTS ( 'NONE', 3,
 ( #15767, #26698, #18202, #26978, #13313, #7287 ),
 .UNSPECIFIED., .F., .F.,
 ( 4, 2, 4 ),
 ( 9.875766617722657020E-18, 0.0006311571484586050301, 0.001262314296917200953 ),
 .UNSPECIFIED. ) ;
#12911=ORIENTED_EDGE ( 'NONE', *, *, #3535, .F. ) ;
#12912=CARTESIAN_POINT ( 'NONE',  ( 25.69398547355839924, 65.78402800526286853, -91.80679989327076385 ) ) ;
#12913=DIRECTION ( 'NONE',  ( 0.5914120900931444380, 0.5938529060132621273, 0.5455001977188111972 ) ) ;
#12914=CARTESIAN_POINT ( 'NONE',  ( 25.64700659047695552, 97.67001118499099732, 56.65258046470288633 ) ) ;
#12915=CARTESIAN_POINT ( 'NONE',  ( 109.1586900883932856, -0.0001010081143884653671, 0.007137750914552287197 ) ) ;
#12917=CONICAL_SURFACE ( 'NONE', #13850, 117.6351876552689504, 0.9945805576725580410 ) ;
#12918=B_SPLINE_CURVE_WITH_KNOTS ( 'NONE', 3,
 ( #11431, #15895, #640, #24402 ),
 .UNSPECIFIED., .F., .F.,
 ( 4, 4 ),
 ( 0.000000000000000000, 0.008383560773332715543 ),
 .UNSPECIFIED. ) ;
#12923=EDGE_CURVE ( 'NONE', #20744, #18597, #6525, .T. ) ;
#12925=B_SPLINE_CURVE_WITH_KNOTS ( 'NONE', 3,
 ( #1812, #19241, #10351, #21266, #10611, #27885 ),
 .UNSPECIFIED., .F., .F.,
 ( 4, 2, 4 ),
 ( 6.952433221959954168E-18, 0.0006311571484586114269, 0.001262314296917216132 ),
 .UNSPECIFIED. ) ;
#12927=CARTESIAN_POINT ( 'NONE',  ( 109.1624594426973118, -0.01438905500501942193, 0.006914244825467924863 ) ) ;
#12928=CARTESIAN_POINT ( 'NONE',  ( 8.186469829614365423, -71.65198613712890108, -131.0413692472661467 ) ) ;
#12929=CARTESIAN_POINT ( 'NONE',  ( 32.73300124599739291, -99.90245962373785460, -62.10906484417343165 ) ) ;
#12932=ADVANCED_FACE ( 'NONE', ( #10985 ), #18841, .F. ) ;
#12934=CARTESIAN_POINT ( 'NONE',  ( 25.64681081121879203, 112.2483031020013442, 12.21581276189844800 ) ) ;
#12937=CARTESIAN_POINT ( 'NONE',  ( 6.224689322667647851, -141.5842213414010473, -43.30635742325521420 ) ) ;
#12939=( BOUNDED_SURFACE ( )  B_SPLINE_SURFACE ( 3, 1, ( 
 ( #8678, #8970 ),
 ( #26095, #2617 ),
 ( #4489, #28377 ),
 ( #11267, #17731 ) ),
 .UNSPECIFIED., .F., .F., .F. ) 
 B_SPLINE_SURFACE_WITH_KNOTS ( ( 4, 4 ),
 ( 2, 2 ),
 ( 0.000000000000000000, 1.000000000000000000 ),
 ( 0.000000000000000000, 1.000000000000000000 ),
 .UNSPECIFIED. ) 
 GEOMETRIC_REPRESENTATION_ITEM ( )  RATIONAL_B_SPLINE_SURFACE ( (
 ( 1.000000000000000000, 1.000000000000000000),
 ( 0.6386103224230316178, 0.9954351624131538845),
 ( 0.6386103224230316178, 0.9954351624131538845),
 ( 1.000000000000000000, 1.000000000000000000) ) ) 
 REPRESENTATION_ITEM ( '' )  SURFACE ( )  );
#12940=CARTESIAN_POINT ( 'NONE',  ( 32.73300124599735739, -28.19767303745682341, 114.2056417606547285 ) ) ;
#12941=CARTESIAN_POINT ( 'NONE',  ( 16.75465622695656265, -141.8562168210795278, 10.24707101927994657 ) ) ;
#12942=VERTEX_POINT ( 'NONE', #22209 ) ;
#12944=CARTESIAN_POINT ( 'NONE',  ( 30.59138290137886784, -115.8270707793589906, -9.457588828076334053 ) ) ;
#12946=B_SPLINE_CURVE_WITH_KNOTS ( 'NONE', 3,
 ( #9394, #17995, #7369, #18277, #26922, #448, #3052, #16137 ),
 .UNSPECIFIED., .F., .F.,
 ( 4, 2, 2, 4 ),
 ( 0.000000000000000000, 0.0002429592666046677884, 0.0004859185332093355768, 0.0009718370664186791767 ),
 .UNSPECIFIED. ) ;
#12947=FACE_OUTER_BOUND ( 'NONE', #28238, .T. ) ;
#12948=ORIENTED_EDGE ( 'NONE', *, *, #619, .F. ) ;
#12949=CARTESIAN_POINT ( 'NONE',  ( 1.893872463202028955, 43.94661640106022560, 138.3372034345892416 ) ) ;
#12950=CARTESIAN_POINT ( 'NONE',  ( 25.64681081121879203, -12.21581276189731469, -112.2483031020014579 ) ) ;
#12951=ORIENTED_EDGE ( 'NONE', *, *, #6081, .F. ) ;
#12952=B_SPLINE_CURVE_WITH_KNOTS ( 'NONE', 3,
 ( #26146, #6437, #15768, #4265, #17499, #15335 ),
 .UNSPECIFIED., .F., .F.,
 ( 4, 2, 4 ),
 ( 1.436393986538261525E-17, 0.0006311636237756931139, 0.001262327247551371916 ),
 .UNSPECIFIED. ) ;
#12953=ORIENTED_EDGE ( 'NONE', *, *, #25489, .T. ) ;
#12954=ORIENTED_EDGE ( 'NONE', *, *, #5207, .T. ) ;
#12956=DIRECTION ( 'NONE',  ( 0.5946245182733607137, 0.2512550613902226337, -0.7637359336799396381 ) ) ;
#12957=CARTESIAN_POINT ( 'NONE',  ( 0.000000000000000000, 0.000000000000000000, 0.000000000000000000 ) ) ;
#12960=CARTESIAN_POINT ( 'NONE',  ( 109.1778270068192853, 0.0003511581237513579715, 0.009307953841270271214 ) ) ;
#12962=EDGE_CURVE ( 'NONE', #2563, #6704, #15384, .T. ) ;
#12963=CIRCLE ( 'NONE', #16657, 151.1787379149930359 ) ;
#12964=ORIENTED_EDGE ( 'NONE', *, *, #21012, .T. ) ;
#12966=CARTESIAN_POINT ( 'NONE',  ( 1.833750490713712322, -44.58740205676232193, -138.0897889879343552 ) ) ;
#12967=EDGE_CURVE ( 'NONE', #5567, #20545, #17778, .T. ) ;
#12968=CARTESIAN_POINT ( 'NONE',  ( 2.108393763691216893, -1.280847988472779697, 145.2872457912031905 ) ) ;
#12974=VECTOR ( 'NONE', #17112, 1000.000000000000227 ) ;
#12976=CARTESIAN_POINT ( 'NONE',  ( -40.00000000000000000, 0.000000000000000000, 0.000000000000000000 ) ) ;
#12977=CARTESIAN_POINT ( 'NONE',  ( 32.73300124599732186, 0.000000000000000000, 0.000000000000000000 ) ) ;
#12978=CARTESIAN_POINT ( 'NONE',  ( 13.36082413113061307, 127.3428651193259640, -84.67697637120282650 ) ) ;
#12980=ORIENTED_EDGE ( 'NONE', *, *, #11374, .F. ) ;
#12982=CARTESIAN_POINT ( 'NONE',  ( 10.93730112725999248, 42.00474393596446987, -145.2260730187398110 ) ) ;
#12983=B_SPLINE_CURVE_WITH_KNOTS ( 'NONE', 3,
 ( #21528, #25997, #4395, #21821, #10884, #15173, #23994, #4110 ),
 .UNSPECIFIED., .F., .F.,
 ( 4, 2, 2, 4 ),
 ( 1.734723475976807094E-18, 0.0002429588503611240324, 0.0004859177007222463302, 0.0009718354014444961298 ),
 .UNSPECIFIED. ) ;
#12984=ORIENTED_EDGE ( 'NONE', *, *, #8815, .F. ) ;
#12988=ORIENTED_EDGE ( 'NONE', *, *, #10305, .F. ) ;
#12989=ORIENTED_EDGE ( 'NONE', *, *, #12388, .T. ) ;
#12990=AXIS2_PLACEMENT_3D ( 'NONE', #1579, #25635, #5066 ) ;
#12991=ADVANCED_FACE ( 'NONE', ( #19476 ), #11854, .F. ) ;
#12992=VECTOR ( 'NONE', #21474, 1000.000000000000114 ) ;
#12994=CARTESIAN_POINT ( 'NONE',  ( 1.834118845439484335, 45.01070051384772341, -137.9527673765101099 ) ) ;
#12995=EDGE_CURVE ( 'NONE', #12174, #7268, #19175, .T. ) ;
#12998=CARTESIAN_POINT ( 'NONE',  ( 2.430230287190581429, 116.8646894862412182, 86.70145658344696926 ) ) ;
#12999=DIRECTION ( 'NONE',  ( -1.000000000000000000, -0.000000000000000000, -0.000000000000000000 ) ) ;
#13000=CARTESIAN_POINT ( 'NONE',  ( 25.64670758986459376, 23.96231489925043334, -110.3390515846396056 ) ) ;
#13002=CARTESIAN_POINT ( 'NONE',  ( 9.884929003653608603, -141.8132360130354357, -50.49804566712268894 ) ) ;
#13005=EDGE_LOOP ( 'NONE', ( #10650, #17, #26148, #4701 ) ) ;
#13006=DIRECTION ( 'NONE',  ( 0.000000000000000000, 0.000000000000000000, 1.000000000000000000 ) ) ;
#13008=CARTESIAN_POINT ( 'NONE',  ( 25.69398547355841700, 22.75551036952080253, -110.6264597420657765 ) ) ;
#13009=CARTESIAN_POINT ( 'NONE',  ( 109.1721716018069657, 0.01699510305644695227, 0.001583175916620114046 ) ) ;
#13011=CARTESIAN_POINT ( 'NONE',  ( 5.340103556456546663, 146.8647350107031855, -13.12023871800969310 ) ) ;
#13015=CARTESIAN_POINT ( 'NONE',  ( 1.893872463202048495, 117.9862474593107891, -84.54426271294305195 ) ) ;
#13016=CARTESIAN_POINT ( 'NONE',  ( 26.28373643307402574, -88.40064398364015119, -91.96212244992481999 ) ) ;
#13018=EDGE_LOOP ( 'NONE', ( #2033, #11720, #8405, #14309 ) ) ;
#13019=FACE_OUTER_BOUND ( 'NONE', #1514, .T. ) ;
#13020=CARTESIAN_POINT ( 'NONE',  ( 25.64681081121879203, 107.2555980796241215, 35.28660243342585545 ) ) ;
#13023=ADVANCED_FACE ( 'NONE', ( #5356 ), #22716, .F. ) ;
#13026=ORIENTED_EDGE ( 'NONE', *, *, #4130, .F. ) ;
#13029=CARTESIAN_POINT ( 'NONE',  ( 26.11404676487259024, 76.59696442953192275, 83.38016054979810576 ) ) ;
#13031=CARTESIAN_POINT ( 'NONE',  ( 109.1778270068192853, -0.008646067828082863033, -0.003465086990435458942 ) ) ;
#13033=B_SPLINE_CURVE_WITH_KNOTS ( 'NONE', 3,
 ( #3170, #26761, #9376, #7218 ),
 .UNSPECIFIED., .F., .F.,
 ( 4, 4 ),
 ( 0.000000000000000000, 0.01077107196513867222 ),
 .UNSPECIFIED. ) ;
#13034=DIRECTION ( 'NONE',  ( 0.5914120900931443270, 0.4101107478122118510, -0.6942916636548122078 ) ) ;
#13036=CARTESIAN_POINT ( 'NONE',  ( 26.11404676487257603, -110.5078194225159223, -24.64483677384961879 ) ) ;
#13037=CARTESIAN_POINT ( 'NONE',  ( 25.64681081121879203, -45.54494737132156246, -103.3177883989783936 ) ) ;
#13038=CARTESIAN_POINT ( 'NONE',  ( 55.49584447822657296, -72.55110015779771970, 0.2676470673954122192 ) ) ;
#13040=EDGE_LOOP ( 'NONE', ( #14612, #20546, #27289, #14582 ) ) ;
#13042=CARTESIAN_POINT ( 'NONE',  ( 28.43349137099853152, 119.3601175884732299, 34.52178142065567101 ) ) ;
#13045=CARTESIAN_POINT ( 'NONE',  ( 119.2224693531408803, 90.00000000000005684, 39.99999999999999289 ) ) ;
#13051=FACE_OUTER_BOUND ( 'NONE', #18335, .T. ) ;
#13054=CARTESIAN_POINT ( 'NONE',  ( 10.93730112726003156, 115.5857507957718440, -97.44200844886164248 ) ) ;
#13055=ORIENTED_EDGE ( 'NONE', *, *, #17942, .F. ) ;
#13056=FACE_OUTER_BOUND ( 'NONE', #10225, .T. ) ;
#13057=ADVANCED_FACE ( 'NONE', ( #20751 ), #1913, .F. ) ;
#13058=CARTESIAN_POINT ( 'NONE',  ( 1.833485406944043827, 14.63699153649552365, -144.3694338680883789 ) ) ;
#13059=CARTESIAN_POINT ( 'NONE',  ( 2.108985857320904600, -60.26444811757312436, -132.2056553747751195 ) ) ;
#13060=ADVANCED_FACE ( 'NONE', ( #752 ), #25663, .F. ) ;
#13061=B_SPLINE_CURVE_WITH_KNOTS ( 'NONE', 3,
 ( #19366, #21389, #23719, #14766 ),
 .UNSPECIFIED., .F., .F.,
 ( 4, 4 ),
 ( 3.324202758929661745E-16, 0.01077107486149808495 ),
 .UNSPECIFIED. ) ;
#13062=ORIENTED_EDGE ( 'NONE', *, *, #26125, .F. ) ;
#13063=DIRECTION ( 'NONE',  ( -1.000000000000000000, 0.000000000000000000, 0.000000000000000000 ) ) ;
#13065=CARTESIAN_POINT ( 'NONE',  ( 26.11404676487257603, 65.63269960453364149, -92.25884714080342519 ) ) ;
#13066=CARTESIAN_POINT ( 'NONE',  ( 2.433796855181233454, 144.8571464219889151, 13.76554153471742481 ) ) ;
#13068=EDGE_CURVE ( 'NONE', #7628, #23299, #13696, .T. ) ;
#13070=CARTESIAN_POINT ( 'NONE',  ( 2.263178607246703056, 132.2496131833837012, -60.41552769843686121 ) ) ;
#13071=CARTESIAN_POINT ( 'NONE',  ( 1.833485406944057594, -138.1714136985305572, -44.33323125130066700 ) ) ;
#13073=CARTESIAN_POINT ( 'NONE',  ( 1.833838850855476155, -132.6005571022083700, 58.94016894581421440 ) ) ;
#13076=CARTESIAN_POINT ( 'NONE',  ( 2.433796855181205476, -71.49415740224986848, -126.7346379669263001 ) ) ;
#13078=EDGE_LOOP ( 'NONE', ( #3614, #25834, #23111, #6833 ) ) ;
#13082=CARTESIAN_POINT ( 'NONE',  ( 1.832998868059858122, 15.69902610990566849, -144.2584710144578821 ) ) ;
#13083=CARTESIAN_POINT ( 'NONE',  ( 109.1778270068192853, -0.007736698406806062980, 0.005186985107080914308 ) ) ;
#13084=CARTESIAN_POINT ( 'NONE',  ( 32.73300124599738581, -39.98094346392232268, -110.6325518752277759 ) ) ;
#13085=CARTESIAN_POINT ( 'NONE',  ( 25.64681081121879203, -91.59071981940525120, -66.03065707439029097 ) ) ;
#13089=FACE_OUTER_BOUND ( 'NONE', #8949, .T. ) ;
#13090=FACE_OUTER_BOUND ( 'NONE', #4405, .T. ) ;
#13093=ADVANCED_FACE ( 'NONE', ( #614, #9405 ), #14981, .T. ) ;
#13094=ORIENTED_EDGE ( 'NONE', *, *, #21290, .F. ) ;
#13095=CARTESIAN_POINT ( 'NONE',  ( 1.833691583653537682, -108.0753610255259360, 96.83253123394176498 ) ) ;
#13097=VERTEX_POINT ( 'NONE', #14419 ) ;
#13098=ADVANCED_FACE ( 'NONE', ( #7977 ), #27484, .F. ) ;
#13099=B_SPLINE_CURVE_WITH_KNOTS ( 'NONE', 3,
 ( #17750, #22072, #4660, #4506, #26666, #24249, #13285 ),
 .UNSPECIFIED., .F., .F.,
 ( 4, 3, 4 ),
 ( 5.935087083004135664E-16, 0.02816610861753244752, 0.04000277880656274987 ),
 .UNSPECIFIED. ) ;
#13100=ORIENTED_EDGE ( 'NONE', *, *, #5940, .F. ) ;
#13105=CARTESIAN_POINT ( 'NONE',  ( 109.1778270068192853, 0.003210287141653799838, 0.008743876326162606724 ) ) ;
#13109=CARTESIAN_POINT ( 'NONE',  ( 55.79472521941426777, 59.28412330436359667, -42.17269936297579136 ) ) ;
#13112=CARTESIAN_POINT ( 'NONE',  ( 10.93730112725932635, 0.000000000000000000, 0.000000000000000000 ) ) ;
#13115=DIRECTION ( 'NONE',  ( -0.000000000000000000, -0.000000000000000000, 1.000000000000000000 ) ) ;
#13118=CARTESIAN_POINT ( 'NONE',  ( 99.22246935314079508, 69.99999999999998579, -40.00000000000000711 ) ) ;
#13119=LINE ( 'NONE', #1892, #2426 ) ;
#13120=CARTESIAN_POINT ( 'NONE',  ( 2.433796855181219243, 142.0211193075560061, -31.67151202412830813 ) ) ;
#13121=ORIENTED_EDGE ( 'NONE', *, *, #23837, .F. ) ;
#13122=ORIENTED_EDGE ( 'NONE', *, *, #22436, .T. ) ;
#13123=CARTESIAN_POINT ( 'NONE',  ( 109.1586900883932856, 0.007137750914550311347, -0.0001010081143976270922 ) ) ;
#13125=EDGE_CURVE ( 'NONE', #11630, #2861, #14844, .T. ) ;
#13126=ORIENTED_EDGE ( 'NONE', *, *, #19306, .F. ) ;
#13128=CARTESIAN_POINT ( 'NONE',  ( 109.1586059443104944, 0.003774052605966631002, 0.005983234375914163114 ) ) ;
#13129=EDGE_CURVE ( 'NONE', #27960, #25020, #2320, .T. ) ;
#13130=B_SPLINE_CURVE_WITH_KNOTS ( 'NONE', 3,
 ( #767, #16018, #11562, #22813 ),
 .UNSPECIFIED., .F., .F.,
 ( 4, 4 ),
 ( 1.962615573354718958E-17, 0.008383560773332712074 ),
 .UNSPECIFIED. ) ;
#13131=EDGE_CURVE ( 'NONE', #24385, #28456, #26702, .T. ) ;
#13134=FACE_OUTER_BOUND ( 'NONE', #8256, .T. ) ;
#13137=CARTESIAN_POINT ( 'NONE',  ( 25.64703792032472052, -110.4127989088531336, 23.62108504469209436 ) ) ;
#13138=CARTESIAN_POINT ( 'NONE',  ( 2.263178607246671525, 60.41552769843821125, 132.2496131833831328 ) ) ;
#13139=CARTESIAN_POINT ( 'NONE',  ( 55.49584447822657296, 66.38758986585156663, -29.26468316696706751 ) ) ;
#13140=CARTESIAN_POINT ( 'NONE',  ( 10.93730112726003156, 108.9902118373755684, -104.7670965581001781 ) ) ;
#13141=VERTEX_POINT ( 'NONE', #25936 ) ;
#13144=FACE_OUTER_BOUND ( 'NONE', #28232, .T. ) ;
#13146=CARTESIAN_POINT ( 'NONE',  ( 32.73300124599735739, 75.82012867748483131, 89.94078864464094636 ) ) ;
#13147=FACE_OUTER_BOUND ( 'NONE', #18642, .T. ) ;
#13153=ORIENTED_EDGE ( 'NONE', *, *, #11122, .F. ) ;
#13154=ORIENTED_EDGE ( 'NONE', *, *, #24088, .F. ) ;
#13156=CARTESIAN_POINT ( 'NONE',  ( 109.1586900883932856, -0.001385221016536901904, -0.007002774699553655259 ) ) ;
#13157=ORIENTED_EDGE ( 'NONE', *, *, #20035, .T. ) ;
#13158=CARTESIAN_POINT ( 'NONE',  ( 5.340103579038085080, 120.6284720963485029, 84.79482754232307684 ) ) ;
#13159=VERTEX_POINT ( 'NONE', #19034 ) ;
#13160=CARTESIAN_POINT ( 'NONE',  ( 1.831572820252008738, -138.3111855986063858, 43.90210991190574674 ) ) ;
#13161=ORIENTED_EDGE ( 'NONE', *, *, #15688, .F. ) ;
#13162=CARTESIAN_POINT ( 'NONE',  ( 2.430230287190592531, -118.5711603495675632, -84.35270093935378100 ) ) ;
#13163=LINE ( 'NONE', #12741, #25352 ) ;
#13165=CARTESIAN_POINT ( 'NONE',  ( 109.1586900883932856, -0.002109621908814847055, 0.006819617742893393543 ) ) ;
#13167=CARTESIAN_POINT ( 'NONE',  ( 32.73300124599738581, -114.2056417606545864, -28.19767303745721065 ) ) ;
#13170=CARTESIAN_POINT ( 'NONE',  ( 94.22246935314088034, -151.1871800109700246, -6.938893903907228378E-15 ) ) ;
#13171=CARTESIAN_POINT ( 'NONE',  ( 21.16825799904933803, 130.1008673867299876, 37.62905626541736126 ) ) ;
#13174=CARTESIAN_POINT ( 'NONE',  ( 109.1778270068192853, 0.009220257877172552408, 0.001322180554006217911 ) ) ;
#13175=CARTESIAN_POINT ( 'NONE',  ( 1.833206310202336820, -125.2945016693816598, 73.19872434058744659 ) ) ;
#13176=EDGE_CURVE ( 'NONE', #28263, #8520, #5136, .T. ) ;
#13177=ORIENTED_EDGE ( 'NONE', *, *, #22844, .F. ) ;
#13178=ADVANCED_FACE ( 'NONE', ( #12131 ), #4872, .F. ) ;
#13179=B_SPLINE_CURVE_WITH_KNOTS ( 'NONE', 3,
 ( #4584, #24183, #2417, #11352, #15508, #26186, #22153, #6905 ),
 .UNSPECIFIED., .F., .F.,
 ( 4, 2, 2, 4 ),
 ( 0.000000000000000000, 0.0002429588503611127567, 0.0004859177007222255135, 0.0009718354014444878898 ),
 .UNSPECIFIED. ) ;
#13181=CARTESIAN_POINT ( 'NONE',  ( 25.64681081121879203, -91.59071981940616070, 66.03065707438906884 ) ) ;
#13182=CARTESIAN_POINT ( 'NONE',  ( 10.93730112725990367, -92.80059208661606363, -119.3442956573281748 ) ) ;
#13183=EDGE_CURVE ( 'NONE', #10454, #3000, #19719, .T. ) ;
#13184=ORIENTED_EDGE ( 'NONE', *, *, #19493, .F. ) ;
#13186=CARTESIAN_POINT ( 'NONE',  ( 109.1778270068192853, 0.001591747944966651496, -0.009177562596833053685 ) ) ;
#13187=CARTESIAN_POINT ( 'NONE',  ( 1.833485406944043827, -97.49333871408762775, 107.4794113447406119 ) ) ;
#13188=ORIENTED_EDGE ( 'NONE', *, *, #7970, .F. ) ;
#13189=CARTESIAN_POINT ( 'NONE',  ( 10.93730112725994275, -36.23586118136433498, -146.7718404940647190 ) ) ;
#13190=CARTESIAN_POINT ( 'NONE',  ( 25.64660436782558861, 65.89729635303032751, -91.68669413043076588 ) ) ;
#13191=EDGE_LOOP ( 'NONE', ( #7701, #28473, #15142, #10843 ) ) ;
#13192=CARTESIAN_POINT ( 'NONE',  ( 25.64708010899968116, 103.1273237223355750, -45.97512510001799768 ) ) ;
#13196=LINE ( 'NONE', #4424, #22793 ) ;
#13197=CARTESIAN_POINT ( 'NONE',  ( 10.93730112725997294, 26.59437931460951177, -148.8212007290660210 ) ) ;
#13199=B_SPLINE_CURVE_WITH_KNOTS ( 'NONE', 3,
 ( #19796, #89, #26423, #6722, #15469, #22406, #26845 ),
 .UNSPECIFIED., .F., .F.,
 ( 4, 3, 4 ),
 ( 0.000000000000000000, 0.02398743853561364353, 0.04000277880656225027 ),
 .UNSPECIFIED. ) ;
#13201=CARTESIAN_POINT ( 'NONE',  ( 13.36082413113061307, 97.52406103376755198, 117.7941133658641917 ) ) ;
#13202=CARTESIAN_POINT ( 'NONE',  ( 24.22246935314087324, 70.00000000000004263, 39.99999999999999289 ) ) ;
#13205=EDGE_CURVE ( 'NONE', #21575, #18167, #9278, .T. ) ;
#13206=ORIENTED_EDGE ( 'NONE', *, *, #11221, .F. ) ;
#13208=CARTESIAN_POINT ( 'NONE',  ( 32.73300124599741423, -92.86301839379967760, -72.21147546950645335 ) ) ;
#13209=DIRECTION ( 'NONE',  ( 0.5946245182733608248, 0.6487139525627683145, 0.4749651461092318505 ) ) ;
#13210=CARTESIAN_POINT ( 'NONE',  ( 109.1586900883932856, 0.005236795036860546551, -0.004851151255037378096 ) ) ;
#13211=CARTESIAN_POINT ( 'NONE',  ( 2.063896406836609909, 60.31174178979808431, 132.1577797566308163 ) ) ;
#13212=CARTESIAN_POINT ( 'NONE',  ( 1.833750490713643266, 72.78591676344139216, -125.5350013574263244 ) ) ;
#13213=CARTESIAN_POINT ( 'NONE',  ( 5.340103556456522682, -43.36842540065395468, -140.9275371673311952 ) ) ;
#13215=ORIENTED_EDGE ( 'NONE', *, *, #10630, .F. ) ;
#13216=DIRECTION ( 'NONE',  ( -1.000000000000000000, -0.000000000000000000, -0.000000000000000000 ) ) ;
#13217=VECTOR ( 'NONE', #5335, 1000.000000000000114 ) ;
#13219=CARTESIAN_POINT ( 'NONE',  ( 25.98107933586718943, -113.1286487641200722, -1.091357942391775637 ) ) ;
#13221=CARTESIAN_POINT ( 'NONE',  ( 1.833838850093517658, 1.769966374633376447E-14, 145.1097630783160923 ) ) ;
#13222=CARTESIAN_POINT ( 'NONE',  ( 9.884929003653626367, 148.0628878137280537, 27.17402761732395433 ) ) ;
#13223=ORIENTED_EDGE ( 'NONE', *, *, #26093, .T. ) ;
#13224=CARTESIAN_POINT ( 'NONE',  ( 1.833838850093465700, -107.8375672471888294, 97.09738632348999943 ) ) ;
#13225=B_SPLINE_CURVE_WITH_KNOTS ( 'NONE', 3,
 ( #21845, #11322, #15201, #13059, #8892, #24153 ),
 .UNSPECIFIED., .F., .F.,
 ( 4, 2, 4 ),
 ( 1.389302603484999005E-17, 0.0006311571484586102343, 0.001262314296917207241 ),
 .UNSPECIFIED. ) ;
#13226=CARTESIAN_POINT ( 'NONE',  ( 1.833809397773873417, -117.2915757704551396, -85.43729755723271069 ) ) ;
#13230=CARTESIAN_POINT ( 'NONE',  ( 2.430230287190572103, 109.1043569252027083, -96.28466919683991421 ) ) ;
#13231=CARTESIAN_POINT ( 'NONE',  ( 13.36082413113063083, 129.1512766091132676, -81.89226687791952486 ) ) ;
#13232=CARTESIAN_POINT ( 'NONE',  ( 109.1721716018069657, -0.003350975118864069589, 0.01673651515803013454 ) ) ;
#13234=EDGE_LOOP ( 'NONE', ( #10701, #8379, #16284, #7241 ) ) ;
#13235=CARTESIAN_POINT ( 'NONE',  ( 1.833838850093465034, 72.55488452980864622, 125.6687394363099628 ) ) ;
#13239=CARTESIAN_POINT ( 'NONE',  ( 55.49584447822657296, 66.38758986585115451, 29.26468316696795569 ) ) ;
#13243=CARTESIAN_POINT ( 'NONE',  ( 25.64681081121879203, -75.24277141833549365, 84.18689316040023130 ) ) ;
#13251=VECTOR ( 'NONE', #8190, 1000.000000000000114 ) ;
#13252=LINE ( 'NONE', #304, #18037 ) ;
#13253=EDGE_CURVE ( 'NONE', #25791, #26744, #23926, .T. ) ;
#13256=VERTEX_POINT ( 'NONE', #15529 ) ;
#13261=VERTEX_POINT ( 'NONE', #23797 ) ;
#13263=( BOUNDED_SURFACE ( )  B_SPLINE_SURFACE ( 3, 1, ( 
 ( #11963, #20739 ),
 ( #9665, #5341 ),
 ( #7521, #23826 ),
 ( #6127, #2052 ) ),
 .UNSPECIFIED., .F., .F., .F. ) 
 B_SPLINE_SURFACE_WITH_KNOTS ( ( 4, 4 ),
 ( 2, 2 ),
 ( 0.000000000000000000, 1.000000000000000000 ),
 ( 0.000000000000000000, 1.000000000000000000 ),
 .UNSPECIFIED. ) 
 GEOMETRIC_REPRESENTATION_ITEM ( )  RATIONAL_B_SPLINE_SURFACE ( (
 ( 1.000000000000000000, 1.000000000000000000),
 ( 0.9956975270656954757, 0.8568959468854893125),
 ( 0.9956975270656954757, 0.8568959468854893125),
 ( 1.000000000000000000, 1.000000000000000000) ) ) 
 REPRESENTATION_ITEM ( '' )  SURFACE ( )  );
#13265=CARTESIAN_POINT ( 'NONE',  ( 1.833206310202334155, -145.1075835704899930, 0.7447039688720614725 ) ) ;
#13266=CARTESIAN_POINT ( 'NONE',  ( 109.1592201516379674, -0.007856029051022764623, 0.0003082430542016628347 ) ) ;
#13267=CARTESIAN_POINT ( 'NONE',  ( 25.64681081121879203, -107.2555980796238657, -35.28660243342658731 ) ) ;
#13269=CARTESIAN_POINT ( 'NONE',  ( 25.64703792032467433, 66.48786612795875328, 91.25955007190242441 ) ) ;
#13270=B_SPLINE_CURVE_WITH_KNOTS ( 'NONE', 3,
 ( #16649, #21662, #27995, #23570, #18948, #1525, #1792 ),
 .UNSPECIFIED., .F., .F.,
 ( 4, 3, 4 ),
 ( 6.242136742649753700E-16, 0.02816610861753246833, 0.04000277880656282620 ),
 .UNSPECIFIED. ) ;
#13272=EDGE_CURVE ( 'NONE', #3393, #16069, #26261, .T. ) ;
#13273=CARTESIAN_POINT ( 'NONE',  ( 55.79472521941426777, -54.55111121764116433, 48.13855120843864910 ) ) ;
#13274=B_SPLINE_CURVE_WITH_KNOTS ( 'NONE', 3,
 ( #9053, #9482, #20257, #24614, #6759, #22440, #404, #13781 ),
 .UNSPECIFIED., .F., .F.,
 ( 4, 2, 2, 4 ),
 ( 0.000000000000000000, 0.0002429588503611127025, 0.0004859177007222254051, 0.0009718354014444663142 ),
 .UNSPECIFIED. ) ;
#13275=CARTESIAN_POINT ( 'NONE',  ( 25.98552792386800192, -65.62435323276234556, 92.15963349013344441 ) ) ;
#13278=ORIENTED_EDGE ( 'NONE', *, *, #13601, .T. ) ;
#13280=CARTESIAN_POINT ( 'NONE',  ( 2.063896406836605024, 108.8509294491477846, -96.20114399516289438 ) ) ;
#13283=CARTESIAN_POINT ( 'NONE',  ( 2.433796855181205476, 96.28145139437683042, 109.1007109081229345 ) ) ;
#13285=CARTESIAN_POINT ( 'NONE',  ( 32.73300124599735739, -110.6325518752276622, 39.98094346392273479 ) ) ;
#13287=CARTESIAN_POINT ( 'NONE',  ( 1.833485406944043827, 145.1085452359073145, 0.5339064996889848480 ) ) ;
#13290=B_SPLINE_CURVE_WITH_KNOTS ( 'NONE', 3,
 ( #12950, #28068, #1457, #10398, #10670, #25657, #5797, #21745, #12531, #10813 ),
 .UNSPECIFIED., .F., .F.,
 ( 4, 3, 3, 4 ),
 ( 8.673617379884035472E-18, 0.0002669560319015772424, 0.0005492286108966412369, 0.0008315040496093445725 ),
 .UNSPECIFIED. ) ;
#13296=CARTESIAN_POINT ( 'NONE',  ( 109.1587776205901577, -0.004240403845337402736, -0.005978137617714210199 ) ) ;
#13297=ORIENTED_EDGE ( 'NONE', *, *, #15965, .F. ) ;
#13298=B_SPLINE_CURVE_WITH_KNOTS ( 'NONE', 3,
 ( #28430, #24279, #24579, #24144 ),
 .UNSPECIFIED., .F., .F.,
 ( 4, 4 ),
 ( 0.0005339083821128836910, 0.001067817517169162081 ),
 .UNSPECIFIED. ) ;
#13299=CARTESIAN_POINT ( 'NONE',  ( 1.833721034905666736, 97.36162733017710025, 107.5990973104326258 ) ) ;
#13300=( BOUNDED_SURFACE ( )  B_SPLINE_SURFACE ( 3, 1, ( 
 ( #12278, #18755 ),
 ( #25540, #23380 ),
 ( #14437, #27385 ),
 ( #3358, #3631 ) ),
 .UNSPECIFIED., .F., .F., .F. ) 
 B_SPLINE_SURFACE_WITH_KNOTS ( ( 4, 4 ),
 ( 2, 2 ),
 ( 0.000000000000000000, 1.000000000000000000 ),
 ( 0.000000000000000000, 1.000000000000000000 ),
 .UNSPECIFIED. ) 
 GEOMETRIC_REPRESENTATION_ITEM ( )  RATIONAL_B_SPLINE_SURFACE ( (
 ( 1.000000000000000000, 1.000000000000000000),
 ( 0.6386103224230302855, 0.9954351624131538845),
 ( 0.6386103224230302855, 0.9954351624131538845),
 ( 1.000000000000000000, 1.000000000000000000) ) ) 
 REPRESENTATION_ITEM ( '' )  SURFACE ( )  );
#13305=EDGE_CURVE ( 'NONE', #16995, #14040, #24738, .T. ) ;
#13308=EDGE_CURVE ( 'NONE', #7877, #23571, #2361, .T. ) ;
#13310=CARTESIAN_POINT ( 'NONE',  ( 30.59138290137891047, -70.47507990428499625, -92.40465044710811071 ) ) ;
#13313=CARTESIAN_POINT ( 'NONE',  ( 2.263178607246682628, 1.401567185706472207, 145.3892423243864300 ) ) ;
#13314=CARTESIAN_POINT ( 'NONE',  ( 109.1721716018069515, 0.01567407524361261531, -0.006757465437533811958 ) ) ;
#13316=CARTESIAN_POINT ( 'NONE',  ( 1.831572820252008738, 58.11906524360477988, 132.9644823688597342 ) ) ;
#13317=CARTESIAN_POINT ( 'NONE',  ( 1.831572820252009626, 138.3111855986061300, 43.90210991190668466 ) ) ;
#13319=CARTESIAN_POINT ( 'NONE',  ( 109.1592201516379674, 0.002913740842103182058, -0.007302213399787563404 ) ) ;
#13320=ORIENTED_EDGE ( 'NONE', *, *, #14464, .F. ) ;
#13322=CARTESIAN_POINT ( 'NONE',  ( 109.1586900883932856, -0.002810909342011641554, -0.006561743627143320871 ) ) ;
#13323=VECTOR ( 'NONE', #3539, 1000.000000000000227 ) ;
#13324=VECTOR ( 'NONE', #27727, 1000.000000000000000 ) ;
#13326=EDGE_CURVE ( 'NONE', #7205, #16763, #13033, .T. ) ;
#13328=CARTESIAN_POINT ( 'NONE',  ( 10.93730112725932635, 0.000000000000000000, 0.000000000000000000 ) ) ;
#13330=FACE_OUTER_BOUND ( 'NONE', #25466, .T. ) ;
#13331=EDGE_CURVE ( 'NONE', #19518, #7680, #17817, .T. ) ;
#13333=LINE ( 'NONE', #25902, #12525 ) ;
#13334=CARTESIAN_POINT ( 'NONE',  ( 1.894214914920954174, -138.3376769255506247, -43.94587946447545335 ) ) ;
#13335=CARTESIAN_POINT ( 'NONE',  ( 24.01988960052067057, -94.47404045191566979, -90.81495976423880734 ) ) ;
#13336=CARTESIAN_POINT ( 'NONE',  ( 25.64699802086724745, 110.4930320910560511, 23.24292564406076522 ) ) ;
#13338=EDGE_LOOP ( 'NONE', ( #8104, #22677, #10697, #26471 ) ) ;
#13339=CARTESIAN_POINT ( 'NONE',  ( 1.832998868059858122, 45.34898734666050757, 137.8420662456171897 ) ) ;
#13340=( BOUNDED_SURFACE ( )  B_SPLINE_SURFACE ( 3, 1, ( 
 ( #16404, #16969 ),
 ( #16703, #18708 ),
 ( #25191, #14666 ),
 ( #7649, #3450 ) ),
 .UNSPECIFIED., .F., .F., .F. ) 
 B_SPLINE_SURFACE_WITH_KNOTS ( ( 4, 4 ),
 ( 2, 2 ),
 ( 0.000000000000000000, 1.000000000000000000 ),
 ( 0.000000000000000000, 1.000000000000000000 ),
 .UNSPECIFIED. ) 
 GEOMETRIC_REPRESENTATION_ITEM ( )  RATIONAL_B_SPLINE_SURFACE ( (
 ( 1.000000000000000000, 1.000000000000000000),
 ( 0.9956975270656954757, 0.8568959468854893125),
 ( 0.9956975270656954757, 0.8568959468854893125),
 ( 1.000000000000000000, 1.000000000000000000) ) ) 
 REPRESENTATION_ITEM ( '' )  SURFACE ( )  );
#13342=CARTESIAN_POINT ( 'NONE',  ( 109.1778270068192853, 0.008743876326162637949, -0.003210287141653713969 ) ) ;
#13344=ORIENTED_EDGE ( 'NONE', *, *, #21904, .F. ) ;
#13345=VERTEX_POINT ( 'NONE', #2588 ) ;
#13347=CARTESIAN_POINT ( 'NONE',  ( 1.893872463202012524, -43.94661640105923794, -138.3372034345896395 ) ) ;
#13348=CARTESIAN_POINT ( 'NONE',  ( 25.64699802086724745, 75.72889180797122322, 83.75009658924024336 ) ) ;
#13349=CIRCLE ( 'NONE', #18412, 151.1787379149930359 ) ;
#13351=FACE_OUTER_BOUND ( 'NONE', #17968, .T. ) ;
#13352=CARTESIAN_POINT ( 'NONE',  ( 25.69398547355838858, 46.61500694509645371, 102.8740393624595413 ) ) ;
#13355=CARTESIAN_POINT ( 'NONE',  ( 1.831572820252009626, 132.1614873090357207, -59.92262167723306021 ) ) ;
#13357=CARTESIAN_POINT ( 'NONE',  ( 109.1778270068192853, 0.006489198140359531998, 0.006682187084648931116 ) ) ;
#13358=CARTESIAN_POINT ( 'NONE',  ( 26.11404676487257603, -74.91683232330916553, -84.89295829319569009 ) ) ;
#13359=FACE_OUTER_BOUND ( 'NONE', #19340, .T. ) ;
#13362=CARTESIAN_POINT ( 'NONE',  ( 1.833603222531958954, -117.1340888386543782, -85.65285110156258952 ) ) ;
#13369=EDGE_CURVE ( 'NONE', #14908, #9272, #10316, .T. ) ;
#13370=CARTESIAN_POINT ( 'NONE',  ( 10.93730112725936188, 148.8212007290658505, 26.59437931460817595 ) ) ;
#13372=EDGE_CURVE ( 'NONE', #25292, #18738, #27095, .T. ) ;
#13373=VERTEX_POINT ( 'NONE', #14528 ) ;
#13376=VERTEX_POINT ( 'NONE', #14669 ) ;
#13377=CARTESIAN_POINT ( 'NONE',  ( 28.37599760073041466, 105.5302221302112713, -45.02094138570479487 ) ) ;
#13378=ORIENTED_EDGE ( 'NONE', *, *, #20466, .F. ) ;
#13380=CARTESIAN_POINT ( 'NONE',  ( 32.73300124599734318, 113.0038235389602477, 32.68291970228275289 ) ) ;
#13384=CARTESIAN_POINT ( 'NONE',  ( 2.430230287190589422, -144.8619874886005903, -13.76600171652792248 ) ) ;
#13385=CARTESIAN_POINT ( 'NONE',  ( 1.831572820252009626, -45.77972211429720062, -137.7011124121622174 ) ) ;
#13387=CARTESIAN_POINT ( 'NONE',  ( 94.22246935314088034, -151.1871800109700246, -6.938893903907228378E-15 ) ) ;
#13389=FACE_OUTER_BOUND ( 'NONE', #4390, .T. ) ;
#13391=CARTESIAN_POINT ( 'NONE',  ( 1.833485406944057594, -44.33323125130021225, 138.1714136985306993 ) ) ;
#13392=CARTESIAN_POINT ( 'NONE',  ( 109.1624594426973118, 0.005372302061316064012, 0.01503296564241279366 ) ) ;
#13394=AXIS2_PLACEMENT_3D ( 'NONE', #14106, #16427, #15987 ) ;
#13396=CARTESIAN_POINT ( 'NONE',  ( 25.64660436782547137, 24.04259444204660667, 110.3216080362391125 ) ) ;
#13400=EDGE_LOOP ( 'NONE', ( #10946, #1040, #7426, #11059 ) ) ;
#13401=ORIENTED_EDGE ( 'NONE', *, *, #7834, .T. ) ;
#13404=EDGE_CURVE ( 'NONE', #16492, #27099, #16462, .T. ) ;
#13405=EDGE_CURVE ( 'NONE', #20253, #16608, #1358, .T. ) ;
#13406=B_SPLINE_CURVE_WITH_KNOTS ( 'NONE', 3,
 ( #17006, #1327, #3348, #12272 ),
 .UNSPECIFIED., .F., .F.,
 ( 4, 4 ),
 ( 3.805030037801212946E-16, 0.01077107486149793923 ),
 .UNSPECIFIED. ) ;
#13408=EDGE_CURVE ( 'NONE', #27092, #12372, #19925, .T. ) ;
#13409=CARTESIAN_POINT ( 'NONE',  ( 2.063896406836605024, 125.1295119249439125, 73.79559738457795959 ) ) ;
#13411=VECTOR ( 'NONE', #14430, 1000.000000000000227 ) ;
#13412=EDGE_CURVE ( 'NONE', #12630, #13718, #8931, .T. ) ;
#13417=CARTESIAN_POINT ( 'NONE',  ( 25.64699802086726521, -110.3941571196682077, 23.70809581152572676 ) ) ;
#13421=EDGE_LOOP ( 'NONE', ( #1522, #12227, #2334, #22721 ) ) ;
#13422=LINE ( 'NONE', #17745, #24027 ) ;
#13425=CARTESIAN_POINT ( 'NONE',  ( 25.64681081121879203, 46.30456157731328659, 102.9795863647030103 ) ) ;
#13426=CARTESIAN_POINT ( 'NONE',  ( 25.73574536432414206, 0.8061344836384856105, -112.9674920590232858 ) ) ;
#13427=CARTESIAN_POINT ( 'NONE',  ( 10.93730112726006354, 150.7858122213665126, -10.89264110824830034 ) ) ;
#13428=ORIENTED_EDGE ( 'NONE', *, *, #13176, .T. ) ;
#13440=CARTESIAN_POINT ( 'NONE',  ( 1.833838848569403046, -97.22964245509687942, -107.7184832843406497 ) ) ;
#13442=EDGE_LOOP ( 'NONE', ( #25817, #17182, #3760, #4890 ) ) ;
#13443=EDGE_CURVE ( 'NONE', #7969, #11307, #339, .T. ) ;
#13444=B_SPLINE_CURVE_WITH_KNOTS ( 'NONE', 3,
 ( #622, #9412, #18164, #26942, #13138, #24819 ),
 .UNSPECIFIED., .F., .F.,
 ( 4, 2, 4 ),
 ( 0.000000000000000000, 0.0006311571484586015607, 0.001262314296917203121 ),
 .UNSPECIFIED. ) ;
#13445=B_SPLINE_CURVE_WITH_KNOTS ( 'NONE', 3,
 ( #21508, #14746, #16918, #10447, #17189, #1645, #19347, #17044 ),
 .UNSPECIFIED., .F., .F.,
 ( 4, 2, 2, 4 ),
 ( 3.469446951953614189E-18, 0.0002429588503611212677, 0.0004859177007222390660, 0.0009718354014444785657 ),
 .UNSPECIFIED. ) ;
#13448=EDGE_CURVE ( 'NONE', #24062, #6049, #7559, .T. ) ;
#13450=CARTESIAN_POINT ( 'NONE',  ( 25.64681081121879203, 110.5293738517608375, 23.06870491922360245 ) ) ;
#13452=CARTESIAN_POINT ( 'NONE',  ( 24.01988960052044320, 108.4726924928710190, -73.52806416353990926 ) ) ;
#13454=FACE_OUTER_BOUND ( 'NONE', #22705, .T. ) ;
#13457=CARTESIAN_POINT ( 'NONE',  ( 10.93730112725939030, 140.0398180619108075, 56.95489579269806057 ) ) ;
#13460=CIRCLE ( 'NONE', #23138, 117.6351876552689504 ) ;
#13461=CARTESIAN_POINT ( 'NONE',  ( 1.832998868059890096, -145.1092030902949830, 0.5339089137742853985 ) ) ;
#13463=DIRECTION ( 'NONE',  ( -0.5914120900931443270, 0.8027508043202534749, 0.07630783613001089483 ) ) ;
#13465=ORIENTED_EDGE ( 'NONE', *, *, #23582, .T. ) ;
#13466=CARTESIAN_POINT ( 'NONE',  ( 1.833838848569417257, -44.67212175381932582, 138.0625820091623837 ) ) ;
#13468=CARTESIAN_POINT ( 'NONE',  ( 21.16825799904930605, 83.13600836828977947, 106.9139171613925470 ) ) ;
#13469=CARTESIAN_POINT ( 'NONE',  ( 25.64699802086724389, 110.3941571196683924, -23.70809581152500911 ) ) ;
#13470=EDGE_LOOP ( 'NONE', ( #13122, #8293, #14196, #3138 ) ) ;
#13471=CARTESIAN_POINT ( 'NONE',  ( 109.1586059443104944, 0.006570129623060872066, -0.002622205828288707002 ) ) ;
#13474=B_SPLINE_CURVE_WITH_KNOTS ( 'NONE', 3,
 ( #16218, #26999, #22725, #2690, #5138, #9171, #7175 ),
 .UNSPECIFIED., .F., .F.,
 ( 4, 3, 4 ),
 ( 6.702613243490674079E-16, 0.02816610861753246139, 0.04000277880656292334 ),
 .UNSPECIFIED. ) ;
#13475=CARTESIAN_POINT ( 'NONE',  ( 109.1592201516379674, 0.006957642258146918765, -0.003661068210037320397 ) ) ;
#13477=ADVANCED_FACE ( 'NONE', ( #27626 ), #24733, .F. ) ;
#13479=ORIENTED_EDGE ( 'NONE', *, *, #19499, .F. ) ;
#13480=CARTESIAN_POINT ( 'NONE',  ( 26.04756280548353686, 112.4366864265129493, -12.93458011762360549 ) ) ;
#13481=VECTOR ( 'NONE', #24690, 1000.000000000000114 ) ;
#13482=EDGE_CURVE ( 'NONE', #28480, #4329, #15752, .T. ) ;
#13484=DIRECTION ( 'NONE',  ( 0.000000000000000000, 0.000000000000000000, 1.000000000000000000 ) ) ;
#13485=VERTEX_POINT ( 'NONE', #9951 ) ;
#13487=CARTESIAN_POINT ( 'NONE',  ( 24.22246935314087324, 0.000000000000000000, 0.000000000000000000 ) ) ;
#13488=CARTESIAN_POINT ( 'NONE',  ( 19.66333377628696510, -121.4767361208140812, 64.94841092372145397 ) ) ;
#13489=LINE ( 'NONE', #22283, #6100 ) ;
#13491=CARTESIAN_POINT ( 'NONE',  ( 109.1586059443104944, 0.002447596125905588706, -0.006637156007973989483 ) ) ;
#13492=VERTEX_POINT ( 'NONE', #6462 ) ;
#13493=CARTESIAN_POINT ( 'NONE',  ( 26.11404676487257603, 57.58742681967449784, 97.48350837663630841 ) ) ;
#13494=CARTESIAN_POINT ( 'NONE',  ( 10.93730112725990011, -150.7858122213662000, -10.89264110825150489 ) ) ;
#13495=ORIENTED_EDGE ( 'NONE', *, *, #5176, .T. ) ;
#13498=CARTESIAN_POINT ( 'NONE',  ( 32.73300124599732186, 0.000000000000000000, 0.000000000000000000 ) ) ;
#13499=CARTESIAN_POINT ( 'NONE',  ( 25.64681081121879203, 102.9795863647028682, 46.30456157731362765 ) ) ;
#13505=ORIENTED_EDGE ( 'NONE', *, *, #11302, .T. ) ;
#13506=CARTESIAN_POINT ( 'NONE',  ( 2.433796855181233454, 31.67151202412969724, 142.0211193075556935 ) ) ;
#13508=CARTESIAN_POINT ( 'NONE',  ( 109.1586900883932856, -0.007002774699553647453, -0.001385221016527435301 ) ) ;
#13509=CARTESIAN_POINT ( 'NONE',  ( 109.1721716018069657, 0.003746085893652563534, 0.01665253177026231046 ) ) ;
#13511=CARTESIAN_POINT ( 'NONE',  ( 109.1721716018069657, 0.01488186354166047033, 0.008358834333183975951 ) ) ;
#13512=ORIENTED_EDGE ( 'NONE', *, *, #9897, .T. ) ;
#13513=CARTESIAN_POINT ( 'NONE',  ( 1.832998868059890096, 72.09222286251085166, 125.9352106559986026 ) ) ;
#13516=CARTESIAN_POINT ( 'NONE',  ( 109.1586900883932856, -0.003481399864227418834, -0.006231977675082094915 ) ) ;
#13517=B_SPLINE_CURVE_WITH_KNOTS ( 'NONE', 3,
 ( #8543, #19479, #26098, #21496 ),
 .UNSPECIFIED., .F., .F.,
 ( 4, 4 ),
 ( 3.213376974838984927E-16, 0.01077107486149750729 ),
 .UNSPECIFIED. ) ;
#13519=EDGE_LOOP ( 'NONE', ( #22228, #24620, #8822, #15701 ) ) ;
#13520=EDGE_CURVE ( 'NONE', #7273, #3933, #21212, .T. ) ;
#13521=ORIENTED_EDGE ( 'NONE', *, *, #2627, .F. ) ;
#13523=DIRECTION ( 'NONE',  ( -0.5914120900931443270, 0.5938529060132731185, -0.5455001977187993178 ) ) ;
#13524=( BOUNDED_SURFACE ( )  B_SPLINE_SURFACE ( 3, 1, ( 
 ( #24231, #28374 ),
 ( #21781, #4635 ),
 ( #181, #4488 ),
 ( #4210, #11266 ) ),
 .UNSPECIFIED., .F., .F., .F. ) 
 B_SPLINE_SURFACE_WITH_KNOTS ( ( 4, 4 ),
 ( 2, 2 ),
 ( 0.000000000000000000, 1.000000000000000000 ),
 ( 0.000000000000000000, 1.000000000000000000 ),
 .UNSPECIFIED. ) 
 GEOMETRIC_REPRESENTATION_ITEM ( )  RATIONAL_B_SPLINE_SURFACE ( (
 ( 1.000000000000000000, 1.000000000000000000),
 ( 0.9956975270656954757, 0.8568959468854893125),
 ( 0.9956975270656954757, 0.8568959468854893125),
 ( 1.000000000000000000, 1.000000000000000000) ) ) 
 REPRESENTATION_ITEM ( '' )  SURFACE ( )  );
#13525=CARTESIAN_POINT ( 'NONE',  ( 25.64681081121879203, -23.06870491922242650, -110.5293738517610933 ) ) ;
#13528=CARTESIAN_POINT ( 'NONE',  ( 1.833485406944043827, 141.8265699653867387, 30.69200235378984232 ) ) ;
#13529=CARTESIAN_POINT ( 'NONE',  ( 1.833206308920067862, -142.0914675761164858, 29.44113170198502161 ) ) ;
#13530=ORIENTED_EDGE ( 'NONE', *, *, #21056, .F. ) ;
#13531=ORIENTED_EDGE ( 'NONE', *, *, #9562, .T. ) ;
#13533=CARTESIAN_POINT ( 'NONE',  ( 25.64692872815577473, -45.63107645358261522, -103.2799065540888677 ) ) ;
#13534=CARTESIAN_POINT ( 'NONE',  ( 2.433796855181205476, 96.28145139437683042, 109.1007109081229345 ) ) ;
#13535=CARTESIAN_POINT ( 'NONE',  ( 2.430230287190572103, 1.451610819319782308, -145.5073573687466535 ) ) ;
#13541=CARTESIAN_POINT ( 'NONE',  ( 109.1592201516379674, -0.007748443302134891582, -0.001331853079201365982 ) ) ;
#13544=EDGE_CURVE ( 'NONE', #25020, #3000, #5497, .T. ) ;
#13545=ORIENTED_EDGE ( 'NONE', *, *, #19740, .F. ) ;
#13548=CARTESIAN_POINT ( 'NONE',  ( 28.37599760073042177, -22.09615888373874526, -112.5845136272808134 ) ) ;
#13550=ORIENTED_EDGE ( 'NONE', *, *, #19225, .F. ) ;
#13551=ADVANCED_FACE ( 'NONE', ( #19680 ), #10932, .F. ) ;
#13552=EDGE_LOOP ( 'NONE', ( #17331, #582, #26056, #5580 ) ) ;
#13553=VERTEX_POINT ( 'NONE', #114 ) ;
#13555=CARTESIAN_POINT ( 'NONE',  ( 1.832998868059858122, -108.1944082009163850, 96.70023740551087599 ) ) ;
#13556=( BOUNDED_SURFACE ( )  B_SPLINE_SURFACE ( 3, 1, ( 
 ( #23669, #8252 ),
 ( #1330, #25805 ),
 ( #27952, #1748 ),
 ( #16751, #1476 ) ),
 .UNSPECIFIED., .F., .F., .F. ) 
 B_SPLINE_SURFACE_WITH_KNOTS ( ( 4, 4 ),
 ( 2, 2 ),
 ( 0.000000000000000000, 1.000000000000000000 ),
 ( 0.000000000000000000, 1.000000000000000000 ),
 .UNSPECIFIED. ) 
 GEOMETRIC_REPRESENTATION_ITEM ( )  RATIONAL_B_SPLINE_SURFACE ( (
 ( 1.000000000000000000, 1.000000000000000000),
 ( 0.6386103224230316178, 0.9954351624131538845),
 ( 0.6386103224230316178, 0.9954351624131538845),
 ( 1.000000000000000000, 1.000000000000000000) ) ) 
 REPRESENTATION_ITEM ( '' )  SURFACE ( )  );
#13558=CARTESIAN_POINT ( 'NONE',  ( 32.73300124599738581, 3.836798148480494497, -117.5726003567928757 ) ) ;
#13559=DIRECTION ( 'NONE',  ( 0.000000000000000000, 0.000000000000000000, 1.000000000000000000 ) ) ;
#13562=CARTESIAN_POINT ( 'NONE',  ( 109.1587776205901577, 0.004240403845337359368, 0.005978137617714240556 ) ) ;
#13563=CARTESIAN_POINT ( 'NONE',  ( 5.340103556456499589, -144.6887562347051244, 28.39990973640018979 ) ) ;
#13566=EDGE_CURVE ( 'NONE', #25151, #17323, #28044, .T. ) ;
#13568=CARTESIAN_POINT ( 'NONE',  ( 1.833485406944043827, -142.0485807715647297, 29.64752363041495542 ) ) ;
#13569=CARTESIAN_POINT ( 'NONE',  ( 32.73300124599737160, -116.5274707358854158, -16.10546300444944023 ) ) ;
#13570=CARTESIAN_POINT ( 'NONE',  ( 25.64681081121879203, -23.06870491922242650, -110.5293738517610933 ) ) ;
#13573=CARTESIAN_POINT ( 'NONE',  ( 109.1589550718174877, -0.006669585340466669190, 0.003591809816104974025 ) ) ;
#13576=CARTESIAN_POINT ( 'NONE',  ( 1.833485406944057594, -15.69895494453287021, -144.2578170162064737 ) ) ;
#13577=EDGE_CURVE ( 'NONE', #17689, #4874, #8263, .T. ) ;
#13578=ORIENTED_EDGE ( 'NONE', *, *, #6249, .T. ) ;
#13580=CARTESIAN_POINT ( 'NONE',  ( 25.98552792386802324, 12.89843290883527693, 112.3992180166319486 ) ) ;
#13581=ORIENTED_EDGE ( 'NONE', *, *, #8768, .F. ) ;
#13584=ORIENTED_EDGE ( 'NONE', *, *, #3071, .F. ) ;
#13585=CARTESIAN_POINT ( 'NONE',  ( 109.1586900883932856, 0.005715190711488718836, 0.004277182003220973000 ) ) ;
#13586=EDGE_LOOP ( 'NONE', ( #14949, #19576, #14496, #11254 ) ) ;
#13588=DIRECTION ( 'NONE',  ( -0.5946245182733608248, 0.3994439555666327024, -0.6977579871484492768 ) ) ;
#13591=CARTESIAN_POINT ( 'NONE',  ( 109.1586059443104944, 0.005067816690886755952, -0.004935564877224700789 ) ) ;
#13592=CARTESIAN_POINT ( 'NONE',  ( 10.93730112725972425, -65.95960219663204782, 136.0306644680981094 ) ) ;
#13593=DIRECTION ( 'NONE',  ( 0.000000000000000000, 0.000000000000000000, 1.000000000000000000 ) ) ;
#13596=CARTESIAN_POINT ( 'NONE',  ( 1.832998868059890096, -96.70023740551050651, -108.1944082009167118 ) ) ;
#13597=EDGE_CURVE ( 'NONE', #6393, #18715, #6876, .T. ) ;
#13600=CARTESIAN_POINT ( 'NONE',  ( 32.73300124599735739, -32.68291970228314369, 113.0038235389601340 ) ) ;
#13601=EDGE_CURVE ( 'NONE', #12529, #21665, #16074, .T. ) ;
#13602=CARTESIAN_POINT ( 'NONE',  ( 1.833485406944057594, -30.69200235378832176, -141.8265699653870513 ) ) ;
#13604=CARTESIAN_POINT ( 'NONE',  ( 21.16825799904896854, -130.1008673867302150, -37.62905626541836313 ) ) ;
#13605=B_SPLINE_CURVE_WITH_KNOTS ( 'NONE', 3,
 ( #25744, #1556, #7635, #18836, #3296, #14793, #23602, #27603 ),
 .UNSPECIFIED., .F., .F.,
 ( 4, 2, 2, 4 ),
 ( 0.000000000000000000, 0.0002429588503611224061, 0.0004859177007222448123, 0.0009718354014444896246 ),
 .UNSPECIFIED. ) ;
#13608=ORIENTED_EDGE ( 'NONE', *, *, #7596, .T. ) ;
#13611=CARTESIAN_POINT ( 'NONE',  ( 1.832998868059858122, -125.4013017422236089, 73.01698022778313657 ) ) ;
#13612=CARTESIAN_POINT ( 'NONE',  ( 55.49584447822657296, -22.16497542184357883, -69.08290406177603415 ) ) ;
#13613=ORIENTED_EDGE ( 'NONE', *, *, #17546, .F. ) ;
#13614=CARTESIAN_POINT ( 'NONE',  ( 25.64681081121879203, 110.5293738517611501, -23.06870491922213873 ) ) ;
#13616=CARTESIAN_POINT ( 'NONE',  ( 32.73300124599736449, -116.5274707358856574, 16.10546300444784507 ) ) ;
#13617=EDGE_CURVE ( 'NONE', #1061, #2385, #22429, .T. ) ;
#13618=CARTESIAN_POINT ( 'NONE',  ( 1.833691583653519919, 15.52203496789107895, -144.2771263798445602 ) ) ;
#13619=VERTEX_POINT ( 'NONE', #680 ) ;
#13620=CARTESIAN_POINT ( 'NONE',  ( 25.69398547355838858, 112.2438548322124490, -12.54367966927931555 ) ) ;
#13621=ORIENTED_EDGE ( 'NONE', *, *, #10379, .F. ) ;
#13622=CARTESIAN_POINT ( 'NONE',  ( 109.1586900883932856, -0.006231977675085013588, -0.003481399864218412150 ) ) ;
#13623=VERTEX_POINT ( 'NONE', #9471 ) ;
#13624=CARTESIAN_POINT ( 'NONE',  ( 25.64708228042121618, 103.1656011680039171, -45.88917180166176024 ) ) ;
#13625=B_SPLINE_CURVE_WITH_KNOTS ( 'NONE', 3,
 ( #20081, #26844, #2818, #22701, #9446, #13743, #11593, #7153 ),
 .UNSPECIFIED., .F., .F.,
 ( 4, 2, 2, 4 ),
 ( 0.000000000000000000, 0.0002429588503611188825, 0.0004859177007222377650, 0.0009718354014444807341 ),
 .UNSPECIFIED. ) ;
#13627=CARTESIAN_POINT ( 'NONE',  ( 8.186469777910962975, 27.65107827750279412, -146.7694294853779695 ) ) ;
#13628=FACE_OUTER_BOUND ( 'NONE', #9698, .T. ) ;
#13629=CARTESIAN_POINT ( 'NONE',  ( 32.73300124599741423, -75.82012867748416340, -89.94078864464141532 ) ) ;
#13630=CARTESIAN_POINT ( 'NONE',  ( 1.833750490713699666, -125.8019536335925324, 72.32354185792516432 ) ) ;
#13632=CARTESIAN_POINT ( 'NONE',  ( 109.1778270068192853, 0.006489198140358630809, -0.006682187084639338963 ) ) ;
#13633=CARTESIAN_POINT ( 'NONE',  ( 2.108985857320905932, -96.26411661813104104, 108.8271972979196818 ) ) ;
#13636=ORIENTED_EDGE ( 'NONE', *, *, #24195, .T. ) ;
#13637=ORIENTED_EDGE ( 'NONE', *, *, #22683, .F. ) ;
#13638=CARTESIAN_POINT ( 'NONE',  ( 25.64670758986457955, -91.05338785329392692, -66.76959937251548638 ) ) ;
#13643=CARTESIAN_POINT ( 'NONE',  ( 1.833603222531958732, 144.2675221341993961, 15.61050054119080244 ) ) ;
#13644=CARTESIAN_POINT ( 'NONE',  ( 16.05277956358204605, -48.70400867629005148, -134.7758735858407988 ) ) ;
#13645=CARTESIAN_POINT ( 'NONE',  ( 109.1592201516379674, -0.006957642258155097119, -0.003661068210032647052 ) ) ;
#13646=EDGE_LOOP ( 'NONE', ( #19756, #13911, #16321, #24403 ) ) ;
#13647=CARTESIAN_POINT ( 'NONE',  ( 109.1592201516379674, 0.005631912476305695608, 0.005485778713193766379 ) ) ;
#13648=CARTESIAN_POINT ( 'NONE',  ( 26.11404676487257603, 90.92995828888199128, 67.46175819463394419 ) ) ;
#13650=CARTESIAN_POINT ( 'NONE',  ( 25.64692872815577473, -0.3216598674791715240, 112.9107203549055498 ) ) ;
#13652=EDGE_CURVE ( 'NONE', #10146, #19, #22331, .T. ) ;
#13654=EDGE_CURVE ( 'NONE', #378, #19503, #26870, .T. ) ;
#13655=CARTESIAN_POINT ( 'NONE',  ( 2.263178113027036531, 142.5035404044877509, -28.85718369185572385 ) ) ;
#13656=CARTESIAN_POINT ( 'NONE',  ( 2.108985857320916146, -142.3791757917250322, -28.95357181520974876 ) ) ;
#13657=ORIENTED_EDGE ( 'NONE', *, *, #513, .F. ) ;
#13658=VERTEX_POINT ( 'NONE', #252 ) ;
#13659=VERTEX_POINT ( 'NONE', #7313 ) ;
#13660=B_SPLINE_CURVE_WITH_KNOTS ( 'NONE', 3,
 ( #26558, #13175, #365, #2373, #20083, #11312 ),
 .UNSPECIFIED., .F., .F.,
 ( 4, 2, 4 ),
 ( 2.778605206969998010E-17, 0.0006311571484586182574, 0.001262314296917208976 ),
 .UNSPECIFIED. ) ;
#13665=CARTESIAN_POINT ( 'NONE',  ( 1.833809397773860761, 125.7576368866153729, -72.40070666294458590 ) ) ;
#13666=CARTESIAN_POINT ( 'NONE',  ( 25.64681081121879203, 66.70335573067988832, -91.10197563707880875 ) ) ;
#13667=CARTESIAN_POINT ( 'NONE',  ( 25.64704443564079028, -103.2037466592377797, 45.80316013050799029 ) ) ;
#13668=LINE ( 'NONE', #13109, #8899 ) ;
#13671=CARTESIAN_POINT ( 'NONE',  ( 2.430230287190572103, -118.5711603495687001, 84.35270093935217517 ) ) ;
#13672=CARTESIAN_POINT ( 'NONE',  ( 21.16825799904894012, 131.4851843440081609, -32.46271504707809896 ) ) ;
#13673=ADVANCED_FACE ( 'NONE', ( #9041 ), #7843, .F. ) ;
#13674=CARTESIAN_POINT ( 'NONE',  ( 1.834118845439484335, -144.2964192726481087, -15.34511559672828795 ) ) ;
#13675=LINE ( 'NONE', #7513, #19316 ) ;
#13676=CARTESIAN_POINT ( 'NONE',  ( 1.833809397773844774, 58.85883548850593883, 132.6366580004809350 ) ) ;
#13682=CARTESIAN_POINT ( 'NONE',  ( 109.1586900883932856, -0.005715190711488750061, -0.004277182003220933101 ) ) ;
#13684=ORIENTED_EDGE ( 'NONE', *, *, #5267, .F. ) ;
#13686=CARTESIAN_POINT ( 'NONE',  ( 109.1586059443104944, 0.005983234375919677800, 0.003774052605959055031 ) ) ;
#13689=ORIENTED_EDGE ( 'NONE', *, *, #3349, .T. ) ;
#13690=ORIENTED_EDGE ( 'NONE', *, *, #7857, .F. ) ;
#13692=DIRECTION ( 'NONE',  ( 0.5946245182733608248, 0.7637359336799388609, 0.2512550613902251873 ) ) ;
#13693=CARTESIAN_POINT ( 'NONE',  ( 32.73300124599735739, 62.10906484417237294, 99.90245962373859356 ) ) ;
#13694=B_SPLINE_CURVE_WITH_KNOTS ( 'NONE', 3,
 ( #21148, #25349, #1289, #5623, #14388, #12239, #21004, #10088, #18854, #24304 ),
 .UNSPECIFIED., .F., .F.,
 ( 4, 3, 3, 4 ),
 ( 3.925231146709437917E-17, 0.0002669559177086282546, 0.0005339118354151181373, 0.001067817517169144300 ),
 .UNSPECIFIED. ) ;
#13695=CARTESIAN_POINT ( 'NONE',  ( 10.93730112726002623, 56.95489579269933955, -140.0398180619107507 ) ) ;
#13696=LINE ( 'NONE', #4928, #5581 ) ;
#13697=CARTESIAN_POINT ( 'NONE',  ( 1.831572820252009626, -145.1082523917587253, 0.9871191512909551768 ) ) ;
#13701=CARTESIAN_POINT ( 'NONE',  ( 10.93730112725972070, -51.37919228020375328, 142.1801301103782293 ) ) ;
#13702=CARTESIAN_POINT ( 'NONE',  ( 25.65782528836479770, 34.34372400279251281, 107.5689571161380229 ) ) ;
#13704=EDGE_CURVE ( 'NONE', #5932, #14392, #21248, .T. ) ;
#13705=CARTESIAN_POINT ( 'NONE',  ( 1.833485406944057594, -108.1939177044919376, -96.69979900902278303 ) ) ;
#13706=CARTESIAN_POINT ( 'NONE',  ( 26.28373643307401153, 119.9673604189463703, -43.35364178852652373 ) ) ;
#13707=VECTOR ( 'NONE', #15956, 1000.000000000000000 ) ;
#13708=CARTESIAN_POINT ( 'NONE',  ( 1.833750490713655479, -117.5529286802293569, 85.07723081767849749 ) ) ;
#13710=CARTESIAN_POINT ( 'NONE',  ( 8.186469829614001270, 134.9918587494112501, 63.89871393833048074 ) ) ;
#13711=DIRECTION ( 'NONE',  ( 0.000000000000000000, 0.000000000000000000, 1.000000000000000000 ) ) ;
#13712=CARTESIAN_POINT ( 'NONE',  ( 25.64699802086721903, 46.14225289916308270, 103.0525896353903335 ) ) ;
#13713=B_SPLINE_CURVE_WITH_KNOTS ( 'NONE', 3,
 ( #15046, #11173, #21684, #24420 ),
 .UNSPECIFIED., .F., .F.,
 ( 4, 4 ),
 ( 3.221104623179000266E-16, 0.01077107486149802423 ),
 .UNSPECIFIED. ) ;
#13714=CARTESIAN_POINT ( 'NONE',  ( 109.1587776205901577, -0.005978137617714252700, 0.004240403845337341153 ) ) ;
#13715=DIRECTION ( 'NONE',  ( 0.000000000000000000, 0.000000000000000000, 1.000000000000000000 ) ) ;
#13716=ORIENTED_EDGE ( 'NONE', *, *, #12696, .T. ) ;
#13717=DIRECTION ( 'NONE',  ( 0.000000000000000000, 0.000000000000000000, 1.000000000000000000 ) ) ;
#13718=VERTEX_POINT ( 'NONE', #25298 ) ;
#13719=CARTESIAN_POINT ( 'NONE',  ( 1.831572820252008738, 84.49389457294135752, 117.9752562883669782 ) ) ;
#13720=CARTESIAN_POINT ( 'NONE',  ( 10.93730112725932635, 0.000000000000000000, 0.000000000000000000 ) ) ;
#13722=FACE_OUTER_BOUND ( 'NONE', #2142, .T. ) ;
#13724=CARTESIAN_POINT ( 'NONE',  ( 32.73300124599739291, 92.86301839380121237, -72.21147546950456331 ) ) ;
#13728=CARTESIAN_POINT ( 'NONE',  ( 32.73300124599737870, -117.5726003567929041, -3.836798148480059734 ) ) ;
#13731=EDGE_CURVE ( 'NONE', #21696, #15588, #3409, .T. ) ;
#13733=CARTESIAN_POINT ( 'NONE',  ( 25.64708228042121974, -66.39944550735333451, 91.32398912287000314 ) ) ;
#13736=CYLINDRICAL_SURFACE ( 'NONE', #10727, 20.00000000000000000 ) ;
#13737=CARTESIAN_POINT ( 'NONE',  ( 25.64660436782548203, -34.33930645842076501, 107.5626123667558289 ) ) ;
#13738=CARTESIAN_POINT ( 'NONE',  ( 24.01988960052056044, -90.81495976423860839, 94.47404045191606770 ) ) ;
#13739=ORIENTED_EDGE ( 'NONE', *, *, #20573, .T. ) ;
#13741=DIRECTION ( 'NONE',  ( -0.5946245182733607137, 0.7992853357633884492, -0.08697490616138101038 ) ) ;
#13742=CARTESIAN_POINT ( 'NONE',  ( 25.64681081121879203, 45.54494737132223747, 103.3177883989780952 ) ) ;
#13743=CARTESIAN_POINT ( 'NONE',  ( 25.86096068574583029, -84.67961880569343691, 74.90357932134600105 ) ) ;
#13746=ORIENTED_EDGE ( 'NONE', *, *, #17059, .F. ) ;
#13747=CARTESIAN_POINT ( 'NONE',  ( 26.28373643307438812, 127.4927519498662321, -4.159810388346843801 ) ) ;
#13749=CARTESIAN_POINT ( 'NONE',  ( 32.73300124599740002, -81.52272205837138586, -84.80615050150450429 ) ) ;
#13750=VERTEX_POINT ( 'NONE', #6014 ) ;
#13751=DIRECTION ( 'NONE',  ( 0.000000000000000000, 0.000000000000000000, 1.000000000000000000 ) ) ;
#13754=CARTESIAN_POINT ( 'NONE',  ( 2.433796855181219243, 132.3327394885239698, -60.50726454507772445 ) ) ;
#13756=CARTESIAN_POINT ( 'NONE',  ( 24.22246935314087324, 2.449293598294706119E-15, 20.00000000000000000 ) ) ;
#13757=EDGE_CURVE ( 'NONE', #9758, #14288, #8213, .T. ) ;
#13758=ORIENTED_EDGE ( 'NONE', *, *, #7857, .T. ) ;
#13760=ADVANCED_FACE ( 'NONE', ( #27297 ), #20664, .F. ) ;
#13761=EDGE_LOOP ( 'NONE', ( #7132, #10606, #20455, #1240 ) ) ;
#13763=B_SPLINE_CURVE_WITH_KNOTS ( 'NONE', 3,
 ( #28002, #12604, #8041, #23577, #10598, #8301, #23723 ),
 .UNSPECIFIED., .F., .F.,
 ( 4, 3, 4 ),
 ( 7.571427111245364237E-17, 0.02816610861753245099, 0.04000277880656218782 ),
 .UNSPECIFIED. ) ;
#13764=CARTESIAN_POINT ( 'NONE',  ( 55.49584447822657296, 7.317474139116590948, -72.18163437663932314 ) ) ;
#13765=AXIS2_PLACEMENT_3D ( 'NONE', #25603, #25170, #27751 ) ;
#13766=ADVANCED_FACE ( 'NONE', ( #24132 ), #10773, .F. ) ;
#13767=CARTESIAN_POINT ( 'NONE',  ( 25.64681081121879203, -35.28660243342623204, 107.2555980796239936 ) ) ;
#13768=DIRECTION ( 'NONE',  ( -1.000000000000000000, -0.000000000000000000, -0.000000000000000000 ) ) ;
#13770=( BOUNDED_SURFACE ( )  B_SPLINE_SURFACE ( 3, 1, ( 
 ( #5487, #7813 ),
 ( #18874, #12527 ),
 ( #27647, #7963 ),
 ( #23357, #12385 ) ),
 .UNSPECIFIED., .F., .F., .F. ) 
 B_SPLINE_SURFACE_WITH_KNOTS ( ( 4, 4 ),
 ( 2, 2 ),
 ( 0.000000000000000000, 1.000000000000000000 ),
 ( 0.000000000000000000, 1.000000000000000000 ),
 .UNSPECIFIED. ) 
 GEOMETRIC_REPRESENTATION_ITEM ( )  RATIONAL_B_SPLINE_SURFACE ( (
 ( 1.000000000000000000, 1.000000000000000000),
 ( 0.9956975270656954757, 0.8568959468854893125),
 ( 0.9956975270656954757, 0.8568959468854893125),
 ( 1.000000000000000000, 1.000000000000000000) ) ) 
 REPRESENTATION_ITEM ( '' )  SURFACE ( )  );
#13771=EDGE_CURVE ( 'NONE', #8435, #20441, #12983, .T. ) ;
#13772=CARTESIAN_POINT ( 'NONE',  ( 2.433796855181205476, 74.00833731765735024, -125.2830755159746445 ) ) ;
#13774=CARTESIAN_POINT ( 'NONE',  ( 25.64681081121879203, 91.10197563707947666, 66.70335573067896462 ) ) ;
#13775=ORIENTED_EDGE ( 'NONE', *, *, #21086, .F. ) ;
#13779=CARTESIAN_POINT ( 'NONE',  ( 1.832998868059858122, -132.7810136645742318, 58.53348008137599834 ) ) ;
#13780=CARTESIAN_POINT ( 'NONE',  ( 109.1778270068192853, -0.009220257877172541999, -0.001322180554006281445 ) ) ;
#13781=CARTESIAN_POINT ( 'NONE',  ( 26.11404676487257603, -24.64483677384923865, 110.5078194225160360 ) ) ;
#13786=ORIENTED_EDGE ( 'NONE', *, *, #6968, .F. ) ;
#13787=CARTESIAN_POINT ( 'NONE',  ( 24.01988960052067412, -123.2441023955613275, -44.53753990739630098 ) ) ;
#13788=CARTESIAN_POINT ( 'NONE',  ( 26.11404676487257603, 97.48350837663606683, 57.58742681967482469 ) ) ;
#13789=CARTESIAN_POINT ( 'NONE',  ( 1.833838848569418367, -145.1097630730648973, 0.1779716374152634506 ) ) ;
#13790=CARTESIAN_POINT ( 'NONE',  ( 6.224689322667630975, 100.9623537450666788, -108.2965163446063883 ) ) ;
#13791=CARTESIAN_POINT ( 'NONE',  ( 30.59141879584285917, -49.72305007553517697, 105.0379937202712313 ) ) ;
#13792=CARTESIAN_POINT ( 'NONE',  ( 1.894214914920944626, 142.1734439042097904, 29.24491455758985481 ) ) ;
#13793=ORIENTED_EDGE ( 'NONE', *, *, #13131, .T. ) ;
#13794=CARTESIAN_POINT ( 'NONE',  ( 109.1586900883932856, -0.001582822706024298925, 0.006960773163856026798 ) ) ;
#13795=EDGE_CURVE ( 'NONE', #1161, #16650, #4251, .T. ) ;
#13796=ORIENTED_EDGE ( 'NONE', *, *, #25943, .T. ) ;
#13801=ORIENTED_EDGE ( 'NONE', *, *, #7169, .T. ) ;
#13802=ORIENTED_EDGE ( 'NONE', *, *, #20637, .T. ) ;
#13803=EDGE_CURVE ( 'NONE', #5626, #15445, #1318, .T. ) ;
#13804=CARTESIAN_POINT ( 'NONE',  ( 25.64660436782549624, 84.29628170537259280, 75.12017330820509642 ) ) ;
#13806=EDGE_CURVE ( 'NONE', #431, #8144, #2079, .T. ) ;
#13808=DIRECTION ( 'NONE',  ( -0.5946245182733608248, 0.1700465163848199623, 0.7858154137795725358 ) ) ;
#13809=CARTESIAN_POINT ( 'NONE',  ( 2.433796855181205476, 43.58222566461644476, 138.8296532063089614 ) ) ;
#13810=ORIENTED_EDGE ( 'NONE', *, *, #22603, .F. ) ;
#13812=AXIS2_PLACEMENT_3D ( 'NONE', #5023, #18256, #7346 ) ;
#13813=CARTESIAN_POINT ( 'NONE',  ( 25.64692232868535626, 35.20209749635309748, 107.2834780834836863 ) ) ;
#13815=ORIENTED_EDGE ( 'NONE', *, *, #10833, .F. ) ;
#13820=CARTESIAN_POINT ( 'NONE',  ( 30.58324630866341920, 117.4177132550300797, -28.99049605145613384 ) ) ;
#13822=B_SPLINE_CURVE_WITH_KNOTS ( 'NONE', 3,
 ( #19837, #1851, #4157, #26179, #8214, #12657, #21726 ),
 .UNSPECIFIED., .F., .F.,
 ( 4, 3, 4 ),
 ( 5.212144047491128852E-16, 0.02816610861753249262, 0.04000277880656270824 ),
 .UNSPECIFIED. ) ;
#13823=FACE_OUTER_BOUND ( 'NONE', #13005, .T. ) ;
#13825=ORIENTED_EDGE ( 'NONE', *, *, #9691, .T. ) ;
#13827=CARTESIAN_POINT ( 'NONE',  ( 10.93730112725932635, 0.000000000000000000, 0.000000000000000000 ) ) ;
#13830=CARTESIAN_POINT ( 'NONE',  ( 25.64681081121879203, -0.4157506337719985012, -112.9102952884414606 ) ) ;
#13832=CARTESIAN_POINT ( 'NONE',  ( 119.2224693531408803, 6.938893903907200768E-15, -19.99999999999997868 ) ) ;
#13836=ORIENTED_EDGE ( 'NONE', *, *, #8647, .F. ) ;
#13841=EDGE_CURVE ( 'NONE', #23252, #3538, #1665, .T. ) ;
#13844=EDGE_CURVE ( 'NONE', #16927, #4626, #12881, .T. ) ;
#13845=CARTESIAN_POINT ( 'NONE',  ( 6.224689322667647851, 129.4863684118287495, 71.79702446228348833 ) ) ;
#13846=EDGE_CURVE ( 'NONE', #16481, #5027, #26045, .T. ) ;
#13849=CARTESIAN_POINT ( 'NONE',  ( 25.64670758986458310, -35.36461833156593570, 107.2298587623394326 ) ) ;
#13850=AXIS2_PLACEMENT_3D ( 'NONE', #27730, #14333, #27867 ) ;
#13851=CARTESIAN_POINT ( 'NONE',  ( 26.11404676487259024, 10.71016160607567080, 112.7148551500680753 ) ) ;
#13852=VECTOR ( 'NONE', #90, 1000.000000000000114 ) ;
#13853=CARTESIAN_POINT ( 'NONE',  ( 1.833838850855487257, -85.22139087168996241, -117.4485666028826785 ) ) ;
#13855=DIRECTION ( 'NONE',  ( -0.5914120900931443270, 0.5455001977188052020, 0.5938529060132676785 ) ) ;
#13856=AXIS2_PLACEMENT_3D ( 'NONE', #1222, #10165, #23404 ) ;
#13857=CARTESIAN_POINT ( 'NONE',  ( 2.430230287190572103, 142.6294793592101655, -28.83279105684286492 ) ) ;
#13858=CARTESIAN_POINT ( 'NONE',  ( 5.340103579038071757, 111.1041836885946594, 96.93942141937336032 ) ) ;
#13859=CARTESIAN_POINT ( 'NONE',  ( 32.73300124599735739, -81.52272205837257957, 84.80615050150346690 ) ) ;
#13861=CARTESIAN_POINT ( 'NONE',  ( 109.1721716018069657, -0.01392660302850761735, -0.009868622090676126835 ) ) ;
#13863=( BOUNDED_SURFACE ( )  B_SPLINE_SURFACE ( 3, 1, ( 
 ( #7276, #19940 ),
 ( #22252, #15757 ),
 ( #9012, #26548 ),
 ( #9295, #790 ) ),
 .UNSPECIFIED., .F., .F., .F. ) 
 B_SPLINE_SURFACE_WITH_KNOTS ( ( 4, 4 ),
 ( 2, 2 ),
 ( 0.000000000000000000, 1.000000000000000000 ),
 ( 0.000000000000000000, 1.000000000000000000 ),
 .UNSPECIFIED. ) 
 GEOMETRIC_REPRESENTATION_ITEM ( )  RATIONAL_B_SPLINE_SURFACE ( (
 ( 1.000000000000000000, 1.000000000000000000),
 ( 0.9960225298536222738, 0.9999952330161893110),
 ( 0.9960225298536222738, 0.9999952330161893110),
 ( 1.000000000000000000, 1.000000000000000000) ) ) 
 REPRESENTATION_ITEM ( '' )  SURFACE ( )  );
#13864=EDGE_CURVE ( 'NONE', #22236, #24138, #10270, .T. ) ;
#13865=VERTEX_POINT ( 'NONE', #3841 ) ;
#13866=CARTESIAN_POINT ( 'NONE',  ( 30.59141879584281654, -14.83090566979504388, 115.2623358717302864 ) ) ;
#13867=ORIENTED_EDGE ( 'NONE', *, *, #4559, .T. ) ;
#13868=CARTESIAN_POINT ( 'NONE',  ( 32.73300124599735739, -32.68291970228314369, 113.0038235389601340 ) ) ;
#13869=CARTESIAN_POINT ( 'NONE',  ( 2.263178113027024541, 1.401567040890216109, -145.3892419963350164 ) ) ;
#13870=EDGE_LOOP ( 'NONE', ( #19348, #18595, #14042, #17974 ) ) ;
#13871=ORIENTED_EDGE ( 'NONE', *, *, #1529, .F. ) ;
#13872=ORIENTED_EDGE ( 'NONE', *, *, #13844, .F. ) ;
#13874=EDGE_CURVE ( 'NONE', #19831, #27159, #27789, .T. ) ;
#13876=AXIS2_PLACEMENT_3D ( 'NONE', #4217, #12999, #21790 ) ;
#13877=CARTESIAN_POINT ( 'NONE',  ( 109.1592201516379674, 0.007302213399787552996, 0.002913740842103208079 ) ) ;
#13878=CARTESIAN_POINT ( 'NONE',  ( 109.1586059443104944, 0.006260042619939234880, -0.003294606663363258692 ) ) ;
#13881=CARTESIAN_POINT ( 'NONE',  ( 2.430230287190581429, 86.70145658344813455, -116.8646894862403514 ) ) ;
#13882=CARTESIAN_POINT ( 'NONE',  ( 21.16825799904929184, 71.50503315297862628, 115.0183107335388399 ) ) ;
#13883=LINE ( 'NONE', #7003, #28168 ) ;
#13884=CARTESIAN_POINT ( 'NONE',  ( 25.64681081121879203, -12.21581276189883170, 112.2483031020013016 ) ) ;
#13885=CARTESIAN_POINT ( 'NONE',  ( 10.93730112725932635, 0.000000000000000000, 0.000000000000000000 ) ) ;
#13886=VERTEX_POINT ( 'NONE', #6712 ) ;
#13888=CARTESIAN_POINT ( 'NONE',  ( 30.59138290137879679, 14.83088430729549323, 115.2623146671590604 ) ) ;
#13889=CARTESIAN_POINT ( 'NONE',  ( 1.833750490713728309, 85.07723081767881013, 117.5529286802290017 ) ) ;
#13890=CARTESIAN_POINT ( 'NONE',  ( 25.70243777736190083, 76.12033502296627319, -83.44449745408456920 ) ) ;
#13891=LINE ( 'NONE', #20373, #9711 ) ;
#13892=CARTESIAN_POINT ( 'NONE',  ( 1.833206308920042549, 138.2356393957902583, -44.13245285122123818 ) ) ;
#13893=CARTESIAN_POINT ( 'NONE',  ( 1.894214914920923087, 144.4515288797483947, 14.22353624692047269 ) ) ;
#13894=VECTOR ( 'NONE', #21567, 1000.000000000000114 ) ;
#13895=ORIENTED_EDGE ( 'NONE', *, *, #21484, .F. ) ;
#13896=CARTESIAN_POINT ( 'NONE',  ( 16.05277956358234448, 143.2298391883437603, -4.672229451528306932 ) ) ;
#13897=CONICAL_SURFACE ( 'NONE', #18506, 117.6351876552689504, 0.9945805576725580410 ) ;
#13898=CARTESIAN_POINT ( 'NONE',  ( 25.64670758986457244, 110.5460908981864776, -22.98827151089179210 ) ) ;
#13899=CARTESIAN_POINT ( 'NONE',  ( 2.430230287190592531, -84.35270093935336888, 118.5711603495678474 ) ) ;
#13900=VERTEX_POINT ( 'NONE', #21393 ) ;
#13902=ORIENTED_EDGE ( 'NONE', *, *, #219, .F. ) ;
#13903=EDGE_CURVE ( 'NONE', #12003, #3421, #20702, .T. ) ;
#13906=ADVANCED_FACE ( 'NONE', ( #6853 ), #23481, .T. ) ;
#13907=EDGE_LOOP ( 'NONE', ( #26177, #27570, #28237, #3905 ) ) ;
#13910=CARTESIAN_POINT ( 'NONE',  ( 109.1624594426973118, 0.01263706729759558715, -0.009754804742280831151 ) ) ;
#13911=ORIENTED_EDGE ( 'NONE', *, *, #10034, .F. ) ;
#13913=VECTOR ( 'NONE', #2048, 1000.000000000000000 ) ;
#13915=CIRCLE ( 'NONE', #14870, 117.6351876552689504 ) ;
#13918=CARTESIAN_POINT ( 'NONE',  ( 25.64692872815574631, 110.3764733653608516, 23.79008960806638484 ) ) ;
#13919=ORIENTED_EDGE ( 'NONE', *, *, #24952, .F. ) ;
#13920=CARTESIAN_POINT ( 'NONE',  ( 25.64707127832796019, 1.378041109049876443E-14, 112.9112343549835487 ) ) ;
#13921=CARTESIAN_POINT ( 'NONE',  ( 5.340103556456308631, 147.4316330165018769, 2.303180381358696405 ) ) ;
#13922=CARTESIAN_POINT ( 'NONE',  ( 24.01988960052073807, -17.94039809062707747, 129.8107982898199566 ) ) ;
#13924=ORIENTED_EDGE ( 'NONE', *, *, #27117, .F. ) ;
#13927=CARTESIAN_POINT ( 'NONE',  ( 1.833206308920082739, -44.13245285122170003, -138.2356393957900593 ) ) ;
#13932=VERTEX_POINT ( 'NONE', #24842 ) ;
#13935=CARTESIAN_POINT ( 'NONE',  ( 1.833691583653582535, -145.1092556475513504, -0.3559373310810099444 ) ) ;
#13936=EDGE_CURVE ( 'NONE', #17335, #20253, #7377, .T. ) ;
#13937=LINE ( 'NONE', #13118, #8323 ) ;
#13939=EDGE_LOOP ( 'NONE', ( #8067, #16577, #27597, #4097 ) ) ;
#13941=CONICAL_SURFACE ( 'NONE', #610, 117.6351876552689504, 0.9945805576725580410 ) ;
#13942=AXIS2_PLACEMENT_3D ( 'NONE', #18385, #7476, #18830 ) ;
#13944=EDGE_CURVE ( 'NONE', #8900, #26223, #5451, .T. ) ;
#13945=CARTESIAN_POINT ( 'NONE',  ( 1.833485406944057594, 132.7804117027888253, 58.53321471326925263 ) ) ;
#13947=EDGE_CURVE ( 'NONE', #2039, #17719, #24411, .T. ) ;
#13950=CARTESIAN_POINT ( 'NONE',  ( 25.64681081121879203, 84.18689316040048709, 75.24277141833519522 ) ) ;
#13952=DIRECTION ( 'NONE',  ( 0.000000000000000000, 0.000000000000000000, 1.000000000000000000 ) ) ;
#13956=CARTESIAN_POINT ( 'NONE',  ( 25.65782528836482257, 66.83837989650189115, -91.01210296572875791 ) ) ;
#13959=VERTEX_POINT ( 'NONE', #22394 ) ;
#13964=CARTESIAN_POINT ( 'NONE',  ( 1.831572820252009626, -141.7320553118907753, 31.13525033585447233 ) ) ;
#13965=CARTESIAN_POINT ( 'NONE',  ( 2.108393763691200018, 96.26428731761981794, 108.8265195087752346 ) ) ;
#13967=ORIENTED_EDGE ( 'NONE', *, *, #16340, .T. ) ;
#13969=DIRECTION ( 'NONE',  ( -1.000000000000000000, -0.000000000000000000, -0.000000000000000000 ) ) ;
#13970=ADVANCED_FACE ( 'NONE', ( #13454 ), #13863, .F. ) ;
#13971=EDGE_CURVE ( 'NONE', #17233, #17407, #10592, .T. ) ;
#13972=B_SPLINE_CURVE_WITH_KNOTS ( 'NONE', 3,
 ( #25840, #20940, #23701, #25569 ),
 .UNSPECIFIED., .F., .F.,
 ( 4, 4 ),
 ( 3.253361034654718625E-16, 0.01077107486149826363 ),
 .UNSPECIFIED. ) ;
#13973=B_SPLINE_CURVE_WITH_KNOTS ( 'NONE', 3,
 ( #235, #20518, #4840, #15609, #11602, #7438, #9587 ),
 .UNSPECIFIED., .F., .F.,
 ( 4, 3, 4 ),
 ( 0.000000000000000000, 0.02398743853561349088, 0.04000277880656218088 ),
 .UNSPECIFIED. ) ;
#13975=CARTESIAN_POINT ( 'NONE',  ( 9.884929003653608603, 149.2134106160916076, 19.90991253123297255 ) ) ;
#13976=CARTESIAN_POINT ( 'NONE',  ( 25.64692232868534560, -107.2834780834837858, 35.20209749635272090 ) ) ;
#13977=AXIS2_PLACEMENT_3D ( 'NONE', #11891, #22415, #5127 ) ;
#13978=ORIENTED_EDGE ( 'NONE', *, *, #2868, .T. ) ;
#13979=CARTESIAN_POINT ( 'NONE',  ( 25.64681081121879203, -75.24277141833549365, 84.18689316040023130 ) ) ;
#13981=VERTEX_POINT ( 'NONE', #9144 ) ;
#13983=ORIENTED_EDGE ( 'NONE', *, *, #14936, .F. ) ;
#13984=CARTESIAN_POINT ( 'NONE',  ( 32.73300124599738581, 44.31599526638102304, -108.9684813982483860 ) ) ;
#13985=CARTESIAN_POINT ( 'NONE',  ( 10.93730112725939030, 136.0306644680981947, 65.95960219663135149 ) ) ;
#13987=CARTESIAN_POINT ( 'NONE',  ( 109.1721716018069515, 0.009868622090669555702, 0.01392660302850061774 ) ) ;
#13991=CARTESIAN_POINT ( 'NONE',  ( 25.86096068574579832, 113.0494979885904314, 0.9975172952962499950 ) ) ;
#13992=CARTESIAN_POINT ( 'NONE',  ( 109.1586900883932856, 0.004851151255037359014, 0.005236795036860563031 ) ) ;
#13993=CARTESIAN_POINT ( 'NONE',  ( 55.49584447822657296, 42.86099773636619403, -58.53775398922213924 ) ) ;
#13996=CARTESIAN_POINT ( 'NONE',  ( 21.16825799904908223, -23.82367662027909816, 133.3214686481435649 ) ) ;
#13997=EDGE_CURVE ( 'NONE', #26534, #26705, #25402, .T. ) ;
#13998=CARTESIAN_POINT ( 'NONE',  ( 25.64681081121879203, 75.86069728268988399, 83.63051021305928145 ) ) ;
#13999=CARTESIAN_POINT ( 'NONE',  ( 26.11404676487257603, -76.59696442953247697, 83.38016054979757996 ) ) ;
#14000=B_SPLINE_CURVE_WITH_KNOTS ( 'NONE', 3,
 ( #23378, #18903, #2271, #5954 ),
 .UNSPECIFIED., .F., .F.,
 ( 4, 4 ),
 ( 3.078407974177840223E-16, 0.01077107486149828965 ),
 .UNSPECIFIED. ) ;
#14001=CARTESIAN_POINT ( 'NONE',  ( 9.884929003653608603, -103.8128997986865159, 109.0134320167729385 ) ) ;
#14002=CARTESIAN_POINT ( 'NONE',  ( 30.58324630866344407, -117.4177132550299518, 28.99049605145693320 ) ) ;
#14003=VERTEX_POINT ( 'NONE', #4960 ) ;
#14006=ADVANCED_FACE ( 'NONE', ( #356 ), #4106, .F. ) ;
#14007=LINE ( 'NONE', #24699, #10693 ) ;
#14008=ORIENTED_EDGE ( 'NONE', *, *, #4748, .T. ) ;
#14009=EDGE_CURVE ( 'NONE', #4553, #28186, #15060, .T. ) ;
#14010=ORIENTED_EDGE ( 'NONE', *, *, #13771, .F. ) ;
#14011=ORIENTED_EDGE ( 'NONE', *, *, #1806, .T. ) ;
#14014=CARTESIAN_POINT ( 'NONE',  ( 2.108393763691210676, 86.43392821214733601, -116.7869873529600540 ) ) ;
#14017=CARTESIAN_POINT ( 'NONE',  ( 32.73300124599732186, 0.000000000000000000, 0.000000000000000000 ) ) ;
#14018=CARTESIAN_POINT ( 'NONE',  ( 1.833750490713699666, 29.90883416717615262, 141.9939712933756084 ) ) ;
#14019=CARTESIAN_POINT ( 'NONE',  ( 10.93730112725945425, 115.5857507957700818, 97.44200844886312041 ) ) ;
#14020=CARTESIAN_POINT ( 'NONE',  ( 1.833691583653535462, -58.69608658929837475, -132.7086741139088133 ) ) ;
#14021=( BOUNDED_SURFACE ( )  B_SPLINE_SURFACE ( 3, 1, ( 
 ( #5553, #9738 ),
 ( #18792, #16638 ),
 ( #10324, #948 ),
 ( #7735, #18507 ) ),
 .UNSPECIFIED., .F., .F., .F. ) 
 B_SPLINE_SURFACE_WITH_KNOTS ( ( 4, 4 ),
 ( 2, 2 ),
 ( 0.000000000000000000, 1.000000000000000000 ),
 ( 0.000000000000000000, 1.000000000000000000 ),
 .UNSPECIFIED. ) 
 GEOMETRIC_REPRESENTATION_ITEM ( )  RATIONAL_B_SPLINE_SURFACE ( (
 ( 1.000000000000000000, 1.000000000000000000),
 ( 0.9956975270656955868, 0.8568959468854907557),
 ( 0.9956975270656955868, 0.8568959468854907557),
 ( 1.000000000000000000, 1.000000000000000000) ) ) 
 REPRESENTATION_ITEM ( '' )  SURFACE ( )  );
#14024=CARTESIAN_POINT ( 'NONE',  ( 2.430230287190581429, -145.5073573687466819, -1.451610819319260726 ) ) ;
#14025=CARTESIAN_POINT ( 'NONE',  ( 10.93730112725932635, 0.000000000000000000, 0.000000000000000000 ) ) ;
#14026=ORIENTED_EDGE ( 'NONE', *, *, #19908, .T. ) ;
#14030=CARTESIAN_POINT ( 'NONE',  ( 109.1589550718174877, -0.004269295012386602368, -0.006257602293694194094 ) ) ;
#14031=ADVANCED_FACE ( 'NONE', ( #24994 ), #23661, .T. ) ;
#14032=CARTESIAN_POINT ( 'NONE',  ( 5.340103556456401002, 13.12023871801123498, 146.8647350107029865 ) ) ;
#14034=CARTESIAN_POINT ( 'NONE',  ( 30.59138290137886429, -115.2623146671591314, 14.83088430729515217 ) ) ;
#14036=ORIENTED_EDGE ( 'NONE', *, *, #7333, .T. ) ;
#14037=FACE_OUTER_BOUND ( 'NONE', #10322, .T. ) ;
#14040=VERTEX_POINT ( 'NONE', #22832 ) ;
#14041=CARTESIAN_POINT ( 'NONE',  ( 2.430230287190572103, -142.6294793592099950, 28.83279105684379573 ) ) ;
#14042=ORIENTED_EDGE ( 'NONE', *, *, #2237, .F. ) ;
#14043=CARTESIAN_POINT ( 'NONE',  ( 21.16825799904897210, -134.1581724640163600, 18.54093663547782000 ) ) ;
#14044=CARTESIAN_POINT ( 'NONE',  ( 16.75465622695655910, 10.24707101928041020, 141.8562168210794425 ) ) ;
#14045=DIRECTION ( 'NONE',  ( -0.5946245182733607137, -0.5955128528260812404, 0.5401723099040858234 ) ) ;
#14046=EDGE_LOOP ( 'NONE', ( #21349, #16256, #19863, #418 ) ) ;
#14047=CARTESIAN_POINT ( 'NONE',  ( 6.224689322667647851, -145.3353551538639010, -28.26953958630769037 ) ) ;
#14050=CARTESIAN_POINT ( 'NONE',  ( 16.75465622695653067, -127.9746229614481763, -62.05388459346018948 ) ) ;
#14051=ORIENTED_EDGE ( 'NONE', *, *, #22603, .T. ) ;
#14054=CARTESIAN_POINT ( 'NONE',  ( 32.73300124599734318, 113.0038235389602477, 32.68291970228275289 ) ) ;
#14056=VERTEX_POINT ( 'NONE', #25123 ) ;
#14057=ADVANCED_FACE ( 'NONE', ( #16329 ), #2240, .F. ) ;
#14058=CARTESIAN_POINT ( 'NONE',  ( 26.11404676487257603, 108.0249973236472130, -33.91085499298264239 ) ) ;
#14059=CARTESIAN_POINT ( 'NONE',  ( 8.186469777910899026, -148.1306754055309511, 19.05650978729151035 ) ) ;
#14060=CARTESIAN_POINT ( 'NONE',  ( 13.84597867724959208, -124.5889929031784220, -77.45414123936355111 ) ) ;
#14061=ORIENTED_EDGE ( 'NONE', *, *, #22204, .F. ) ;
#14066=B_SPLINE_CURVE_WITH_KNOTS ( 'NONE', 3,
 ( #20456, #9528, #18281, #27065, #27649, #5202, #25083, #14113, #25367, #3190 ),
 .UNSPECIFIED., .F., .F.,
 ( 4, 3, 3, 4 ),
 ( 3.404394821604483923E-17, 0.0002669559177086211531, 0.0005339118354151021996, 0.001067817517169162515 ),
 .UNSPECIFIED. ) ;
#14067=CARTESIAN_POINT ( 'NONE',  ( 109.1586900883932856, 0.007088091345232578992, 0.0008465529156546068058 ) ) ;
#14069=CARTESIAN_POINT ( 'NONE',  ( 25.64681081121880624, 23.88203588908233499, -110.3564950173079353 ) ) ;
#14073=LINE ( 'NONE', #16680, #15300 ) ;
#14074=ORIENTED_EDGE ( 'NONE', *, *, #6104, .F. ) ;
#14075=CARTESIAN_POINT ( 'NONE',  ( 5.340103556456552880, 120.6284720803338217, -84.79482753886428270 ) ) ;
#14078=CARTESIAN_POINT ( 'NONE',  ( 28.37599760073042532, 86.45296943207121387, -75.42809173301522208 ) ) ;
#14079=CARTESIAN_POINT ( 'NONE',  ( 2.433796855181205476, -1.451562450950653949, 145.5024947199069629 ) ) ;
#14082=CARTESIAN_POINT ( 'NONE',  ( 1.832998868059858122, -137.8420662456173034, 45.34898734666001729 ) ) ;
#14084=CARTESIAN_POINT ( 'NONE',  ( 28.43349137099852086, 54.21282462801762847, 111.8014342888385926 ) ) ;
#14086=ORIENTED_EDGE ( 'NONE', *, *, #6045, .T. ) ;
#14090=CARTESIAN_POINT ( 'NONE',  ( 55.49584447822657296, 15.34602024131287479, 70.91003759562320852 ) ) ;
#14094=CARTESIAN_POINT ( 'NONE',  ( 1.833691583653536128, 45.17974255430996067, -137.8971124741063647 ) ) ;
#14096=CARTESIAN_POINT ( 'NONE',  ( 2.263178113027037419, -116.7985471375926068, -86.59154384226296486 ) ) ;
#14097=ORIENTED_EDGE ( 'NONE', *, *, #3094, .T. ) ;
#14098=EDGE_CURVE ( 'NONE', #17799, #15221, #9249, .T. ) ;
#14099=ORIENTED_EDGE ( 'NONE', *, *, #21951, .T. ) ;
#14100=CARTESIAN_POINT ( 'NONE',  ( 2.433796855181219243, -71.49415740225165905, 126.7346379669253622 ) ) ;
#14101=LINE ( 'NONE', #12106, #26585 ) ;
#14102=DIRECTION ( 'NONE',  ( -1.000000000000000000, -0.000000000000000000, -0.000000000000000000 ) ) ;
#14103=CARTESIAN_POINT ( 'NONE',  ( 1.834118845439484335, -107.7186227765460984, 97.22976650547388999 ) ) ;
#14104=VERTEX_POINT ( 'NONE', #11397 ) ;
#14106=CARTESIAN_POINT ( 'NONE',  ( 32.73300124599732186, 0.000000000000000000, 0.000000000000000000 ) ) ;
#14107=CARTESIAN_POINT ( 'NONE',  ( 109.1589550718174877, 0.007008495014548470070, -0.002874971999843682711 ) ) ;
#14112=B_SPLINE_CURVE_WITH_KNOTS ( 'NONE', 3,
 ( #25362, #735, #5635, #9523 ),
 .UNSPECIFIED., .F., .F.,
 ( 4, 4 ),
 ( 3.375586461644079052E-16, 0.01077107486149832608 ),
 .UNSPECIFIED. ) ;
#14113=CARTESIAN_POINT ( 'NONE',  ( 1.833838848569439239, 145.1097630730648120, -0.1779716374162767789 ) ) ;
#14114=VERTEX_POINT ( 'NONE', #11693 ) ;
#14115=VERTEX_POINT ( 'NONE', #20173 ) ;
#14116=EDGE_LOOP ( 'NONE', ( #28476, #8816, #24149, #12948 ) ) ;
#14117=CARTESIAN_POINT ( 'NONE',  ( 30.59138290137875771, 60.43009393261964135, 99.26509990456028731 ) ) ;
#14122=FACE_OUTER_BOUND ( 'NONE', #27270, .T. ) ;
#14124=EDGE_CURVE ( 'NONE', #5185, #195, #20992, .T. ) ;
#14125=CARTESIAN_POINT ( 'NONE',  ( 25.65782528836481191, 107.5689571161383924, -34.34372400279139725 ) ) ;
#14126=CARTESIAN_POINT ( 'NONE',  ( 10.93730112725990011, -128.3908183996585990, -79.81734490846054086 ) ) ;
#14130=CARTESIAN_POINT ( 'NONE',  ( 10.93730112725971004, 51.37919228020272300, 142.1801301103785420 ) ) ;
#14132=LINE ( 'NONE', #21196, #17383 ) ;
#14134=CARTESIAN_POINT ( 'NONE',  ( 26.11404676487257603, -112.7148551500681037, 10.71016160607530310 ) ) ;
#14135=CARTESIAN_POINT ( 'NONE',  ( 1.831572820252009626, 84.49389457294292072, -117.9752562883658555 ) ) ;
#14136=CARTESIAN_POINT ( 'NONE',  ( 25.64681081121879203, 84.18689316040146764, -75.24277141833410099 ) ) ;
#14139=CONICAL_SURFACE ( 'NONE', #353, 117.6351876552689504, 0.9945805576725580410 ) ;
#14140=ORIENTED_EDGE ( 'NONE', *, *, #15679, .T. ) ;
#14142=CARTESIAN_POINT ( 'NONE',  ( 119.2224693531408803, -69.99999999999998579, -20.00000000000000355 ) ) ;
#14143=ORIENTED_EDGE ( 'NONE', *, *, #4713, .T. ) ;
#14144=ORIENTED_EDGE ( 'NONE', *, *, #19472, .F. ) ;
#14145=VERTEX_POINT ( 'NONE', #9100 ) ;
#14146=B_SPLINE_CURVE_WITH_KNOTS ( 'NONE', 3,
 ( #1823, #10075, #23322, #14798, #10491, #16839, #5896 ),
 .UNSPECIFIED., .F., .F.,
 ( 4, 3, 4 ),
 ( 0.000000000000000000, 0.02398743853561349434, 0.04000277880656215312 ),
 .UNSPECIFIED. ) ;
#14148=CARTESIAN_POINT ( 'NONE',  ( 109.1778270068192853, 0.007885345421907800564, 0.004958088776550132609 ) ) ;
#14149=DIRECTION ( 'NONE',  ( 0.5914120900931444380, -0.1754905759872953386, 0.7870418015781028842 ) ) ;
#14151=CONICAL_SURFACE ( 'NONE', #12782, 117.6351876552689504, 0.9945805576725580410 ) ;
#14152=CARTESIAN_POINT ( 'NONE',  ( 109.1586900883932856, 0.005236795036868158518, 0.004851151255031872951 ) ) ;
#14153=CARTESIAN_POINT ( 'NONE',  ( 25.64704443564079739, -66.47548630737917108, 91.26857357624537315 ) ) ;
#14154=CARTESIAN_POINT ( 'NONE',  ( 28.37644542392842339, -124.2737818798214562, -4.054996728115485283 ) ) ;
#14155=ADVANCED_FACE ( 'NONE', ( #17861 ), #6901, .F. ) ;
#14157=CARTESIAN_POINT ( 'NONE',  ( 1.833485406944057594, -132.7804117027884274, -58.53321471327013370 ) ) ;
#14159=CARTESIAN_POINT ( 'NONE',  ( 1.893872463202043166, -86.08597552418957832, 116.8661275359695679 ) ) ;
#14160=CARTESIAN_POINT ( 'NONE',  ( 2.108393763691198686, 60.26375949664372200, -132.2055356348356554 ) ) ;
#14163=ORIENTED_EDGE ( 'NONE', *, *, #25483, .F. ) ;
#14164=LINE ( 'NONE', #5544, #16160 ) ;
#14169=EDGE_LOOP ( 'NONE', ( #11862, #14757, #19027, #22084, #24175, #17050 ) ) ;
#14171=CARTESIAN_POINT ( 'NONE',  ( 1.833603222531969834, 44.41798579679541348, 138.1443021179082677 ) ) ;
#14175=DIRECTION ( 'NONE',  ( 0.000000000000000000, 0.000000000000000000, 1.000000000000000000 ) ) ;
#14177=CARTESIAN_POINT ( 'NONE',  ( 109.1586900883932856, 0.003481399864227374599, 0.006231977675082119202 ) ) ;
#14178=VERTEX_POINT ( 'NONE', #21135 ) ;
#14179=CARTESIAN_POINT ( 'NONE',  ( 26.11404676487257603, -113.2169081140374232, 1.130420376096734847 ) ) ;
#14181=EDGE_LOOP ( 'NONE', ( #14061, #9156 ) ) ;
#14188=CARTESIAN_POINT ( 'NONE',  ( 2.430230287190581429, 142.0258656395021717, 31.67257033707551628 ) ) ;
#14189=EDGE_CURVE ( 'NONE', #1025, #2880, #28409, .T. ) ;
#14195=VERTEX_POINT ( 'NONE', #10230 ) ;
#14196=ORIENTED_EDGE ( 'NONE', *, *, #22872, .T. ) ;
#14197=ORIENTED_EDGE ( 'NONE', *, *, #2720, .T. ) ;
#14199=CARTESIAN_POINT ( 'NONE',  ( 2.433796855181233454, -74.00833731765476386, -125.2830755159761935 ) ) ;
#14202=CARTESIAN_POINT ( 'NONE',  ( 26.11404676487257603, -110.5078194225159223, -24.64483677384961879 ) ) ;
#14203=CARTESIAN_POINT ( 'NONE',  ( 25.64692232868534560, -83.69035111837253282, 75.79483800045747444 ) ) ;
#14204=CARTESIAN_POINT ( 'NONE',  ( 10.93730112725932635, 0.000000000000000000, 0.000000000000000000 ) ) ;
#14205=VERTEX_POINT ( 'NONE', #14932 ) ;
#14206=CARTESIAN_POINT ( 'NONE',  ( 1.833485406944057594, 145.1085452359073429, -0.5339064996889759662 ) ) ;
#14209=CARTESIAN_POINT ( 'NONE',  ( 32.73300124599739291, 89.94078864464164269, -75.82012867748392182 ) ) ;
#14210=CARTESIAN_POINT ( 'NONE',  ( 25.64708010899963853, 107.4019003251856645, 34.83947233573714186 ) ) ;
#14212=CARTESIAN_POINT ( 'NONE',  ( 109.1589550718175161, 0.007132058561966984379, -0.002553077953680959675 ) ) ;
#14214=CARTESIAN_POINT ( 'NONE',  ( 2.433796855181219243, 28.83182736670734059, -142.6247129145645829 ) ) ;
#14215=FACE_OUTER_BOUND ( 'NONE', #8944, .T. ) ;
#14218=ADVANCED_FACE ( 'NONE', ( #26025 ), #16961, .T. ) ;
#14219=ORIENTED_EDGE ( 'NONE', *, *, #23102, .F. ) ;
#14221=EDGE_CURVE ( 'NONE', #5798, #18731, #16774, .T. ) ;
#14223=CARTESIAN_POINT ( 'NONE',  ( 109.1586900883932856, 0.002301750759607898694, 0.006757191295056137574 ) ) ;
#14224=EDGE_LOOP ( 'NONE', ( #9460, #20847, #21350, #16138 ) ) ;
#14225=CARTESIAN_POINT ( 'NONE',  ( 94.22246935314088034, -90.00000000000005684, -12.50000000000000888 ) ) ;
#14226=( BOUNDED_SURFACE ( )  B_SPLINE_SURFACE ( 3, 1, ( 
 ( #15462, #23730 ),
 ( #21679, #11168 ),
 ( #4534, #10603 ),
 ( #15176, #10754 ) ),
 .UNSPECIFIED., .F., .F., .F. ) 
 B_SPLINE_SURFACE_WITH_KNOTS ( ( 4, 4 ),
 ( 2, 2 ),
 ( 0.000000000000000000, 1.000000000000000000 ),
 ( 0.000000000000000000, 1.000000000000000000 ),
 .UNSPECIFIED. ) 
 GEOMETRIC_REPRESENTATION_ITEM ( )  RATIONAL_B_SPLINE_SURFACE ( (
 ( 1.000000000000000000, 1.000000000000000000),
 ( 0.9956975270656954757, 0.8568959468854893125),
 ( 0.9956975270656954757, 0.8568959468854893125),
 ( 1.000000000000000000, 1.000000000000000000) ) ) 
 REPRESENTATION_ITEM ( '' )  SURFACE ( )  );
#14227=CARTESIAN_POINT ( 'NONE',  ( 2.433796855181219243, -116.8607839509062671, 86.69855925933937613 ) ) ;
#14228=CARTESIAN_POINT ( 'NONE',  ( 26.04756280548354042, 97.45505646068907879, -57.54844730865563918 ) ) ;
#14230=CARTESIAN_POINT ( 'NONE',  ( 16.75465622695658041, 102.5353941815402834, 98.56308464785089996 ) ) ;
#14231=CARTESIAN_POINT ( 'NONE',  ( 26.04756280548352976, 45.01666824410909129, -103.8403168215170922 ) ) ;
#14232=CARTESIAN_POINT ( 'NONE',  ( 1.833485406944057594, 97.49333871408690300, 107.4794113447412940 ) ) ;
#14233=CARTESIAN_POINT ( 'NONE',  ( 26.04756280548354752, -45.01666824410835943, 103.8403168215173906 ) ) ;
#14234=ORIENTED_EDGE ( 'NONE', *, *, #25164, .T. ) ;
#14235=VERTEX_POINT ( 'NONE', #6315 ) ;
#14238=CARTESIAN_POINT ( 'NONE',  ( 1.832998868059890096, 132.7810136645746297, -58.53348008137516700 ) ) ;
#14239=AXIS2_PLACEMENT_3D ( 'NONE', #19811, #13063, #2242 ) ;
#14240=CARTESIAN_POINT ( 'NONE',  ( 25.64700659047694487, -83.75695331063684534, -75.72132282458959196 ) ) ;
#14242=ORIENTED_EDGE ( 'NONE', *, *, #3882, .F. ) ;
#14243=CARTESIAN_POINT ( 'NONE',  ( 1.833838848569441016, 59.18404309081362413, 132.4919773286271152 ) ) ;
#14244=CARTESIAN_POINT ( 'NONE',  ( 1.893872463202054490, 16.11957794552959200, -144.2520230501563958 ) ) ;
#14245=CARTESIAN_POINT ( 'NONE',  ( 26.11404676487257603, -10.71016160607490875, -112.7148551500681606 ) ) ;
#14246=B_SPLINE_CURVE_WITH_KNOTS ( 'NONE', 3,
 ( #893, #16149, #3064, #23087, #5357, #20609 ),
 .UNSPECIFIED., .F., .F.,
 ( 4, 2, 4 ),
 ( 1.389302603484999005E-17, 0.0006311571484586006933, 0.001262314296917187509 ),
 .UNSPECIFIED. ) ;
#14247=B_SPLINE_CURVE_WITH_KNOTS ( 'NONE', 3,
 ( #25266, #9867, #5834, #22830 ),
 .UNSPECIFIED., .F., .F.,
 ( 4, 4 ),
 ( 2.027772282892422897E-16, 0.008383748772659654902 ),
 .UNSPECIFIED. ) ;
#14248=CARTESIAN_POINT ( 'NONE',  ( 1.831572820252009626, -58.11906524360567516, 132.9644823688593362 ) ) ;
#14249=ORIENTED_EDGE ( 'NONE', *, *, #28280, .F. ) ;
#14250=CARTESIAN_POINT ( 'NONE',  ( 25.64700659047697684, -75.72132282458926511, 83.75695331063708693 ) ) ;
#14254=ORIENTED_EDGE ( 'NONE', *, *, #21461, .F. ) ;
#14255=EDGE_CURVE ( 'NONE', #16104, #21261, #18862, .T. ) ;
#14256=ORIENTED_EDGE ( 'NONE', *, *, #15281, .T. ) ;
#14260=CARTESIAN_POINT ( 'NONE',  ( 55.79472521941428198, -59.28412330436272981, -42.17269936297700639 ) ) ;
#14261=CARTESIAN_POINT ( 'NONE',  ( 1.832998868059890096, 0.5339089137767937254, -145.1092030902949830 ) ) ;
#14262=VECTOR ( 'NONE', #2618, 1000.000000000000000 ) ;
#14271=CARTESIAN_POINT ( 'NONE',  ( 26.11404676487257603, -110.5078194225162918, 24.64483677384812665 ) ) ;
#14272=CARTESIAN_POINT ( 'NONE',  ( 25.65782528836481191, -55.95807498711414496, -98.07785559018930144 ) ) ;
#14273=AXIS2_PLACEMENT_3D ( 'NONE', #13832, #22640, #24365 ) ;
#14275=CONICAL_SURFACE ( 'NONE', #3718, 117.6351876552689504, 0.9945805576725580410 ) ;
#14277=CARTESIAN_POINT ( 'NONE',  ( 30.59141879584286983, -88.14706749784099316, 75.73279557183273880 ) ) ;
#14278=B_SPLINE_CURVE_WITH_KNOTS ( 'NONE', 3,
 ( #23122, #27412, #3383, #3656, #18331, #7722 ),
 .UNSPECIFIED., .F., .F.,
 ( 4, 2, 4 ),
 ( 8.673617379884035472E-19, 0.0006311636237756757667, 0.001262327247551350666 ),
 .UNSPECIFIED. ) ;
#14280=CARTESIAN_POINT ( 'NONE',  ( 16.05277956358204605, -113.1291064380268665, 87.96830019103622078 ) ) ;
#14281=CARTESIAN_POINT ( 'NONE',  ( 109.1624594426973260, 0.006914244825461633021, -0.01438905500501229048 ) ) ;
#14285=ADVANCED_FACE ( 'NONE', ( #10369 ), #16099, .T. ) ;
#14286=ORIENTED_EDGE ( 'NONE', *, *, #23216, .F. ) ;
#14288=VERTEX_POINT ( 'NONE', #6047 ) ;
#14292=ORIENTED_EDGE ( 'NONE', *, *, #13731, .F. ) ;
#14293=EDGE_CURVE ( 'NONE', #7383, #9793, #22648, .T. ) ;
#14294=ADVANCED_FACE ( 'NONE', ( #5764 ), #5209, .F. ) ;
#14295=CARTESIAN_POINT ( 'NONE',  ( 1.834118845439484335, -125.5799175751974985, 72.70910183320523856 ) ) ;
#14296=VECTOR ( 'NONE', #10679, 1000.000000000000000 ) ;
#14297=CARTESIAN_POINT ( 'NONE',  ( 25.64681081121880624, -56.81519825470823548, 97.57530875170583329 ) ) ;
#14299=AXIS2_PLACEMENT_3D ( 'NONE', #6439, #9586, #2822 ) ;
#14300=DIRECTION ( 'NONE',  ( 0.5914120900931445490, 0.3206367055789390852, 0.7398809652418038008 ) ) ;
#14302=CARTESIAN_POINT ( 'NONE',  ( 25.65782528836480125, 35.44279022896630948, -107.2118488517898101 ) ) ;
#14303=CARTESIAN_POINT ( 'NONE',  ( 2.433796855181205476, -107.1581411821778858, -98.43889364293970345 ) ) ;
#14305=CARTESIAN_POINT ( 'NONE',  ( 109.1586900883932856, 0.0001010081143975987133, 0.007137750914550313082 ) ) ;
#14309=ORIENTED_EDGE ( 'NONE', *, *, #7292, .F. ) ;
#14311=FACE_OUTER_BOUND ( 'NONE', #17493, .T. ) ;
#14313=CARTESIAN_POINT ( 'NONE',  ( 2.063896406836609909, 126.4736179849647897, 71.46753739786058190 ) ) ;
#14314=CARTESIAN_POINT ( 'NONE',  ( 25.64681081121880624, -23.06870491922396837, 110.5293738517607665 ) ) ;
#14315=CARTESIAN_POINT ( 'NONE',  ( 25.69398547355842055, 11.06723946918908297, -112.3990349503583985 ) ) ;
#14318=CARTESIAN_POINT ( 'NONE',  ( 1.832998868059858122, -45.34898734666143838, 137.8420662456168770 ) ) ;
#14319=EDGE_CURVE ( 'NONE', #12511, #106, #15669, .T. ) ;
#14320=CARTESIAN_POINT ( 'NONE',  ( 2.430230287190572103, 43.58368230469392302, 138.8342928068221624 ) ) ;
#14322=VERTEX_POINT ( 'NONE', #13189 ) ;
#14324=EDGE_CURVE ( 'NONE', #5184, #15977, #26661, .T. ) ;
#14325=B_SPLINE_CURVE_WITH_KNOTS ( 'NONE', 3,
 ( #2636, #24689, #5078, #26662, #24389, #6690, #2191, #20187, #9119, #22069 ),
 .UNSPECIFIED., .F., .F.,
 ( 4, 3, 3, 4 ),
 ( 3.469446951953614189E-17, 0.0002669559177086212615, 0.0005339118354151003564, 0.001067817517169159696 ),
 .UNSPECIFIED. ) ;
#14327=VERTEX_POINT ( 'NONE', #6595 ) ;
#14328=VECTOR ( 'NONE', #27075, 1000.000000000000114 ) ;
#14329=EDGE_CURVE ( 'NONE', #19, #21184, #21552, .T. ) ;
#14333=DIRECTION ( 'NONE',  ( -1.000000000000000000, -0.000000000000000000, -0.000000000000000000 ) ) ;
#14334=CARTESIAN_POINT ( 'NONE',  ( 2.063896406836609909, 28.88716984836516133, -142.3682421260904789 ) ) ;
#14338=AXIS2_PLACEMENT_3D ( 'NONE', #25930, #3903, #21596 ) ;
#14340=CARTESIAN_POINT ( 'NONE',  ( 109.1589550718174877, 0.001793588804091230705, -0.007359857714023724726 ) ) ;
#14343=CARTESIAN_POINT ( 'NONE',  ( 2.433796855181205476, -142.0211193075553524, -31.67151202413115385 ) ) ;
#14344=CARTESIAN_POINT ( 'NONE',  ( 16.05277956358235159, 109.5668455727257111, 92.36732600443201591 ) ) ;
#14345=CARTESIAN_POINT ( 'NONE',  ( 10.93730112725986281, -149.7554878793150408, 20.69552240458288850 ) ) ;
#14347=EDGE_LOOP ( 'NONE', ( #17134, #10028, #27706, #24591 ) ) ;
#14349=VERTEX_POINT ( 'NONE', #26434 ) ;
#14351=LINE ( 'NONE', #25309, #25432 ) ;
#14352=CARTESIAN_POINT ( 'NONE',  ( 1.833838848569429691, 107.7184832843409055, -97.22964245509652415 ) ) ;
#14353=CARTESIAN_POINT ( 'NONE',  ( 16.75465622695639212, -131.7467602971413783, 53.58152542127637474 ) ) ;
#14355=CARTESIAN_POINT ( 'NONE',  ( 1.833809397773830785, -132.4918864201824533, -59.18399778167268011 ) ) ;
#14358=CARTESIAN_POINT ( 'NONE',  ( 25.64704443564075476, 46.04703398841431294, -103.0951670221010943 ) ) ;
#14359=EDGE_LOOP ( 'NONE', ( #11093, #20171, #7994, #8366 ) ) ;
#14360=CARTESIAN_POINT ( 'NONE',  ( 13.36082413113061307, 142.1654513177095964, -56.35051087434822392 ) ) ;
#14361=CARTESIAN_POINT ( 'NONE',  ( 25.64681081121880624, -112.2483031020014295, 12.21581276189770904 ) ) ;
#14362=FACE_OUTER_BOUND ( 'NONE', #13191, .T. ) ;
#14365=CARTESIAN_POINT ( 'NONE',  ( 25.81918753295379432, -84.61657260023591220, -74.93271318951809690 ) ) ;
#14368=B_SPLINE_CURVE_WITH_KNOTS ( 'NONE', 3,
 ( #554, #19696, #13213, #22004 ),
 .UNSPECIFIED., .F., .F.,
 ( 4, 4 ),
 ( 0.000000000000000000, 0.01077107196513880927 ),
 .UNSPECIFIED. ) ;
#14370=DIRECTION ( 'NONE',  ( -1.000000000000000000, -0.000000000000000000, -0.000000000000000000 ) ) ;
#14373=EDGE_CURVE ( 'NONE', #8156, #4782, #5769, .T. ) ;
#14379=VECTOR ( 'NONE', #15610, 1000.000000000000114 ) ;
#14381=CARTESIAN_POINT ( 'NONE',  ( 26.11404676487257603, -57.58742681967381571, -97.48350837663670632 ) ) ;
#14386=CARTESIAN_POINT ( 'NONE',  ( 13.84597867724989406, 105.7628030201717877, 101.6650905919613166 ) ) ;
#14388=CARTESIAN_POINT ( 'NONE',  ( 1.833809397773857208, -125.5796696653632978, -72.70895493223498818 ) ) ;
#14389=CARTESIAN_POINT ( 'NONE',  ( 1.894214914920966608, 97.83100278581407849, 107.2270864706593301 ) ) ;
#14391=ORIENTED_EDGE ( 'NONE', *, *, #21188, .F. ) ;
#14392=VERTEX_POINT ( 'NONE', #6452 ) ;
#14393=CARTESIAN_POINT ( 'NONE',  ( 10.93730112725936188, 148.8212007290658505, 26.59437931460817595 ) ) ;
#14395=CARTESIAN_POINT ( 'NONE',  ( 109.1778270068192853, 0.002278716897417739154, 0.009031542838325988531 ) ) ;
#14397=CARTESIAN_POINT ( 'NONE',  ( 1.833485406944043827, -84.86072343962486286, -117.7091014914958578 ) ) ;
#14398=EDGE_CURVE ( 'NONE', #21026, #13718, #24388, .T. ) ;
#14400=VERTEX_POINT ( 'NONE', #10908 ) ;
#14401=CARTESIAN_POINT ( 'NONE',  ( 28.37644542392845537, 95.06674036596312760, -80.14194118792616450 ) ) ;
#14406=CARTESIAN_POINT ( 'NONE',  ( 1.832998868059858122, -58.53348008137736258, 132.7810136645736350 ) ) ;
#14407=LINE ( 'NONE', #10261, #1413 ) ;
#14409=DIRECTION ( 'NONE',  ( -1.000000000000000000, -0.000000000000000000, -0.000000000000000000 ) ) ;
#14411=ORIENTED_EDGE ( 'NONE', *, *, #16448, .F. ) ;
#14412=VERTEX_POINT ( 'NONE', #960 ) ;
#14413=VECTOR ( 'NONE', #878, 1000.000000000000114 ) ;
#14414=ORIENTED_EDGE ( 'NONE', *, *, #26157, .T. ) ;
#14416=CARTESIAN_POINT ( 'NONE',  ( 2.433796855181233454, 84.34988187691088513, -118.5671979538048504 ) ) ;
#14417=CARTESIAN_POINT ( 'NONE',  ( 1.834118845439484335, -0.1779704863060149744, -145.1099497418795750 ) ) ;
#14419=CARTESIAN_POINT ( 'NONE',  ( 99.22246935314079508, -69.99999999999998579, -40.00000000000002132 ) ) ;
#14420=B_SPLINE_CURVE_WITH_KNOTS ( 'NONE', 3,
 ( #10497, #19265, #19543, #28311, #23890, #28174, #8608, #12914, #12775, #8199 ),
 .UNSPECIFIED., .F., .F.,
 ( 4, 3, 3, 4 ),
 ( 1.387778780781445676E-17, 0.0002669560319015946981, 0.0005492286108966590178, 0.0008315040496093431630 ),
 .UNSPECIFIED. ) ;
#14422=EDGE_CURVE ( 'NONE', #15393, #13492, #24866, .T. ) ;
#14424=ORIENTED_EDGE ( 'NONE', *, *, #22750, .F. ) ;
#14425=CARTESIAN_POINT ( 'NONE',  ( 1.833603222531956289, 132.3826570575583048, 59.42758433816011632 ) ) ;
#14429=DIRECTION ( 'NONE',  ( 0.5946245182733608248, -0.4749651461092338489, 0.6487139525627668712 ) ) ;
#14430=DIRECTION ( 'NONE',  ( -0.5946245182733607137, 0.002950380665384895029, 0.8039981203473693938 ) ) ;
#14431=CARTESIAN_POINT ( 'NONE',  ( 26.11404676487257603, 110.5078194225161070, 24.64483677384886917 ) ) ;
#14432=DIRECTION ( 'NONE',  ( -0.5946245182733608248, 0.2456431038754911811, -0.7655593692108981774 ) ) ;
#14435=ADVANCED_FACE ( 'NONE', ( #7304 ), #22897, .F. ) ;
#14436=LINE ( 'NONE', #16454, #11087 ) ;
#14437=CARTESIAN_POINT ( 'NONE',  ( 109.1721716018069657, -0.0002019688922674237259, -0.01706748904932341507 ) ) ;
#14439=CARTESIAN_POINT ( 'NONE',  ( 1.833603222531971833, -0.4449221977529563277, 145.1089511853978422 ) ) ;
#14440=ORIENTED_EDGE ( 'NONE', *, *, #19441, .T. ) ;
#14442=ORIENTED_EDGE ( 'NONE', *, *, #18083, .T. ) ;
#14444=CARTESIAN_POINT ( 'NONE',  ( 109.1778270068192853, -0.009031542838325997205, 0.002278716897417708363 ) ) ;
#14445=ORIENTED_EDGE ( 'NONE', *, *, #27521, .F. ) ;
#14446=ORIENTED_EDGE ( 'NONE', *, *, #24230, .F. ) ;
#14448=CARTESIAN_POINT ( 'NONE',  ( 109.1586900883932856, 0.004113747441000919873, 0.005833932871487526248 ) ) ;
#14449=( BOUNDED_SURFACE ( )  B_SPLINE_SURFACE ( 3, 1, ( 
 ( #8198, #4282 ),
 ( #16964, #17514 ),
 ( #28172, #8340 ),
 ( #17371, #17238 ) ),
 .UNSPECIFIED., .F., .F., .F. ) 
 B_SPLINE_SURFACE_WITH_KNOTS ( ( 4, 4 ),
 ( 2, 2 ),
 ( 0.000000000000000000, 1.000000000000000000 ),
 ( 0.000000000000000000, 1.000000000000000000 ),
 .UNSPECIFIED. ) 
 GEOMETRIC_REPRESENTATION_ITEM ( )  RATIONAL_B_SPLINE_SURFACE ( (
 ( 1.000000000000000000, 1.000000000000000000),
 ( 0.6386103224230302855, 0.9954351624131538845),
 ( 0.6386103224230302855, 0.9954351624131538845),
 ( 1.000000000000000000, 1.000000000000000000) ) ) 
 REPRESENTATION_ITEM ( '' )  SURFACE ( )  );
#14450=CARTESIAN_POINT ( 'NONE',  ( 1.833485406944043827, -125.9346397303440455, 72.09189602597663793 ) ) ;
#14451=EDGE_CURVE ( 'NONE', #26705, #26589, #5058, .T. ) ;
#14452=DIRECTION ( 'NONE',  ( -0.5946245182733608248, -0.2456431038754863239, 0.7655593692108998427 ) ) ;
#14454=CARTESIAN_POINT ( 'NONE',  ( 10.93730112725969938, 71.28103789254939215, 133.3192575531800799 ) ) ;
#14455=LINE ( 'NONE', #25700, #3287 ) ;
#14456=EDGE_CURVE ( 'NONE', #1896, #7383, #28056, .T. ) ;
#14457=VERTEX_POINT ( 'NONE', #13756 ) ;
#14458=ORIENTED_EDGE ( 'NONE', *, *, #15688, .T. ) ;
#14460=LINE ( 'NONE', #21367, #12056 ) ;
#14461=CARTESIAN_POINT ( 'NONE',  ( 25.98107933586731733, 57.50946808479366723, -97.42660475433878275 ) ) ;
#14462=CARTESIAN_POINT ( 'NONE',  ( 26.11404676487259024, -83.38016054979834735, 76.59696442953165274 ) ) ;
#14464=EDGE_CURVE ( 'NONE', #17753, #15393, #17411, .T. ) ;
#14465=ORIENTED_EDGE ( 'NONE', *, *, #13448, .T. ) ;
#14466=CARTESIAN_POINT ( 'NONE',  ( 32.73300124599732186, 0.000000000000000000, 0.000000000000000000 ) ) ;
#14469=VERTEX_POINT ( 'NONE', #12047 ) ;
#14471=B_SPLINE_CURVE_WITH_KNOTS ( 'NONE', 3,
 ( #12431, #23120, #16776, #25418 ),
 .UNSPECIFIED., .F., .F.,
 ( 4, 4 ),
 ( 0.000000000000000000, 0.01077107196513850396 ),
 .UNSPECIFIED. ) ;
#14474=EDGE_LOOP ( 'NONE', ( #17116, #19736, #13872, #23500 ) ) ;
#14475=CARTESIAN_POINT ( 'NONE',  ( -90.83090735639699176, 0.000000000000000000, -37.50000000000001421 ) ) ;
#14476=EDGE_LOOP ( 'NONE', ( #7703, #15976, #27315, #2985, #12532, #9414 ) ) ;
#14479=SHAPE_DEFINITION_REPRESENTATION ( #24189, #7571 ) ;
#14480=LINE ( 'NONE', #6562, #17440 ) ;
#14482=( BOUNDED_SURFACE ( )  B_SPLINE_SURFACE ( 3, 1, ( 
 ( #28255, #2059 ),
 ( #26110, #23312 ),
 ( #7921, #3565 ),
 ( #12076, #14360 ) ),
 .UNSPECIFIED., .F., .F., .F. ) 
 B_SPLINE_SURFACE_WITH_KNOTS ( ( 4, 4 ),
 ( 2, 2 ),
 ( 0.000000000000000000, 1.000000000000000000 ),
 ( 0.000000000000000000, 1.000000000000000000 ),
 .UNSPECIFIED. ) 
 GEOMETRIC_REPRESENTATION_ITEM ( )  RATIONAL_B_SPLINE_SURFACE ( (
 ( 1.000000000000000000, 1.000000000000000000),
 ( 0.6386103224230302855, 0.9954351624131538845),
 ( 0.6386103224230302855, 0.9954351624131538845),
 ( 1.000000000000000000, 1.000000000000000000) ) ) 
 REPRESENTATION_ITEM ( '' )  SURFACE ( )  );
#14486=CARTESIAN_POINT ( 'NONE',  ( 25.64681081121880624, -46.30456157731397582, 102.9795863647027119 ) ) ;
#14487=CARTESIAN_POINT ( 'NONE',  ( 2.108985857320889501, -141.8463279126003442, 31.46042399111197696 ) ) ;
#14489=VERTEX_POINT ( 'NONE', #20951 ) ;
#14493=CARTESIAN_POINT ( 'NONE',  ( 25.86096068574581608, -102.8701285401538996, -46.89265070732224672 ) ) ;
#14494=ORIENTED_EDGE ( 'NONE', *, *, #24882, .T. ) ;
#14495=ADVANCED_FACE ( 'NONE', ( #1239 ), #242, .F. ) ;
#14496=ORIENTED_EDGE ( 'NONE', *, *, #18888, .T. ) ;
#14497=EDGE_LOOP ( 'NONE', ( #101, #19587, #27360, #22606 ) ) ;
#14499=CARTESIAN_POINT ( 'NONE',  ( 109.1586059443104944, 0.006570129623063769922, 0.002622205828279770140 ) ) ;
#14500=CARTESIAN_POINT ( 'NONE',  ( 1.832998868059858122, 144.2584710144582516, -15.69902610990227210 ) ) ;
#14503=CARTESIAN_POINT ( 'NONE',  ( 55.79472521941426777, 42.17269936297639532, 59.28412330436317745 ) ) ;
#14504=CARTESIAN_POINT ( 'NONE',  ( 55.79472521941426777, -30.25520714117951471, 66.16469064668288524 ) ) ;
#14506=EDGE_CURVE ( 'NONE', #28052, #8915, #17062, .T. ) ;
#14511=CARTESIAN_POINT ( 'NONE',  ( 10.93730112725972781, -56.95489579269845137, 140.0398180619108359 ) ) ;
#14512=CARTESIAN_POINT ( 'NONE',  ( 25.64708228042120908, 107.3728320282188662, 34.92896069507321499 ) ) ;
#14513=CARTESIAN_POINT ( 'NONE',  ( 109.1589550718175161, 0.004269295012381917748, -0.006257602293702372448 ) ) ;
#14514=CARTESIAN_POINT ( 'NONE',  ( 26.04756280548354042, -84.84709444968852665, -74.90181827458434327 ) ) ;
#14515=ORIENTED_EDGE ( 'NONE', *, *, #7141, .F. ) ;
#14517=CARTESIAN_POINT ( 'NONE',  ( 10.93730112725943471, 125.1380233598475229, 84.82621002473483429 ) ) ;
#14518=CARTESIAN_POINT ( 'NONE',  ( 109.1778270068192853, 0.0003511581237571051103, -0.009307953841262539552 ) ) ;
#14519=B_SPLINE_CURVE_WITH_KNOTS ( 'NONE', 3,
 ( #26463, #6766, #411, #4586, #7057, #13650, #700 ),
 .UNSPECIFIED., .F., .F.,
 ( 4, 3, 4 ),
 ( 0.0004157520161273759373, 0.0005492286108966323464, 0.0008315040496093444641 ),
 .UNSPECIFIED. ) ;
#14520=ORIENTED_EDGE ( 'NONE', *, *, #721, .F. ) ;
#14524=CARTESIAN_POINT ( 'NONE',  ( 1.831572820252009626, -73.40899645745918178, -125.1738732943817780 ) ) ;
#14526=CARTESIAN_POINT ( 'NONE',  ( 26.11404676487259024, 107.3263591096435476, -36.06104232266339693 ) ) ;
#14527=CARTESIAN_POINT ( 'NONE',  ( 1.833809397773815242, -137.9524943416723204, -45.01060836636663254 ) ) ;
#14528=CARTESIAN_POINT ( 'NONE',  ( 26.11404676487257603, -45.01677474591340911, -103.8885755249573606 ) ) ;
#14529=ADVANCED_FACE ( 'NONE', ( #14899 ), #3197, .F. ) ;
#14530=CARTESIAN_POINT ( 'NONE',  ( 1.833721034905629210, -58.69612512971697527, 132.7087680342066278 ) ) ;
#14532=DIRECTION ( 'NONE',  ( -0.5946245182733608248, 0.5955128528260846821, -0.5401723099040819376 ) ) ;
#14533=ORIENTED_EDGE ( 'NONE', *, *, #16210, .F. ) ;
#14534=EDGE_CURVE ( 'NONE', #6084, #19831, #3354, .T. ) ;
#14537=VERTEX_POINT ( 'NONE', #21244 ) ;
#14538=CARTESIAN_POINT ( 'NONE',  ( 25.73574536432414916, -97.42965068311185917, -57.18187897120895968 ) ) ;
#14541=CARTESIAN_POINT ( 'NONE',  ( 26.11404676487259024, 24.64483677385001315, -110.5078194225158654 ) ) ;
#14544=CARTESIAN_POINT ( 'NONE',  ( 10.93730112726003156, 84.82621002473607064, -125.1380233598471960 ) ) ;
#14545=VERTEX_POINT ( 'NONE', #14761 ) ;
#14547=CARTESIAN_POINT ( 'NONE',  ( 6.224689322667647851, 144.2687111683199817, -33.28770499679192341 ) ) ;
#14548=CARTESIAN_POINT ( 'NONE',  ( 8.186469777910767576, 90.56875928602713088, 118.7566730872903804 ) ) ;
#14552=CARTESIAN_POINT ( 'NONE',  ( 28.37644542392846247, -122.4011828058665827, 21.87158679436156206 ) ) ;
#14554=CARTESIAN_POINT ( 'NONE',  ( 109.1586059443104944, 0.006260042619943050404, 0.003294606663354673979 ) ) ;
#14555=CARTESIAN_POINT ( 'NONE',  ( 55.49584447822657296, 69.08290406177610521, -22.16497542184333369 ) ) ;
#14559=CARTESIAN_POINT ( 'NONE',  ( 30.58324630866345117, -28.99049605145642516, -117.4177132550299945 ) ) ;
#14560=CARTESIAN_POINT ( 'NONE',  ( 2.430230287190589422, -132.3371620660954875, 60.50928654924707217 ) ) ;
#14561=B_SPLINE_CURVE_WITH_KNOTS ( 'NONE', 3,
 ( #10009, #21355, #15001, #10430, #14589, #23819, #6117 ),
 .UNSPECIFIED., .F., .F.,
 ( 4, 3, 4 ),
 ( 0.000000000000000000, 0.02398743853561351169, 0.04000277880656213925 ),
 .UNSPECIFIED. ) ;
#14562=CARTESIAN_POINT ( 'NONE',  ( 109.1587776205901861, 0.004965871434398043752, 0.005390665547495595948 ) ) ;
#14563=EDGE_CURVE ( 'NONE', #27099, #27156, #13270, .T. ) ;
#14564=B_SPLINE_CURVE_WITH_KNOTS ( 'NONE', 3,
 ( #21040, #10130, #3207, #14572 ),
 .UNSPECIFIED., .F., .F.,
 ( 4, 4 ),
 ( 0.000000000000000000, 0.008383560773332715543 ),
 .UNSPECIFIED. ) ;
#14565=CARTESIAN_POINT ( 'NONE',  ( 2.430230287190572103, 116.8646894862412182, 86.70145658344696926 ) ) ;
#14566=EDGE_CURVE ( 'NONE', #23015, #20282, #2310, .T. ) ;
#14567=DIRECTION ( 'NONE',  ( 0.000000000000000000, 0.000000000000000000, 1.000000000000000000 ) ) ;
#14569=B_SPLINE_CURVE_WITH_KNOTS ( 'NONE', 3,
 ( #24573, #12023, #9574, #11876 ),
 .UNSPECIFIED., .F., .F.,
 ( 4, 4 ),
 ( 3.736708725176135323E-17, 0.008383748772659748577 ),
 .UNSPECIFIED. ) ;
#14570=EDGE_CURVE ( 'NONE', #16169, #23901, #603, .T. ) ;
#14572=CARTESIAN_POINT ( 'NONE',  ( 32.73300124599738581, -32.68291970228155918, -113.0038235389605461 ) ) ;
#14573=CARTESIAN_POINT ( 'NONE',  ( 25.64704443564076541, -11.93517308299214541, 112.2786464378873035 ) ) ;
#14574=B_SPLINE_CURVE_WITH_KNOTS ( 'NONE', 3,
 ( #20415, #22890, #14075, #5010 ),
 .UNSPECIFIED., .F., .F.,
 ( 4, 4 ),
 ( 0.000000000000000000, 0.01077107196513892723 ),
 .UNSPECIFIED. ) ;
#14575=CARTESIAN_POINT ( 'NONE',  ( 55.49584447822657296, -62.96491934285969450, -36.04376091928610037 ) ) ;
#14577=CARTESIAN_POINT ( 'NONE',  ( 2.063896406836609909, 133.2511741302120640, 57.85593781835461158 ) ) ;
#14579=DIRECTION ( 'NONE',  ( -0.5946245182733607137, 0.8039981203473692828, -0.002950380665387701811 ) ) ;
#14580=ORIENTED_EDGE ( 'NONE', *, *, #23574, .T. ) ;
#14582=ORIENTED_EDGE ( 'NONE', *, *, #3759, .F. ) ;
#14583=CARTESIAN_POINT ( 'NONE',  ( 109.1589550718174877, -0.007359857714023708246, -0.001793588804091302696 ) ) ;
#14584=CARTESIAN_POINT ( 'NONE',  ( 32.73300124599734318, 108.9684813982489118, 44.31599526637995012 ) ) ;
#14585=VERTEX_POINT ( 'NONE', #10332 ) ;
#14586=ORIENTED_EDGE ( 'NONE', *, *, #13803, .T. ) ;
#14589=CARTESIAN_POINT ( 'NONE',  ( 16.75465622695661594, 91.67104679059893613, 108.7410129416637830 ) ) ;
#14591=EDGE_CURVE ( 'NONE', #28326, #437, #7889, .T. ) ;
#14593=DIRECTION ( 'NONE',  ( 0.000000000000000000, -1.000000000000000000, 0.000000000000000000 ) ) ;
#14597=CARTESIAN_POINT ( 'NONE',  ( 25.64692232868533139, 56.73833653200244242, 97.62014907493897908 ) ) ;
#14598=CARTESIAN_POINT ( 'NONE',  ( 1.833809397773915828, 132.6366580004814750, -58.85883548850453906 ) ) ;
#14599=ORIENTED_EDGE ( 'NONE', *, *, #13597, .F. ) ;
#14601=CARTESIAN_POINT ( 'NONE',  ( 109.1589550718175161, 0.003284595046935036983, 0.006826119083824142356 ) ) ;
#14602=CARTESIAN_POINT ( 'NONE',  ( 25.64700659047696618, 112.9110011064639139, 0.2275682798790891748 ) ) ;
#14603=FACE_OUTER_BOUND ( 'NONE', #5285, .T. ) ;
#14605=CARTESIAN_POINT ( 'NONE',  ( 109.1589550718175161, 0.007453082872782197839, 0.001354998915253799886 ) ) ;
#14607=ORIENTED_EDGE ( 'NONE', *, *, #15154, .T. ) ;
#14609=FACE_OUTER_BOUND ( 'NONE', #20780, .T. ) ;
#14610=CARTESIAN_POINT ( 'NONE',  ( 10.93730112725978110, -119.3442956573278479, 92.80059208661636205 ) ) ;
#14611=ORIENTED_EDGE ( 'NONE', *, *, #18432, .T. ) ;
#14612=ORIENTED_EDGE ( 'NONE', *, *, #8785, .F. ) ;
#14613=B_SPLINE_CURVE_WITH_KNOTS ( 'NONE', 3,
 ( #18925, #11872, #27701, #5247 ),
 .UNSPECIFIED., .F., .F.,
 ( 4, 4 ),
 ( 3.344554059698260450E-16, 0.01077107486149801382 ),
 .UNSPECIFIED. ) ;
#14615=ORIENTED_EDGE ( 'NONE', *, *, #20471, .F. ) ;
#14616=ORIENTED_EDGE ( 'NONE', *, *, #9804, .F. ) ;
#14617=B_SPLINE_CURVE_WITH_KNOTS ( 'NONE', 3,
 ( #21721, #1992, #21862, #10924 ),
 .UNSPECIFIED., .F., .F.,
 ( 4, 4 ),
 ( 1.636534854170084423E-17, 0.008383748772659484899 ),
 .UNSPECIFIED. ) ;
#14618=( BOUNDED_SURFACE ( )  B_SPLINE_SURFACE ( 3, 1, ( 
 ( #11659, #15968 ),
 ( #24639, #22763 ),
 ( #4892, #427 ),
 ( #27034, #9368 ) ),
 .UNSPECIFIED., .F., .F., .F. ) 
 B_SPLINE_SURFACE_WITH_KNOTS ( ( 4, 4 ),
 ( 2, 2 ),
 ( 0.000000000000000000, 1.000000000000000000 ),
 ( 0.000000000000000000, 1.000000000000000000 ),
 .UNSPECIFIED. ) 
 GEOMETRIC_REPRESENTATION_ITEM ( )  RATIONAL_B_SPLINE_SURFACE ( (
 ( 1.000000000000000000, 1.000000000000000000),
 ( 0.6386103224230302855, 0.9954351624131538845),
 ( 0.6386103224230302855, 0.9954351624131538845),
 ( 1.000000000000000000, 1.000000000000000000) ) ) 
 REPRESENTATION_ITEM ( '' )  SURFACE ( )  );
#14619=CARTESIAN_POINT ( 'NONE',  ( 1.833838848569415925, 97.22964245509760417, 107.7184832843399533 ) ) ;
#14620=EDGE_CURVE ( 'NONE', #12568, #11237, #19165, .T. ) ;
#14621=EDGE_CURVE ( 'NONE', #6991, #25151, #6779, .T. ) ;
#14625=CARTESIAN_POINT ( 'NONE',  ( 109.1592201516379674, -0.006536841731953435194, 0.004368284148528988643 ) ) ;
#14626=CARTESIAN_POINT ( 'NONE',  ( 2.263178607246657315, -118.4461883615809654, -84.32376080825676468 ) ) ;
#14627=CARTESIAN_POINT ( 'NONE',  ( 25.64692872815575342, 83.69378511050568648, 75.79105864157416761 ) ) ;
#14628=CARTESIAN_POINT ( 'NONE',  ( 1.833721034905647862, -108.0754384393928120, -96.83259691102610134 ) ) ;
#14629=ORIENTED_EDGE ( 'NONE', *, *, #18728, .F. ) ;
#14632=CARTESIAN_POINT ( 'NONE',  ( 25.64692232868534560, -97.94691534265392363, -56.17236075412048990 ) ) ;
#14633=CARTESIAN_POINT ( 'NONE',  ( 9.884929003653608603, 19.90991253123445404, -149.2134106160914087 ) ) ;
#14635=ORIENTED_EDGE ( 'NONE', *, *, #8143, .F. ) ;
#14637=CARTESIAN_POINT ( 'NONE',  ( 25.64681081121879203, 56.09509703373481670, -97.99105938547863559 ) ) ;
#14643=CARTESIAN_POINT ( 'NONE',  ( 2.108393763691158718, 71.53437599919816137, 126.4628696952921416 ) ) ;
#14645=ORIENTED_EDGE ( 'NONE', *, *, #26608, .T. ) ;
#14646=CARTESIAN_POINT ( 'NONE',  ( 25.64703792032472052, -112.2770217641848660, 11.95040607427947776 ) ) ;
#14647=AXIS2_PLACEMENT_3D ( 'NONE', #1296, #5330, #27637 ) ;
#14651=ORIENTED_EDGE ( 'NONE', *, *, #18054, .T. ) ;
#14652=CARTESIAN_POINT ( 'NONE',  ( 9.884929003653626367, 11.54837932063230888, -150.0922431698403727 ) ) ;
#14654=CARTESIAN_POINT ( 'NONE',  ( 10.93730112726005999, 136.0306644680993600, -65.95960219662998725 ) ) ;
#14655=EDGE_CURVE ( 'NONE', #13865, #6991, #24316, .T. ) ;
#14657=CARTESIAN_POINT ( 'NONE',  ( 2.433796855181205476, 116.8607839509056561, 86.69855925934011509 ) ) ;
#14658=B_SPLINE_CURVE_WITH_KNOTS ( 'NONE', 3,
 ( #10169, #27559, #18646, #21076, #7584, #7730, #9879, #1225, #9732, #12030 ),
 .UNSPECIFIED., .F., .F.,
 ( 4, 3, 3, 4 ),
 ( 3.103167691559091397E-17, 0.0002669559177086257068, 0.0005339118354151221489, 0.001067817517169156877 ),
 .UNSPECIFIED. ) ;
#14659=VERTEX_POINT ( 'NONE', #8569 ) ;
#14660=( BOUNDED_SURFACE ( )  B_SPLINE_SURFACE ( 3, 1, ( 
 ( #5820, #1481 ),
 ( #17161, #17292 ),
 ( #19312, #23672 ),
 ( #25683, #19598 ) ),
 .UNSPECIFIED., .F., .F., .F. ) 
 B_SPLINE_SURFACE_WITH_KNOTS ( ( 4, 4 ),
 ( 2, 2 ),
 ( 0.000000000000000000, 1.000000000000000000 ),
 ( 0.000000000000000000, 1.000000000000000000 ),
 .UNSPECIFIED. ) 
 GEOMETRIC_REPRESENTATION_ITEM ( )  RATIONAL_B_SPLINE_SURFACE ( (
 ( 1.000000000000000000, 1.000000000000000000),
 ( 0.6386103224230316178, 0.9954351624131538845),
 ( 0.6386103224230316178, 0.9954351624131538845),
 ( 1.000000000000000000, 1.000000000000000000) ) ) 
 REPRESENTATION_ITEM ( '' )  SURFACE ( )  );
#14662=ORIENTED_EDGE ( 'NONE', *, *, #19741, .F. ) ;
#14664=CARTESIAN_POINT ( 'NONE',  ( 2.063896406836609909, -73.79559738457666640, -125.1295119249446941 ) ) ;
#14665=ADVANCED_FACE ( 'NONE', ( #11158 ), #12019, .F. ) ;
#14666=CARTESIAN_POINT ( 'NONE',  ( 1.831572820252009626, 108.4969585352555015, 96.36280042115966182 ) ) ;
#14667=CARTESIAN_POINT ( 'NONE',  ( 25.64692872815579250, -23.79008960806674722, 110.3764733653607237 ) ) ;
#14668=CARTESIAN_POINT ( 'NONE',  ( 1.834118845439484335, 30.34413640949697921, 141.9019470378988501 ) ) ;
#14669=CARTESIAN_POINT ( 'NONE',  ( 25.64681081121879203, -0.4157506337735756285, 112.9102952884414464 ) ) ;
#14671=CARTESIAN_POINT ( 'NONE',  ( 26.04756280548352976, -74.90181827458404484, 84.84709444968881087 ) ) ;
#14673=VERTEX_POINT ( 'NONE', #17763 ) ;
#14675=CARTESIAN_POINT ( 'NONE',  ( 109.1778270068192853, -0.004349865064712347094, -0.008236503545664854500 ) ) ;
#14676=CARTESIAN_POINT ( 'NONE',  ( 21.16825799904903604, -75.99073816868381925, 112.1052598354962271 ) ) ;
#14678=CARTESIAN_POINT ( 'NONE',  ( 2.108393763691175149, 144.3574619851892464, 16.46048390411847606 ) ) ;
#14682=ORIENTED_EDGE ( 'NONE', *, *, #15033, .F. ) ;
#14683=CARTESIAN_POINT ( 'NONE',  ( 10.93730112725943471, 119.3442956573271516, 92.80059208661684522 ) ) ;
#14685=CARTESIAN_POINT ( 'NONE',  ( 32.73300124599732186, 0.000000000000000000, 0.000000000000000000 ) ) ;
#14686=CARTESIAN_POINT ( 'NONE',  ( 25.87036335909428075, 0.9898498320587705290, 113.0557711752706922 ) ) ;
#14687=CARTESIAN_POINT ( 'NONE',  ( 25.64707127832796019, 6.059145946834079367E-17, -112.9112343549835487 ) ) ;
#14688=VERTEX_POINT ( 'NONE', #21949 ) ;
#14689=CARTESIAN_POINT ( 'NONE',  ( 1.834118845439484335, 45.01070051384593995, 137.9527673765107068 ) ) ;
#14690=CARTESIAN_POINT ( 'NONE',  ( 32.73300124599732186, 0.000000000000000000, 0.000000000000000000 ) ) ;
#14691=ORIENTED_EDGE ( 'NONE', *, *, #19125, .T. ) ;
#14693=ORIENTED_EDGE ( 'NONE', *, *, #5701, .T. ) ;
#14695=EDGE_CURVE ( 'NONE', #27686, #13623, #23958, .T. ) ;
#14701=CARTESIAN_POINT ( 'NONE',  ( 1.833485406944043827, 117.7091014914961420, -84.86072343962446496 ) ) ;
#14702=CARTESIAN_POINT ( 'NONE',  ( 109.1586059443104944, -0.006637156007973997289, -0.002447596125905566588 ) ) ;
#14703=( BOUNDED_SURFACE ( )  B_SPLINE_SURFACE ( 3, 1, ( 
 ( #3603, #12252 ),
 ( #14107, #5337 ),
 ( #21020, #7811 ),
 ( #3183, #7669 ) ),
 .UNSPECIFIED., .F., .F., .F. ) 
 B_SPLINE_SURFACE_WITH_KNOTS ( ( 4, 4 ),
 ( 2, 2 ),
 ( 0.000000000000000000, 1.000000000000000000 ),
 ( 0.000000000000000000, 1.000000000000000000 ),
 .UNSPECIFIED. ) 
 GEOMETRIC_REPRESENTATION_ITEM ( )  RATIONAL_B_SPLINE_SURFACE ( (
 ( 1.000000000000000000, 1.000000000000000000),
 ( 0.9956975270656954757, 0.8568959468854893125),
 ( 0.9956975270656954757, 0.8568959468854893125),
 ( 1.000000000000000000, 1.000000000000000000) ) ) 
 REPRESENTATION_ITEM ( '' )  SURFACE ( )  );
#14705=CARTESIAN_POINT ( 'NONE',  ( 1.832998868059890096, 144.3700883710216942, 14.63705790014057406 ) ) ;
#14707=CARTESIAN_POINT ( 'NONE',  ( 1.831572820252008738, 73.40899645746179658, -125.1738732943802290 ) ) ;
#14708=CARTESIAN_POINT ( 'NONE',  ( 30.59141879584272061, 109.6600586137414126, 38.47120193631498353 ) ) ;
#14709=CARTESIAN_POINT ( 'NONE',  ( 1.832998868059858122, 132.7810136645738055, 58.53348008137690783 ) ) ;
#14710=CARTESIAN_POINT ( 'NONE',  ( 109.1587776205901577, -0.001442274045003953805, -0.007186028091163427188 ) ) ;
#14711=CARTESIAN_POINT ( 'NONE',  ( 26.11404676487257603, 12.95861723607603544, -112.4785329405480780 ) ) ;
#14714=CARTESIAN_POINT ( 'NONE',  ( 25.64660436782568098, -24.04259444204576113, -110.3216080362390699 ) ) ;
#14715=CIRCLE ( 'NONE', #2286, 117.6351876552689504 ) ;
#14716=CARTESIAN_POINT ( 'NONE',  ( 109.1592201516379674, -0.001127733110588171120, -0.007780772729122754396 ) ) ;
#14717=VERTEX_POINT ( 'NONE', #10742 ) ;
#14719=VECTOR ( 'NONE', #9534, 1000.000000000000000 ) ;
#14721=ORIENTED_EDGE ( 'NONE', *, *, #14534, .F. ) ;
#14723=ADVANCED_FACE ( 'NONE', ( #19636 ), #14957, .F. ) ;
#14725=B_SPLINE_CURVE_WITH_KNOTS ( 'NONE', 3,
 ( #19294, #6219, #4173, #12949, #21744, #8229 ),
 .UNSPECIFIED., .F., .F.,
 ( 4, 2, 4 ),
 ( 7.372574772901430151E-18, 0.0006311636237756882350, 0.001262327247551369314 ),
 .UNSPECIFIED. ) ;
#14726=CARTESIAN_POINT ( 'NONE',  ( 1.832998868059890096, -59.50898020732424243, -132.3466930259799881 ) ) ;
#14728=CARTESIAN_POINT ( 'NONE',  ( 2.063896406836605024, 116.7302989755737741, 86.47093297169037385 ) ) ;
#14731=CONICAL_SURFACE ( 'NONE', #13812, 117.6351876552689504, 0.9945805576725580410 ) ;
#14732=B_SPLINE_CURVE_WITH_KNOTS ( 'NONE', 3,
 ( #1809, #8453, #24004, #10759 ),
 .UNSPECIFIED., .F., .F.,
 ( 4, 4 ),
 ( 3.805030037801212946E-16, 0.01077107486149815434 ),
 .UNSPECIFIED. ) ;
#14733=EDGE_CURVE ( 'NONE', #14040, #18219, #12628, .T. ) ;
#14734=CARTESIAN_POINT ( 'NONE',  ( 1.832998868059890096, -72.09222286250997058, -125.9352106559991142 ) ) ;
#14735=CARTESIAN_POINT ( 'NONE',  ( 1.893872463202056045, 59.90695624048866819, -132.2106029832896752 ) ) ;
#14738=CIRCLE ( 'NONE', #12434, 80.00000000000000000 ) ;
#14741=CARTESIAN_POINT ( 'NONE',  ( 25.64692232868534560, -107.4854307433084841, -34.58055111992153741 ) ) ;
#14743=CARTESIAN_POINT ( 'NONE',  ( 13.36082413113063083, -129.1512766091127276, 81.89226687792040593 ) ) ;
#14744=CARTESIAN_POINT ( 'NONE',  ( 0.000000000000000000, 0.000000000000000000, -143.8872038478949946 ) ) ;
#14745=CARTESIAN_POINT ( 'NONE',  ( 109.1587776205901861, 0.006995903587863974010, 0.002185517590237709071 ) ) ;
#14746=CARTESIAN_POINT ( 'NONE',  ( 25.64670758986457599, 112.3434365398309893, -11.30712635241874153 ) ) ;
#14748=VERTEX_POINT ( 'NONE', #24835 ) ;
#14750=CARTESIAN_POINT ( 'NONE',  ( 109.1721716018069657, -0.01550977894512761864, 0.007126480965770868800 ) ) ;
#14751=CARTESIAN_POINT ( 'NONE',  ( 8.186469777910820866, -84.95702201436492373, 122.8338388711457441 ) ) ;
#14752=ORIENTED_EDGE ( 'NONE', *, *, #3131, .F. ) ;
#14753=VERTEX_POINT ( 'NONE', #7409 ) ;
#14757=ORIENTED_EDGE ( 'NONE', *, *, #13068, .T. ) ;
#14758=ORIENTED_EDGE ( 'NONE', *, *, #4041, .F. ) ;
#14759=AXIS2_PLACEMENT_3D ( 'NONE', #23407, #11882, #3664 ) ;
#14760=CONICAL_SURFACE ( 'NONE', #12011, 117.6351876552689504, 0.9945805576725580410 ) ;
#14761=CARTESIAN_POINT ( 'NONE',  ( 26.11404676487257603, 98.61392875273440950, -55.62948129436141897 ) ) ;
#14762=VECTOR ( 'NONE', #5728, 1000.000000000000227 ) ;
#14763=VERTEX_POINT ( 'NONE', #3088 ) ;
#14764=FACE_OUTER_BOUND ( 'NONE', #1640, .T. ) ;
#14765=CARTESIAN_POINT ( 'NONE',  ( 32.73300124599737160, -117.5726003567929610, 3.836798148478423265 ) ) ;
#14766=CARTESIAN_POINT ( 'NONE',  ( 10.93730112725977932, -128.3908183996597074, 79.81734490845860819 ) ) ;
#14768=CARTESIAN_POINT ( 'NONE',  ( 13.36082413113063083, -119.8836995922732882, 94.94363694444014357 ) ) ;
#14769=CARTESIAN_POINT ( 'NONE',  ( 1.833206310202320610, -141.7818020564280630, 30.89799345102914074 ) ) ;
#14770=B_SPLINE_CURVE_WITH_KNOTS ( 'NONE', 3,
 ( #18463, #12273, #18899, #27231 ),
 .UNSPECIFIED., .F., .F.,
 ( 4, 4 ),
 ( 5.049803577358454571E-16, 0.008383748772659955009 ),
 .UNSPECIFIED. ) ;
#14771=B_SPLINE_CURVE_WITH_KNOTS ( 'NONE', 3,
 ( #9152, #24145, #21692, #19529, #24428, #19953, #15190, #13466, #10899, #21970 ),
 .UNSPECIFIED., .F., .F.,
 ( 4, 3, 3, 4 ),
 ( 3.469446951953614189E-17, 0.0002669559177086352477, 0.0005339118354151166194, 0.001067817517169169887 ),
 .UNSPECIFIED. ) ;
#14772=CARTESIAN_POINT ( 'NONE',  ( 10.93730112725932635, 0.000000000000000000, 0.000000000000000000 ) ) ;
#14773=CARTESIAN_POINT ( 'NONE',  ( 25.64708228042119487, -97.76433875577606614, -56.48974615489026974 ) ) ;
#14774=CARTESIAN_POINT ( 'NONE',  ( 25.87036335909423812, -10.83311869338149869, 112.5399073133628320 ) ) ;
#14775=CARTESIAN_POINT ( 'NONE',  ( 55.79472521941426777, -8.328398066092255192, 72.27573336313948005 ) ) ;
#14779=CARTESIAN_POINT ( 'NONE',  ( 2.433796855181233454, 118.5671979538056888, 84.34988187690970562 ) ) ;
#14781=AXIS2_PLACEMENT_3D ( 'NONE', #18203, #3665, #6135 ) ;
#14783=DIRECTION ( 'NONE',  ( 0.5946245182733607137, 0.6948076064830630560, 0.4045541647807504582 ) ) ;
#14785=CARTESIAN_POINT ( 'NONE',  ( 55.79472521941428198, -0.7279028900788538925, -72.75035398477137960 ) ) ;
#14786=CARTESIAN_POINT ( 'NONE',  ( 109.1586059443104944, -0.006344953511164451443, -0.003127959656212844081 ) ) ;
#14787=ADVANCED_FACE ( 'NONE', ( #15900 ), #20861, .F. ) ;
#14790=CIRCLE ( 'NONE', #14299, 151.1787379149930359 ) ;
#14792=ADVANCED_FACE ( 'NONE', ( #5382 ), #23814, .F. ) ;
#14793=CARTESIAN_POINT ( 'NONE',  ( 25.86096068574579121, 74.90357932134628527, 84.67961880569320954 ) ) ;
#14795=CARTESIAN_POINT ( 'NONE',  ( 25.69398547355839568, -55.82723250638839119, 98.18017599249827754 ) ) ;
#14796=EDGE_CURVE ( 'NONE', #3608, #7265, #9858, .T. ) ;
#14797=ORIENTED_EDGE ( 'NONE', *, *, #7729, .F. ) ;
#14798=CARTESIAN_POINT ( 'NONE',  ( 19.66333377628708945, -33.01772659807196675, 133.7337774474998469 ) ) ;
#14799=( BOUNDED_SURFACE ( )  B_SPLINE_SURFACE ( 3, 1, ( 
 ( #8025, #14320 ),
 ( #8154, #3528 ),
 ( #14750, #5409 ),
 ( #7590, #7880 ) ),
 .UNSPECIFIED., .F., .F., .F. ) 
 B_SPLINE_SURFACE_WITH_KNOTS ( ( 4, 4 ),
 ( 2, 2 ),
 ( 0.000000000000000000, 1.000000000000000000 ),
 ( 0.000000000000000000, 1.000000000000000000 ),
 .UNSPECIFIED. ) 
 GEOMETRIC_REPRESENTATION_ITEM ( )  RATIONAL_B_SPLINE_SURFACE ( (
 ( 1.000000000000000000, 1.000000000000000000),
 ( 0.6386103224230302855, 0.9954351624131538845),
 ( 0.6386103224230302855, 0.9954351624131538845),
 ( 1.000000000000000000, 1.000000000000000000) ) ) 
 REPRESENTATION_ITEM ( '' )  SURFACE ( )  );
#14801=EDGE_LOOP ( 'NONE', ( #22308, #7526, #27535, #4302 ) ) ;
#14805=AXIS2_PLACEMENT_3D ( 'NONE', #2816, #12170, #5112 ) ;
#14806=CARTESIAN_POINT ( 'NONE',  ( 1.832998868059890096, 29.64765804470269472, -142.0492247521719946 ) ) ;
#14808=AXIS2_PLACEMENT_3D ( 'NONE', #10412, #7982, #14567 ) ;
#14810=CARTESIAN_POINT ( 'NONE',  ( 1.833838850855473712, 138.0350826608193699, -44.75675607098784781 ) ) ;
#14811=CARTESIAN_POINT ( 'NONE',  ( 109.1587776205901861, -0.006944419901758113779, 0.002343968083398812255 ) ) ;
#14814=CARTESIAN_POINT ( 'NONE',  ( 25.64700659047694131, 35.10784848926805779, -107.3144208978481515 ) ) ;
#14816=EDGE_CURVE ( 'NONE', #14114, #6438, #956, .T. ) ;
#14821=CARTESIAN_POINT ( 'NONE',  ( 25.64692232868534560, -84.12764974007976093, -75.30916867847187746 ) ) ;
#14822=CARTESIAN_POINT ( 'NONE',  ( 32.73300124599740002, 116.5274707358857142, -16.10546300444702794 ) ) ;
#14823=CARTESIAN_POINT ( 'NONE',  ( 1.834118845439484335, -141.9019470378985659, -30.34413640949841096 ) ) ;
#14825=ORIENTED_EDGE ( 'NONE', *, *, #18431, .T. ) ;
#14826=CARTESIAN_POINT ( 'NONE',  ( 1.833750490713730752, -144.3424379351781397, 14.90257883162705532 ) ) ;
#14828=EDGE_CURVE ( 'NONE', #26408, #15445, #9198, .T. ) ;
#14829=CARTESIAN_POINT ( 'NONE',  ( 1.834118845439484335, 15.34511559672683489, 144.2964192726482793 ) ) ;
#14830=CIRCLE ( 'NONE', #17132, 151.1787379149930359 ) ;
#14831=CARTESIAN_POINT ( 'NONE',  ( 25.64670758986459731, 65.96397693491162784, 91.63870681572846877 ) ) ;
#14833=VECTOR ( 'NONE', #6899, 1000.000000000000227 ) ;
#14835=CARTESIAN_POINT ( 'NONE',  ( 25.64708228042118776, -45.96113332231410453, 103.1335618347710295 ) ) ;
#14840=CARTESIAN_POINT ( 'NONE',  ( 1.893872463202069145, 29.24569695044243645, 142.1730500379299826 ) ) ;
#14841=CIRCLE ( 'NONE', #26339, 151.1787379149930359 ) ;
#14842=CARTESIAN_POINT ( 'NONE',  ( 109.1589550718174877, 0.007571935245604908930, 0.0002241941239240737905 ) ) ;
#14844=LINE ( 'NONE', #3621, #516 ) ;
#14847=CARTESIAN_POINT ( 'NONE',  ( 10.93730112725972425, -42.00474393596362432, 145.2260730187398678 ) ) ;
#14848=ORIENTED_EDGE ( 'NONE', *, *, #17573, .T. ) ;
#14849=CARTESIAN_POINT ( 'NONE',  ( 109.1592201516379674, 0.006044422199831473233, 0.005027640251764405217 ) ) ;
#14851=B_SPLINE_CURVE_WITH_KNOTS ( 'NONE', 3,
 ( #1740, #10539, #23928, #21183, #6356, #10408, #21329 ),
 .UNSPECIFIED., .F., .F.,
 ( 4, 3, 4 ),
 ( 0.000000000000000000, 0.02398743853561430966, 0.04000277880656213925 ),
 .UNSPECIFIED. ) ;
#14852=CARTESIAN_POINT ( 'NONE',  ( 1.833838848569426805, 58.85887272891370259, -132.6367525013571367 ) ) ;
#14853=CARTESIAN_POINT ( 'NONE',  ( 6.224689322667630975, -108.2965163446067152, -100.9623537450662809 ) ) ;
#14854=EDGE_CURVE ( 'NONE', #21976, #21463, #20210, .T. ) ;
#14855=CARTESIAN_POINT ( 'NONE',  ( 2.433796855181205476, -138.8296532063090751, 43.58222566461595449 ) ) ;
#14856=CARTESIAN_POINT ( 'NONE',  ( 1.833750490713697223, 97.29556423840286072, -107.6587173638736630 ) ) ;
#14857=CARTESIAN_POINT ( 'NONE',  ( 30.59138290137919469, 99.26509990456105470, -60.43009393261889528 ) ) ;
#14858=ADVANCED_FACE ( 'NONE', ( #11542 ), #26710, .F. ) ;
#14860=DIRECTION ( 'NONE',  ( -0.5946245182733607137, -0.2512550613902121976, -0.7637359336799429688 ) ) ;
#14863=ORIENTED_EDGE ( 'NONE', *, *, #522, .T. ) ;
#14864=ORIENTED_EDGE ( 'NONE', *, *, #14938, .F. ) ;
#14865=CARTESIAN_POINT ( 'NONE',  ( 1.832998868059890096, -141.8272129421610828, 30.69214149073967590 ) ) ;
#14866=CARTESIAN_POINT ( 'NONE',  ( 21.16825799904901828, 37.62905626541876103, -130.1008673867301297 ) ) ;
#14867=VERTEX_POINT ( 'NONE', #13985 ) ;
#14869=ORIENTED_EDGE ( 'NONE', *, *, #2728, .T. ) ;
#14870=AXIS2_PLACEMENT_3D ( 'NONE', #3140, #20686, #9915 ) ;
#14875=FACE_OUTER_BOUND ( 'NONE', #2591, .T. ) ;
#14877=DIRECTION ( 'NONE',  ( -0.5914120900931443270, 0.8010740644654249509, -0.09226095020377109157 ) ) ;
#14878=ADVANCED_FACE ( 'NONE', ( #20749 ), #9504, .F. ) ;
#14879=FACE_OUTER_BOUND ( 'NONE', #10140, .T. ) ;
#14882=VERTEX_POINT ( 'NONE', #25088 ) ;
#14884=CARTESIAN_POINT ( 'NONE',  ( 109.1586900883932856, 0.0001010081143975987133, 0.007137750914550313082 ) ) ;
#14886=EDGE_CURVE ( 'NONE', #26705, #21599, #5384, .T. ) ;
#14887=CARTESIAN_POINT ( 'NONE',  ( 25.64708010899960655, -103.1718249732472117, -45.87517365398588964 ) ) ;
#14888=CARTESIAN_POINT ( 'NONE',  ( 25.73574536432413851, 91.86645484851398180, -65.74844932374561779 ) ) ;
#14890=CARTESIAN_POINT ( 'NONE',  ( 2.430230287190581429, -46.34481016236919260, 137.9371479820460991 ) ) ;
#14891=CARTESIAN_POINT ( 'NONE',  ( 1.833485406944043827, -144.2578170162061895, -15.69895494453532869 ) ) ;
#14895=B_SPLINE_CURVE_WITH_KNOTS ( 'NONE', 3,
 ( #17284, #21898, #4334, #12966, #21761, #7, #24210, #26350, #26486, #11100 ),
 .UNSPECIFIED., .F., .F.,
 ( 4, 3, 3, 4 ),
 ( 3.469446951953614189E-17, 0.0002669559177086189305, 0.0005339118354150960196, 0.001067817517169165984 ),
 .UNSPECIFIED. ) ;
#14899=FACE_OUTER_BOUND ( 'NONE', #25111, .T. ) ;
#14901=CARTESIAN_POINT ( 'NONE',  ( 30.59141879584294088, -55.75104644134820120, -101.9665761624296181 ) ) ;
#14903=CARTESIAN_POINT ( 'NONE',  ( 1.833485406944043827, 141.8265699653867387, 30.69200235378984232 ) ) ;
#14904=CARTESIAN_POINT ( 'NONE',  ( 25.64660436782541808, -107.2041192742818509, 35.44263474731908303 ) ) ;
#14905=CARTESIAN_POINT ( 'NONE',  ( 1.831572820252009626, -116.8148281295974868, 86.09108691067734753 ) ) ;
#14906=DIRECTION ( 'NONE',  ( 0.000000000000000000, 0.000000000000000000, 1.000000000000000000 ) ) ;
#14907=EDGE_CURVE ( 'NONE', #24734, #18908, #20524, .T. ) ;
#14908=VERTEX_POINT ( 'NONE', #14416 ) ;
#14909=CARTESIAN_POINT ( 'NONE',  ( 25.64660436782539321, 103.3839381879733992, 45.39454672041161132 ) ) ;
#14911=DIRECTION ( 'NONE',  ( 0.000000000000000000, 1.000000000000000000, -6.938893903907228378E-16 ) ) ;
#14912=EDGE_CURVE ( 'NONE', #21365, #25689, #10273, .T. ) ;
#14913=ORIENTED_EDGE ( 'NONE', *, *, #4099, .F. ) ;
#14917=CARTESIAN_POINT ( 'NONE',  ( 109.1592201516379674, 0.005485778713202931790, 0.005631912476303835985 ) ) ;
#14920=VERTEX_POINT ( 'NONE', #19032 ) ;
#14922=CARTESIAN_POINT ( 'NONE',  ( 109.1586900883932856, -0.006757191295060861226, -0.002301750759599751131 ) ) ;
#14924=CARTESIAN_POINT ( 'NONE',  ( 25.64692872815576408, -112.3258062264003172, 11.48248630407242743 ) ) ;
#14925=CARTESIAN_POINT ( 'NONE',  ( 1.832998868059890096, 141.8272129421608838, 30.69214149074059961 ) ) ;
#14927=CARTESIAN_POINT ( 'NONE',  ( 28.37599760073042887, 75.42809173301607473, 86.45296943207047491 ) ) ;
#14929=ORIENTED_EDGE ( 'NONE', *, *, #26407, .T. ) ;
#14930=CARTESIAN_POINT ( 'NONE',  ( 109.1592201516379674, 0.004867031887010210903, -0.006174480289200333372 ) ) ;
#14931=ORIENTED_EDGE ( 'NONE', *, *, #26065, .F. ) ;
#14932=CARTESIAN_POINT ( 'NONE',  ( 32.73300124599739291, -113.0038235389599635, -32.68291970228351317 ) ) ;
#14933=CARTESIAN_POINT ( 'NONE',  ( 25.81918753295377300, 65.67738364544850072, -91.98563552012969069 ) ) ;
#14934=CARTESIAN_POINT ( 'NONE',  ( 25.64699802086727942, 103.0525896353907882, -46.14225289916203110 ) ) ;
#14935=CARTESIAN_POINT ( 'NONE',  ( 55.49584447822657296, 36.04376091928632064, -62.96491934285955239 ) ) ;
#14936=EDGE_CURVE ( 'NONE', #119, #24971, #8160, .T. ) ;
#14938=EDGE_CURVE ( 'NONE', #2577, #10758, #22214, .T. ) ;
#14940=CARTESIAN_POINT ( 'NONE',  ( 1.833485406944043827, 137.8414413349092058, -45.34878176254091642 ) ) ;
#14942=CARTESIAN_POINT ( 'NONE',  ( 1.833485406944043827, -132.3460930279895535, 59.50871042846178938 ) ) ;
#14943=EDGE_CURVE ( 'NONE', #14322, #309, #28074, .T. ) ;
#14947=CARTESIAN_POINT ( 'NONE',  ( 109.1721716018069657, -0.01695288006057377866, 0.001984900887706570523 ) ) ;
#14949=ORIENTED_EDGE ( 'NONE', *, *, #22802, .F. ) ;
#14952=CARTESIAN_POINT ( 'NONE',  ( 109.1592201516379674, -0.006536841731953435194, 0.004368284148528988643 ) ) ;
#14953=CARTESIAN_POINT ( 'NONE',  ( 55.49584447822657296, -58.53775398922227424, -42.86099773636601640 ) ) ;
#14954=CARTESIAN_POINT ( 'NONE',  ( 26.11404676487256893, -92.25884714080449100, 65.63269960453210672 ) ) ;
#14955=LINE ( 'NONE', #17121, #22562 ) ;
#14956=DIRECTION ( 'NONE',  ( -1.000000000000000000, -0.000000000000000000, -0.000000000000000000 ) ) ;
#14957=( BOUNDED_SURFACE ( )  B_SPLINE_SURFACE ( 3, 1, ( 
 ( #24983, #22682 ),
 ( #20636, #5526 ),
 ( #27100, #26829 ),
 ( #20357, #16322 ) ),
 .UNSPECIFIED., .F., .F., .F. ) 
 B_SPLINE_SURFACE_WITH_KNOTS ( ( 4, 4 ),
 ( 2, 2 ),
 ( 0.000000000000000000, 1.000000000000000000 ),
 ( 0.000000000000000000, 1.000000000000000000 ),
 .UNSPECIFIED. ) 
 GEOMETRIC_REPRESENTATION_ITEM ( )  RATIONAL_B_SPLINE_SURFACE ( (
 ( 1.000000000000000000, 1.000000000000000000),
 ( 0.9956975270656955868, 0.8568959468854907557),
 ( 0.9956975270656955868, 0.8568959468854907557),
 ( 1.000000000000000000, 1.000000000000000000) ) ) 
 REPRESENTATION_ITEM ( '' )  SURFACE ( )  );
#14960=ORIENTED_EDGE ( 'NONE', *, *, #20732, .T. ) ;
#14961=CARTESIAN_POINT ( 'NONE',  ( 2.063896406836609909, 107.0521644432430577, -98.19887492195755385 ) ) ;
#14964=CARTESIAN_POINT ( 'NONE',  ( 1.834118845439484335, 14.99112450600249424, 144.3336252355297802 ) ) ;
#14966=CARTESIAN_POINT ( 'NONE',  ( 32.73300124599741423, -97.37344512919810313, -66.00340565729437969 ) ) ;
#14971=EDGE_LOOP ( 'NONE', ( #26678, #14515, #26878, #9422 ) ) ;
#14973=ORIENTED_EDGE ( 'NONE', *, *, #21320, .T. ) ;
#14975=CONICAL_SURFACE ( 'NONE', #18658, 117.6351876552689504, 0.9945805576725580410 ) ;
#14976=CARTESIAN_POINT ( 'NONE',  ( 1.834118845439484335, -117.5010238212704081, 85.14950727125821572 ) ) ;
#14980=B_SPLINE_CURVE_WITH_KNOTS ( 'NONE', 3,
 ( #14989, #14857, #4053, #21614 ),
 .UNSPECIFIED., .F., .F.,
 ( 4, 4 ),
 ( 6.469565094841817044E-16, 0.008383748772660085113 ),
 .UNSPECIFIED. ) ;
#14981=PLANE ( 'NONE',  #23075 ) ;
#14982=CARTESIAN_POINT ( 'NONE',  ( 8.186469777910764023, -42.84118569629447393, 143.0750864738774908 ) ) ;
#14983=ORIENTED_EDGE ( 'NONE', *, *, #24594, .F. ) ;
#14985=B_SPLINE_CURVE_WITH_KNOTS ( 'NONE', 3,
 ( #15417, #25824, #19609, #21630, #6119, #23684, #24232, #12707 ),
 .UNSPECIFIED., .F., .F.,
 ( 4, 2, 2, 4 ),
 ( 1.993045536433795054E-17, 0.0002429588503611392926, 0.0004859177007222586901, 0.0009718354014445028518 ),
 .UNSPECIFIED. ) ;
#14989=CARTESIAN_POINT ( 'NONE',  ( 32.73300124599738581, 99.90245962373917621, -62.10906484417127871 ) ) ;
#14990=LINE ( 'NONE', #26211, #9242 ) ;
#14992=ORIENTED_EDGE ( 'NONE', *, *, #5666, .T. ) ;
#14993=ORIENTED_EDGE ( 'NONE', *, *, #21951, .F. ) ;
#14998=VERTEX_POINT ( 'NONE', #9980 ) ;
#15000=EDGE_CURVE ( 'NONE', #823, #17620, #8791, .T. ) ;
#15001=CARTESIAN_POINT ( 'NONE',  ( 24.01988960052059596, 84.46375358746919915, 100.1926921796487022 ) ) ;
#15002=ADVANCED_FACE ( 'NONE', ( #24065 ), #26213, .F. ) ;
#15006=DIRECTION ( 'NONE',  ( -0.5914120900931443270, 0.3352908775637156724, 0.7333565075147365775 ) ) ;
#15007=CARTESIAN_POINT ( 'NONE',  ( 28.37603512858453669, -65.97809844506187460, 93.86378016273945946 ) ) ;
#15008=CARTESIAN_POINT ( 'NONE',  ( 1.833485406944043827, -14.63699153649261575, -144.3694338680886347 ) ) ;
#15009=CARTESIAN_POINT ( 'NONE',  ( 6.224689322667630975, 144.2687111683195269, 33.28770499679384187 ) ) ;
#15011=CARTESIAN_POINT ( 'NONE',  ( 1.833721034905678948, 132.4192200895890323, -59.34646046113644502 ) ) ;
#15014=CARTESIAN_POINT ( 'NONE',  ( 2.263178113027034755, 144.7392881653025825, -13.80342493153361971 ) ) ;
#15017=CARTESIAN_POINT ( 'NONE',  ( 109.1778270068192853, 0.008360410075196072002, -0.004106684808170042375 ) ) ;
#15018=ADVANCED_FACE ( 'NONE', ( #26338 ), #20496, .F. ) ;
#15020=ORIENTED_EDGE ( 'NONE', *, *, #16176, .F. ) ;
#15021=CARTESIAN_POINT ( 'NONE',  ( 26.11404676487256893, -12.95861723607530003, 112.4785329405481349 ) ) ;
#15022=CARTESIAN_POINT ( 'NONE',  ( 32.73300124599732186, 0.000000000000000000, 0.000000000000000000 ) ) ;
#15025=EDGE_LOOP ( 'NONE', ( #20601, #14292, #8419, #3395 ) ) ;
#15027=CARTESIAN_POINT ( 'NONE',  ( 2.433796855181233454, 118.5671979538056888, 84.34988187690970562 ) ) ;
#15028=ORIENTED_EDGE ( 'NONE', *, *, #17280, .F. ) ;
#15029=ADVANCED_FACE ( 'NONE', ( #15390 ), #22536, .F. ) ;
#15030=B_SPLINE_CURVE_WITH_KNOTS ( 'NONE', 3,
 ( #10658, #17122, #4024, #8218, #23634, #6337, #14822 ),
 .UNSPECIFIED., .F., .F.,
 ( 4, 3, 4 ),
 ( 4.987111262633357592E-16, 0.02816610861753247180, 0.04000277880656273599 ),
 .UNSPECIFIED. ) ;
#15031=CARTESIAN_POINT ( 'NONE',  ( 2.433796855181205476, -13.76554153471595043, -144.8571464219890572 ) ) ;
#15033=EDGE_CURVE ( 'NONE', #16027, #19236, #6449, .T. ) ;
#15036=CARTESIAN_POINT ( 'NONE',  ( 25.81918753295379432, -110.7464580477335971, -22.58534689649783544 ) ) ;
#15037=CARTESIAN_POINT ( 'NONE',  ( 55.79472521941426777, 71.31192372336693097, -14.41365263906483207 ) ) ;
#15039=DIRECTION ( 'NONE',  ( -0.5914120900931443270, 0.7693434820005534691, 0.2415416038592990700 ) ) ;
#15040=CARTESIAN_POINT ( 'NONE',  ( 10.93730112726006354, 150.7858122213665126, -10.89264110824830034 ) ) ;
#15041=LINE ( 'NONE', #13038, #18961 ) ;
#15042=CARTESIAN_POINT ( 'NONE',  ( 8.186469829614045679, 97.33125097511879176, 113.2805153378639886 ) ) ;
#15044=EDGE_LOOP ( 'NONE', ( #8653, #2669, #18178, #5612 ) ) ;
#15045=VERTEX_POINT ( 'NONE', #8644 ) ;
#15046=CARTESIAN_POINT ( 'NONE',  ( 2.433796855181233454, 16.65276281464563723, 144.5536872373192807 ) ) ;
#15049=CARTESIAN_POINT ( 'NONE',  ( 28.37644542392839142, 58.62516076110045304, 109.6517504963491518 ) ) ;
#15050=CARTESIAN_POINT ( 'NONE',  ( 25.81918753295378011, -90.88802830332004135, 67.18811037444402245 ) ) ;
#15053=CARTESIAN_POINT ( 'NONE',  ( 109.1592201516379674, 0.007376275279032895593, -0.002720803050370492436 ) ) ;
#15055=CARTESIAN_POINT ( 'NONE',  ( 25.87036335909428075, -55.67065048714079012, 98.40409479825417804 ) ) ;
#15056=ORIENTED_EDGE ( 'NONE', *, *, #27325, .T. ) ;
#15058=AXIS2_PLACEMENT_3D ( 'NONE', #12664, #6214, #23780 ) ;
#15059=CARTESIAN_POINT ( 'NONE',  ( 109.1586900883932856, 0.002109621908814802386, -0.006819617742893407421 ) ) ;
#15060=B_SPLINE_CURVE_WITH_KNOTS ( 'NONE', 3,
 ( #5537, #1610, #14020, #23119, #7720, #25268, #10410, #5249, #20643, #8388 ),
 .UNSPECIFIED., .F., .F.,
 ( 4, 3, 3, 4 ),
 ( 2.775557561562891351E-17, 0.0002669559177086295015, 0.0005339118354150786724, 0.001067817517169166635 ),
 .UNSPECIFIED. ) ;
#15061=ADVANCED_FACE ( 'NONE', ( #19444 ), #2678, .F. ) ;
#15066=CARTESIAN_POINT ( 'NONE',  ( 2.263178607246642216, 108.9830946142713941, 96.24282447295480836 ) ) ;
#15067=EDGE_CURVE ( 'NONE', #9049, #11142, #4672, .T. ) ;
#15073=B_SPLINE_CURVE_WITH_KNOTS ( 'NONE', 3,
 ( #13020, #4385, #21810, #2068, #6408, #1933, #8705, #21947 ),
 .UNSPECIFIED., .F., .F.,
 ( 4, 2, 2, 4 ),
 ( 0.000000000000000000, 0.0002429588503611198041, 0.0004859177007222396081, 0.0009718354014444737952 ),
 .UNSPECIFIED. ) ;
#15074=CARTESIAN_POINT ( 'NONE',  ( 21.16825799904898631, 23.82367662028005384, -133.3214686481435081 ) ) ;
#15078=CARTESIAN_POINT ( 'NONE',  ( 25.69398547355838858, -46.61500694509577158, -102.8740393624598681 ) ) ;
#15080=ORIENTED_EDGE ( 'NONE', *, *, #20280, .F. ) ;
#15081=EDGE_LOOP ( 'NONE', ( #25812, #22146, #8375, #22383 ) ) ;
#15082=ORIENTED_EDGE ( 'NONE', *, *, #17631, .F. ) ;
#15089=ADVANCED_FACE ( 'NONE', ( #26902 ), #14618, .F. ) ;
#15090=CARTESIAN_POINT ( 'NONE',  ( 16.75465622695626067, 75.09093759627036491, -120.7871673903169238 ) ) ;
#15091=CARTESIAN_POINT ( 'NONE',  ( 1.833206308920069638, 97.64934899952852732, -107.3376449983717720 ) ) ;
#15092=ORIENTED_EDGE ( 'NONE', *, *, #18024, .F. ) ;
#15093=CARTESIAN_POINT ( 'NONE',  ( 32.73300124599735739, 39.98094346392311138, 110.6325518752275485 ) ) ;
#15094=CARTESIAN_POINT ( 'NONE',  ( 26.28373643307409324, -55.65614982951218082, -114.7784771129679910 ) ) ;
#15095=CARTESIAN_POINT ( 'NONE',  ( 25.64699802086725455, 23.24292564406190564, -110.4930320910558663 ) ) ;
#15096=CARTESIAN_POINT ( 'NONE',  ( 1.832998868059890096, 15.69902610990374647, 144.2584710144581095 ) ) ;
#15099=CARTESIAN_POINT ( 'NONE',  ( 25.64708228042120908, -112.2886173090158763, -11.84161204513374699 ) ) ;
#15100=DIRECTION ( 'NONE',  ( 0.000000000000000000, 0.000000000000000000, 1.000000000000000000 ) ) ;
#15101=ORIENTED_EDGE ( 'NONE', *, *, #16125, .F. ) ;
#15103=ORIENTED_EDGE ( 'NONE', *, *, #2764, .T. ) ;
#15104=VERTEX_POINT ( 'NONE', #712 ) ;
#15105=CARTESIAN_POINT ( 'NONE',  ( 109.1586059443104944, 0.005438258427225613027, -0.004524147648833186895 ) ) ;
#15107=CARTESIAN_POINT ( 'NONE',  ( 1.833603222531960730, 72.16916166673740918, 125.8904991419469468 ) ) ;
#15109=LINE ( 'NONE', #1468, #22054 ) ;
#15115=B_SPLINE_CURVE_WITH_KNOTS ( 'NONE', 3,
 ( #26053, #16988, #3602, #15094, #25922, #25781, #5928 ),
 .UNSPECIFIED., .F., .F.,
 ( 4, 3, 4 ),
 ( 5.174130838430530436E-16, 0.02816610861753244405, 0.04000277880656296497 ),
 .UNSPECIFIED. ) ;
#15116=CARTESIAN_POINT ( 'NONE',  ( 1.833603222531973609, 97.42748212378425876, -107.5392551439144313 ) ) ;
#15118=CARTESIAN_POINT ( 'NONE',  ( 2.430230287190592531, 43.58368230469574200, -138.8342928068215656 ) ) ;
#15119=CARTESIAN_POINT ( 'NONE',  ( 2.430230287190572103, -142.0258656395019443, -31.67257033707649683 ) ) ;
#15120=EDGE_CURVE ( 'NONE', #8537, #7646, #1381, .T. ) ;
#15122=ADVANCED_FACE ( 'NONE', ( #26756 ), #14731, .T. ) ;
#15123=ORIENTED_EDGE ( 'NONE', *, *, #3384, .F. ) ;
#15124=CARTESIAN_POINT ( 'NONE',  ( 109.1586059443104944, -0.0002768082440195784389, 0.007068659269322299411 ) ) ;
#15126=ORIENTED_EDGE ( 'NONE', *, *, #11901, .T. ) ;
#15128=ORIENTED_EDGE ( 'NONE', *, *, #25197, .T. ) ;
#15129=B_SPLINE_CURVE_WITH_KNOTS ( 'NONE', 3,
 ( #8193, #6442, #23879, #21553, #26153, #3863 ),
 .UNSPECIFIED., .F., .F.,
 ( 4, 2, 4 ),
 ( 3.903127820947815962E-18, 0.0006311636237756731646, 0.001262327247551342426 ),
 .UNSPECIFIED. ) ;
#15130=CARTESIAN_POINT ( 'NONE',  ( 1.833838850093465700, 138.0075868208086547, 44.84137955663270247 ) ) ;
#15133=( BOUNDED_SURFACE ( )  B_SPLINE_SURFACE ( 3, 1, ( 
 ( #24681, #15718 ),
 ( #24534, #4798 ),
 ( #13562, #26806 ),
 ( #13992, #11408 ) ),
 .UNSPECIFIED., .F., .F., .F. ) 
 B_SPLINE_SURFACE_WITH_KNOTS ( ( 4, 4 ),
 ( 2, 2 ),
 ( 0.000000000000000000, 1.000000000000000000 ),
 ( 0.000000000000000000, 1.000000000000000000 ),
 .UNSPECIFIED. ) 
 GEOMETRIC_REPRESENTATION_ITEM ( )  RATIONAL_B_SPLINE_SURFACE ( (
 ( 1.000000000000000000, 1.000000000000000000),
 ( 0.9956975270656954757, 0.8568959468854893125),
 ( 0.9956975270656954757, 0.8568959468854893125),
 ( 1.000000000000000000, 1.000000000000000000) ) ) 
 REPRESENTATION_ITEM ( '' )  SURFACE ( )  );
#15134=DIRECTION ( 'NONE',  ( -0.5914120900931443270, -0.7693434820005518038, -0.2415416038593042602 ) ) ;
#15135=CARTESIAN_POINT ( 'NONE',  ( 109.1587776205901861, -0.006995903587863990490, -0.002185517590237659631 ) ) ;
#15138=CARTESIAN_POINT ( 'NONE',  ( 1.834118845439484335, -72.40084790867243214, -125.7578880615052412 ) ) ;
#15139=DIRECTION ( 'NONE',  ( 0.5946245182733607137, -0.7356888587241680044, 0.3243201896541516027 ) ) ;
#15142=ORIENTED_EDGE ( 'NONE', *, *, #15603, .F. ) ;
#15143=EDGE_CURVE ( 'NONE', #26642, #2443, #19110, .T. ) ;
#15144=CARTESIAN_POINT ( 'NONE',  ( 1.831572820252008738, 108.4969585352567663, -96.36280042115824074 ) ) ;
#15145=CARTESIAN_POINT ( 'NONE',  ( 26.11404676487259024, -57.58742681967517285, 97.48350837663589630 ) ) ;
#15150=CARTESIAN_POINT ( 'NONE',  ( 10.93730112725932635, 0.000000000000000000, 0.000000000000000000 ) ) ;
#15151=CARTESIAN_POINT ( 'NONE',  ( 109.1589550718174877, 0.006257602293694210574, -0.004269295012386581552 ) ) ;
#15152=VERTEX_POINT ( 'NONE', #11229 ) ;
#15154=EDGE_CURVE ( 'NONE', #12210, #2861, #20473, .T. ) ;
#15155=CARTESIAN_POINT ( 'NONE',  ( 2.263178113027048077, 118.4461880110615084, -84.32376073259102611 ) ) ;
#15160=ADVANCED_FACE ( 'NONE', ( #2582 ), #28070, .F. ) ;
#15162=CARTESIAN_POINT ( 'NONE',  ( 2.063896406836609909, 118.3103904147681789, 84.29612368209191686 ) ) ;
#15164=CARTESIAN_POINT ( 'NONE',  ( 109.1589550718175161, 0.005477029346534926200, -0.005233222325307182281 ) ) ;
#15166=AXIS2_PLACEMENT_3D ( 'NONE', #5862, #10188, #1528 ) ;
#15167=FACE_OUTER_BOUND ( 'NONE', #4057, .T. ) ;
#15168=CARTESIAN_POINT ( 'NONE',  ( 109.1778270068192853, -0.007885345421917336339, 0.004958088776549072693 ) ) ;
#15169=AXIS2_PLACEMENT_3D ( 'NONE', #19607, #26507, #2174 ) ;
#15170=B_SPLINE_CURVE_WITH_KNOTS ( 'NONE', 3,
 ( #2994, #7181, #22288, #2548 ),
 .UNSPECIFIED., .F., .F.,
 ( 4, 4 ),
 ( 0.000000000000000000, 0.01077107196513873988 ),
 .UNSPECIFIED. ) ;
#15171=CARTESIAN_POINT ( 'NONE',  ( 109.1587776205901577, -0.003057017121591250504, 0.006661366261224488383 ) ) ;
#15172=CARTESIAN_POINT ( 'NONE',  ( 109.1586900883932856, 0.006479576224398247292, -0.002995460350188419631 ) ) ;
#15173=CARTESIAN_POINT ( 'NONE',  ( 25.86096068574580187, -112.3259320600844120, -12.80894308910849055 ) ) ;
#15176=CARTESIAN_POINT ( 'NONE',  ( 109.1586900883932856, 0.007109207791180751322, 0.0006456433529069300226 ) ) ;
#15179=EDGE_CURVE ( 'NONE', #27431, #11422, #7442, .T. ) ;
#15186=CARTESIAN_POINT ( 'NONE',  ( 25.64681081121880624, -75.86069728268932977, -83.63051021305977883 ) ) ;
#15187=CARTESIAN_POINT ( 'NONE',  ( 25.70243777736189728, 97.44734253939077462, 57.10783651464997490 ) ) ;
#15188=CARTESIAN_POINT ( 'NONE',  ( 25.69398547355838502, 90.93418986874891630, -66.98507266663659721 ) ) ;
#15189=ORIENTED_EDGE ( 'NONE', *, *, #313, .T. ) ;
#15190=CARTESIAN_POINT ( 'NONE',  ( 1.833838850093440387, -44.84137955663319275, 138.0075868208085694 ) ) ;
#15194=CARTESIAN_POINT ( 'NONE',  ( 2.430230287190581429, -60.50928654924843642, 132.3371620660948906 ) ) ;
#15195=CARTESIAN_POINT ( 'NONE',  ( 2.433796855181205476, -145.5024947199069629, -1.451562450951161987 ) ) ;
#15196=CARTESIAN_POINT ( 'NONE',  ( 25.64681081121880624, -56.09509703373412748, 97.99105938547904771 ) ) ;
#15199=CARTESIAN_POINT ( 'NONE',  ( 109.1589550718175161, -0.004632048724982944926, -0.005994046294305891559 ) ) ;
#15201=CARTESIAN_POINT ( 'NONE',  ( 1.894214914920945514, -59.90782071839110756, -132.2104617488243150 ) ) ;
#15202=ORIENTED_EDGE ( 'NONE', *, *, #3299, .F. ) ;
#15203=CARTESIAN_POINT ( 'NONE',  ( 10.93730112725932635, 0.000000000000000000, 0.000000000000000000 ) ) ;
#15205=DIRECTION ( 'NONE',  ( 0.000000000000000000, 0.000000000000000000, -1.000000000000000000 ) ) ;
#15207=CARTESIAN_POINT ( 'NONE',  ( 10.93730112725932635, 0.000000000000000000, 0.000000000000000000 ) ) ;
#15213=CARTESIAN_POINT ( 'NONE',  ( 119.2224693531408803, -69.99999999999998579, -40.00000000000002132 ) ) ;
#15216=CARTESIAN_POINT ( 'NONE',  ( 2.063896406836605024, 132.1577797566306458, 60.31174178979853195 ) ) ;
#15217=LINE ( 'NONE', #10507, #12974 ) ;
#15219=ORIENTED_EDGE ( 'NONE', *, *, #15285, .F. ) ;
#15220=AXIS2_PLACEMENT_3D ( 'NONE', #15440, #21802, #21652 ) ;
#15221=VERTEX_POINT ( 'NONE', #27618 ) ;
#15223=DIRECTION ( 'NONE',  ( 0.000000000000000000, 0.000000000000000000, 1.000000000000000000 ) ) ;
#15226=CARTESIAN_POINT ( 'NONE',  ( 109.1587776205901861, 0.001605238040368368738, 0.007151389024635758027 ) ) ;
#15227=DIRECTION ( 'NONE',  ( 0.5914120900931445490, -0.6476200150380184706, -0.4804373588864787603 ) ) ;
#15229=CARTESIAN_POINT ( 'NONE',  ( 32.73300124599738581, -16.10546300444743650, -116.5274707358856858 ) ) ;
#15230=CARTESIAN_POINT ( 'NONE',  ( 13.84597867724974662, -146.3210145202069725, 10.56985607909754776 ) ) ;
#15234=CARTESIAN_POINT ( 'NONE',  ( 2.430230287190572103, -43.58368230469294247, -138.8342928068224751 ) ) ;
#15235=CARTESIAN_POINT ( 'NONE',  ( 25.65782528836479415, -112.9169519833626509, -0.5778133093789715735 ) ) ;
#15236=ADVANCED_FACE ( 'NONE', ( #3583 ), #21433, .F. ) ;
#15237=EDGE_CURVE ( 'NONE', #20966, #10454, #10208, .T. ) ;
#15239=EDGE_LOOP ( 'NONE', ( #4627, #5679, #19093, #13055 ) ) ;
#15244=VERTEX_POINT ( 'NONE', #25494 ) ;
#15245=VECTOR ( 'NONE', #7946, 1000.000000000000227 ) ;
#15248=DIRECTION ( 'NONE',  ( 0.000000000000000000, 0.000000000000000000, -1.000000000000000000 ) ) ;
#15249=ORIENTED_EDGE ( 'NONE', *, *, #20467, .T. ) ;
#15253=CONICAL_SURFACE ( 'NONE', #23127, 117.6351876552689504, 0.9945805576725580410 ) ;
#15254=DIRECTION ( 'NONE',  ( -1.000000000000000000, -0.000000000000000000, -0.000000000000000000 ) ) ;
#15255=ADVANCED_FACE ( 'NONE', ( #8342 ), #16115, .T. ) ;
#15256=CARTESIAN_POINT ( 'NONE',  ( 55.49584447822657296, 36.50733923851198170, 62.69727227546415094 ) ) ;
#15257=CARTESIAN_POINT ( 'NONE',  ( 2.063896406836609909, -144.6078654718900793, -13.84738934186338355 ) ) ;
#15258=CIRCLE ( 'NONE', #2898, 117.6351876552689504 ) ;
#15259=CARTESIAN_POINT ( 'NONE',  ( 32.73300124599735739, -62.10906484417306928, 99.90245962373816724 ) ) ;
#15262=VECTOR ( 'NONE', #23812, 1000.000000000000000 ) ;
#15263=CARTESIAN_POINT ( 'NONE',  ( 109.1586059443104944, 0.003127959656212866632, -0.006344953511164441902 ) ) ;
#15265=ORIENTED_EDGE ( 'NONE', *, *, #12962, .F. ) ;
#15266=ORIENTED_EDGE ( 'NONE', *, *, #8333, .F. ) ;
#15269=VERTEX_POINT ( 'NONE', #21565 ) ;
#15272=DIRECTION ( 'NONE',  ( -1.000000000000000000, -0.000000000000000000, -0.000000000000000000 ) ) ;
#15273=CIRCLE ( 'NONE', #15741, 117.6351876552689504 ) ;
#15274=( BOUNDED_SURFACE ( )  B_SPLINE_SURFACE ( 3, 1, ( 
 ( #11646, #9492 ),
 ( #702, #27021 ),
 ( #15263, #17570 ),
 ( #24902, #26356 ) ),
 .UNSPECIFIED., .F., .F., .F. ) 
 B_SPLINE_SURFACE_WITH_KNOTS ( ( 4, 4 ),
 ( 2, 2 ),
 ( 0.000000000000000000, 1.000000000000000000 ),
 ( 0.000000000000000000, 1.000000000000000000 ),
 .UNSPECIFIED. ) 
 GEOMETRIC_REPRESENTATION_ITEM ( )  RATIONAL_B_SPLINE_SURFACE ( (
 ( 1.000000000000000000, 1.000000000000000000),
 ( 0.9960225298536222738, 0.9999952330161893110),
 ( 0.9960225298536222738, 0.9999952330161893110),
 ( 1.000000000000000000, 1.000000000000000000) ) ) 
 REPRESENTATION_ITEM ( '' )  SURFACE ( )  );
#15275=FACE_OUTER_BOUND ( 'NONE', #18205, .T. ) ;
#15276=CIRCLE ( 'NONE', #2903, 151.1787379149930359 ) ;
#15277=CARTESIAN_POINT ( 'NONE',  ( 30.59138290137887140, -101.9665464510083694, -55.75105126024025282 ) ) ;
#15279=EDGE_CURVE ( 'NONE', #8696, #24633, #25989, .T. ) ;
#15281=EDGE_CURVE ( 'NONE', #13658, #21691, #6473, .T. ) ;
#15282=CARTESIAN_POINT ( 'NONE',  ( 109.1592201516379674, -0.002913740842103232798, 0.007302213399787543455 ) ) ;
#15285=EDGE_CURVE ( 'NONE', #28115, #2245, #2780, .T. ) ;
#15287=CARTESIAN_POINT ( 'NONE',  ( 13.36082413113063083, -137.0038452127805328, 67.94366799842767080 ) ) ;
#15291=DIRECTION ( 'NONE',  ( -1.000000000000000000, -0.000000000000000000, -0.000000000000000000 ) ) ;
#15292=CARTESIAN_POINT ( 'NONE',  ( 30.59141879584314694, 60.43012207291116766, -99.26511058698837076 ) ) ;
#15295=CARTESIAN_POINT ( 'NONE',  ( 1.833485406944057594, -0.5339064996874559599, -145.1085452359073429 ) ) ;
#15296=CARTESIAN_POINT ( 'NONE',  ( 28.43349137099835033, -80.08535015163967330, 94.99961975860227881 ) ) ;
#15300=VECTOR ( 'NONE', #9922, 1000.000000000000114 ) ;
#15301=FACE_OUTER_BOUND ( 'NONE', #12101, .T. ) ;
#15304=ORIENTED_EDGE ( 'NONE', *, *, #713, .F. ) ;
#15306=FACE_OUTER_BOUND ( 'NONE', #5698, .T. ) ;
#15307=ORIENTED_EDGE ( 'NONE', *, *, #9388, .F. ) ;
#15311=AXIS2_PLACEMENT_3D ( 'NONE', #5794, #23356, #27930 ) ;
#15312=( BOUNDED_SURFACE ( )  B_SPLINE_SURFACE ( 3, 1, ( 
 ( #8924, #4873 ),
 ( #15506, #18105 ),
 ( #26321, #15812 ),
 ( #13645, #17952 ) ),
 .UNSPECIFIED., .F., .F., .F. ) 
 B_SPLINE_SURFACE_WITH_KNOTS ( ( 4, 4 ),
 ( 2, 2 ),
 ( 0.000000000000000000, 1.000000000000000000 ),
 ( 0.000000000000000000, 1.000000000000000000 ),
 .UNSPECIFIED. ) 
 GEOMETRIC_REPRESENTATION_ITEM ( )  RATIONAL_B_SPLINE_SURFACE ( (
 ( 1.000000000000000000, 1.000000000000000000),
 ( 0.9956975270656955868, 0.8568959468854907557),
 ( 0.9956975270656955868, 0.8568959468854907557),
 ( 1.000000000000000000, 1.000000000000000000) ) ) 
 REPRESENTATION_ITEM ( '' )  SURFACE ( )  );
#15315=CARTESIAN_POINT ( 'NONE',  ( 6.224689322667647851, -121.2721959030532162, -84.93872395423099420 ) ) ;
#15316=CARTESIAN_POINT ( 'NONE',  ( 28.37599760073041821, -55.80522390574049041, -100.2461467136616307 ) ) ;
#15318=EDGE_CURVE ( 'NONE', #3680, #13750, #16346, .T. ) ;
#15322=CARTESIAN_POINT ( 'NONE',  ( 32.73300124599735739, 44.31599526637956643, 108.9684813982490539 ) ) ;
#15323=CARTESIAN_POINT ( 'NONE',  ( 1.833485406944057594, 125.9346397303435197, 72.09189602597754742 ) ) ;
#15324=CARTESIAN_POINT ( 'NONE',  ( 2.433796855181205476, -118.5671979538062146, 84.34988187690890982 ) ) ;
#15326=ORIENTED_EDGE ( 'NONE', *, *, #2905, .F. ) ;
#15327=CARTESIAN_POINT ( 'NONE',  ( 25.64703792032468499, 56.32669596053575134, -97.85829113439902471 ) ) ;
#15328=CARTESIAN_POINT ( 'NONE',  ( 1.831572820252009626, -86.09108691067693542, -116.8148281295977995 ) ) ;
#15330=CARTESIAN_POINT ( 'NONE',  ( 25.65782528836481902, 45.39960327191609935, 103.3897864210297115 ) ) ;
#15331=B_SPLINE_CURVE_WITH_KNOTS ( 'NONE', 3,
 ( #21370, #16788, #1226, #17188, #25976, #14315, #10025, #18787 ),
 .UNSPECIFIED., .F., .F.,
 ( 4, 2, 2, 4 ),
 ( 0.000000000000000000, 0.0002429592666046771667, 0.0004859185332093543335, 0.0009718370664186896934 ),
 .UNSPECIFIED. ) ;
#15332=PLANE ( 'NONE',  #17477 ) ;
#15333=CARTESIAN_POINT ( 'NONE',  ( 25.64681081121879203, 97.57530875170606066, 56.81519825470789442 ) ) ;
#15335=CARTESIAN_POINT ( 'NONE',  ( 1.833485406944043827, -137.8414413349082110, -45.34878176254374438 ) ) ;
#15336=ORIENTED_EDGE ( 'NONE', *, *, #26608, .F. ) ;
#15338=FACE_OUTER_BOUND ( 'NONE', #4043, .T. ) ;
#15339=CARTESIAN_POINT ( 'NONE',  ( 10.93730112725990367, -108.9902118373734652, -104.7670965581022671 ) ) ;
#15340=CARTESIAN_POINT ( 'NONE',  ( 32.73300124599732186, 0.000000000000000000, 0.000000000000000000 ) ) ;
#15341=CARTESIAN_POINT ( 'NONE',  ( 25.64708010899966339, 75.51173009720632479, -83.94602815988591260 ) ) ;
#15342=ORIENTED_EDGE ( 'NONE', *, *, #23793, .F. ) ;
#15344=CARTESIAN_POINT ( 'NONE',  ( 6.224689322667630975, -97.14981701196246888, -111.7293398381274869 ) ) ;
#15345=CARTESIAN_POINT ( 'NONE',  ( 1.833838850093440165, -97.09738119087785435, 107.8375718686136508 ) ) ;
#15347=CARTESIAN_POINT ( 'NONE',  ( 32.73300124599738581, 32.68291970228383292, -113.0038235389598782 ) ) ;
#15348=ADVANCED_FACE ( 'NONE', ( #26165 ), #1753, .F. ) ;
#15349=CARTESIAN_POINT ( 'NONE',  ( 32.73300124599734318, 97.37344512919861472, 66.00340565729376863 ) ) ;
#15351=EDGE_CURVE ( 'NONE', #9272, #25971, #13349, .T. ) ;
#15355=CARTESIAN_POINT ( 'NONE',  ( 2.108985857320913038, 132.2056553747752901, -60.26444811757266251 ) ) ;
#15356=CARTESIAN_POINT ( 'NONE',  ( 109.1624594426973260, 0.002129375066970632790, -0.01582142368018301867 ) ) ;
#15357=DIRECTION ( 'NONE',  ( 0.5914120900931444380, -0.008020494143007482132, 0.8063295922669342364 ) ) ;
#15358=CARTESIAN_POINT ( 'NONE',  ( 2.430230287190592531, -142.0258656395023706, 31.67257033707456770 ) ) ;
#15359=DIRECTION ( 'NONE',  ( 0.000000000000000000, 0.000000000000000000, 1.000000000000000000 ) ) ;
#15361=EDGE_CURVE ( 'NONE', #1094, #20246, #4824, .T. ) ;
#15362=DIRECTION ( 'NONE',  ( -1.000000000000000000, -0.000000000000000000, -0.000000000000000000 ) ) ;
#15363=DIRECTION ( 'NONE',  ( 0.000000000000000000, 0.000000000000000000, 1.000000000000000000 ) ) ;
#15364=CARTESIAN_POINT ( 'NONE',  ( 26.04756280548352620, -98.56594554799085017, -55.62433096787529507 ) ) ;
#15367=DIRECTION ( 'NONE',  ( 1.000000000000000000, -0.000000000000000000, -0.000000000000000000 ) ) ;
#15371=CARTESIAN_POINT ( 'NONE',  ( 32.73300124599738581, -97.37344512919901263, 66.00340565729310072 ) ) ;
#15372=DIRECTION ( 'NONE',  ( -0.000000000000000000, -0.000000000000000000, 1.000000000000000000 ) ) ;
#15374=ORIENTED_EDGE ( 'NONE', *, *, #13544, .F. ) ;
#15375=CARTESIAN_POINT ( 'NONE',  ( 1.893872463202053824, 132.2106029832902720, 59.90695624048730394 ) ) ;
#15377=CARTESIAN_POINT ( 'NONE',  ( 109.1721716018069657, 0.01550977894512766374, -0.007126480965770760380 ) ) ;
#15380=CARTESIAN_POINT ( 'NONE',  ( 13.36082413113061307, -81.89226687792178438, 129.1512766091118749 ) ) ;
#15381=CARTESIAN_POINT ( 'NONE',  ( 1.833485406944043827, 132.7804117027896211, -58.53321471326746916 ) ) ;
#15382=CARTESIAN_POINT ( 'NONE',  ( 25.64692872815576408, -56.17679456083732958, -97.94438212068882876 ) ) ;
#15383=ORIENTED_EDGE ( 'NONE', *, *, #24594, .T. ) ;
#15384=B_SPLINE_CURVE_WITH_KNOTS ( 'NONE', 3,
 ( #26648, #15277, #22051, #6962 ),
 .UNSPECIFIED., .F., .F.,
 ( 4, 4 ),
 ( 2.372452373067096320E-16, 0.008383748772659710413 ),
 .UNSPECIFIED. ) ;
#15385=ORIENTED_EDGE ( 'NONE', *, *, #19235, .T. ) ;
#15386=ORIENTED_EDGE ( 'NONE', *, *, #11026, .F. ) ;
#15389=FACE_OUTER_BOUND ( 'NONE', #28116, .T. ) ;
#15390=FACE_OUTER_BOUND ( 'NONE', #28066, .T. ) ;
#15392=ADVANCED_FACE ( 'NONE', ( #24709 ), #668, .F. ) ;
#15393=VERTEX_POINT ( 'NONE', #925 ) ;
#15395=CARTESIAN_POINT ( 'NONE',  ( 2.430230287190589422, 71.49654683843687053, -126.7388733285337281 ) ) ;
#15396=ORIENTED_EDGE ( 'NONE', *, *, #23790, .T. ) ;
#15401=CARTESIAN_POINT ( 'NONE',  ( 10.93730112725990189, -97.44200844886194091, -115.5857507957714461 ) ) ;
#15402=CARTESIAN_POINT ( 'NONE',  ( 109.1624594426973118, 0.01531968460306869402, 0.004489871836309402252 ) ) ;
#15404=CARTESIAN_POINT ( 'NONE',  ( 28.37599760073042177, 33.74340001061105454, 109.6580863494831135 ) ) ;
#15406=CARTESIAN_POINT ( 'NONE',  ( 1.833750490713699444, 14.90257883162752961, 144.3424379351781113 ) ) ;
#15407=CARTESIAN_POINT ( 'NONE',  ( 109.1586059443104944, -0.005067816690893775511, -0.004935564877218384661 ) ) ;
#15408=VERTEX_POINT ( 'NONE', #14297 ) ;
#15411=CARTESIAN_POINT ( 'NONE',  ( 25.64660436782546427, 35.44263474731944541, 107.2041192742817088 ) ) ;
#15414=ORIENTED_EDGE ( 'NONE', *, *, #6446, .F. ) ;
#15415=ADVANCED_FACE ( 'NONE', ( #24836 ), #27313, .F. ) ;
#15416=EDGE_CURVE ( 'NONE', #12008, #24090, #19335, .T. ) ;
#15417=CARTESIAN_POINT ( 'NONE',  ( 25.64681081121879203, -83.63051021305848565, -75.86069728269076506 ) ) ;
#15418=CARTESIAN_POINT ( 'NONE',  ( 25.64670758986457244, 11.30712635241989794, 112.3434365398308898 ) ) ;
#15419=EDGE_CURVE ( 'NONE', #11951, #24512, #21624, .T. ) ;
#15421=CARTESIAN_POINT ( 'NONE',  ( 2.433796855181205476, 132.3327394885231456, 60.50726454507948660 ) ) ;
#15425=CARTESIAN_POINT ( 'NONE',  ( 10.93730112725932635, 1.851405574867327964E-14, 151.1787379149930359 ) ) ;
#15428=CARTESIAN_POINT ( 'NONE',  ( 25.64681081121879203, -35.28660243342475411, -107.2555980796244910 ) ) ;
#15431=ORIENTED_EDGE ( 'NONE', *, *, #15584, .T. ) ;
#15432=CARTESIAN_POINT ( 'NONE',  ( 25.64700659047694131, 91.21315746821524328, 66.55152787776158618 ) ) ;
#15433=CARTESIAN_POINT ( 'NONE',  ( 25.64681081121879203, -66.70335573067806934, -91.10197563708015878 ) ) ;
#15434=CARTESIAN_POINT ( 'NONE',  ( 26.11404676487257603, -110.5078194225162918, 24.64483677384812665 ) ) ;
#15436=CARTESIAN_POINT ( 'NONE',  ( 25.98107933586734575, 110.4296102877914905, 24.58827779736819963 ) ) ;
#15437=CARTESIAN_POINT ( 'NONE',  ( 109.1587776205901577, 0.005502145856754162359, -0.004842060007774067441 ) ) ;
#15440=CARTESIAN_POINT ( 'NONE',  ( 32.73300124599732186, 0.000000000000000000, 0.000000000000000000 ) ) ;
#15441=VERTEX_POINT ( 'NONE', #7414 ) ;
#15442=CARTESIAN_POINT ( 'NONE',  ( 109.1592201516379674, -0.007302213399787572945, -0.002913740842103159506 ) ) ;
#15444=ORIENTED_EDGE ( 'NONE', *, *, #17728, .T. ) ;
#15445=VERTEX_POINT ( 'NONE', #18769 ) ;
#15447=( BOUNDED_SURFACE ( )  B_SPLINE_SURFACE ( 3, 1, ( 
 ( #8195, #3865 ),
 ( #12495, #25888 ),
 ( #19127, #6184 ),
 ( #16958, #1693 ) ),
 .UNSPECIFIED., .F., .F., .F. ) 
 B_SPLINE_SURFACE_WITH_KNOTS ( ( 4, 4 ),
 ( 2, 2 ),
 ( 0.000000000000000000, 1.000000000000000000 ),
 ( 0.000000000000000000, 1.000000000000000000 ),
 .UNSPECIFIED. ) 
 GEOMETRIC_REPRESENTATION_ITEM ( )  RATIONAL_B_SPLINE_SURFACE ( (
 ( 1.000000000000000000, 1.000000000000000000),
 ( 0.6386103224230302855, 0.9954351624131538845),
 ( 0.6386103224230302855, 0.9954351624131538845),
 ( 1.000000000000000000, 1.000000000000000000) ) ) 
 REPRESENTATION_ITEM ( '' )  SURFACE ( )  );
#15448=EDGE_CURVE ( 'NONE', #17039, #23477, #7090, .T. ) ;
#15449=ORIENTED_EDGE ( 'NONE', *, *, #19031, .F. ) ;
#15451=EDGE_LOOP ( 'NONE', ( #19053, #25370, #3772, #12951 ) ) ;
#15454=CARTESIAN_POINT ( 'NONE',  ( 26.11404676487259024, 67.46175819463365997, 90.92995828888226129 ) ) ;
#15458=CARTESIAN_POINT ( 'NONE',  ( 2.430230287190572103, -126.7388733285349787, 71.49654683843465364 ) ) ;
#15459=CARTESIAN_POINT ( 'NONE',  ( 2.430230287190572103, 71.49654683843509417, 126.7388733285347513 ) ) ;
#15460=CARTESIAN_POINT ( 'NONE',  ( 30.59141879584282364, 44.78722686469206593, 107.2355637993502029 ) ) ;
#15461=CARTESIAN_POINT ( 'NONE',  ( 109.1624594426973118, -0.0004639210235603736013, -0.01595733256932006794 ) ) ;
#15462=CARTESIAN_POINT ( 'NONE',  ( 109.1592201516379674, 0.007051465909551715011, 0.003476928926125415296 ) ) ;
#15463=CARTESIAN_POINT ( 'NONE',  ( 26.04756280548354397, -33.91579348271593375, 107.9769918539638951 ) ) ;
#15464=CARTESIAN_POINT ( 'NONE',  ( 25.64699802086723679, -56.24956056770090385, 97.90265915240011907 ) ) ;
#15465=ORIENTED_EDGE ( 'NONE', *, *, #24597, .F. ) ;
#15466=CARTESIAN_POINT ( 'NONE',  ( 5.340103579038186332, -96.93942141937377244, 111.1041836885944036 ) ) ;
#15468=CARTESIAN_POINT ( 'NONE',  ( 26.11404676487257603, -102.9690087468798509, -47.08215554553621729 ) ) ;
#15469=CARTESIAN_POINT ( 'NONE',  ( 16.75465622695644896, 131.7467602971417762, -53.58152542127552209 ) ) ;
#15470=CARTESIAN_POINT ( 'NONE',  ( 32.73300124599734318, 114.2056417606548706, 28.19767303745648945 ) ) ;
#15472=CARTESIAN_POINT ( 'NONE',  ( 25.64703792032468854, -35.03296646432486483, -107.3388703233125909 ) ) ;
#15473=CARTESIAN_POINT ( 'NONE',  ( 25.64681081121879203, 112.2483031020013442, 12.21581276189844800 ) ) ;
#15474=CARTESIAN_POINT ( 'NONE',  ( 1.834118845439484335, 97.22976650547570898, -107.7186227765444642 ) ) ;
#15475=ORIENTED_EDGE ( 'NONE', *, *, #22610, .F. ) ;
#15476=CARTESIAN_POINT ( 'NONE',  ( 109.1778270068192853, -0.008236503545668662218, -0.004349865064721219338 ) ) ;
#15478=( BOUNDED_SURFACE ( )  B_SPLINE_SURFACE ( 3, 1, ( 
 ( #13174, #24277 ),
 ( #13314, #1814 ),
 ( #21831, #17498 ),
 ( #19243, #12895 ) ),
 .UNSPECIFIED., .F., .F., .F. ) 
 B_SPLINE_SURFACE_WITH_KNOTS ( ( 4, 4 ),
 ( 2, 2 ),
 ( 0.000000000000000000, 1.000000000000000000 ),
 ( 0.000000000000000000, 1.000000000000000000 ),
 .UNSPECIFIED. ) 
 GEOMETRIC_REPRESENTATION_ITEM ( )  RATIONAL_B_SPLINE_SURFACE ( (
 ( 1.000000000000000000, 1.000000000000000000),
 ( 0.6386103224230316178, 0.9954351624131538845),
 ( 0.6386103224230316178, 0.9954351624131538845),
 ( 1.000000000000000000, 1.000000000000000000) ) ) 
 REPRESENTATION_ITEM ( '' )  SURFACE ( )  );
#15479=ADVANCED_FACE ( 'NONE', ( #1634 ), #4703, .F. ) ;
#15480=CARTESIAN_POINT ( 'NONE',  ( 1.833838850855463720, -97.16351016225966930, 107.7780290788693947 ) ) ;
#15481=ORIENTED_EDGE ( 'NONE', *, *, #25590, .F. ) ;
#15483=CARTESIAN_POINT ( 'NONE',  ( 30.59141879584321444, 95.58042137919564141, -66.10404588653692315 ) ) ;
#15485=B_SPLINE_CURVE_WITH_KNOTS ( 'NONE', 3,
 ( #11605, #11039, #19802, #2530, #26706, #95, #18074 ),
 .UNSPECIFIED., .F., .F.,
 ( 4, 3, 4 ),
 ( 5.916500692592983104E-16, 0.02816610861753241976, 0.04000277880656278456 ),
 .UNSPECIFIED. ) ;
#15486=CARTESIAN_POINT ( 'NONE',  ( 32.73300124599735739, -105.8473486001054482, 51.32617430724869223 ) ) ;
#15487=DIRECTION ( 'NONE',  ( 0.000000000000000000, 1.000000000000000000, -6.938893903907228378E-16 ) ) ;
#15488=CARTESIAN_POINT ( 'NONE',  ( 25.64708010899963497, 23.52908206539902025, 110.4325102642035574 ) ) ;
#15489=FACE_OUTER_BOUND ( 'NONE', #794, .T. ) ;
#15491=EDGE_LOOP ( 'NONE', ( #9473, #10511, #17609, #18272, #24224, #17403 ) ) ;
#15492=CARTESIAN_POINT ( 'NONE',  ( 9.884929003653626367, -103.8128997986850095, -109.0134320167743880 ) ) ;
#15493=EDGE_CURVE ( 'NONE', #26221, #9758, #5714, .T. ) ;
#15495=CARTESIAN_POINT ( 'NONE',  ( 25.87036335909428075, -46.88819766600042271, -102.8789780196093204 ) ) ;
#15496=CARTESIAN_POINT ( 'NONE',  ( 25.81918753295377655, -98.34688456803354484, -55.70247894228274532 ) ) ;
#15498=ORIENTED_EDGE ( 'NONE', *, *, #27288, .T. ) ;
#15499=ORIENTED_EDGE ( 'NONE', *, *, #21119, .T. ) ;
#15504=CARTESIAN_POINT ( 'NONE',  ( 109.1589550718174877, 0.006669585340466646639, -0.003591809816105017393 ) ) ;
#15505=CARTESIAN_POINT ( 'NONE',  ( 1.833485406944057594, 59.50871042846225834, 132.3460930279893262 ) ) ;
#15506=CARTESIAN_POINT ( 'NONE',  ( 109.1587776205901861, -0.005502145856762338978, -0.004842060007769368075 ) ) ;
#15508=CARTESIAN_POINT ( 'NONE',  ( 25.73574536432414916, -34.14219540448061707, -107.6875787074510811 ) ) ;
#15509=CARTESIAN_POINT ( 'NONE',  ( 1.833485406944043827, -117.7091014914955309, 84.86072343962528919 ) ) ;
#15510=CARTESIAN_POINT ( 'NONE',  ( 2.433796855181205476, -57.85512797797802165, -133.5135467655523769 ) ) ;
#15514=B_SPLINE_CURVE_WITH_KNOTS ( 'NONE', 3,
 ( #1575, #25903, #12779, #25497 ),
 .UNSPECIFIED., .F., .F.,
 ( 4, 4 ),
 ( 0.000000000000000000, 0.008383560773332736360 ),
 .UNSPECIFIED. ) ;
#15515=CARTESIAN_POINT ( 'NONE',  ( 25.86096068574578766, -74.90357932134571683, -84.67961880569373534 ) ) ;
#15517=DIRECTION ( 'NONE',  ( -1.000000000000000000, -0.000000000000000000, -0.000000000000000000 ) ) ;
#15518=EDGE_CURVE ( 'NONE', #21137, #19603, #21139, .T. ) ;
#15522=ORIENTED_EDGE ( 'NONE', *, *, #25822, .T. ) ;
#15524=CARTESIAN_POINT ( 'NONE',  ( 6.224689322667630975, 111.7293398381277569, -97.14981701196212782 ) ) ;
#15525=( BOUNDED_SURFACE ( )  B_SPLINE_SURFACE ( 3, 1, ( 
 ( #2369, #19948 ),
 ( #228, #17777 ),
 ( #26006, #7008 ),
 ( #22841, #20510 ) ),
 .UNSPECIFIED., .F., .F., .F. ) 
 B_SPLINE_SURFACE_WITH_KNOTS ( ( 4, 4 ),
 ( 2, 2 ),
 ( 0.000000000000000000, 1.000000000000000000 ),
 ( 0.000000000000000000, 1.000000000000000000 ),
 .UNSPECIFIED. ) 
 GEOMETRIC_REPRESENTATION_ITEM ( )  RATIONAL_B_SPLINE_SURFACE ( (
 ( 1.000000000000000000, 1.000000000000000000),
 ( 0.9956975270656955868, 0.8568959468854907557),
 ( 0.9956975270656955868, 0.8568959468854907557),
 ( 1.000000000000000000, 1.000000000000000000) ) ) 
 REPRESENTATION_ITEM ( '' )  SURFACE ( )  );
#15529=CARTESIAN_POINT ( 'NONE',  ( 99.22246935314075245, -69.99999999999998579, 40.00000000000003553 ) ) ;
#15531=VERTEX_POINT ( 'NONE', #28104 ) ;
#15532=LINE ( 'NONE', #20679, #20322 ) ;
#15533=ORIENTED_EDGE ( 'NONE', *, *, #10963, .F. ) ;
#15534=DIRECTION ( 'NONE',  ( -0.5946245182733608248, 0.7356888587241636746, 0.3243201896541614282 ) ) ;
#15535=CARTESIAN_POINT ( 'NONE',  ( 55.79472521941428198, 15.83764557006269946, 71.00924468211162832 ) ) ;
#15536=B_SPLINE_CURVE_WITH_KNOTS ( 'NONE', 3,
 ( #12374, #7951, #18718, #5780, #5477, #16714 ),
 .UNSPECIFIED., .F., .F.,
 ( 4, 2, 4 ),
 ( 2.168404344971008868E-18, 0.0006311636237756631899, 0.001262327247551324211 ),
 .UNSPECIFIED. ) ;
#15537=CARTESIAN_POINT ( 'NONE',  ( 55.79472521941428198, -62.63970324008288770, 37.00555938668237133 ) ) ;
#15538=CARTESIAN_POINT ( 'NONE',  ( 2.108985857320909929, 73.75356715683084019, 125.1820688103224342 ) ) ;
#15539=CARTESIAN_POINT ( 'NONE',  ( 109.1587776205901577, -8.330235397649874362E-05, 0.007328861771496576576 ) ) ;
#15540=CARTESIAN_POINT ( 'NONE',  ( 25.64681081121879203, -23.06870491922242650, -110.5293738517610933 ) ) ;
#15543=DIRECTION ( 'NONE',  ( 0.000000000000000000, 0.000000000000000000, 1.000000000000000000 ) ) ;
#15544=CARTESIAN_POINT ( 'NONE',  ( 25.64681081121879203, -66.70335573067929147, 91.10197563707923507 ) ) ;
#15547=AXIS2_PLACEMENT_3D ( 'NONE', #25642, #7952, #25204 ) ;
#15552=ORIENTED_EDGE ( 'NONE', *, *, #1633, .T. ) ;
#15557=CARTESIAN_POINT ( 'NONE',  ( 1.833809397773845218, 137.9524943416725478, 45.01060836636568041 ) ) ;
#15558=( BOUNDED_SURFACE ( )  B_SPLINE_SURFACE ( 3, 1, ( 
 ( #22009, #24186 ),
 ( #4444, #13790 ),
 ( #24470, #843 ),
 ( #11794, #4736 ) ),
 .UNSPECIFIED., .F., .F., .F. ) 
 B_SPLINE_SURFACE_WITH_KNOTS ( ( 4, 4 ),
 ( 2, 2 ),
 ( 0.000000000000000000, 1.000000000000000000 ),
 ( 0.000000000000000000, 1.000000000000000000 ),
 .UNSPECIFIED. ) 
 GEOMETRIC_REPRESENTATION_ITEM ( )  RATIONAL_B_SPLINE_SURFACE ( (
 ( 1.000000000000000000, 1.000000000000000000),
 ( 0.6386103224230302855, 0.9954351624131538845),
 ( 0.6386103224230302855, 0.9954351624131538845),
 ( 1.000000000000000000, 1.000000000000000000) ) ) 
 REPRESENTATION_ITEM ( '' )  SURFACE ( )  );
#15559=B_SPLINE_CURVE_WITH_KNOTS ( 'NONE', 3,
 ( #7867, #5696, #23265, #21069, #14598, #23401, #8954, #20155, #15011, #1773 ),
 .UNSPECIFIED., .F., .F.,
 ( 4, 3, 3, 4 ),
 ( 1.387778780781445676E-17, 0.0002669559177086280378, 0.0005339118354151154268, 0.001067817517169168152 ),
 .UNSPECIFIED. ) ;
#15563=CARTESIAN_POINT ( 'NONE',  ( 1.894214914920941961, 43.94587946447585125, -138.3376769255504541 ) ) ;
#15566=LINE ( 'NONE', #13273, #20862 ) ;
#15567=CARTESIAN_POINT ( 'NONE',  ( 30.58324630866340499, 113.7441547345752468, -41.10517620771084779 ) ) ;
#15568=CARTESIAN_POINT ( 'NONE',  ( 109.1586900883932856, 0.003656351050324885277, -0.006130969560693676386 ) ) ;
#15572=EDGE_CURVE ( 'NONE', #23252, #27866, #2624, .T. ) ;
#15573=CARTESIAN_POINT ( 'NONE',  ( 25.86096068574579121, -22.52859312382108214, -110.7864907291861556 ) ) ;
#15575=CARTESIAN_POINT ( 'NONE',  ( 30.58324630866344052, -77.95273942827404312, 92.47020419020155657 ) ) ;
#15576=ORIENTED_EDGE ( 'NONE', *, *, #23329, .T. ) ;
#15578=ORIENTED_EDGE ( 'NONE', *, *, #26475, .F. ) ;
#15580=ADVANCED_FACE ( 'NONE', ( #759 ), #26222, .T. ) ;
#15581=CARTESIAN_POINT ( 'NONE',  ( 26.11404676487256893, -12.95861723607530003, 112.4785329405481349 ) ) ;
#15583=VERTEX_POINT ( 'NONE', #27230 ) ;
#15584=EDGE_CURVE ( 'NONE', #11640, #20199, #7816, .T. ) ;
#15585=DIRECTION ( 'NONE',  ( 0.000000000000000000, 0.000000000000000000, 1.000000000000000000 ) ) ;
#15587=CARTESIAN_POINT ( 'NONE',  ( 30.59138290137915206, 92.40465044710842335, -70.47507990428483993 ) ) ;
#15588=VERTEX_POINT ( 'NONE', #13705 ) ;
#15589=CARTESIAN_POINT ( 'NONE',  ( 25.98552792386801258, 67.36997957637663603, 90.89136171349112203 ) ) ;
#15593=CARTESIAN_POINT ( 'NONE',  ( 26.11404676487257603, 112.7148551500681890, -10.71016160607451262 ) ) ;
#15595=EDGE_CURVE ( 'NONE', #22601, #13932, #7690, .T. ) ;
#15599=B_SPLINE_CURVE_WITH_KNOTS ( 'NONE', 3,
 ( #12794, #22002, #1717, #11068, #10930, #10798 ),
 .UNSPECIFIED., .F., .F.,
 ( 4, 2, 4 ),
 ( 4.336808689942017736E-19, 0.0006311571484586052470, 0.001262314296917210060 ),
 .UNSPECIFIED. ) ;
#15600=ORIENTED_EDGE ( 'NONE', *, *, #11341, .T. ) ;
#15601=CARTESIAN_POINT ( 'NONE',  ( 26.04756280548352620, 83.36043467252123662, -76.55292122839955482 ) ) ;
#15603=EDGE_CURVE ( 'NONE', #7969, #8336, #18020, .T. ) ;
#15604=CARTESIAN_POINT ( 'NONE',  ( 1.831572820252009626, -43.90210991190716072, 138.3111855986059595 ) ) ;
#15606=( BOUNDED_SURFACE ( )  B_SPLINE_SURFACE ( 3, 1, ( 
 ( #15613, #24435 ),
 ( #12906, #4702 ),
 ( #13471, #21697 ),
 ( #22269, #2532 ) ),
 .UNSPECIFIED., .F., .F., .F. ) 
 B_SPLINE_SURFACE_WITH_KNOTS ( ( 4, 4 ),
 ( 2, 2 ),
 ( 0.000000000000000000, 1.000000000000000000 ),
 ( 0.000000000000000000, 1.000000000000000000 ),
 .UNSPECIFIED. ) 
 GEOMETRIC_REPRESENTATION_ITEM ( )  RATIONAL_B_SPLINE_SURFACE ( (
 ( 1.000000000000000000, 1.000000000000000000),
 ( 0.9960225298536222738, 0.9999952330161893110),
 ( 0.9960225298536222738, 0.9999952330161893110),
 ( 1.000000000000000000, 1.000000000000000000) ) ) 
 REPRESENTATION_ITEM ( '' )  SURFACE ( )  );
#15609=CARTESIAN_POINT ( 'NONE',  ( 19.66333377628710366, -51.89484018353753214, -127.6002314355563243 ) ) ;
#15610=DIRECTION ( 'NONE',  ( -0.5946245182733608248, -0.3243201896541638707, 0.7356888587241625643 ) ) ;
#15611=CARTESIAN_POINT ( 'NONE',  ( 32.73300124599735739, -39.98094346392385745, 110.6325518752272501 ) ) ;
#15613=CARTESIAN_POINT ( 'NONE',  ( 109.1586900883932856, 0.007088091345229654248, -0.0008465529156635364033 ) ) ;
#15614=VECTOR ( 'NONE', #9960, 1000.000000000000114 ) ;
#15615=B_SPLINE_CURVE_WITH_KNOTS ( 'NONE', 3,
 ( #10131, #12691, #8117, #18901, #25535, #10547, #14573, #27819, #19310, #3628 ),
 .UNSPECIFIED., .F., .F.,
 ( 4, 3, 3, 4 ),
 ( 1.040834085586084257E-17, 0.0002669560319015743151, 0.0005492286108966385264, 0.0008315040496093428378 ),
 .UNSPECIFIED. ) ;
#15617=VECTOR ( 'NONE', #15905, 1000.000000000000114 ) ;
#15619=CARTESIAN_POINT ( 'NONE',  ( 13.36082413113061307, 84.67697637120410548, 127.3428651193251113 ) ) ;
#15620=CARTESIAN_POINT ( 'NONE',  ( 55.79472521941428198, 14.41365263906652139, -71.31192372336661833 ) ) ;
#15621=CARTESIAN_POINT ( 'NONE',  ( 24.22246935314087324, 70.00000000000004263, 39.99999999999999289 ) ) ;
#15622=ORIENTED_EDGE ( 'NONE', *, *, #9380, .F. ) ;
#15623=DIRECTION ( 'NONE',  ( 1.000000000000000000, 0.000000000000000000, 0.000000000000000000 ) ) ;
#15624=DIRECTION ( 'NONE',  ( 0.5914120900931444380, 0.07630783613000277632, 0.8027508043202542520 ) ) ;
#15625=CARTESIAN_POINT ( 'NONE',  ( 25.64700659047694131, -35.10784848926738988, 107.3144208978484073 ) ) ;
#15626=CARTESIAN_POINT ( 'NONE',  ( 25.64703792032469210, 23.62108504469244963, 110.4127989088530910 ) ) ;
#15627=CARTESIAN_POINT ( 'NONE',  ( 26.11404676487257603, -74.91683232330916553, -84.89295829319569009 ) ) ;
#15628=CARTESIAN_POINT ( 'NONE',  ( 1.833485406944057594, -125.4007332306550921, 73.01664920992921282 ) ) ;
#15629=ORIENTED_EDGE ( 'NONE', *, *, #19363, .F. ) ;
#15630=FACE_OUTER_BOUND ( 'NONE', #21597, .T. ) ;
#15633=CARTESIAN_POINT ( 'NONE',  ( 25.64660436782550335, 34.33930645842144003, -107.5626123667555731 ) ) ;
#15635=ORIENTED_EDGE ( 'NONE', *, *, #15828, .T. ) ;
#15636=ADVANCED_FACE ( 'NONE', ( #21038 ), #14275, .T. ) ;
#15639=ORIENTED_EDGE ( 'NONE', *, *, #27615, .T. ) ;
#15641=CARTESIAN_POINT ( 'NONE',  ( 26.11404676487257603, 67.46175819463486789, -90.92995828888132337 ) ) ;
#15646=B_SPLINE_CURVE_WITH_KNOTS ( 'NONE', 3,
 ( #2366, #15463, #6855, #11444, #20506, #24415, #13737, #792 ),
 .UNSPECIFIED., .F., .F.,
 ( 4, 2, 2, 4 ),
 ( 6.938893903907228378E-18, 0.0002429592666046760283, 0.0004859185332093451178, 0.0009718370664186966323 ),
 .UNSPECIFIED. ) ;
#15647=CARTESIAN_POINT ( 'NONE',  ( 94.22246935314088034, -90.00000000000005684, 12.49999999999999467 ) ) ;
#15649=CARTESIAN_POINT ( 'NONE',  ( 16.75465622695678647, -117.7275519421679633, 79.80233222761944489 ) ) ;
#15650=ORIENTED_EDGE ( 'NONE', *, *, #7445, .T. ) ;
#15653=( BOUNDED_SURFACE ( )  B_SPLINE_SURFACE ( 3, 1, ( 
 ( #27115, #20931 ),
 ( #16477, #10017 ),
 ( #16188, #3514 ),
 ( #18777, #14024 ) ),
 .UNSPECIFIED., .F., .F., .F. ) 
 B_SPLINE_SURFACE_WITH_KNOTS ( ( 4, 4 ),
 ( 2, 2 ),
 ( 0.000000000000000000, 1.000000000000000000 ),
 ( 0.000000000000000000, 1.000000000000000000 ),
 .UNSPECIFIED. ) 
 GEOMETRIC_REPRESENTATION_ITEM ( )  RATIONAL_B_SPLINE_SURFACE ( (
 ( 1.000000000000000000, 1.000000000000000000),
 ( 0.9956975270656955868, 0.8568959468854907557),
 ( 0.9956975270656955868, 0.8568959468854907557),
 ( 1.000000000000000000, 1.000000000000000000) ) ) 
 REPRESENTATION_ITEM ( '' )  SURFACE ( )  );
#15654=AXIS2_PLACEMENT_3D ( 'NONE', #10891, #23868, #26420 ) ;
#15655=CARTESIAN_POINT ( 'NONE',  ( 1.833485406944057594, -145.1085452359073429, 0.5339064996879626657 ) ) ;
#15656=CARTESIAN_POINT ( 'NONE',  ( 32.73300124599734318, 108.9684813982489118, 44.31599526637995012 ) ) ;
#15657=CARTESIAN_POINT ( 'NONE',  ( 26.11404676487257603, 102.9690087468801352, 47.08215554553553517 ) ) ;
#15658=ORIENTED_EDGE ( 'NONE', *, *, #13841, .T. ) ;
#15659=CARTESIAN_POINT ( 'NONE',  ( 109.1624594426973118, -0.01102230012606818417, -0.01154818537151451434 ) ) ;
#15662=DIRECTION ( 'NONE',  ( -1.000000000000000000, -0.000000000000000000, -0.000000000000000000 ) ) ;
#15664=ORIENTED_EDGE ( 'NONE', *, *, #24154, .T. ) ;
#15669=B_SPLINE_CURVE_WITH_KNOTS ( 'NONE', 3,
 ( #15347, #24438, #11187, #4279 ),
 .UNSPECIFIED., .F., .F.,
 ( 4, 4 ),
 ( 5.513692426328523236E-16, 0.008383748772660020929 ),
 .UNSPECIFIED. ) ;
#15670=CARTESIAN_POINT ( 'NONE',  ( 32.73300124599735739, -32.68291970228314369, 113.0038235389601340 ) ) ;
#15671=CARTESIAN_POINT ( 'NONE',  ( 25.81918753295378011, 84.61657260023643801, 74.93271318951751425 ) ) ;
#15673=AXIS2_PLACEMENT_3D ( 'NONE', #10173, #3669, #12176 ) ;
#15675=ORIENTED_EDGE ( 'NONE', *, *, #13731, .T. ) ;
#15677=DIRECTION ( 'NONE',  ( 0.5914120900931444380, -0.6570486713847307758, 0.4674599267565279770 ) ) ;
#15678=VERTEX_POINT ( 'NONE', #7833 ) ;
#15679=EDGE_CURVE ( 'NONE', #12673, #20443, #16658, .T. ) ;
#15680=CARTESIAN_POINT ( 'NONE',  ( 25.98552792386800547, 92.15963349013364336, 65.62435323276200450 ) ) ;
#15682=CARTESIAN_POINT ( 'NONE',  ( 2.263178607246661755, 126.6115608827437455, 71.48082837426046865 ) ) ;
#15684=CARTESIAN_POINT ( 'NONE',  ( 1.832998868059890096, -144.2584710144579390, -15.69902610990519776 ) ) ;
#15685=CARTESIAN_POINT ( 'NONE',  ( 1.893872463202051604, 96.41404152942938310, 108.5026245911422222 ) ) ;
#15688=EDGE_CURVE ( 'NONE', #1116, #5458, #11758, .T. ) ;
#15689=CARTESIAN_POINT ( 'NONE',  ( 109.1624594426973118, 0.01503296564241277805, -0.005372302061316116054 ) ) ;
#15691=VECTOR ( 'NONE', #3814, 1000.000000000000227 ) ;
#15692=B_SPLINE_CURVE_WITH_KNOTS ( 'NONE', 3,
 ( #6860, #26285, #19526, #15470 ),
 .UNSPECIFIED., .F., .F.,
 ( 4, 4 ),
 ( 0.000000000000000000, 0.008383560773332725952 ),
 .UNSPECIFIED. ) ;
#15695=CARTESIAN_POINT ( 'NONE',  ( 1.833206310202347256, -44.13245377365727506, 138.2356391007181173 ) ) ;
#15697=ORIENTED_EDGE ( 'NONE', *, *, #11773, .F. ) ;
#15698=AXIS2_PLACEMENT_3D ( 'NONE', #1326, #1611, #16744 ) ;
#15699=VERTEX_POINT ( 'NONE', #13754 ) ;
#15701=ORIENTED_EDGE ( 'NONE', *, *, #17643, .T. ) ;
#15702=( BOUNDED_SURFACE ( )  B_SPLINE_SURFACE ( 3, 1, ( 
 ( #3683, #12460 ),
 ( #25581, #1527 ),
 ( #16653, #1107 ),
 ( #25446, #18663 ) ),
 .UNSPECIFIED., .F., .F., .F. ) 
 B_SPLINE_SURFACE_WITH_KNOTS ( ( 4, 4 ),
 ( 2, 2 ),
 ( 0.000000000000000000, 1.000000000000000000 ),
 ( 0.000000000000000000, 1.000000000000000000 ),
 .UNSPECIFIED. ) 
 GEOMETRIC_REPRESENTATION_ITEM ( )  RATIONAL_B_SPLINE_SURFACE ( (
 ( 1.000000000000000000, 1.000000000000000000),
 ( 0.9960225298536222738, 0.9999952330161893110),
 ( 0.9960225298536222738, 0.9999952330161893110),
 ( 1.000000000000000000, 1.000000000000000000) ) ) 
 REPRESENTATION_ITEM ( '' )  SURFACE ( )  );
#15704=ORIENTED_EDGE ( 'NONE', *, *, #5940, .T. ) ;
#15706=CARTESIAN_POINT ( 'NONE',  ( 1.833485406944057594, 138.1714136985308699, 44.33323125129973619 ) ) ;
#15707=ORIENTED_EDGE ( 'NONE', *, *, #17916, .T. ) ;
#15709=EDGE_CURVE ( 'NONE', #3000, #16465, #25586, .T. ) ;
#15716=CARTESIAN_POINT ( 'NONE',  ( 32.73300124599738581, -92.86301839380070078, 72.21147546950520280 ) ) ;
#15717=CARTESIAN_POINT ( 'NONE',  ( 2.433796855181233454, 138.8296532063088193, 43.58222566461690661 ) ) ;
#15718=CARTESIAN_POINT ( 'NONE',  ( 2.430230287190589422, -118.5711603495675490, -84.35270093935379521 ) ) ;
#15719=EDGE_CURVE ( 'NONE', #17840, #5960, #1874, .T. ) ;
#15721=FACE_OUTER_BOUND ( 'NONE', #6917, .T. ) ;
#15722=CARTESIAN_POINT ( 'NONE',  ( 16.75465622695668699, -75.09093759626914277, 120.7871673903169096 ) ) ;
#15728=CARTESIAN_POINT ( 'NONE',  ( 10.93730112725945425, 115.5857507957700818, 97.44200844886312041 ) ) ;
#15730=B_SPLINE_CURVE_WITH_KNOTS ( 'NONE', 3,
 ( #21124, #11930, #18693, #20697, #991, #9783, #7634, #7778 ),
 .UNSPECIFIED., .F., .F.,
 ( 4, 2, 2, 4 ),
 ( 6.938893903907228378E-18, 0.0002429592666046787117, 0.0004859185332093504846, 0.0009718370664186806946 ),
 .UNSPECIFIED. ) ;
#15733=ORIENTED_EDGE ( 'NONE', *, *, #25751, .F. ) ;
#15734=CARTESIAN_POINT ( 'NONE',  ( 1.833838848569439017, -15.34509722932435416, -144.2962335061012595 ) ) ;
#15735=ORIENTED_EDGE ( 'NONE', *, *, #20637, .F. ) ;
#15737=CARTESIAN_POINT ( 'NONE',  ( 1.833721034905663183, -29.82176961967010342, 142.0123736691685963 ) ) ;
#15739=ORIENTED_EDGE ( 'NONE', *, *, #16903, .F. ) ;
#15741=AXIS2_PLACEMENT_3D ( 'NONE', #229, #16290, #15996 ) ;
#15742=ORIENTED_EDGE ( 'NONE', *, *, #26929, .F. ) ;
#15743=CARTESIAN_POINT ( 'NONE',  ( 119.2224693531408803, -69.99999999999998579, 19.99999999999996092 ) ) ;
#15744=CIRCLE ( 'NONE', #22678, 151.1787379149930359 ) ;
#15745=( BOUNDED_SURFACE ( )  B_SPLINE_SURFACE ( 3, 1, ( 
 ( #16305, #13857 ),
 ( #20335, #23097 ),
 ( #3076, #5511 ),
 ( #18467, #11849 ) ),
 .UNSPECIFIED., .F., .F., .F. ) 
 B_SPLINE_SURFACE_WITH_KNOTS ( ( 4, 4 ),
 ( 2, 2 ),
 ( 0.000000000000000000, 1.000000000000000000 ),
 ( 0.000000000000000000, 1.000000000000000000 ),
 .UNSPECIFIED. ) 
 GEOMETRIC_REPRESENTATION_ITEM ( )  RATIONAL_B_SPLINE_SURFACE ( (
 ( 1.000000000000000000, 1.000000000000000000),
 ( 0.6386103224230302855, 0.9954351624131538845),
 ( 0.6386103224230302855, 0.9954351624131538845),
 ( 1.000000000000000000, 1.000000000000000000) ) ) 
 REPRESENTATION_ITEM ( '' )  SURFACE ( )  );
#15747=B_SPLINE_CURVE_WITH_KNOTS ( 'NONE', 3,
 ( #5607, #5018, #3444, #12223, #7338, #18842, #15961, #9497 ),
 .UNSPECIFIED., .F., .F.,
 ( 4, 2, 2, 4 ),
 ( 3.469446951953614189E-18, 0.0002429592666046780070, 0.0004859185332093525446, 0.0009718370664186804777 ),
 .UNSPECIFIED. ) ;
#15748=CARTESIAN_POINT ( 'NONE',  ( 2.263178113027049854, -125.2099934853446115, -73.90841366068515583 ) ) ;
#15749=EDGE_CURVE ( 'NONE', #28186, #10573, #13225, .T. ) ;
#15750=DIRECTION ( 'NONE',  ( 0.000000000000000000, 0.000000000000000000, 1.000000000000000000 ) ) ;
#15751=B_SPLINE_CURVE_WITH_KNOTS ( 'NONE', 3,
 ( #25358, #10099, #12247, #1298 ),
 .UNSPECIFIED., .F., .F.,
 ( 4, 4 ),
 ( 3.353811493843786478E-16, 0.01077107486149842322 ),
 .UNSPECIFIED. ) ;
#15752=B_SPLINE_CURVE_WITH_KNOTS ( 'NONE', 3,
 ( #19271, #16409, #12098, #5468, #23051, #1158 ),
 .UNSPECIFIED., .F., .F.,
 ( 4, 2, 4 ),
 ( 1.604619215278546562E-17, 0.0006311636237756963665, 0.001262327247551376036 ),
 .UNSPECIFIED. ) ;
#15753=CARTESIAN_POINT ( 'NONE',  ( 2.263178113027048521, 137.8402779654370534, 46.26071604342116927 ) ) ;
#15756=CARTESIAN_POINT ( 'NONE',  ( 109.1586059443104944, 0.004378796245583033847, -0.005555961672780077194 ) ) ;
#15757=CARTESIAN_POINT ( 'NONE',  ( 1.834118845439484335, 107.9567937753793530, 96.96525081350034725 ) ) ;
#15758=EDGE_CURVE ( 'NONE', #8378, #16670, #20426, .T. ) ;
#15759=AXIS2_PLACEMENT_3D ( 'NONE', #13487, #11051, #18087 ) ;
#15760=CARTESIAN_POINT ( 'NONE',  ( 109.1592201516379674, 0.005485778713193748164, -0.005631912476305715558 ) ) ;
#15762=AXIS2_PLACEMENT_3D ( 'NONE', #22038, #4475, #15543 ) ;
#15764=CARTESIAN_POINT ( 'NONE',  ( 109.1586059443104944, 0.007058870754606102506, 0.0004635842312796298998 ) ) ;
#15765=AXIS2_PLACEMENT_3D ( 'NONE', #26909, #24782, #22622 ) ;
#15767=CARTESIAN_POINT ( 'NONE',  ( 1.833485406944057594, 0.5339064996884692604, 145.1085452359073429 ) ) ;
#15768=CARTESIAN_POINT ( 'NONE',  ( 2.108393763691195577, -137.7805780486502840, -46.11438684123302068 ) ) ;
#15770=CARTESIAN_POINT ( 'NONE',  ( 1.833838850093440387, 44.84138612521095268, 138.0075846865482845 ) ) ;
#15771=CARTESIAN_POINT ( 'NONE',  ( 1.831572820252009626, -125.1738732943815364, 73.40899645745960811 ) ) ;
#15773=CARTESIAN_POINT ( 'NONE',  ( 109.1586900883932856, -0.003656351050324926043, 0.006130969560693652967 ) ) ;
#15774=ORIENTED_EDGE ( 'NONE', *, *, #12696, .F. ) ;
#15775=CARTESIAN_POINT ( 'NONE',  ( 25.64681081121880624, -112.3352186517031441, 11.38886654529637887 ) ) ;
#15778=CARTESIAN_POINT ( 'NONE',  ( 1.833838848569414370, -96.96512505224302458, 107.9566558236573570 ) ) ;
#15783=ORIENTED_EDGE ( 'NONE', *, *, #10859, .T. ) ;
#15789=B_SPLINE_CURVE_WITH_KNOTS ( 'NONE', 3,
 ( #7589, #14171, #3252, #12035, #20809, #1095, #15770, #24580, #4839, #5119 ),
 .UNSPECIFIED., .F., .F.,
 ( 4, 3, 3, 4 ),
 ( 2.081668171172168513E-17, 0.0002669559177086255441, 0.0005339118354151051269, 0.001067817517169169670 ),
 .UNSPECIFIED. ) ;
#15792=CARTESIAN_POINT ( 'NONE',  ( 1.832998868059890096, 117.0819875546707038, -85.72499093307982321 ) ) ;
#15793=CARTESIAN_POINT ( 'NONE',  ( 25.81918753295379076, 107.7789657594975097, 34.03777907511953771 ) ) ;
#15798=( BOUNDED_SURFACE ( )  B_SPLINE_SURFACE ( 3, 1, ( 
 ( #5188, #11378 ),
 ( #2894, #20446 ),
 ( #26625, #13964 ),
 ( #20153, #15980 ) ),
 .UNSPECIFIED., .F., .F., .F. ) 
 B_SPLINE_SURFACE_WITH_KNOTS ( ( 4, 4 ),
 ( 2, 2 ),
 ( 0.000000000000000000, 1.000000000000000000 ),
 ( 0.000000000000000000, 1.000000000000000000 ),
 .UNSPECIFIED. ) 
 GEOMETRIC_REPRESENTATION_ITEM ( )  RATIONAL_B_SPLINE_SURFACE ( (
 ( 1.000000000000000000, 1.000000000000000000),
 ( 0.9956975270656954757, 0.8568959468854893125),
 ( 0.9956975270656954757, 0.8568959468854893125),
 ( 1.000000000000000000, 1.000000000000000000) ) ) 
 REPRESENTATION_ITEM ( '' )  SURFACE ( )  );
#15799=VECTOR ( 'NONE', #16691, 1000.000000000000114 ) ;
#15801=CARTESIAN_POINT ( 'NONE',  ( 2.433796855181233454, -60.50726454507816499, -132.3327394885237425 ) ) ;
#15804=VERTEX_POINT ( 'NONE', #527 ) ;
#15808=CARTESIAN_POINT ( 'NONE',  ( 2.063896406836605024, -133.2511741302124335, 57.85593781835370208 ) ) ;
#15809=CARTESIAN_POINT ( 'NONE',  ( 26.11404676487256893, -12.95861723607530003, 112.4785329405481349 ) ) ;
#15810=CARTESIAN_POINT ( 'NONE',  ( 1.833721034905651637, 144.3516387774751593, 14.81406766075982695 ) ) ;
#15811=CARTESIAN_POINT ( 'NONE',  ( 25.98107933586732088, -103.7920584735895773, 45.01656174308536862 ) ) ;
#15812=CARTESIAN_POINT ( 'NONE',  ( 2.063896406836605024, 71.46753739786015558, 126.4736179849650313 ) ) ;
#15813=ORIENTED_EDGE ( 'NONE', *, *, #12736, .F. ) ;
#15814=CARTESIAN_POINT ( 'NONE',  ( 8.186469777910893697, -146.7694294853781685, -27.65107827750229674 ) ) ;
#15816=CARTESIAN_POINT ( 'NONE',  ( 1.833485406944043827, -145.1085452359073145, -0.5339064996899981486 ) ) ;
#15818=CARTESIAN_POINT ( 'NONE',  ( 13.36082413113061307, 94.94363694444213309, -119.8836995922717108 ) ) ;
#15821=CARTESIAN_POINT ( 'NONE',  ( 1.893872463202029399, 45.75900850850183588, -137.7483215415844597 ) ) ;
#15822=CARTESIAN_POINT ( 'NONE',  ( 30.58324630866350446, 8.712468656082224427, -120.6294372749320587 ) ) ;
#15825=VERTEX_POINT ( 'NONE', #24811 ) ;
#15828=EDGE_CURVE ( 'NONE', #27008, #12942, #14246, .T. ) ;
#15829=CARTESIAN_POINT ( 'NONE',  ( 16.05277956358211711, -39.81690014528761168, 137.6634701901228084 ) ) ;
#15830=CARTESIAN_POINT ( 'NONE',  ( 30.59138290137884653, -113.0806461017755140, 26.79783179610965504 ) ) ;
#15832=CARTESIAN_POINT ( 'NONE',  ( 26.04756280548354397, 57.54844730865669788, 97.45505646068853878 ) ) ;
#15833=CARTESIAN_POINT ( 'NONE',  ( 2.433796855181233454, 57.85512797798071460, -133.5135467655512400 ) ) ;
#15834=DIRECTION ( 'NONE',  ( -0.5946245182733607137, 0.5994612328333183138, 0.5357871896547470314 ) ) ;
#15837=CARTESIAN_POINT ( 'NONE',  ( 1.831572820252009626, -16.14965423926112464, -144.2101521542832074 ) ) ;
#15839=ORIENTED_EDGE ( 'NONE', *, *, #21609, .T. ) ;
#15842=ORIENTED_EDGE ( 'NONE', *, *, #3090, .F. ) ;
#15843=CARTESIAN_POINT ( 'NONE',  ( 1.833485406944043827, 30.69200235379130959, -141.8265699653863976 ) ) ;
#15844=CARTESIAN_POINT ( 'NONE',  ( 25.64681081121879203, -45.54494737132156246, -103.3177883989783936 ) ) ;
#15847=CARTESIAN_POINT ( 'NONE',  ( 2.433796855181205476, 60.50726454508082952, -132.3327394885224919 ) ) ;
#15848=CARTESIAN_POINT ( 'NONE',  ( 32.73300124599740002, -89.94078864464006529, -75.82012867748569818 ) ) ;
#15849=CARTESIAN_POINT ( 'NONE',  ( 2.433796855181205476, 16.65276281464756636, -144.5536872373190533 ) ) ;
#15850=B_SPLINE_CURVE_WITH_KNOTS ( 'NONE', 3,
 ( #24381, #4799, #13275, #470, #323, #8979, #2183, #15875 ),
 .UNSPECIFIED., .F., .F.,
 ( 4, 2, 2, 4 ),
 ( 1.551583845779545699E-17, 0.0002429592666046909361, 0.0004859185332093663681, 0.0009718370664186812367 ),
 .UNSPECIFIED. ) ;
#15851=B_SPLINE_CURVE_WITH_KNOTS ( 'NONE', 3,
 ( #18937, #17322, #27854, #27713, #5845, #8281, #12583, #8151 ),
 .UNSPECIFIED., .F., .F.,
 ( 4, 2, 2, 4 ),
 ( 0.000000000000000000, 0.0002429588503611205359, 0.0004859177007222410718, 0.0009718354014444899498 ),
 .UNSPECIFIED. ) ;
#15852=CARTESIAN_POINT ( 'NONE',  ( 1.831572820252008738, 107.1759352627506416, 97.82994539998418304 ) ) ;
#15853=CARTESIAN_POINT ( 'NONE',  ( 1.833485406944057594, 58.53321471327059555, -132.7804117027882285 ) ) ;
#15854=CARTESIAN_POINT ( 'NONE',  ( 25.64708010899965629, -107.3680906278374323, 34.94352788466252235 ) ) ;
#15855=B_SPLINE_CURVE_WITH_KNOTS ( 'NONE', 3,
 ( #13648, #2004, #11213, #22007 ),
 .UNSPECIFIED., .F., .F.,
 ( 4, 4 ),
 ( 0.000000000000000000, 0.008383560773332738095 ),
 .UNSPECIFIED. ) ;
#15856=EDGE_CURVE ( 'NONE', #1309, #2120, #20469, .T. ) ;
#15859=CARTESIAN_POINT ( 'NONE',  ( 2.433796855181205476, 71.49415740225076377, 126.7346379669258312 ) ) ;
#15860=ORIENTED_EDGE ( 'NONE', *, *, #22939, .T. ) ;
#15865=EDGE_CURVE ( 'NONE', #27652, #8378, #10150, .T. ) ;
#15870=CARTESIAN_POINT ( 'NONE',  ( 2.430230287190581429, 118.5711603495692827, -84.35270093935136515 ) ) ;
#15871=CARTESIAN_POINT ( 'NONE',  ( 13.84597867724970577, -49.85807424839853752, 137.9700459519988556 ) ) ;
#15872=CARTESIAN_POINT ( 'NONE',  ( 32.73300124599735739, 3.836798148478847370, 117.5726003567930178 ) ) ;
#15873=CARTESIAN_POINT ( 'NONE',  ( 109.1778270068192853, -0.006682187084648866932, 0.006489198140359601387 ) ) ;
#15875=CARTESIAN_POINT ( 'NONE',  ( 25.64681081121879203, -66.03065707438999254, 91.59071981940550700 ) ) ;
#15878=VERTEX_POINT ( 'NONE', #11700 ) ;
#15879=CARTESIAN_POINT ( 'NONE',  ( 25.64708010899965984, -66.41183455464074825, -91.31497827399797984 ) ) ;
#15880=CARTESIAN_POINT ( 'NONE',  ( 2.430230287190592531, -126.7388733285340123, -71.49654683843642999 ) ) ;
#15881=CARTESIAN_POINT ( 'NONE',  ( 1.834118845439484335, -125.7578880615040049, -72.40084790867462061 ) ) ;
#15883=CARTESIAN_POINT ( 'NONE',  ( 21.16825799904902539, -131.4851843440079335, 32.46271504707898714 ) ) ;
#15890=ORIENTED_EDGE ( 'NONE', *, *, #7996, .T. ) ;
#15891=EDGE_CURVE ( 'NONE', #14327, #15152, #21452, .T. ) ;
#15892=B_SPLINE_CURVE_WITH_KNOTS ( 'NONE', 3,
 ( #200, #17749, #26391, #6692, #13426, #17878, #6266, #25103 ),
 .UNSPECIFIED., .F., .F.,
 ( 4, 2, 2, 4 ),
 ( 0.000000000000000000, 0.0002429588503611167412, 0.0004859177007222334824, 0.0009718354014444809509 ),
 .UNSPECIFIED. ) ;
#15893=CARTESIAN_POINT ( 'NONE',  ( 30.59138290137878613, 26.79783179610999255, 113.0806461017753861 ) ) ;
#15894=EDGE_LOOP ( 'NONE', ( #24120, #627, #2002, #9851 ) ) ;
#15895=CARTESIAN_POINT ( 'NONE',  ( 28.37599760073042532, -98.45181492308078930, -58.91309773266252847 ) ) ;
#15896=ORIENTED_EDGE ( 'NONE', *, *, #28129, .T. ) ;
#15900=FACE_OUTER_BOUND ( 'NONE', #25523, .T. ) ;
#15901=EDGE_CURVE ( 'NONE', #17999, #14115, #17658, .T. ) ;
#15902=CARTESIAN_POINT ( 'NONE',  ( 10.93730112725990367, -149.7554878793147566, -20.69552240458495973 ) ) ;
#15904=CARTESIAN_POINT ( 'NONE',  ( 109.1586059443104944, -0.006856640434643085195, 0.001740416220259381535 ) ) ;
#15905=DIRECTION ( 'NONE',  ( -0.5946245182733607137, 0.08697490616138922603, 0.7992853357633875611 ) ) ;
#15906=CARTESIAN_POINT ( 'NONE',  ( 25.98107933586738483, -110.4296102877912631, -24.58827779736892438 ) ) ;
#15908=CARTESIAN_POINT ( 'NONE',  ( 13.84597867724971465, -101.6650905919619419, 105.7628030201716456 ) ) ;
#15909=ORIENTED_EDGE ( 'NONE', *, *, #12725, .T. ) ;
#15913=CARTESIAN_POINT ( 'NONE',  ( 109.1587776205901577, 0.004375189885414170615, -0.005880209827417003793 ) ) ;
#15915=ORIENTED_EDGE ( 'NONE', *, *, #9594, .T. ) ;
#15916=DIRECTION ( 'NONE',  ( -1.000000000000000000, 0.000000000000000000, 0.000000000000000000 ) ) ;
#15918=CARTESIAN_POINT ( 'NONE',  ( 6.224689322667647851, -84.93872395423059629, 121.2721959030534862 ) ) ;
#15919=ORIENTED_EDGE ( 'NONE', *, *, #22680, .T. ) ;
#15920=CARTESIAN_POINT ( 'NONE',  ( 109.1589550718175161, 0.003591809816099524391, -0.006669585340474280290 ) ) ;
#15921=ADVANCED_FACE ( 'NONE', ( #1323 ), #24218, .F. ) ;
#15924=EDGE_CURVE ( 'NONE', #13159, #20294, #20058, .T. ) ;
#15925=VERTEX_POINT ( 'NONE', #22654 ) ;
#15928=B_SPLINE_CURVE_WITH_KNOTS ( 'NONE', 3,
 ( #2538, #17927, #14014, #16467, #17656, #5383 ),
 .UNSPECIFIED., .F., .F.,
 ( 4, 2, 4 ),
 ( 4.336808689942017736E-19, 0.0006311636237756775014, 0.001262327247551354569 ),
 .UNSPECIFIED. ) ;
#15930=B_SPLINE_CURVE_WITH_KNOTS ( 'NONE', 3,
 ( #5842, #15014, #3662, #1359, #12438, #27980 ),
 .UNSPECIFIED., .F., .F.,
 ( 4, 2, 4 ),
 ( 2.602085213965210642E-18, 0.0006311636237756776098, 0.001262327247551352618 ),
 .UNSPECIFIED. ) ;
#15934=CARTESIAN_POINT ( 'NONE',  ( 119.2224693531408803, 69.99999999999998579, -40.00000000000000711 ) ) ;
#15935=VERTEX_POINT ( 'NONE', #26169 ) ;
#15936=CARTESIAN_POINT ( 'NONE',  ( 25.64699802086723679, 0.2377811728597830354, 112.9109702078780089 ) ) ;
#15937=CARTESIAN_POINT ( 'NONE',  ( 8.186469829613953308, 149.3111477833936078, 3.468244397267471246 ) ) ;
#15939=ORIENTED_EDGE ( 'NONE', *, *, #11680, .T. ) ;
#15940=B_SPLINE_CURVE_WITH_KNOTS ( 'NONE', 3,
 ( #1859, #10519, #25513, #1449 ),
 .UNSPECIFIED., .F., .F.,
 ( 4, 4 ),
 ( 0.000000000000000000, 0.01077107196513845538 ),
 .UNSPECIFIED. ) ;
#15944=CARTESIAN_POINT ( 'NONE',  ( 109.1589550718175161, 0.004900004919101233827, -0.005777059646713199673 ) ) ;
#15946=CARTESIAN_POINT ( 'NONE',  ( 13.84597867724975728, 49.85807424839934043, -137.9700459519982871 ) ) ;
#15947=LINE ( 'NONE', #9775, #14833 ) ;
#15950=ORIENTED_EDGE ( 'NONE', *, *, #459, .T. ) ;
#15951=FACE_OUTER_BOUND ( 'NONE', #11974, .T. ) ;
#15952=CARTESIAN_POINT ( 'NONE',  ( 8.186469829614265947, -102.4860667297603243, 108.6390983847746980 ) ) ;
#15953=CARTESIAN_POINT ( 'NONE',  ( 1.833838850855461722, -145.1097630809418320, -0.08898185259725979734 ) ) ;
#15954=FACE_OUTER_BOUND ( 'NONE', #9169, .T. ) ;
#15956=DIRECTION ( 'NONE',  ( 0.5914120900931444380, 0.7398809652418028016, -0.3206367055789413611 ) ) ;
#15959=CARTESIAN_POINT ( 'NONE',  ( 32.73300124599740002, 66.00340565729470654, -97.37344512919790418 ) ) ;
#15960=EDGE_LOOP ( 'NONE', ( #5137, #5778 ) ) ;
#15961=CARTESIAN_POINT ( 'NONE',  ( 25.64660436782563480, 110.3216080362391409, -24.04259444204547336 ) ) ;
#15962=EDGE_CURVE ( 'NONE', #335, #18831, #20777, .T. ) ;
#15963=CARTESIAN_POINT ( 'NONE',  ( 2.430230287190581429, -86.70145658344736717, 116.8646894862409198 ) ) ;
#15964=ORIENTED_EDGE ( 'NONE', *, *, #4745, .T. ) ;
#15965=EDGE_CURVE ( 'NONE', #27450, #11640, #3960, .T. ) ;
#15966=VERTEX_POINT ( 'NONE', #24166 ) ;
#15968=CARTESIAN_POINT ( 'NONE',  ( 2.430230287190572103, 107.1617224697464366, 98.44218333480806393 ) ) ;
#15970=DIRECTION ( 'NONE',  ( -1.000000000000000000, -0.000000000000000000, -0.000000000000000000 ) ) ;
#15971=CARTESIAN_POINT ( 'NONE',  ( 24.01988960052056754, 17.94039809062794788, -129.8107982898199566 ) ) ;
#15972=CARTESIAN_POINT ( 'NONE',  ( 16.05277956358199276, 121.7045645913028693, -75.66118899150391996 ) ) ;
#15973=CARTESIAN_POINT ( 'NONE',  ( 25.64708010899967405, 34.94352788466287763, 107.3680906278372760 ) ) ;
#15976=ORIENTED_EDGE ( 'NONE', *, *, #8545, .F. ) ;
#15977=VERTEX_POINT ( 'NONE', #21569 ) ;
#15980=CARTESIAN_POINT ( 'NONE',  ( 1.832998868059858122, -141.8272129421610543, 30.69214149073968656 ) ) ;
#15981=DIRECTION ( 'NONE',  ( 0.8320502949607718746, 0.000000000000000000, -0.5547001952908368061 ) ) ;
#15982=DIRECTION ( 'NONE',  ( 0.5946245182733607137, -0.2456431038754811613, -0.7655593692109013970 ) ) ;
#15985=EDGE_LOOP ( 'NONE', ( #807, #22370, #21269, #18092 ) ) ;
#15987=DIRECTION ( 'NONE',  ( 0.000000000000000000, 0.000000000000000000, 1.000000000000000000 ) ) ;
#15989=B_SPLINE_CURVE_WITH_KNOTS ( 'NONE', 3,
 ( #14054, #4856, #16221, #11621 ),
 .UNSPECIFIED., .F., .F.,
 ( 4, 4 ),
 ( 2.596296363159515209E-17, 0.008383748772659474491 ),
 .UNSPECIFIED. ) ;
#15990=DIRECTION ( 'NONE',  ( -1.000000000000000000, -0.000000000000000000, -0.000000000000000000 ) ) ;
#15994=ORIENTED_EDGE ( 'NONE', *, *, #14329, .T. ) ;
#15995=ORIENTED_EDGE ( 'NONE', *, *, #8466, .T. ) ;
#15996=DIRECTION ( 'NONE',  ( 0.000000000000000000, 0.000000000000000000, 1.000000000000000000 ) ) ;
#15998=B_SPLINE_CURVE_WITH_KNOTS ( 'NONE', 3,
 ( #22337, #10965, #21902, #299 ),
 .UNSPECIFIED., .F., .F.,
 ( 4, 4 ),
 ( 0.000000000000000000, 0.01077107196513877110 ),
 .UNSPECIFIED. ) ;
#16000=UNCERTAINTY_MEASURE_WITH_UNIT (LENGTH_MEASURE( 1.000000000000000082E-05 ), #25277, 'distance_accuracy_value', 'NONE');
#16002=CARTESIAN_POINT ( 'NONE',  ( 109.1586059443104944, 0.004935564877224682574, 0.005067816690886773300 ) ) ;
#16003=CARTESIAN_POINT ( 'NONE',  ( 28.37603512858443011, -105.5302493666424084, -45.02094145483482635 ) ) ;
#16007=CARTESIAN_POINT ( 'NONE',  ( 2.263178113027064953, -31.59906256848382000, 141.9207360579561055 ) ) ;
#16008=ADVANCED_FACE ( 'NONE', ( #1986, #28317, #15489, #23762 ), #19410, .F. ) ;
#16010=CARTESIAN_POINT ( 'NONE',  ( 109.1586059443104944, 0.001921075557418361855, -0.006808232911146196685 ) ) ;
#16011=LINE ( 'NONE', #5072, #4071 ) ;
#16012=EDGE_CURVE ( 'NONE', #13097, #17077, #28180, .T. ) ;
#16014=EDGE_CURVE ( 'NONE', #20645, #18370, #17380, .T. ) ;
#16015=LINE ( 'NONE', #17876, #27622 ) ;
#16016=FACE_OUTER_BOUND ( 'NONE', #12259, .T. ) ;
#16017=B_SPLINE_CURVE_WITH_KNOTS ( 'NONE', 3,
 ( #22397, #5107, #20212, #17902 ),
 .UNSPECIFIED., .F., .F.,
 ( 4, 4 ),
 ( 3.113236650999850422E-16, 0.008383748772659758985 ),
 .UNSPECIFIED. ) ;
#16018=CARTESIAN_POINT ( 'NONE',  ( 28.37599760073042177, 65.97809271467136227, 93.86375353586188908 ) ) ;
#16019=CARTESIAN_POINT ( 'NONE',  ( 109.1721716018069515, 0.01281875973823902275, -0.01127028715939376591 ) ) ;
#16020=ORIENTED_EDGE ( 'NONE', *, *, #15758, .T. ) ;
#16022=ORIENTED_EDGE ( 'NONE', *, *, #21580, .T. ) ;
#16024=CARTESIAN_POINT ( 'NONE',  ( 1.833838850855487479, -30.25705358194946726, 141.9202662332486682 ) ) ;
#16025=ORIENTED_EDGE ( 'NONE', *, *, #12570, .F. ) ;
#16026=ORIENTED_EDGE ( 'NONE', *, *, #26690, .T. ) ;
#16027=VERTEX_POINT ( 'NONE', #19823 ) ;
#16028=ORIENTED_EDGE ( 'NONE', *, *, #4559, .F. ) ;
#16031=DIRECTION ( 'NONE',  ( -1.000000000000000000, -0.000000000000000000, -0.000000000000000000 ) ) ;
#16032=B_SPLINE_CURVE_WITH_KNOTS ( 'NONE', 3,
 ( #5782, #12516, #7661, #27348, #5629, #8089 ),
 .UNSPECIFIED., .F., .F.,
 ( 4, 2, 4 ),
 ( 1.965608005753612659E-17, 0.0006311571484586163058, 0.001262314296917213096 ),
 .UNSPECIFIED. ) ;
#16033=CARTESIAN_POINT ( 'NONE',  ( 1.834118845439484335, -132.4921483272732132, 59.18411796427007232 ) ) ;
#16036=CARTESIAN_POINT ( 'NONE',  ( 13.36082413113063083, 67.94366799842813975, 137.0038452127802771 ) ) ;
#16040=( BOUNDED_SURFACE ( )  B_SPLINE_SURFACE ( 3, 1, ( 
 ( #27302, #16369 ),
 ( #27155, #25162 ),
 ( #24748, #542 ),
 ( #22580, #7183 ) ),
 .UNSPECIFIED., .F., .F., .F. ) 
 B_SPLINE_SURFACE_WITH_KNOTS ( ( 4, 4 ),
 ( 2, 2 ),
 ( 0.000000000000000000, 1.000000000000000000 ),
 ( 0.000000000000000000, 1.000000000000000000 ),
 .UNSPECIFIED. ) 
 GEOMETRIC_REPRESENTATION_ITEM ( )  RATIONAL_B_SPLINE_SURFACE ( (
 ( 1.000000000000000000, 1.000000000000000000),
 ( 0.9960225298536222738, 0.9999952330161893110),
 ( 0.9960225298536222738, 0.9999952330161893110),
 ( 1.000000000000000000, 1.000000000000000000) ) ) 
 REPRESENTATION_ITEM ( '' )  SURFACE ( )  );
#16041=CARTESIAN_POINT ( 'NONE',  ( -90.83090735639699176, 0.000000000000000000, 0.000000000000000000 ) ) ;
#16042=DIRECTION ( 'NONE',  ( -1.000000000000000000, -0.000000000000000000, -0.000000000000000000 ) ) ;
#16046=VERTEX_POINT ( 'NONE', #18367 ) ;
#16048=CARTESIAN_POINT ( 'NONE',  ( 25.64708228042119487, 66.39944550735394557, -91.32398912286959103 ) ) ;
#16051=CARTESIAN_POINT ( 'NONE',  ( 109.1586059443104944, 0.001740416220250473730, -0.006856640434645987388 ) ) ;
#16052=CARTESIAN_POINT ( 'NONE',  ( 32.73300124599732186, 0.000000000000000000, 0.000000000000000000 ) ) ;
#16055=ORIENTED_EDGE ( 'NONE', *, *, #21886, .T. ) ;
#16056=CARTESIAN_POINT ( 'NONE',  ( 109.1589550718175161, -0.004269295012381961116, 0.006257602293702343825 ) ) ;
#16058=DIRECTION ( 'NONE',  ( 0.000000000000000000, 0.000000000000000000, 1.000000000000000000 ) ) ;
#16061=ORIENTED_EDGE ( 'NONE', *, *, #14566, .T. ) ;
#16063=CARTESIAN_POINT ( 'NONE',  ( 13.84597867724985143, 10.56985607909801850, 146.3210145202068873 ) ) ;
#16064=CARTESIAN_POINT ( 'NONE',  ( 1.833485406944043827, -132.3460930279895535, 59.50871042846178938 ) ) ;
#16065=ORIENTED_EDGE ( 'NONE', *, *, #12290, .F. ) ;
#16066=DIRECTION ( 'NONE',  ( -1.000000000000000000, -0.000000000000000000, -0.000000000000000000 ) ) ;
#16067=ORIENTED_EDGE ( 'NONE', *, *, #3349, .F. ) ;
#16068=CARTESIAN_POINT ( 'NONE',  ( 5.340103556456534228, 135.6222865117690617, -57.86178752079183596 ) ) ;
#16069=VERTEX_POINT ( 'NONE', #6883 ) ;
#16070=CARTESIAN_POINT ( 'NONE',  ( 10.93730112725978287, -133.3192575531804209, 71.28103789254889477 ) ) ;
#16071=EDGE_CURVE ( 'NONE', #16310, #5798, #1568, .T. ) ;
#16072=CARTESIAN_POINT ( 'NONE',  ( 1.834118845439484335, 117.5010238212710050, -85.14950727125739149 ) ) ;
#16074=LINE ( 'NONE', #24745, #7437 ) ;
#16079=CARTESIAN_POINT ( 'NONE',  ( 26.11404676487257603, 98.61392875273364211, 55.62948129436280453 ) ) ;
#16080=ORIENTED_EDGE ( 'NONE', *, *, #9388, .T. ) ;
#16081=EDGE_CURVE ( 'NONE', #21691, #8288, #23559, .T. ) ;
#16082=ORIENTED_EDGE ( 'NONE', *, *, #8466, .F. ) ;
#16085=LINE ( 'NONE', #11632, #9329 ) ;
#16086=CARTESIAN_POINT ( 'NONE',  ( 109.1592201516379674, 0.003476928926125392744, -0.007051465909551727154 ) ) ;
#16088=CARTESIAN_POINT ( 'NONE',  ( 30.59138290137886784, -114.2039707400270601, -21.51300488027244739 ) ) ;
#16089=CARTESIAN_POINT ( 'NONE',  ( 1.833485406944043827, 144.2578170162062747, 15.69895494453433393 ) ) ;
#16090=DIRECTION ( 'NONE',  ( 0.000000000000000000, 1.000000000000000000, -6.938893903907228378E-16 ) ) ;
#16093=CARTESIAN_POINT ( 'NONE',  ( 109.1721716018069515, -0.005082060336465163246, -0.01629455849719228799 ) ) ;
#16094=CARTESIAN_POINT ( 'NONE',  ( 5.340103556456485379, -100.3626145793569577, 108.0219267027626984 ) ) ;
#16095=CARTESIAN_POINT ( 'NONE',  ( 25.64703792032471341, 11.95040607427984725, 112.2770217641848660 ) ) ;
#16098=CARTESIAN_POINT ( 'NONE',  ( 2.433796855181205476, -28.83182736670433499, -142.6247129145651229 ) ) ;
#16099=CONICAL_SURFACE ( 'NONE', #12855, 117.6351876552689504, 0.9945805576725580410 ) ;
#16100=ORIENTED_EDGE ( 'NONE', *, *, #28034, .F. ) ;
#16101=CARTESIAN_POINT ( 'NONE',  ( 109.1721716018069515, -0.01699510305643761945, 0.001583175916617738993 ) ) ;
#16102=CARTESIAN_POINT ( 'NONE',  ( 26.11404676487257603, -45.01677474591340911, -103.8885755249573606 ) ) ;
#16103=CARTESIAN_POINT ( 'NONE',  ( 1.832998868059858122, -85.72499093308182694, 117.0819875546692543 ) ) ;
#16104=VERTEX_POINT ( 'NONE', #25455 ) ;
#16106=ORIENTED_EDGE ( 'NONE', *, *, #7284, .T. ) ;
#16107=CARTESIAN_POINT ( 'NONE',  ( 26.11404676487257603, -110.5078194225162918, 24.64483677384812665 ) ) ;
#16109=VECTOR ( 'NONE', #20588, 1000.000000000000114 ) ;
#16111=CIRCLE ( 'NONE', #24406, 151.1787379149930359 ) ;
#16114=EDGE_CURVE ( 'NONE', #26886, #19738, #5339, .T. ) ;
#16115=CONICAL_SURFACE ( 'NONE', #18883, 117.6351876552689504, 0.9945805576725580410 ) ;
#16116=CARTESIAN_POINT ( 'NONE',  ( 109.1586900883932856, -0.0006456433529069550677, 0.007109207791180748720 ) ) ;
#16119=CIRCLE ( 'NONE', #3723, 151.1787379149930359 ) ;
#16122=CARTESIAN_POINT ( 'NONE',  ( 9.884929003653608603, -124.2095058357583213, 85.04731144912473439 ) ) ;
#16123=CARTESIAN_POINT ( 'NONE',  ( 2.433796855181205476, -31.67151202413066713, 142.0211193075554945 ) ) ;
#16125=EDGE_CURVE ( 'NONE', #23136, #17852, #21252, .T. ) ;
#16126=CARTESIAN_POINT ( 'NONE',  ( 1.833485406944043827, 96.69979900902167458, 108.1939177044929323 ) ) ;
#16128=CARTESIAN_POINT ( 'NONE',  ( 1.833485406944043827, -138.1714136985311256, 44.33323125129879116 ) ) ;
#16129=CARTESIAN_POINT ( 'NONE',  ( 32.73300124599732186, 0.000000000000000000, 0.000000000000000000 ) ) ;
#16133=AXIS2_PLACEMENT_3D ( 'NONE', #20324, #616, #24374 ) ;
#16134=B_SPLINE_CURVE_WITH_KNOTS ( 'NONE', 3,
 ( #10920, #12783, #21571, #26171, #19550, #17382, #2255, #17246 ),
 .UNSPECIFIED., .F., .F.,
 ( 4, 2, 2, 4 ),
 ( 7.757919228897728493E-18, 0.0002429592666046879546, 0.0004859185332093681571, 0.0009718370664186953313 ),
 .UNSPECIFIED. ) ;
#16137=CARTESIAN_POINT ( 'NONE',  ( 25.64681081121879203, -107.5125461021400355, -34.49579773461893950 ) ) ;
#16138=ORIENTED_EDGE ( 'NONE', *, *, #18278, .F. ) ;
#16139=DIRECTION ( 'NONE',  ( 0.000000000000000000, 0.000000000000000000, 1.000000000000000000 ) ) ;
#16140=CIRCLE ( 'NONE', #2801, 117.6351876552689504 ) ;
#16141=ORIENTED_EDGE ( 'NONE', *, *, #9688, .F. ) ;
#16142=CIRCLE ( 'NONE', #11535, 12.50000000000000178 ) ;
#16143=ORIENTED_EDGE ( 'NONE', *, *, #4847, .T. ) ;
#16144=EDGE_LOOP ( 'NONE', ( #3871, #27935, #18523, #17531 ) ) ;
#16147=CARTESIAN_POINT ( 'NONE',  ( 109.1589550718175161, 0.006445391216541647428, -0.003980125429509243432 ) ) ;
#16148=ADVANCED_FACE ( 'NONE', ( #18668 ), #22015, .T. ) ;
#16149=CARTESIAN_POINT ( 'NONE',  ( 1.833206310202334155, -14.42724831649452000, 144.3905118062893393 ) ) ;
#16151=CARTESIAN_POINT ( 'NONE',  ( 2.263178607246657759, -144.7392885066942938, -13.80342482180235208 ) ) ;
#16152=CONICAL_SURFACE ( 'NONE', #7908, 117.6351876552689504, 0.9945805576725580410 ) ;
#16153=CARTESIAN_POINT ( 'NONE',  ( 2.433796855181205476, 1.451562450951669803, -145.5024947199069345 ) ) ;
#16154=CARTESIAN_POINT ( 'NONE',  ( 109.1586059443104944, -0.006260042619943072088, -0.003294606663354631478 ) ) ;
#16155=AXIS2_PLACEMENT_3D ( 'NONE', #24617, #4437, #11209 ) ;
#16156=CARTESIAN_POINT ( 'NONE',  ( 1.833485406944043827, -30.69200235379031838, 141.8265699653866250 ) ) ;
#16158=CARTESIAN_POINT ( 'NONE',  ( 1.834118845439484335, -30.34413640949792423, 141.9019470378987080 ) ) ;
#16159=CARTESIAN_POINT ( 'NONE',  ( 25.98107933586721074, -55.61918067932663234, -98.51796269673104689 ) ) ;
#16160=VECTOR ( 'NONE', #22984, 1000.000000000000000 ) ;
#16162=CARTESIAN_POINT ( 'NONE',  ( 10.93730112725972070, -26.59437931460858451, 148.8212007290659642 ) ) ;
#16166=CARTESIAN_POINT ( 'NONE',  ( 2.430230287190572103, -98.44218333480843341, 107.1617224697460813 ) ) ;
#16167=CARTESIAN_POINT ( 'NONE',  ( 25.64704443564076186, 83.99864088993871292, -75.45310550990073750 ) ) ;
#16168=LINE ( 'NONE', #24970, #17106 ) ;
#16169=VERTEX_POINT ( 'NONE', #25156 ) ;
#16172=ORIENTED_EDGE ( 'NONE', *, *, #9897, .F. ) ;
#16173=ORIENTED_EDGE ( 'NONE', *, *, #2691, .T. ) ;
#16174=ORIENTED_EDGE ( 'NONE', *, *, #12117, .T. ) ;
#16175=CARTESIAN_POINT ( 'NONE',  ( 13.36082413113063083, 94.94363694444052726, 119.8836995922729898 ) ) ;
#16176=EDGE_CURVE ( 'NONE', #6096, #23697, #18808, .T. ) ;
#16177=CARTESIAN_POINT ( 'NONE',  ( 10.93730112725945247, 108.9902118373741331, 104.7670965581011302 ) ) ;
#16179=ADVANCED_FACE ( 'NONE', ( #18528 ), #7678, .F. ) ;
#16180=CARTESIAN_POINT ( 'NONE',  ( 32.73300124599737160, -116.5274707358854158, -16.10546300444944023 ) ) ;
#16181=EDGE_CURVE ( 'NONE', #16536, #1646, #19342, .T. ) ;
#16182=CARTESIAN_POINT ( 'NONE',  ( 1.833691583653541235, 144.3515375443197115, -14.81406002961166912 ) ) ;
#16188=CARTESIAN_POINT ( 'NONE',  ( 109.1589550718175161, 0.006826119083824131080, -0.003284595046935060401 ) ) ;
#16189=CARTESIAN_POINT ( 'NONE',  ( 25.98107933586740259, 83.34070894055855661, 76.50887835172548535 ) ) ;
#16190=ORIENTED_EDGE ( 'NONE', *, *, #24162, .F. ) ;
#16191=EDGE_LOOP ( 'NONE', ( #918, #23867, #8235, #21746 ) ) ;
#16195=CARTESIAN_POINT ( 'NONE',  ( 2.108985857320902824, 86.43462668039136076, 116.7869613039522676 ) ) ;
#16197=VECTOR ( 'NONE', #25729, 1000.000000000000227 ) ;
#16199=CARTESIAN_POINT ( 'NONE',  ( -90.83090735639699176, 0.000000000000000000, 0.000000000000000000 ) ) ;
#16203=ORIENTED_EDGE ( 'NONE', *, *, #3094, .F. ) ;
#16204=CARTESIAN_POINT ( 'NONE',  ( 25.64700659047696618, -97.89757946487048912, 56.25842064176056567 ) ) ;
#16205=CARTESIAN_POINT ( 'NONE',  ( 2.433796855181233454, 116.8607839509068498, -86.69855925933855190 ) ) ;
#16208=ORIENTED_EDGE ( 'NONE', *, *, #14907, .F. ) ;
#16210=EDGE_CURVE ( 'NONE', #546, #8144, #5277, .T. ) ;
#16212=ORIENTED_EDGE ( 'NONE', *, *, #15351, .F. ) ;
#16213=CARTESIAN_POINT ( 'NONE',  ( 32.73300124599739291, -105.8473486001047235, -51.32617430725011332 ) ) ;
#16214=ORIENTED_EDGE ( 'NONE', *, *, #5701, .F. ) ;
#16218=CARTESIAN_POINT ( 'NONE',  ( 10.93730112725990011, -115.5857507957697976, -97.44200844886394464 ) ) ;
#16219=CIRCLE ( 'NONE', #7033, 117.6351876552689504 ) ;
#16221=CARTESIAN_POINT ( 'NONE',  ( 28.37603512858449051, 109.6581134439367560, 33.74339723237822852 ) ) ;
#16224=ORIENTED_EDGE ( 'NONE', *, *, #8461, .T. ) ;
#16225=CARTESIAN_POINT ( 'NONE',  ( 30.59138290137876481, 49.72302320601791337, 105.0379801549009784 ) ) ;
#16227=VERTEX_POINT ( 'NONE', #10883 ) ;
#16228=VERTEX_POINT ( 'NONE', #21820 ) ;
#16230=CARTESIAN_POINT ( 'NONE',  ( 25.86096068574579832, -90.87263912324372939, -67.25583614083940631 ) ) ;
#16232=CARTESIAN_POINT ( 'NONE',  ( 109.1624594426973260, -0.01102230012606011597, 0.01154818537150955997 ) ) ;
#16233=CARTESIAN_POINT ( 'NONE',  ( 2.430230287190581429, -142.0258656395019443, -31.67257033707648262 ) ) ;
#16234=CARTESIAN_POINT ( 'NONE',  ( 19.66333377628726353, 46.81583828063228481, -129.5498775999577958 ) ) ;
#16237=CARTESIAN_POINT ( 'NONE',  ( 21.16825799904898986, -135.3612955721067692, 4.416019842157926867 ) ) ;
#16241=CARTESIAN_POINT ( 'NONE',  ( 32.73300124599732186, 0.000000000000000000, 0.000000000000000000 ) ) ;
#16243=CARTESIAN_POINT ( 'NONE',  ( 109.1586900883932856, -0.004277182003220988613, 0.005715190711488708428 ) ) ;
#16244=B_SPLINE_CURVE_WITH_KNOTS ( 'NONE', 3,
 ( #13695, #7245, #4927, #22650, #2921, #9831, #18600 ),
 .UNSPECIFIED., .F., .F.,
 ( 4, 3, 4 ),
 ( 5.683119316658233806E-16, 0.02816610861753246833, 0.04000277880656280538 ),
 .UNSPECIFIED. ) ;
#16245=CARTESIAN_POINT ( 'NONE',  ( 109.1587776205901861, 0.007151389024635753690, -0.001605238040368390639 ) ) ;
#16246=ORIENTED_EDGE ( 'NONE', *, *, #15493, .F. ) ;
#16247=CARTESIAN_POINT ( 'NONE',  ( 109.1592201516379674, -0.002720803050361364321, 0.007376275279030867701 ) ) ;
#16248=( GEOMETRIC_REPRESENTATION_CONTEXT ( 3 ) GLOBAL_UNCERTAINTY_ASSIGNED_CONTEXT ( ( #26936 ) ) GLOBAL_UNIT_ASSIGNED_CONTEXT ( ( #22572, #9170, #20238 ) ) REPRESENTATION_CONTEXT ( 'NONE', 'WORKASPACE' ) );
#16250=EDGE_CURVE ( 'NONE', #16696, #25619, #7026, .T. ) ;
#16253=ADVANCED_FACE ( 'NONE', ( #10751 ), #12425, .F. ) ;
#16255=ORIENTED_EDGE ( 'NONE', *, *, #6141, .T. ) ;
#16256=ORIENTED_EDGE ( 'NONE', *, *, #16700, .F. ) ;
#16257=EDGE_CURVE ( 'NONE', #11422, #10623, #8302, .T. ) ;
#16261=ADVANCED_FACE ( 'NONE', ( #24131 ), #18297, .F. ) ;
#16263=( BOUNDED_SURFACE ( )  B_SPLINE_SURFACE ( 3, 1, ( 
 ( #20222, #518 ),
 ( #9314, #18072 ),
 ( #16794, #10452 ),
 ( #3254, #21083 ) ),
 .UNSPECIFIED., .F., .F., .F. ) 
 B_SPLINE_SURFACE_WITH_KNOTS ( ( 4, 4 ),
 ( 2, 2 ),
 ( 0.000000000000000000, 1.000000000000000000 ),
 ( 0.000000000000000000, 1.000000000000000000 ),
 .UNSPECIFIED. ) 
 GEOMETRIC_REPRESENTATION_ITEM ( )  RATIONAL_B_SPLINE_SURFACE ( (
 ( 1.000000000000000000, 1.000000000000000000),
 ( 0.9956975270656955868, 0.8568959468854907557),
 ( 0.9956975270656955868, 0.8568959468854907557),
 ( 1.000000000000000000, 1.000000000000000000) ) ) 
 REPRESENTATION_ITEM ( '' )  SURFACE ( )  );
#16264=FACE_OUTER_BOUND ( 'NONE', #25201, .T. ) ;
#16265=CARTESIAN_POINT ( 'NONE',  ( 10.93730112725945247, 108.9902118373741331, 104.7670965581011302 ) ) ;
#16268=CARTESIAN_POINT ( 'NONE',  ( 1.833721034905632097, 44.50273803002120587, -138.1171912769426058 ) ) ;
#16270=ORIENTED_EDGE ( 'NONE', *, *, #25718, .T. ) ;
#16271=ORIENTED_EDGE ( 'NONE', *, *, #18083, .F. ) ;
#16273=CARTESIAN_POINT ( 'NONE',  ( 28.37599760073042177, 114.7183216384031397, 1.794331790579828390 ) ) ;
#16274=FACE_OUTER_BOUND ( 'NONE', #11889, .T. ) ;
#16278=ORIENTED_EDGE ( 'NONE', *, *, #14398, .T. ) ;
#16279=LINE ( 'NONE', #25075, #13217 ) ;
#16281=FACE_OUTER_BOUND ( 'NONE', #26911, .T. ) ;
#16283=CARTESIAN_POINT ( 'NONE',  ( 25.64699802086725455, -107.3112355540543206, 35.11755197949801754 ) ) ;
#16284=ORIENTED_EDGE ( 'NONE', *, *, #9464, .T. ) ;
#16285=CARTESIAN_POINT ( 'NONE',  ( 25.64681081121879203, -75.86069728269045243, 83.63051021305875565 ) ) ;
#16286=ORIENTED_EDGE ( 'NONE', *, *, #9132, .T. ) ;
#16288=ORIENTED_EDGE ( 'NONE', *, *, #25584, .T. ) ;
#16289=ORIENTED_EDGE ( 'NONE', *, *, #9411, .F. ) ;
#16290=DIRECTION ( 'NONE',  ( -1.000000000000000000, -0.000000000000000000, -0.000000000000000000 ) ) ;
#16291=EDGE_CURVE ( 'NONE', #378, #23697, #21358, .T. ) ;
#16292=CARTESIAN_POINT ( 'NONE',  ( 2.430230287190581429, -109.1043569252020689, 96.28466919684062475 ) ) ;
#16293=CARTESIAN_POINT ( 'NONE',  ( 16.75465622695671186, 127.9746229614483752, 62.05388459345925867 ) ) ;
#16295=CARTESIAN_POINT ( 'NONE',  ( 109.1778270068192853, 0.008646067828078115095, -0.003465086990427118391 ) ) ;
#16297=DIRECTION ( 'NONE',  ( 0.000000000000000000, 0.000000000000000000, 1.000000000000000000 ) ) ;
#16298=CARTESIAN_POINT ( 'NONE',  ( 1.833485406944043827, 132.3460930279890704, 59.50871042846269177 ) ) ;
#16299=B_SPLINE_CURVE_WITH_KNOTS ( 'NONE', 3,
 ( #16909, #3805, #21223, #10438, #3515, #27705, #8273, #16778 ),
 .UNSPECIFIED., .F., .F.,
 ( 4, 2, 2, 4 ),
 ( 7.757919228897728493E-18, 0.0002429592666046734262, 0.0004859185332093391005, 0.0009718370664186894766 ),
 .UNSPECIFIED. ) ;
#16300=CARTESIAN_POINT ( 'NONE',  ( 109.1586900883932856, -0.007088091345229661187, 0.0008465529156634868553 ) ) ;
#16303=CARTESIAN_POINT ( 'NONE',  ( 25.64703792032473828, -75.66285916808242007, -83.80974623566366688 ) ) ;
#16305=CARTESIAN_POINT ( 'NONE',  ( 109.1592201516379674, -0.005631912476303850730, 0.005485778713202916178 ) ) ;
#16307=CARTESIAN_POINT ( 'NONE',  ( 25.86096068574580542, 112.3259320600845115, 12.80894308910771962 ) ) ;
#16308=CARTESIAN_POINT ( 'NONE',  ( 2.063896406836609909, 84.29612368209309636, -118.3103904147673404 ) ) ;
#16309=CARTESIAN_POINT ( 'NONE',  ( 32.73300124599736449, -114.2056417606550127, 28.19767303745571496 ) ) ;
#16310=VERTEX_POINT ( 'NONE', #26800 ) ;
#16311=CARTESIAN_POINT ( 'NONE',  ( 1.833485406944043827, -14.63699153649261575, -144.3694338680886347 ) ) ;
#16316=ADVANCED_FACE ( 'NONE', ( #18159 ), #28384, .F. ) ;
#16321=ORIENTED_EDGE ( 'NONE', *, *, #18184, .T. ) ;
#16322=CARTESIAN_POINT ( 'NONE',  ( 2.430230287190581429, 60.50928654924932459, -132.3371620660944643 ) ) ;
#16327=CARTESIAN_POINT ( 'NONE',  ( 2.433796855181233454, 71.49415740225254012, -126.7346379669248222 ) ) ;
#16329=FACE_OUTER_BOUND ( 'NONE', #3932, .T. ) ;
#16330=CARTESIAN_POINT ( 'NONE',  ( 2.108393763691172484, -86.43392821214661126, 116.7869873529606224 ) ) ;
#16333=ORIENTED_EDGE ( 'NONE', *, *, #20304, .T. ) ;
#16334=VERTEX_POINT ( 'NONE', #26649 ) ;
#16338=CARTESIAN_POINT ( 'NONE',  ( 26.11404676487259024, -108.0249973236465308, -33.91085499298486639 ) ) ;
#16339=CARTESIAN_POINT ( 'NONE',  ( 2.433796855181205476, -71.49415740224986848, -126.7346379669263001 ) ) ;
#16340=EDGE_CURVE ( 'NONE', #9431, #6438, #3242, .T. ) ;
#16341=ORIENTED_EDGE ( 'NONE', *, *, #7357, .F. ) ;
#16342=CARTESIAN_POINT ( 'NONE',  ( 25.98107933586698337, 98.51796269673161532, -55.61918067932647602 ) ) ;
#16343=CARTESIAN_POINT ( 'NONE',  ( 25.87036335909428431, -35.87755773825644923, -107.2165474610298332 ) ) ;
#16345=ORIENTED_EDGE ( 'NONE', *, *, #1078, .F. ) ;
#16346=B_SPLINE_CURVE_WITH_KNOTS ( 'NONE', 3,
 ( #17104, #8609, #26832, #20205, #8478, #28176 ),
 .UNSPECIFIED., .F., .F.,
 ( 4, 2, 4 ),
 ( 4.770489558936219510E-18, 0.0006311636237756751162, 0.001262327247551345245 ),
 .UNSPECIFIED. ) ;
#16347=EDGE_CURVE ( 'NONE', #195, #8387, #17301, .T. ) ;
#16348=B_SPLINE_CURVE_WITH_KNOTS ( 'NONE', 3,
 ( #17242, #19821, #17378, #11193, #26167, #10916, #17662, #26440 ),
 .UNSPECIFIED., .F., .F.,
 ( 4, 2, 2, 4 ),
 ( 6.938893903907228378E-18, 0.0002429588503611288571, 0.0004859177007222507754, 0.0009718354014444767226 ),
 .UNSPECIFIED. ) ;
#16349=B_SPLINE_CURVE_WITH_KNOTS ( 'NONE', 3,
 ( #28118, #10722, #19487, #28251, #8552, #17317, #4224, #15145 ),
 .UNSPECIFIED., .F., .F.,
 ( 4, 2, 2, 4 ),
 ( 6.938893903907228378E-18, 0.0002429588503611293450, 0.0004859177007222517512, 0.0009718354014444924435 ),
 .UNSPECIFIED. ) ;
#16350=CARTESIAN_POINT ( 'NONE',  ( 2.263178607246663976, 116.7985473178714955, -86.59154415224485035 ) ) ;
#16355=ORIENTED_EDGE ( 'NONE', *, *, #15679, .F. ) ;
#16358=CARTESIAN_POINT ( 'NONE',  ( 2.430230287190572103, -116.8646894862406072, -86.70145658344777928 ) ) ;
#16364=ORIENTED_EDGE ( 'NONE', *, *, #16012, .F. ) ;
#16365=B_SPLINE_CURVE_WITH_KNOTS ( 'NONE', 3,
 ( #3015, #844, #13791, #18111 ),
 .UNSPECIFIED., .F., .F.,
 ( 4, 4 ),
 ( 3.469446951953614189E-18, 0.008383560773332722482 ),
 .UNSPECIFIED. ) ;
#16366=CARTESIAN_POINT ( 'NONE',  ( 8.186469829614351212, -145.3272524103320222, -34.43598812953259625 ) ) ;
#16367=DIRECTION ( 'NONE',  ( -0.000000000000000000, -1.000000000000000000, -3.469446951953603342E-16 ) ) ;
#16368=CARTESIAN_POINT ( 'NONE',  ( 6.224689322667630975, 18.02516478984339088, -146.9579047224767692 ) ) ;
#16369=CARTESIAN_POINT ( 'NONE',  ( 1.832998868059890096, 141.8272129421612817, -30.69214149073874864 ) ) ;
#16372=ORIENTED_EDGE ( 'NONE', *, *, #7381, .T. ) ;
#16375=CARTESIAN_POINT ( 'NONE',  ( 109.1721716018069515, -0.01567407524361265347, 0.006757465437533703538 ) ) ;
#16376=CARTESIAN_POINT ( 'NONE',  ( 10.93730112725969938, 56.95489579269752767, 140.0398180619111770 ) ) ;
#16378=CARTESIAN_POINT ( 'NONE',  ( 1.833485406944043827, -132.3460930279887293, -59.50871042846357994 ) ) ;
#16382=EDGE_LOOP ( 'NONE', ( #6392, #17964, #2196, #5800 ) ) ;
#16383=CARTESIAN_POINT ( 'NONE',  ( 109.1624594426973260, -0.01033277910988589232, -0.01216903288310119090 ) ) ;
#16386=CARTESIAN_POINT ( 'NONE',  ( 109.1592201516379674, -0.007845213074654437332, 0.0005146241775982539042 ) ) ;
#16388=( BOUNDED_SURFACE ( )  B_SPLINE_SURFACE ( 3, 1, ( 
 ( #23693, #4220 ),
 ( #8547, #3804 ),
 ( #3944, #13002 ),
 ( #21792, #17180 ) ),
 .UNSPECIFIED., .F., .F., .F. ) 
 B_SPLINE_SURFACE_WITH_KNOTS ( ( 4, 4 ),
 ( 2, 2 ),
 ( 0.000000000000000000, 1.000000000000000000 ),
 ( 0.000000000000000000, 1.000000000000000000 ),
 .UNSPECIFIED. ) 
 GEOMETRIC_REPRESENTATION_ITEM ( )  RATIONAL_B_SPLINE_SURFACE ( (
 ( 1.000000000000000000, 1.000000000000000000),
 ( 0.6386103224230302855, 0.9954351624131538845),
 ( 0.6386103224230302855, 0.9954351624131538845),
 ( 1.000000000000000000, 1.000000000000000000) ) ) 
 REPRESENTATION_ITEM ( '' )  SURFACE ( )  );
#16390=CARTESIAN_POINT ( 'NONE',  ( 94.22246935314088034, -69.99999999999998579, -6.938893903907228378E-15 ) ) ;
#16391=VECTOR ( 'NONE', #6331, 1000.000000000000000 ) ;
#16392=VERTEX_POINT ( 'NONE', #318 ) ;
#16393=B_SPLINE_CURVE_WITH_KNOTS ( 'NONE', 3,
 ( #15324, #28147, #19648, #26272, #28420, #3975 ),
 .UNSPECIFIED., .F., .F.,
 ( 4, 2, 4 ),
 ( 2.024876365526581719E-17, 0.0006311636237756984265, 0.001262327247551376687 ),
 .UNSPECIFIED. ) ;
#16394=CONICAL_SURFACE ( 'NONE', #5561, 111.9614997405030152, 0.5880026024245678107 ) ;
#16395=CARTESIAN_POINT ( 'NONE',  ( 2.263178607246687957, 28.85718361841115254, -142.5035407554792073 ) ) ;
#16396=CARTESIAN_POINT ( 'NONE',  ( 10.93730112725977932, -115.5857507957709913, 97.44200844886238144 ) ) ;
#16397=CARTESIAN_POINT ( 'NONE',  ( 32.73300124599739291, -3.836798148478013371, -117.5726003567929610 ) ) ;
#16399=ORIENTED_EDGE ( 'NONE', *, *, #166, .F. ) ;
#16400=VERTEX_POINT ( 'NONE', #13558 ) ;
#16404=CARTESIAN_POINT ( 'NONE',  ( 109.1592201516379674, -0.002134489919774417484, -0.007566779963318545632 ) ) ;
#16405=B_SPLINE_CURVE_WITH_KNOTS ( 'NONE', 3,
 ( #16213, #24737, #18085, #24870, #14050, #22421, #11902 ),
 .UNSPECIFIED., .F., .F.,
 ( 4, 3, 4 ),
 ( 0.000000000000000000, 0.02398743853561349781, 0.04000277880656220864 ),
 .UNSPECIFIED. ) ;
#16406=CARTESIAN_POINT ( 'NONE',  ( 2.433796855181233454, 126.7346379669255754, 71.49415740225120430 ) ) ;
#16409=CARTESIAN_POINT ( 'NONE',  ( 2.263178113027075611, -144.7392881653025256, 13.80342493153463579 ) ) ;
#16410=B_SPLINE_CURVE_WITH_KNOTS ( 'NONE', 3,
 ( #14126, #322, #9111, #27052 ),
 .UNSPECIFIED., .F., .F.,
 ( 4, 4 ),
 ( 0.000000000000000000, 0.01077107196513872947 ),
 .UNSPECIFIED. ) ;
#16413=CARTESIAN_POINT ( 'NONE',  ( 1.831572820252009626, 71.69925593429985611, -126.1609924456722354 ) ) ;
#16419=CARTESIAN_POINT ( 'NONE',  ( 32.73300124599731475, 117.5726003567930178, 3.836798148479249715 ) ) ;
#16420=CARTESIAN_POINT ( 'NONE',  ( 32.73300124599738581, -72.21147546950486174, -92.86301839380092815 ) ) ;
#16422=CARTESIAN_POINT ( 'NONE',  ( 1.833485406944057594, 141.8265699653871366, -30.69200235378795227 ) ) ;
#16424=CARTESIAN_POINT ( 'NONE',  ( 109.1586900883932856, -0.006561743627145281976, -0.002810909342002382467 ) ) ;
#16425=ORIENTED_EDGE ( 'NONE', *, *, #1562, .T. ) ;
#16427=DIRECTION ( 'NONE',  ( -1.000000000000000000, -0.000000000000000000, -0.000000000000000000 ) ) ;
#16429=EDGE_CURVE ( 'NONE', #10703, #14998, #17961, .T. ) ;
#16430=CARTESIAN_POINT ( 'NONE',  ( 2.063896406836609909, -57.85593781835507343, 133.2511741302118651 ) ) ;
#16433=EDGE_LOOP ( 'NONE', ( #4344, #9206, #9425, #7168 ) ) ;
#16434=CARTESIAN_POINT ( 'NONE',  ( 25.64670758986457599, 22.98827151089287568, 110.5460908981863071 ) ) ;
#16437=ORIENTED_EDGE ( 'NONE', *, *, #27725, .T. ) ;
#16438=VERTEX_POINT ( 'NONE', #6188 ) ;
#16439=( BOUNDED_SURFACE ( )  B_SPLINE_SURFACE ( 3, 1, ( 
 ( #7792, #18709 ),
 ( #12502, #5620 ),
 ( #7943, #27907 ),
 ( #12235, #27480 ) ),
 .UNSPECIFIED., .F., .F., .F. ) 
 B_SPLINE_SURFACE_WITH_KNOTS ( ( 4, 4 ),
 ( 2, 2 ),
 ( 0.000000000000000000, 1.000000000000000000 ),
 ( 0.000000000000000000, 1.000000000000000000 ),
 .UNSPECIFIED. ) 
 GEOMETRIC_REPRESENTATION_ITEM ( )  RATIONAL_B_SPLINE_SURFACE ( (
 ( 1.000000000000000000, 1.000000000000000000),
 ( 0.9960225298536222738, 0.9999952330161893110),
 ( 0.9960225298536222738, 0.9999952330161893110),
 ( 1.000000000000000000, 1.000000000000000000) ) ) 
 REPRESENTATION_ITEM ( '' )  SURFACE ( )  );
#16441=CARTESIAN_POINT ( 'NONE',  ( 2.433796855181205476, -138.8296532063090751, 43.58222566461595449 ) ) ;
#16442=CARTESIAN_POINT ( 'NONE',  ( 109.1592201516379674, 0.007748443302128555504, -0.001331853079208340871 ) ) ;
#16443=B_SPLINE_CURVE_WITH_KNOTS ( 'NONE', 3,
 ( #18294, #9410, #11843, #9986, #11703, #13991, #5067, #7252 ),
 .UNSPECIFIED., .F., .F.,
 ( 4, 2, 2, 4 ),
 ( 0.000000000000000000, 0.0002429588503611235717, 0.0004859177007222471433, 0.0009718354014444888656 ),
 .UNSPECIFIED. ) ;
#16444=CARTESIAN_POINT ( 'NONE',  ( 2.108393763691192024, -98.16799842733318826, 107.1124103264145901 ) ) ;
#16445=CARTESIAN_POINT ( 'NONE',  ( 2.430230287190581429, 142.6294793592101655, -28.83279105684287913 ) ) ;
#16448=EDGE_CURVE ( 'NONE', #213, #19162, #23507, .T. ) ;
#16451=CARTESIAN_POINT ( 'NONE',  ( 55.49584447822657296, -72.12568090333337523, -7.849835876629073006 ) ) ;
#16452=ADVANCED_FACE ( 'NONE', ( #23888 ), #14449, .F. ) ;
#16453=CARTESIAN_POINT ( 'NONE',  ( 6.224689322667647851, -12.92299475787058860, 147.4941644018827844 ) ) ;
#16454=CARTESIAN_POINT ( 'NONE',  ( 55.79472521941426777, 37.00555938668347977, -62.63970324008221979 ) ) ;
#16455=CARTESIAN_POINT ( 'NONE',  ( 26.11404676487259024, -22.43340081644844020, 110.9778746459746372 ) ) ;
#16457=VERTEX_POINT ( 'NONE', #3873 ) ;
#16458=FACE_OUTER_BOUND ( 'NONE', #12717, .T. ) ;
#16459=ORIENTED_EDGE ( 'NONE', *, *, #2691, .F. ) ;
#16462=B_SPLINE_CURVE_WITH_KNOTS ( 'NONE', 3,
 ( #27782, #5771, #18712, #27909 ),
 .UNSPECIFIED., .F., .F.,
 ( 4, 4 ),
 ( 3.481441887456309019E-16, 0.01077107486149842842 ),
 .UNSPECIFIED. ) ;
#16463=EDGE_LOOP ( 'NONE', ( #1141, #21805, #15658, #8666 ) ) ;
#16465=VERTEX_POINT ( 'NONE', #23755 ) ;
#16466=CARTESIAN_POINT ( 'NONE',  ( 32.73300124599732186, 0.000000000000000000, 0.000000000000000000 ) ) ;
#16467=CARTESIAN_POINT ( 'NONE',  ( 1.893872463202064260, 86.08597552419035992, -116.8661275359689427 ) ) ;
#16468=CARTESIAN_POINT ( 'NONE',  ( 109.1587776205901861, -0.001605238040368415576, -0.007151389024635748486 ) ) ;
#16469=AXIS2_PLACEMENT_3D ( 'NONE', #8790, #4597, #4891 ) ;
#16475=EDGE_CURVE ( 'NONE', #10330, #21420, #26161, .T. ) ;
#16476=FACE_OUTER_BOUND ( 'NONE', #22546, .T. ) ;
#16477=CARTESIAN_POINT ( 'NONE',  ( 109.1587776205901861, 0.006944419901758130259, -0.002343968083398764550 ) ) ;
#16479=EDGE_CURVE ( 'NONE', #709, #18117, #28250, .T. ) ;
#16480=EDGE_LOOP ( 'NONE', ( #2434, #2069, #917, #606 ) ) ;
#16481=VERTEX_POINT ( 'NONE', #6048 ) ;
#16482=DIRECTION ( 'NONE',  ( -1.000000000000000000, -0.000000000000000000, -0.000000000000000000 ) ) ;
#16483=CARTESIAN_POINT ( 'NONE',  ( 1.833838850855486147, 85.22139087169075822, 117.4485666028820958 ) ) ;
#16484=CARTESIAN_POINT ( 'NONE',  ( 25.64670758986456889, 75.92149922855311672, -83.57526425215419863 ) ) ;
#16486=CARTESIAN_POINT ( 'NONE',  ( 2.433796855181219243, -28.83182736670634583, 142.6247129145647534 ) ) ;
#16487=ORIENTED_EDGE ( 'NONE', *, *, #11300, .T. ) ;
#16488=EDGE_LOOP ( 'NONE', ( #23734, #1603, #18376, #24401 ) ) ;
#16490=CARTESIAN_POINT ( 'NONE',  ( 25.64660436782551400, -35.44263474731867092, -107.2041192742819078 ) ) ;
#16491=CARTESIAN_POINT ( 'NONE',  ( 30.59138290137920890, 115.2623146671594441, -14.83088430729453400 ) ) ;
#16492=VERTEX_POINT ( 'NONE', #8747 ) ;
#16498=VERTEX_POINT ( 'NONE', #12774 ) ;
#16499=CARTESIAN_POINT ( 'NONE',  ( 2.433796855181205476, 138.8296532063094162, -43.58222566461498815 ) ) ;
#16500=ORIENTED_EDGE ( 'NONE', *, *, #716, .F. ) ;
#16502=CARTESIAN_POINT ( 'NONE',  ( 2.430230287190589422, 28.83279105684624000, -142.6294793592095118 ) ) ;
#16506=CARTESIAN_POINT ( 'NONE',  ( 28.37603512858453669, 100.2461737936630612, 55.80522682147307734 ) ) ;
#16507=( BOUNDED_SURFACE ( )  B_SPLINE_SURFACE ( 3, 1, ( 
 ( #982, #7623 ),
 ( #25040, #27163 ),
 ( #23305, #20843 ),
 ( #18972, #16233 ) ),
 .UNSPECIFIED., .F., .F., .F. ) 
 B_SPLINE_SURFACE_WITH_KNOTS ( ( 4, 4 ),
 ( 2, 2 ),
 ( 0.000000000000000000, 1.000000000000000000 ),
 ( 0.000000000000000000, 1.000000000000000000 ),
 .UNSPECIFIED. ) 
 GEOMETRIC_REPRESENTATION_ITEM ( )  RATIONAL_B_SPLINE_SURFACE ( (
 ( 1.000000000000000000, 1.000000000000000000),
 ( 0.9956975270656955868, 0.8568959468854907557),
 ( 0.9956975270656955868, 0.8568959468854907557),
 ( 1.000000000000000000, 1.000000000000000000) ) ) 
 REPRESENTATION_ITEM ( '' )  SURFACE ( )  );
#16508=CARTESIAN_POINT ( 'NONE',  ( 1.894214914920971937, -117.9869255019025900, -84.54370816135696032 ) ) ;
#16509=CARTESIAN_POINT ( 'NONE',  ( 25.64670758986458310, -46.37945960491945385, 102.9458331681483685 ) ) ;
#16510=CARTESIAN_POINT ( 'NONE',  ( 28.37644542392825997, 116.9383271603247891, 42.25924161793936662 ) ) ;
#16511=EDGE_CURVE ( 'NONE', #20724, #21385, #26226, .T. ) ;
#16513=B_SPLINE_CURVE_WITH_KNOTS ( 'NONE', 3,
 ( #23181, #21411, #16683, #23313, #25477, #5751, #28159 ),
 .UNSPECIFIED., .F., .F.,
 ( 4, 3, 4 ),
 ( 0.000000000000000000, 0.02398743853561352210, 0.04000277880656218088 ),
 .UNSPECIFIED. ) ;
#16515=LINE ( 'NONE', #25302, #9309 ) ;
#16519=ORIENTED_EDGE ( 'NONE', *, *, #25015, .F. ) ;
#16521=CARTESIAN_POINT ( 'NONE',  ( 2.433796855181233454, 60.50726454507903895, 132.3327394885233446 ) ) ;
#16522=CARTESIAN_POINT ( 'NONE',  ( 9.884929003653626367, -78.87917189084822667, -128.2151425008049728 ) ) ;
#16523=CARTESIAN_POINT ( 'NONE',  ( 13.84597867724970044, -135.8932891738221542, 55.26821062125512896 ) ) ;
#16524=CARTESIAN_POINT ( 'NONE',  ( 2.108985857320903712, 133.2480631238193496, 57.92316197981703851 ) ) ;
#16525=CARTESIAN_POINT ( 'NONE',  ( 1.831572820252009626, -126.1609924456724912, -71.69925593429942978 ) ) ;
#16526=EDGE_LOOP ( 'NONE', ( #15552, #20667, #4852, #16923 ) ) ;
#16527=CARTESIAN_POINT ( 'NONE',  ( 25.64708010899965629, -83.87281825978668337, 75.59303792846597503 ) ) ;
#16528=CARTESIAN_POINT ( 'NONE',  ( 24.22246935314087324, 0.000000000000000000, 0.000000000000000000 ) ) ;
#16530=CARTESIAN_POINT ( 'NONE',  ( 2.433796855181219243, 133.5135467655526043, -57.85512797797757401 ) ) ;
#16532=CARTESIAN_POINT ( 'NONE',  ( 9.884929003653626367, 97.56484214660780196, -114.6392083957107815 ) ) ;
#16535=CARTESIAN_POINT ( 'NONE',  ( 2.430230287190592531, -133.5180086894987710, -57.85706160874279647 ) ) ;
#16536=VERTEX_POINT ( 'NONE', #6316 ) ;
#16537=CARTESIAN_POINT ( 'NONE',  ( 32.73300124599732186, 0.000000000000000000, 0.000000000000000000 ) ) ;
#16538=CARTESIAN_POINT ( 'NONE',  ( 1.833485406944057594, -30.69200235378832176, -141.8265699653870513 ) ) ;
#16539=CARTESIAN_POINT ( 'NONE',  ( 32.73300124599736449, -116.5274707358856574, 16.10546300444784507 ) ) ;
#16540=ORIENTED_EDGE ( 'NONE', *, *, #5300, .F. ) ;
#16542=ORIENTED_EDGE ( 'NONE', *, *, #24663, .T. ) ;
#16544=EDGE_CURVE ( 'NONE', #9793, #2416, #11327, .T. ) ;
#16545=EDGE_CURVE ( 'NONE', #5021, #24828, #382, .T. ) ;
#16546=CARTESIAN_POINT ( 'NONE',  ( 32.73300124599740002, 110.6325518752278896, -39.98094346392192477 ) ) ;
#16547=B_SPLINE_CURVE_WITH_KNOTS ( 'NONE', 3,
 ( #23006, #8166, #27439, #7749 ),
 .UNSPECIFIED., .F., .F.,
 ( 4, 4 ),
 ( 0.000000000000000000, 0.008383560773332738095 ),
 .UNSPECIFIED. ) ;
#16548=CARTESIAN_POINT ( 'NONE',  ( 21.16825799904901473, 63.85626241912904533, -119.4343305756972597 ) ) ;
#16549=ORIENTED_EDGE ( 'NONE', *, *, #13129, .T. ) ;
#16551=EDGE_CURVE ( 'NONE', #22112, #17196, #4167, .T. ) ;
#16553=CARTESIAN_POINT ( 'NONE',  ( 2.063896406836609909, 71.46753739786191773, -126.4736179849640365 ) ) ;
#16554=ORIENTED_EDGE ( 'NONE', *, *, #10235, .F. ) ;
#16557=B_SPLINE_CURVE_WITH_KNOTS ( 'NONE', 3,
 ( #5621, #6055, #12366, #23196, #21001, #14810, #1286, #3587, #12236, #14940 ),
 .UNSPECIFIED., .F., .F.,
 ( 4, 3, 3, 4 ),
 ( 3.469446951953614189E-17, 0.0002669559177086236468, 0.0005339118354151006817, 0.001067817517169172489 ),
 .UNSPECIFIED. ) ;
#16558=CARTESIAN_POINT ( 'NONE',  ( 32.73300124599736449, -66.00340565729409548, 97.37344512919831629 ) ) ;
#16559=CARTESIAN_POINT ( 'NONE',  ( 109.1586900883932856, -0.006960773163852201732, 0.001582822706032804708 ) ) ;
#16561=CARTESIAN_POINT ( 'NONE',  ( 26.11404676487257603, -102.9690087468804762, 47.08215554553482463 ) ) ;
#16565=ORIENTED_EDGE ( 'NONE', *, *, #748, .F. ) ;
#16566=DIRECTION ( 'NONE',  ( 0.000000000000000000, 0.000000000000000000, 1.000000000000000000 ) ) ;
#16571=( BOUNDED_SURFACE ( )  B_SPLINE_SURFACE ( 3, 1, ( 
 ( #17278, #14565 ),
 ( #3622, #12398 ),
 ( #12543, #23798 ),
 ( #12960, #23659 ) ),
 .UNSPECIFIED., .F., .F., .F. ) 
 B_SPLINE_SURFACE_WITH_KNOTS ( ( 4, 4 ),
 ( 2, 2 ),
 ( 0.000000000000000000, 1.000000000000000000 ),
 ( 0.000000000000000000, 1.000000000000000000 ),
 .UNSPECIFIED. ) 
 GEOMETRIC_REPRESENTATION_ITEM ( )  RATIONAL_B_SPLINE_SURFACE ( (
 ( 1.000000000000000000, 1.000000000000000000),
 ( 0.6386103224230302855, 0.9954351624131538845),
 ( 0.6386103224230302855, 0.9954351624131538845),
 ( 1.000000000000000000, 1.000000000000000000) ) ) 
 REPRESENTATION_ITEM ( '' )  SURFACE ( )  );
#16573=CARTESIAN_POINT ( 'NONE',  ( 25.64692872815578184, -75.79105864157443762, 83.69378511050537384 ) ) ;
#16574=CARTESIAN_POINT ( 'NONE',  ( 24.01988960052043609, 115.5642432877701822, -61.78678588189911380 ) ) ;
#16575=ORIENTED_EDGE ( 'NONE', *, *, #4600, .T. ) ;
#16577=ORIENTED_EDGE ( 'NONE', *, *, #22975, .T. ) ;
#16581=CARTESIAN_POINT ( 'NONE',  ( 25.64681081121879203, -110.3564950173080206, -23.88203588908195130 ) ) ;
#16584=EDGE_CURVE ( 'NONE', #7936, #3978, #15928, .T. ) ;
#16585=CARTESIAN_POINT ( 'NONE',  ( 109.1592201516379674, 0.0005146241775982810093, 0.007845213074654433863 ) ) ;
#16586=CARTESIAN_POINT ( 'NONE',  ( 55.79472521941428198, -21.78881894124752350, 69.41463258328505503 ) ) ;
#16587=EDGE_CURVE ( 'NONE', #12739, #16046, #27101, .T. ) ;
#16591=CARTESIAN_POINT ( 'NONE',  ( 25.64699802086722968, 84.06830990999330311, 75.37548011155753613 ) ) ;
#16593=LINE ( 'NONE', #23238, #569 ) ;
#16594=CARTESIAN_POINT ( 'NONE',  ( 25.87036335909427009, -110.3794299719621677, 24.47383578007097782 ) ) ;
#16595=CARTESIAN_POINT ( 'NONE',  ( 32.73300124599739291, -103.7392577722171865, -55.46353551262117776 ) ) ;
#16596=CIRCLE ( 'NONE', #8788, 117.6351876552689504 ) ;
#16597=VECTOR ( 'NONE', #22304, 1000.000000000000000 ) ;
#16598=CARTESIAN_POINT ( 'NONE',  ( 26.28373643307413232, -22.43832507403739385, 125.5716026420346196 ) ) ;
#16601=CARTESIAN_POINT ( 'NONE',  ( 26.11404676487257603, -84.89295829319543429, 74.91683232330944975 ) ) ;
#16604=ORIENTED_EDGE ( 'NONE', *, *, #12995, .F. ) ;
#16605=DIRECTION ( 'NONE',  ( -0.5914120900931443270, -0.5455001977188012052, -0.5938529060132713422 ) ) ;
#16606=( BOUNDED_SURFACE ( )  B_SPLINE_SURFACE ( 3, 1, ( 
 ( #11856, #11565 ),
 ( #911, #9696 ),
 ( #334, #18174 ),
 ( #22519, #2491 ) ),
 .UNSPECIFIED., .F., .F., .F. ) 
 B_SPLINE_SURFACE_WITH_KNOTS ( ( 4, 4 ),
 ( 2, 2 ),
 ( 0.000000000000000000, 1.000000000000000000 ),
 ( 0.000000000000000000, 1.000000000000000000 ),
 .UNSPECIFIED. ) 
 GEOMETRIC_REPRESENTATION_ITEM ( )  RATIONAL_B_SPLINE_SURFACE ( (
 ( 1.000000000000000000, 1.000000000000000000),
 ( 0.6386103224230316178, 0.9954351624131538845),
 ( 0.6386103224230316178, 0.9954351624131538845),
 ( 1.000000000000000000, 1.000000000000000000) ) ) 
 REPRESENTATION_ITEM ( '' )  SURFACE ( )  );
#16608=VERTEX_POINT ( 'NONE', #16177 ) ;
#16609=CARTESIAN_POINT ( 'NONE',  ( 2.263178607246653318, -16.59120332983045998, -144.4462811785178076 ) ) ;
#16610=CARTESIAN_POINT ( 'NONE',  ( 94.22246935314088034, 90.00000000000005684, -12.50000000000000888 ) ) ;
#16611=ORIENTED_EDGE ( 'NONE', *, *, #2942, .F. ) ;
#16614=ORIENTED_EDGE ( 'NONE', *, *, #22034, .T. ) ;
#16615=ADVANCED_FACE ( 'NONE', ( #24984 ), #17384, .F. ) ;
#16616=EDGE_CURVE ( 'NONE', #23443, #20437, #27253, .T. ) ;
#16617=EDGE_CURVE ( 'NONE', #11082, #21644, #14561, .T. ) ;
#16618=B_SPLINE_CURVE_WITH_KNOTS ( 'NONE', 3,
 ( #19571, #26468, #2273, #4447 ),
 .UNSPECIFIED., .F., .F.,
 ( 4, 4 ),
 ( 0.000000000000000000, 0.008383560773332720747 ),
 .UNSPECIFIED. ) ;
#16619=VECTOR ( 'NONE', #27795, 1000.000000000000000 ) ;
#16621=EDGE_CURVE ( 'NONE', #25689, #22240, #4248, .T. ) ;
#16622=CONICAL_SURFACE ( 'NONE', #13856, 117.6351876552689504, 0.9945805576725580410 ) ;
#16627=DIRECTION ( 'NONE',  ( -0.5946245182733607137, -0.7637359336799420806, 0.2512550613902148622 ) ) ;
#16630=CARTESIAN_POINT ( 'NONE',  ( 2.063896406836605024, 1.344106060022389526, -145.2631347824382431 ) ) ;
#16631=CARTESIAN_POINT ( 'NONE',  ( 109.1586900883932856, 0.002810909342011597319, 0.006561743627143340821 ) ) ;
#16635=VERTEX_POINT ( 'NONE', #27966 ) ;
#16636=VERTEX_POINT ( 'NONE', #19195 ) ;
#16638=CARTESIAN_POINT ( 'NONE',  ( 1.831572820252008738, 144.2101521542830369, 16.14965423926257770 ) ) ;
#16639=B_SPLINE_CURVE_WITH_KNOTS ( 'NONE', 3,
 ( #11396, #17582, #180, #21917 ),
 .UNSPECIFIED., .F., .F.,
 ( 4, 4 ),
 ( 0.000000000000000000, 0.008383560773332715543 ),
 .UNSPECIFIED. ) ;
#16640=CARTESIAN_POINT ( 'NONE',  ( 24.01988960052061373, -127.2243989116373371, -31.41104197353454452 ) ) ;
#16641=ORIENTED_EDGE ( 'NONE', *, *, #13874, .F. ) ;
#16645=AXIS2_PLACEMENT_3D ( 'NONE', #2786, #25106, #13717 ) ;
#16649=CARTESIAN_POINT ( 'NONE',  ( 10.93730112726003156, 119.3442956573285443, -92.80059208661575099 ) ) ;
#16650=VERTEX_POINT ( 'NONE', #7853 ) ;
#16653=CARTESIAN_POINT ( 'NONE',  ( 109.1586059443104944, 0.006971743774738786009, -0.001198897580748364746 ) ) ;
#16657=AXIS2_PLACEMENT_3D ( 'NONE', #4037, #23919, #27805 ) ;
#16658=B_SPLINE_CURVE_WITH_KNOTS ( 'NONE', 3,
 ( #25017, #12045, #22715, #22857 ),
 .UNSPECIFIED., .F., .F.,
 ( 4, 4 ),
 ( 3.469446951953614189E-18, 0.008383560773332732891 ),
 .UNSPECIFIED. ) ;
#16660=CARTESIAN_POINT ( 'NONE',  ( 2.063896406836605024, 141.8093313989361093, 31.51663808384605403 ) ) ;
#16661=CARTESIAN_POINT ( 'NONE',  ( 1.833809397773843219, -107.7184108265657443, -97.22957127128945842 ) ) ;
#16664=CARTESIAN_POINT ( 'NONE',  ( 21.16825799904903960, -4.416019842157457909, -135.3612955721066839 ) ) ;
#16666=FACE_OUTER_BOUND ( 'NONE', #1394, .T. ) ;
#16668=ORIENTED_EDGE ( 'NONE', *, *, #15962, .T. ) ;
#16670=VERTEX_POINT ( 'NONE', #23683 ) ;
#16672=CARTESIAN_POINT ( 'NONE',  ( 10.93730112725994097, -51.37919228020192008, -142.1801301103790536 ) ) ;
#16673=CARTESIAN_POINT ( 'NONE',  ( 1.832998868059890096, -138.1720401012263721, -44.33343224355374446 ) ) ;
#16674=CARTESIAN_POINT ( 'NONE',  ( 16.75465622695653067, 112.2763423369180771, 87.30527857298483241 ) ) ;
#16675=CARTESIAN_POINT ( 'NONE',  ( 26.11404676487259024, 102.9690087468808031, -47.08215554553414961 ) ) ;
#16678=EDGE_LOOP ( 'NONE', ( #281, #11432, #7448, #743 ) ) ;
#16679=CARTESIAN_POINT ( 'NONE',  ( 2.263178113027040084, 71.48082833565062799, 126.6115605262340438 ) ) ;
#16680=CARTESIAN_POINT ( 'NONE',  ( 55.79472521941426777, -14.41365263906501681, -71.31192372336690255 ) ) ;
#16681=VERTEX_POINT ( 'NONE', #10559 ) ;
#16683=CARTESIAN_POINT ( 'NONE',  ( 24.01988960052063504, -23.05141021591188277, -129.0012934948649672 ) ) ;
#16684=CARTESIAN_POINT ( 'NONE',  ( 25.86096068574580897, -67.25583614083905104, 90.87263912324389992 ) ) ;
#16685=CARTESIAN_POINT ( 'NONE',  ( 1.831572820252009626, 116.8148281295980695, -86.09108691067652330 ) ) ;
#16686=B_SPLINE_CURVE_WITH_KNOTS ( 'NONE', 3,
 ( #18107, #25045, #9780, #18549 ),
 .UNSPECIFIED., .F., .F.,
 ( 4, 4 ),
 ( 0.000000000000000000, 0.008383560773332712074 ),
 .UNSPECIFIED. ) ;
#16687=CARTESIAN_POINT ( 'NONE',  ( 32.73300124599732186, 0.000000000000000000, 0.000000000000000000 ) ) ;
#16689=CARTESIAN_POINT ( 'NONE',  ( 10.93730112725978287, -125.1380233598484182, 84.82621002473399585 ) ) ;
#16690=ORIENTED_EDGE ( 'NONE', *, *, #10334, .T. ) ;
#16691=DIRECTION ( 'NONE',  ( 0.5946245182733607137, -0.1700465163848307315, 0.7858154137795702043 ) ) ;
#16692=CARTESIAN_POINT ( 'NONE',  ( 8.186469777910600598, 122.8338388711459430, 84.95702201436446899 ) ) ;
#16694=EDGE_CURVE ( 'NONE', #13886, #14659, #27142, .T. ) ;
#16696=VERTEX_POINT ( 'NONE', #19742 ) ;
#16699=ADVANCED_FACE ( 'NONE', ( #6382 ), #13524, .F. ) ;
#16700=EDGE_CURVE ( 'NONE', #26952, #18945, #2146, .T. ) ;
#16701=CARTESIAN_POINT ( 'NONE',  ( 9.884929003653608603, 128.2151425008041201, 78.87917189084957670 ) ) ;
#16702=CARTESIAN_POINT ( 'NONE',  ( 25.64660436782548203, -102.9120797476511484, 46.45435812945208198 ) ) ;
#16703=CARTESIAN_POINT ( 'NONE',  ( 109.1589550718174877, -0.002874971999843706130, -0.007008495014548460529 ) ) ;
#16706=CARTESIAN_POINT ( 'NONE',  ( 1.833838850093439943, 141.9387673160886152, 30.17001281793409717 ) ) ;
#16707=B_SPLINE_CURVE_WITH_KNOTS ( 'NONE', 3,
 ( #3632, #27955, #23522, #5956 ),
 .UNSPECIFIED., .F., .F.,
 ( 4, 4 ),
 ( 3.214625617059125298E-16, 0.01077107486149843710 ),
 .UNSPECIFIED. ) ;
#16708=LINE ( 'NONE', #19141, #24482 ) ;
#16711=VERTEX_POINT ( 'NONE', #17439 ) ;
#16713=CARTESIAN_POINT ( 'NONE',  ( 1.833750490713687009, -30.43107162405965482, 141.8829662951652040 ) ) ;
#16714=CARTESIAN_POINT ( 'NONE',  ( 1.833485406944043827, 107.4794113447409529, 97.49333871408727248 ) ) ;
#16715=CARTESIAN_POINT ( 'NONE',  ( 26.28373643307411811, -17.46364395087380572, -126.3595147275200219 ) ) ;
#16717=CARTESIAN_POINT ( 'NONE',  ( 2.433796855181219243, 107.1581411821798895, -98.43889364293755762 ) ) ;
#16718=VECTOR ( 'NONE', #14429, 1000.000000000000114 ) ;
#16720=ORIENTED_EDGE ( 'NONE', *, *, #20176, .F. ) ;
#16721=CARTESIAN_POINT ( 'NONE',  ( 32.73300124599732186, 0.000000000000000000, 0.000000000000000000 ) ) ;
#16722=CARTESIAN_POINT ( 'NONE',  ( 13.36082413113063083, 148.1362653801007809, -37.97423473099148339 ) ) ;
#16726=CARTESIAN_POINT ( 'NONE',  ( 13.84597867724975906, -144.4146018799364981, 25.80666409311521647 ) ) ;
#16727=EDGE_CURVE ( 'NONE', #20281, #23165, #10846, .T. ) ;
#16728=VERTEX_POINT ( 'NONE', #24371 ) ;
#16732=CARTESIAN_POINT ( 'NONE',  ( 1.832998868059858122, -29.64765804470168931, 142.0492247521721936 ) ) ;
#16733=ORIENTED_EDGE ( 'NONE', *, *, #8098, .T. ) ;
#16734=ADVANCED_FACE ( 'NONE', ( #15275 ), #19413, .F. ) ;
#16736=ORIENTED_EDGE ( 'NONE', *, *, #18184, .F. ) ;
#16737=CIRCLE ( 'NONE', #4297, 111.9614997405030152 ) ;
#16738=EDGE_LOOP ( 'NONE', ( #9244, #18816, #1236, #17538 ) ) ;
#16740=FACE_OUTER_BOUND ( 'NONE', #23402, .T. ) ;
#16744=DIRECTION ( 'NONE',  ( 0.000000000000000000, 0.000000000000000000, 1.000000000000000000 ) ) ;
#16747=CARTESIAN_POINT ( 'NONE',  ( 1.833809397773843219, -85.14934054436398014, -117.5007887865417331 ) ) ;
#16748=CARTESIAN_POINT ( 'NONE',  ( 10.93730112725932635, 0.000000000000000000, 0.000000000000000000 ) ) ;
#16750=CARTESIAN_POINT ( 'NONE',  ( 13.84597867724977149, -77.45414123936289741, 124.5889929031783936 ) ) ;
#16751=CARTESIAN_POINT ( 'NONE',  ( 109.1592201516379674, -0.007302213399779945366, 0.002913740842108614778 ) ) ;
#16752=EDGE_CURVE ( 'NONE', #5056, #26248, #8690, .T. ) ;
#16754=CARTESIAN_POINT ( 'NONE',  ( 10.93730112725990367, -149.7554878793147566, -20.69552240458495973 ) ) ;
#16755=CARTESIAN_POINT ( 'NONE',  ( 25.64707127832796019, 6.059145946834079367E-17, -112.9112343549835487 ) ) ;
#16756=CARTESIAN_POINT ( 'NONE',  ( 109.1587776205901577, -0.005390665547499397595, -0.004965871434389434319 ) ) ;
#16757=CARTESIAN_POINT ( 'NONE',  ( 10.93730112726006354, 150.7858122213665126, -10.89264110824830034 ) ) ;
#16758=CARTESIAN_POINT ( 'NONE',  ( 10.93730112725972425, -42.00474393596362432, 145.2260730187398678 ) ) ;
#16760=ORIENTED_EDGE ( 'NONE', *, *, #1696, .T. ) ;
#16761=CARTESIAN_POINT ( 'NONE',  ( 26.11404676487259024, 45.01677474591551942, -103.8885755249565079 ) ) ;
#16763=VERTEX_POINT ( 'NONE', #16441 ) ;
#16765=CARTESIAN_POINT ( 'NONE',  ( 55.49584447822657296, -70.91003759562305220, -15.34602024131360487 ) ) ;
#16766=EDGE_LOOP ( 'NONE', ( #5000, #27721, #18099, #13690 ) ) ;
#16767=B_SPLINE_CURVE_WITH_KNOTS ( 'NONE', 3,
 ( #20195, #484, #9277, #18177 ),
 .UNSPECIFIED., .F., .F.,
 ( 4, 4 ),
 ( 2.501853776554200607E-17, 0.008383560773332712074 ),
 .UNSPECIFIED. ) ;
#16769=ORIENTED_EDGE ( 'NONE', *, *, #16114, .T. ) ;
#16770=CARTESIAN_POINT ( 'NONE',  ( 1.833809397773846328, -141.9756687985004930, 29.99591688577042703 ) ) ;
#16774=B_SPLINE_CURVE_WITH_KNOTS ( 'NONE', 3,
 ( #8075, #10628, #1974, #4138, #12498, #19397, #3870 ),
 .UNSPECIFIED., .F., .F.,
 ( 4, 3, 4 ),
 ( 0.000000000000000000, 0.02398743853561352557, 0.04000277880656219476 ),
 .UNSPECIFIED. ) ;
#16776=CARTESIAN_POINT ( 'NONE',  ( 5.340103556456385903, 28.39990973640068717, 144.6887562347050959 ) ) ;
#16777=CARTESIAN_POINT ( 'NONE',  ( 25.64703792032472052, 56.58441811305608127, 97.70949518026519343 ) ) ;
#16778=CARTESIAN_POINT ( 'NONE',  ( 25.64681081121879203, -112.3352186517029878, -11.38886654529789233 ) ) ;
#16783=CARTESIAN_POINT ( 'NONE',  ( 1.833206308920053429, -29.44113170198447094, -142.0914675761167132 ) ) ;
#16786=DIRECTION ( 'NONE',  ( -0.5914120900931443270, -0.1754905759872788518, -0.7870418015781065479 ) ) ;
#16787=CARTESIAN_POINT ( 'NONE',  ( 26.11404676487257603, -107.3263591096432776, 36.06104232266415721 ) ) ;
#16788=CARTESIAN_POINT ( 'NONE',  ( 26.04756280548354397, 10.72497307632943730, -112.6689254848258059 ) ) ;
#16789=CARTESIAN_POINT ( 'NONE',  ( 26.11404676487257603, 92.25884714080498838, -65.63269960453146723 ) ) ;
#16791=CARTESIAN_POINT ( 'NONE',  ( 1.833485406944043827, 137.8414413349092058, -45.34878176254091642 ) ) ;
#16794=CARTESIAN_POINT ( 'NONE',  ( 109.1589550718175161, 0.001014448720249546245, 0.007507020724820358780 ) ) ;
#16795=ORIENTED_EDGE ( 'NONE', *, *, #26728, .T. ) ;
#16797=ORIENTED_EDGE ( 'NONE', *, *, #22975, .F. ) ;
#16798=LINE ( 'NONE', #16925, #17644 ) ;
#16799=EDGE_CURVE ( 'NONE', #17966, #14867, #25226, .T. ) ;
#16800=EDGE_LOOP ( 'NONE', ( #11324, #2463, #22457, #14864 ) ) ;
#16801=ORIENTED_EDGE ( 'NONE', *, *, #22872, .F. ) ;
#16802=CARTESIAN_POINT ( 'NONE',  ( 1.833809397773859429, 96.96506043213450710, 107.9565774559014670 ) ) ;
#16803=ORIENTED_EDGE ( 'NONE', *, *, #9635, .T. ) ;
#16806=CARTESIAN_POINT ( 'NONE',  ( 1.832998868059858122, 58.53348008137825076, -132.7810136645732371 ) ) ;
#16807=CARTESIAN_POINT ( 'NONE',  ( 55.49584447822657296, -29.75369869230999242, 66.16986612640766907 ) ) ;
#16808=CARTESIAN_POINT ( 'NONE',  ( 25.69398547355838502, -107.1830796521256843, 35.60637981494814142 ) ) ;
#16809=CARTESIAN_POINT ( 'NONE',  ( 25.70243777736188306, -46.60897284577234956, 102.8829101922929681 ) ) ;
#16811=ORIENTED_EDGE ( 'NONE', *, *, #8812, .T. ) ;
#16813=CARTESIAN_POINT ( 'NONE',  ( 55.49584447822657296, -58.85239198729215104, 42.42793568432939111 ) ) ;
#16814=CARTESIAN_POINT ( 'NONE',  ( 13.36082413113061307, 22.28175172543762272, -151.2941478187905489 ) ) ;
#16816=VERTEX_POINT ( 'NONE', #612 ) ;
#16817=ORIENTED_EDGE ( 'NONE', *, *, #14563, .F. ) ;
#16820=EDGE_CURVE ( 'NONE', #3533, #6430, #12462, .T. ) ;
#16821=FACE_OUTER_BOUND ( 'NONE', #13761, .T. ) ;
#16822=CARTESIAN_POINT ( 'NONE',  ( 2.433796855181233454, 137.9325382748291418, -46.34326152018600453 ) ) ;
#16824=CARTESIAN_POINT ( 'NONE',  ( 1.833691583653511259, -132.4191286035302539, -59.34641645332771986 ) ) ;
#16826=DIRECTION ( 'NONE',  ( -0.5914120900931443270, -0.4101107478122021921, -0.6942916636548178699 ) ) ;
#16828=VECTOR ( 'NONE', #25394, 1000.000000000000000 ) ;
#16833=DIRECTION ( 'NONE',  ( 1.000000000000000000, 0.000000000000000000, 0.000000000000000000 ) ) ;
#16834=ADVANCED_FACE ( 'NONE', ( #22938 ), #1418, .T. ) ;
#16837=CARTESIAN_POINT ( 'NONE',  ( 13.36082413113063083, -142.1654513177084311, -56.35051087435107320 ) ) ;
#16838=ORIENTED_EDGE ( 'NONE', *, *, #22996, .F. ) ;
#16839=CARTESIAN_POINT ( 'NONE',  ( 13.84597867724975195, -35.16314962059933436, 142.4258194868991438 ) ) ;
#16840=( BOUNDED_SURFACE ( )  B_SPLINE_SURFACE ( 3, 1, ( 
 ( #11751, #2528 ),
 ( #805, #20085 ),
 ( #18347, #15771 ),
 ( #27130, #13611 ) ),
 .UNSPECIFIED., .F., .F., .F. ) 
 B_SPLINE_SURFACE_WITH_KNOTS ( ( 4, 4 ),
 ( 2, 2 ),
 ( 0.000000000000000000, 1.000000000000000000 ),
 ( 0.000000000000000000, 1.000000000000000000 ),
 .UNSPECIFIED. ) 
 GEOMETRIC_REPRESENTATION_ITEM ( )  RATIONAL_B_SPLINE_SURFACE ( (
 ( 1.000000000000000000, 1.000000000000000000),
 ( 0.9956975270656954757, 0.8568959468854893125),
 ( 0.9956975270656954757, 0.8568959468854893125),
 ( 1.000000000000000000, 1.000000000000000000) ) ) 
 REPRESENTATION_ITEM ( '' )  SURFACE ( )  );
#16841=VERTEX_POINT ( 'NONE', #24675 ) ;
#16842=CARTESIAN_POINT ( 'NONE',  ( 13.36082413113061307, -37.97423473099395608, 148.1362653801001841 ) ) ;
#16845=CARTESIAN_POINT ( 'NONE',  ( 109.1778270068192853, -0.005755170886745476951, 0.007323887274071875716 ) ) ;
#16846=DIRECTION ( 'NONE',  ( -0.5946245182733607137, 0.6948076064830713827, -0.4045541647807359142 ) ) ;
#16847=B_SPLINE_CURVE_WITH_KNOTS ( 'NONE', 3,
 ( #13979, #1037, #3471, #7525, #5488, #12257, #27211, #14250, #16573, #16285 ),
 .UNSPECIFIED., .F., .F.,
 ( 4, 3, 3, 4 ),
 ( 0.000000000000000000, 0.0002669560319015770256, 0.0005492286108966617283, 0.0008315040496093522703 ),
 .UNSPECIFIED. ) ;
#16848=CARTESIAN_POINT ( 'NONE',  ( 26.04756280548354042, 74.90181827458462749, -84.84709444968828507 ) ) ;
#16849=DIRECTION ( 'NONE',  ( -0.5914120900931443270, 0.2415416038593066195, -0.7693434820005511376 ) ) ;
#16853=ORIENTED_EDGE ( 'NONE', *, *, #20662, .T. ) ;
#16854=ORIENTED_EDGE ( 'NONE', *, *, #9276, .T. ) ;
#16855=CARTESIAN_POINT ( 'NONE',  ( 32.73300124599734318, 89.94078864464067635, 75.82012867748514395 ) ) ;
#16857=EDGE_CURVE ( 'NONE', #26, #26730, #16244, .T. ) ;
#16858=CARTESIAN_POINT ( 'NONE',  ( 109.1721716018069657, -0.005082060336469301429, 0.01629455849720095120 ) ) ;
#16859=CARTESIAN_POINT ( 'NONE',  ( 25.64692872815578539, -83.69378511050511804, -75.79105864157472183 ) ) ;
#16861=CARTESIAN_POINT ( 'NONE',  ( 1.832998868059890096, -141.8272129421606564, -30.69214149074156595 ) ) ;
#16864=CARTESIAN_POINT ( 'NONE',  ( 16.75465622695658396, 108.7410129416647493, -91.67104679059791295 ) ) ;
#16866=CARTESIAN_POINT ( 'NONE',  ( 32.73300124599737160, -75.82012867748541396, 89.94078864464039214 ) ) ;
#16867=EDGE_CURVE ( 'NONE', #28198, #14392, #7868, .T. ) ;
#16868=EDGE_CURVE ( 'NONE', #8004, #7205, #6615, .T. ) ;
#16869=FACE_BOUND ( 'NONE', #7610, .T. ) ;
#16871=CARTESIAN_POINT ( 'NONE',  ( 109.1586059443104944, -0.001740416220259453526, -0.006856640434643066981 ) ) ;
#16872=CARTESIAN_POINT ( 'NONE',  ( 25.81918753295379076, -97.41320410180124156, 57.31966094783169297 ) ) ;
#16873=ORIENTED_EDGE ( 'NONE', *, *, #7209, .F. ) ;
#16876=VECTOR ( 'NONE', #14532, 1000.000000000000114 ) ;
#16877=CARTESIAN_POINT ( 'NONE',  ( 25.64703792032470631, -110.4746717456747689, -23.32999623362237784 ) ) ;
#16878=ADVANCED_FACE ( 'NONE', ( #3769 ), #10433, .F. ) ;
#16879=CARTESIAN_POINT ( 'NONE',  ( 1.832998868059890096, -0.5339089137737788038, -145.1092030902949830 ) ) ;
#16880=EDGE_CURVE ( 'NONE', #18117, #22173, #24459, .T. ) ;
#16883=CARTESIAN_POINT ( 'NONE',  ( 1.833838850093452821, 59.02145475724827151, -132.5643663243751860 ) ) ;
#16884=CARTESIAN_POINT ( 'NONE',  ( 109.1624594426973118, 0.01358749486988782354, -0.008380433676412963467 ) ) ;
#16885=ADVANCED_FACE ( 'NONE', ( #16740 ), #5084, .T. ) ;
#16887=CARTESIAN_POINT ( 'NONE',  ( 1.834118845439484335, 72.70910183320742703, -125.5799175751962196 ) ) ;
#16888=FACE_OUTER_BOUND ( 'NONE', #2546, .T. ) ;
#16889=CARTESIAN_POINT ( 'NONE',  ( 109.1586059443104944, -0.003774052605966671768, -0.005983234375914136226 ) ) ;
#16890=CARTESIAN_POINT ( 'NONE',  ( 109.1592201516379674, -0.004368284148529054563, -0.006536841731953389224 ) ) ;
#16896=DIRECTION ( 'NONE',  ( -1.000000000000000000, -0.000000000000000000, -0.000000000000000000 ) ) ;
#16901=ADVANCED_FACE ( 'NONE', ( #19033 ), #25316, .F. ) ;
#16902=CARTESIAN_POINT ( 'NONE',  ( 6.224689322667647851, 28.26953958630820551, -145.3353551538638158 ) ) ;
#16903=EDGE_CURVE ( 'NONE', #27586, #9124, #10406, .T. ) ;
#16905=CARTESIAN_POINT ( 'NONE',  ( 55.49584447822657296, -48.74506217377846440, -53.73688382046314871 ) ) ;
#16907=CARTESIAN_POINT ( 'NONE',  ( 25.64681081121880624, 102.9795863647034935, -46.30456157731225630 ) ) ;
#16909=CARTESIAN_POINT ( 'NONE',  ( 26.11404676487259024, -112.7148551500679616, -10.71016160607683432 ) ) ;
#16914=CARTESIAN_POINT ( 'NONE',  ( 5.340103579038172121, -13.12023871299826538, 146.8647350263016733 ) ) ;
#16916=CARTESIAN_POINT ( 'NONE',  ( 25.64708228042121974, -103.1335618347708589, -45.96113332231442428 ) ) ;
#16918=CARTESIAN_POINT ( 'NONE',  ( 25.65782528836483323, 112.3587790429871376, -11.22838748007500342 ) ) ;
#16920=CARTESIAN_POINT ( 'NONE',  ( 109.1587776205901861, -8.330235398541230849E-05, -0.007328861771499511728 ) ) ;
#16921=CARTESIAN_POINT ( 'NONE',  ( 26.11404676487257603, -36.06104232266378062, -107.3263591096434197 ) ) ;
#16923=ORIENTED_EDGE ( 'NONE', *, *, #17053, .F. ) ;
#16925=CARTESIAN_POINT ( 'NONE',  ( 55.79472521941426777, 62.63970324008261059, 37.00555938668281897 ) ) ;
#16927=VERTEX_POINT ( 'NONE', #10274 ) ;
#16928=CARTESIAN_POINT ( 'NONE',  ( 1.833485406944057594, -85.72460230293616235, -117.0814567582553281 ) ) ;
#16930=ORIENTED_EDGE ( 'NONE', *, *, #22408, .F. ) ;
#16931=CARTESIAN_POINT ( 'NONE',  ( 109.1587776205901577, -0.003736572840486988237, 0.006305329297952406813 ) ) ;
#16934=CARTESIAN_POINT ( 'NONE',  ( 25.98552792386798060, -107.2612904323492415, 35.98568266743475874 ) ) ;
#16936=ADVANCED_FACE ( 'NONE', ( #23796 ), #28230, .F. ) ;
#16938=DIRECTION ( 'NONE',  ( -0.5946245182733608248, -0.7999021332774018944, -0.08110646981859884197 ) ) ;
#16943=CARTESIAN_POINT ( 'NONE',  ( 26.11404676487256893, 1.130420376098718593, -113.2169081140373663 ) ) ;
#16946=CARTESIAN_POINT ( 'NONE',  ( 32.73300124599735028, -8.473903470906931190, 117.3295799645429156 ) ) ;
#16947=ORIENTED_EDGE ( 'NONE', *, *, #9691, .F. ) ;
#16949=CONICAL_SURFACE ( 'NONE', #4520, 117.6351876552689504, 0.9945805576725580410 ) ;
#16950=CARTESIAN_POINT ( 'NONE',  ( 109.1586059443104944, -0.005881369279880122557, -0.003930911098385057520 ) ) ;
#16951=VERTEX_POINT ( 'NONE', #24202 ) ;
#16952=CARTESIAN_POINT ( 'NONE',  ( 25.64708010899966695, -112.2870082086266876, 11.85684669924934020 ) ) ;
#16953=LINE ( 'NONE', #27893, #13251 ) ;
#16954=CARTESIAN_POINT ( 'NONE',  ( 8.186469777910977186, 71.65198614410387279, -131.0413692044505183 ) ) ;
#16957=ORIENTED_EDGE ( 'NONE', *, *, #21531, .F. ) ;
#16958=CARTESIAN_POINT ( 'NONE',  ( 109.1778270068192853, -0.005967275455179280735, 0.007152128381196012907 ) ) ;
#16960=ORIENTED_EDGE ( 'NONE', *, *, #12506, .F. ) ;
#16961=PLANE ( 'NONE',  #26647 ) ;
#16964=CARTESIAN_POINT ( 'NONE',  ( 109.1624594426973118, 0.01582142368019176168, -0.002129375066974309536 ) ) ;
#16965=EDGE_CURVE ( 'NONE', #20839, #21026, #11757, .T. ) ;
#16966=ORIENTED_EDGE ( 'NONE', *, *, #15281, .F. ) ;
#16969=CARTESIAN_POINT ( 'NONE',  ( 2.430230287190589422, 109.1043569252014436, 96.28466919684133529 ) ) ;
#16970=EDGE_CURVE ( 'NONE', #7524, #27159, #8773, .T. ) ;
#16973=CARTESIAN_POINT ( 'NONE',  ( 13.84597867724996689, 145.3211459389820561, 20.08297016719431127 ) ) ;
#16975=CARTESIAN_POINT ( 'NONE',  ( 25.64708010899964563, 112.2870082086267871, -11.85684669924855328 ) ) ;
#16976=CARTESIAN_POINT ( 'NONE',  ( 25.64703792032469920, 34.74993974077101200, -107.4308312803555197 ) ) ;
#16978=ORIENTED_EDGE ( 'NONE', *, *, #25998, .T. ) ;
#16979=CARTESIAN_POINT ( 'NONE',  ( 25.86096068574580187, -97.40497849554850518, -57.38862431273688003 ) ) ;
#16982=DIRECTION ( 'NONE',  ( 0.000000000000000000, 0.000000000000000000, 1.000000000000000000 ) ) ;
#16984=CARTESIAN_POINT ( 'NONE',  ( 1.832998868059858122, 132.7810136645746582, -58.53348008137513858 ) ) ;
#16987=CARTESIAN_POINT ( 'NONE',  ( 2.433796855181205476, 116.8607839509056561, 86.69855925934011509 ) ) ;
#16988=CARTESIAN_POINT ( 'NONE',  ( 16.05277956358206382, -62.52511797226036094, -128.9466020665980750 ) ) ;
#16989=CARTESIAN_POINT ( 'NONE',  ( 13.36082413113061307, -41.18148072373512747, -147.2768864064171908 ) ) ;
#16990=CARTESIAN_POINT ( 'NONE',  ( 25.98552792386800192, 1.078856412010833266, 113.1317367103341098 ) ) ;
#16991=EDGE_LOOP ( 'NONE', ( #25382, #27212, #28372, #11262 ) ) ;
#16994=ORIENTED_EDGE ( 'NONE', *, *, #13253, .F. ) ;
#16995=VERTEX_POINT ( 'NONE', #17699 ) ;
#16998=DIRECTION ( 'NONE',  ( -0.5914120900931443270, -0.6570486713847213389, -0.4674599267565414662 ) ) ;
#16999=DIRECTION ( 'NONE',  ( -1.000000000000000000, -0.000000000000000000, -0.000000000000000000 ) ) ;
#17001=CARTESIAN_POINT ( 'NONE',  ( 109.1592201516379674, 0.006536841731962000392, 0.004368284148525281539 ) ) ;
#17002=EDGE_CURVE ( 'NONE', #4028, #10703, #27915, .T. ) ;
#17005=DIRECTION ( 'NONE',  ( 0.5914120900931444380, -0.4804373588864852551, 0.6476200150380136966 ) ) ;
#17006=CARTESIAN_POINT ( 'NONE',  ( 2.433796855181233454, 46.34326152018744693, 137.9325382748286870 ) ) ;
#17009=CARTESIAN_POINT ( 'NONE',  ( 1.833485406944043827, 97.49333871408838093, -107.4794113447399297 ) ) ;
#17011=DIRECTION ( 'NONE',  ( -0.000000000000000000, -0.000000000000000000, 1.000000000000000000 ) ) ;
#17012=CYLINDRICAL_SURFACE ( 'NONE', #26777, 80.00000000000000000 ) ;
#17014=CARTESIAN_POINT ( 'NONE',  ( 25.64681081121879203, 12.21581276189956711, -112.2483031020012305 ) ) ;
#17016=ORIENTED_EDGE ( 'NONE', *, *, #9207, .T. ) ;
#17020=EDGE_LOOP ( 'NONE', ( #27248, #16500, #9954, #23769 ) ) ;
#17022=ORIENTED_EDGE ( 'NONE', *, *, #96, .F. ) ;
#17028=EDGE_CURVE ( 'NONE', #13981, #17451, #14738, .T. ) ;
#17032=LINE ( 'NONE', #19613, #26773 ) ;
#17034=CARTESIAN_POINT ( 'NONE',  ( 30.59138290137916627, 84.53179630244103748, -79.74792615266086671 ) ) ;
#17035=CARTESIAN_POINT ( 'NONE',  ( 25.98552792386800192, 102.9121737515627188, -47.00040718953673036 ) ) ;
#17036=CARTESIAN_POINT ( 'NONE',  ( 26.04756280548354397, 113.1727782765313890, -1.110889087302899592 ) ) ;
#17038=ORIENTED_EDGE ( 'NONE', *, *, #24952, .T. ) ;
#17039=VERTEX_POINT ( 'NONE', #17274 ) ;
#17040=CARTESIAN_POINT ( 'NONE',  ( 8.186469777910764023, -12.15801985874078284, 148.8557359139591938 ) ) ;
#17042=CARTESIAN_POINT ( 'NONE',  ( 25.64681081121880624, 23.06870491922473931, -110.5293738517606243 ) ) ;
#17043=CARTESIAN_POINT ( 'NONE',  ( 2.063896406836605024, -116.7302989755731772, -86.47093297169119808 ) ) ;
#17044=CARTESIAN_POINT ( 'NONE',  ( 26.11404676487257603, 112.7148551500681890, -10.71016160607451262 ) ) ;
#17047=CARTESIAN_POINT ( 'NONE',  ( 25.64692872815577473, 91.53575854059506867, -66.10702795113321883 ) ) ;
#17050=ORIENTED_EDGE ( 'NONE', *, *, #20269, .T. ) ;
#17051=ORIENTED_EDGE ( 'NONE', *, *, #4056, .T. ) ;
#17053=EDGE_CURVE ( 'NONE', #21599, #3668, #27546, .T. ) ;
#17054=VERTEX_POINT ( 'NONE', #22615 ) ;
#17055=EDGE_LOOP ( 'NONE', ( #16797, #6109, #10204, #7949 ) ) ;
#17058=AXIS2_PLACEMENT_3D ( 'NONE', #13170, #2086, #22103 ) ;
#17059=EDGE_CURVE ( 'NONE', #15152, #7370, #16119, .T. ) ;
#17060=B_SPLINE_CURVE_WITH_KNOTS ( 'NONE', 3,
 ( #16406, #10500, #19000, #28041 ),
 .UNSPECIFIED., .F., .F.,
 ( 4, 4 ),
 ( 3.625240045095802037E-16, 0.01077107486149760443 ),
 .UNSPECIFIED. ) ;
#17061=EDGE_CURVE ( 'NONE', #10330, #28326, #19783, .T. ) ;
#17062=LINE ( 'NONE', #1658, #10593 ) ;
#17063=VECTOR ( 'NONE', #25467, 1000.000000000000227 ) ;
#17067=CARTESIAN_POINT ( 'NONE',  ( 32.73300124599735739, -72.21147546950616913, 92.86301839379999024 ) ) ;
#17068=B_SPLINE_CURVE_WITH_KNOTS ( 'NONE', 3,
 ( #2576, #11359, #20132, #13656, #22456, #17691 ),
 .UNSPECIFIED., .F., .F.,
 ( 4, 2, 4 ),
 ( 3.476216610979977084E-18, 0.0006311571484585997175, 0.001262314296917196616 ),
 .UNSPECIFIED. ) ;
#17069=CARTESIAN_POINT ( 'NONE',  ( 25.98552792386800192, -110.8838436908324638, -22.46612985365086246 ) ) ;
#17070=CARTESIAN_POINT ( 'NONE',  ( 25.73574536432415627, 55.78561308781485195, 98.23578516674979255 ) ) ;
#17071=CARTESIAN_POINT ( 'NONE',  ( 109.1589550718175161, 0.007571935245608774762, -0.0002241941239326223723 ) ) ;
#17073=CARTESIAN_POINT ( 'NONE',  ( 1.833838850093440165, 85.29337590730699503, -117.3962664098815338 ) ) ;
#17075=DIRECTION ( 'NONE',  ( -1.000000000000000000, -0.000000000000000000, -0.000000000000000000 ) ) ;
#17076=ORIENTED_EDGE ( 'NONE', *, *, #28005, .T. ) ;
#17077=VERTEX_POINT ( 'NONE', #5177 ) ;
#17078=LINE ( 'NONE', #12335, #17063 ) ;
#17080=CIRCLE ( 'NONE', #14781, 151.1787379149930359 ) ;
#17081=CARTESIAN_POINT ( 'NONE',  ( 1.833485406944057594, 125.4007332306555895, -73.01664920992834595 ) ) ;
#17082=CARTESIAN_POINT ( 'NONE',  ( 26.04756280548354042, -90.90573670389279926, 67.42001818240436251 ) ) ;
#17085=CARTESIAN_POINT ( 'NONE',  ( 1.834118845439484335, 125.5799175751969727, 72.70910183320610543 ) ) ;
#17088=CARTESIAN_POINT ( 'NONE',  ( 1.834118845439484335, 141.9019470378987933, 30.34413640949744106 ) ) ;
#17090=CARTESIAN_POINT ( 'NONE',  ( 109.1589550718174877, -0.005477029346537810178, -0.005233222325298206822 ) ) ;
#17091=CARTESIAN_POINT ( 'NONE',  ( 8.186469777910810208, -108.6390983781763708, 102.4860666868859340 ) ) ;
#17092=CARTESIAN_POINT ( 'NONE',  ( 5.340103556456523570, 111.1041836730292260, -96.93942141425958425 ) ) ;
#17093=ORIENTED_EDGE ( 'NONE', *, *, #17344, .F. ) ;
#17097=CARTESIAN_POINT ( 'NONE',  ( 2.430230287190592531, 116.8646894862423835, -86.70145658344540607 ) ) ;
#17098=ORIENTED_EDGE ( 'NONE', *, *, #3773, .T. ) ;
#17099=CARTESIAN_POINT ( 'NONE',  ( 10.93730112725997294, 36.23586118136742584, -146.7718404940639516 ) ) ;
#17102=CARTESIAN_POINT ( 'NONE',  ( 119.2224693531408803, -90.00000000000000000, 19.99999999999990052 ) ) ;
#17104=CARTESIAN_POINT ( 'NONE',  ( 2.433796855181205476, 125.2830755159753977, 74.00833731765604284 ) ) ;
#17106=VECTOR ( 'NONE', #5230, 1000.000000000000000 ) ;
#17112=DIRECTION ( 'NONE',  ( -0.5946245182733607137, 0.5357871896547532486, -0.5994612328333126516 ) ) ;
#17113=CARTESIAN_POINT ( 'NONE',  ( 2.433796855181219243, -144.8571464219890004, 13.76554153471645847 ) ) ;
#17114=ORIENTED_EDGE ( 'NONE', *, *, #18432, .F. ) ;
#17116=ORIENTED_EDGE ( 'NONE', *, *, #25018, .T. ) ;
#17118=CARTESIAN_POINT ( 'NONE',  ( 10.93730112725983439, -146.7718404940644916, 36.23586118136483236 ) ) ;
#17119=CARTESIAN_POINT ( 'NONE',  ( 1.834118845439484335, -85.43746956709928497, 117.2918069668798040 ) ) ;
#17121=CARTESIAN_POINT ( 'NONE',  ( 55.79472521941426777, 58.42842213658327921, 43.35047097963469298 ) ) ;
#17122=CARTESIAN_POINT ( 'NONE',  ( 16.05277956358206737, 141.9568301782832123, -19.61822947415828722 ) ) ;
#17123=CARTESIAN_POINT ( 'NONE',  ( 109.1586059443104944, 0.007001002073871745619, 0.001014167950280808750 ) ) ;
#17124=CARTESIAN_POINT ( 'NONE',  ( 2.108393763691180922, 98.16799842733396986, -107.1124103264139364 ) ) ;
#17125=ORIENTED_EDGE ( 'NONE', *, *, #14451, .F. ) ;
#17126=FACE_OUTER_BOUND ( 'NONE', #24552, .T. ) ;
#17128=CARTESIAN_POINT ( 'NONE',  ( 1.831572820252008738, -0.9871191512924697431, 145.1082523917587253 ) ) ;
#17129=ADVANCED_FACE ( 'NONE', ( #24486 ), #5649, .F. ) ;
#17130=EDGE_CURVE ( 'NONE', #8996, #5673, #429, .T. ) ;
#17132=AXIS2_PLACEMENT_3D ( 'NONE', #11474, #9609, #20248 ) ;
#17133=AXIS2_PLACEMENT_3D ( 'NONE', #12481, #5591, #21115 ) ;
#17134=ORIENTED_EDGE ( 'NONE', *, *, #11089, .T. ) ;
#17136=ADVANCED_FACE ( 'NONE', ( #25061 ), #8739, .F. ) ;
#17137=DIRECTION ( 'NONE',  ( 0.5946245182733607137, 0.8039981203473692828, 0.002950380665393250324 ) ) ;
#17140=ORIENTED_EDGE ( 'NONE', *, *, #1377, .T. ) ;
#17142=B_SPLINE_CURVE_WITH_KNOTS ( 'NONE', 3,
 ( #12795, #23347, #19012, #19561, #21160, #1445, #10251, #21729 ),
 .UNSPECIFIED., .F., .F.,
 ( 4, 2, 2, 4 ),
 ( 1.551583845779545699E-17, 0.0002429592666046831570, 0.0004859185332093508098, 0.0009718370664186806946 ),
 .UNSPECIFIED. ) ;
#17143=CARTESIAN_POINT ( 'NONE',  ( 1.832998868059890096, -117.0819875546701070, 85.72499093308064744 ) ) ;
#17146=CARTESIAN_POINT ( 'NONE',  ( 1.832998868059858122, -58.53348008137559333, -132.7810136645744024 ) ) ;
#17148=( BOUNDED_SURFACE ( )  B_SPLINE_SURFACE ( 3, 1, ( 
 ( #4619, #9230 ),
 ( #27053, #591 ),
 ( #9389, #17988 ),
 ( #18140, #6938 ) ),
 .UNSPECIFIED., .F., .F., .F. ) 
 B_SPLINE_SURFACE_WITH_KNOTS ( ( 4, 4 ),
 ( 2, 2 ),
 ( 0.000000000000000000, 1.000000000000000000 ),
 ( 0.000000000000000000, 1.000000000000000000 ),
 .UNSPECIFIED. ) 
 GEOMETRIC_REPRESENTATION_ITEM ( )  RATIONAL_B_SPLINE_SURFACE ( (
 ( 1.000000000000000000, 1.000000000000000000),
 ( 0.6386103224230316178, 0.9954351624131538845),
 ( 0.6386103224230316178, 0.9954351624131538845),
 ( 1.000000000000000000, 1.000000000000000000) ) ) 
 REPRESENTATION_ITEM ( '' )  SURFACE ( )  );
#17149=VECTOR ( 'NONE', #13209, 1000.000000000000114 ) ;
#17150=CARTESIAN_POINT ( 'NONE',  ( 13.36082413113063083, -6.345145185216972905, -152.7944199136427983 ) ) ;
#17152=CARTESIAN_POINT ( 'NONE',  ( 2.430230287190581429, -43.58368230469295668, -138.8342928068224467 ) ) ;
#17154=B_SPLINE_CURVE_WITH_KNOTS ( 'NONE', 3,
 ( #24347, #8654, #17841, #2154, #15682, #292 ),
 .UNSPECIFIED., .F., .F.,
 ( 4, 2, 4 ),
 ( 1.392007502815792650E-17, 0.0006311571484586138122, 0.001262314296917213963 ),
 .UNSPECIFIED. ) ;
#17159=CARTESIAN_POINT ( 'NONE',  ( 1.832998868059890096, 85.72499093308101692, 117.0819875546698512 ) ) ;
#17160=CARTESIAN_POINT ( 'NONE',  ( 13.36082413113063083, -117.7941133658631827, -97.52406103376877411 ) ) ;
#17161=CARTESIAN_POINT ( 'NONE',  ( 109.1721716018069515, -0.01368917435590581710, -0.01019541462303050379 ) ) ;
#17162=ORIENTED_EDGE ( 'NONE', *, *, #1648, .F. ) ;
#17167=CARTESIAN_POINT ( 'NONE',  ( 32.73300124599732186, 0.000000000000000000, 0.000000000000000000 ) ) ;
#17168=ORIENTED_EDGE ( 'NONE', *, *, #19225, .T. ) ;
#17169=ORIENTED_EDGE ( 'NONE', *, *, #9975, .T. ) ;
#17170=ORIENTED_EDGE ( 'NONE', *, *, #5128, .F. ) ;
#17174=( BOUNDED_SURFACE ( )  B_SPLINE_SURFACE ( 3, 1, ( 
 ( #477, #24825 ),
 ( #9269, #15881 ),
 ( #18029, #26816 ),
 ( #906, #4940 ) ),
 .UNSPECIFIED., .F., .F., .F. ) 
 B_SPLINE_SURFACE_WITH_KNOTS ( ( 4, 4 ),
 ( 2, 2 ),
 ( 0.000000000000000000, 1.000000000000000000 ),
 ( 0.000000000000000000, 1.000000000000000000 ),
 .UNSPECIFIED. ) 
 GEOMETRIC_REPRESENTATION_ITEM ( )  RATIONAL_B_SPLINE_SURFACE ( (
 ( 1.000000000000000000, 1.000000000000000000),
 ( 0.9960225298536222738, 0.9999952330161893110),
 ( 0.9960225298536222738, 0.9999952330161893110),
 ( 1.000000000000000000, 1.000000000000000000) ) ) 
 REPRESENTATION_ITEM ( '' )  SURFACE ( )  );
#17178=B_SPLINE_CURVE_WITH_KNOTS ( 'NONE', 3,
 ( #20489, #26956, #11287, #22076, #22380, #26532 ),
 .UNSPECIFIED., .F., .F.,
 ( 4, 2, 4 ),
 ( 3.106877759296670001E-17, 0.0006311571484586191248, 0.001262314296917207024 ),
 .UNSPECIFIED. ) ;
#17180=CARTESIAN_POINT ( 'NONE',  ( 13.36082413113061307, -143.3553710183985572, -53.25066407421950743 ) ) ;
#17181=CARTESIAN_POINT ( 'NONE',  ( 99.22246935314079508, 90.00000000000005684, 39.99999999999999289 ) ) ;
#17182=ORIENTED_EDGE ( 'NONE', *, *, #12447, .T. ) ;
#17183=ORIENTED_EDGE ( 'NONE', *, *, #16727, .T. ) ;
#17185=CARTESIAN_POINT ( 'NONE',  ( 1.833838850093517214, 1.355257560975019971E-17, -145.1097630783160923 ) ) ;
#17186=ADVANCED_FACE ( 'NONE', ( #5909 ), #13340, .F. ) ;
#17188=CARTESIAN_POINT ( 'NONE',  ( 25.87036335909427009, 10.83311869338221278, -112.5399073133627326 ) ) ;
#17189=CARTESIAN_POINT ( 'NONE',  ( 25.73574536432415627, 112.4329083163019760, -11.00659994954035525 ) ) ;
#17196=VERTEX_POINT ( 'NONE', #14225 ) ;
#17197=ORIENTED_EDGE ( 'NONE', *, *, #11335, .F. ) ;
#17200=VERTEX_POINT ( 'NONE', #8752 ) ;
#17201=EDGE_LOOP ( 'NONE', ( #208, #26853, #18400, #17623 ) ) ;
#17204=CARTESIAN_POINT ( 'NONE',  ( 16.75465622695656265, 138.0797984721905038, 34.09043808962460531 ) ) ;
#17206=CARTESIAN_POINT ( 'NONE',  ( 16.75465622695648804, -87.30527857298524452, 112.2763423369178213 ) ) ;
#17207=CARTESIAN_POINT ( 'NONE',  ( 1.831572820252009626, 14.18623102066960229, -144.4165162501761301 ) ) ;
#17210=CARTESIAN_POINT ( 'NONE',  ( 55.49584447822657296, 62.96491934285994319, 36.04376091928565273 ) ) ;
#17214=CARTESIAN_POINT ( 'NONE',  ( 109.1587776205901861, -0.0008489206734501101009, -0.007280006032835104751 ) ) ;
#17216=ORIENTED_EDGE ( 'NONE', *, *, #3479, .F. ) ;
#17218=CARTESIAN_POINT ( 'NONE',  ( 8.186469777910783563, -97.33125097303785367, 113.2805152945353058 ) ) ;
#17219=CARTESIAN_POINT ( 'NONE',  ( 1.833206310202321943, 117.8322271314364400, 84.68961945193495922 ) ) ;
#17220=LINE ( 'NONE', #12892, #7978 ) ;
#17221=CARTESIAN_POINT ( 'NONE',  ( 25.98107933586715390, -98.51796269673099005, 55.61918067932703025 ) ) ;
#17222=EDGE_CURVE ( 'NONE', #7617, #1094, #22044, .T. ) ;
#17225=CARTESIAN_POINT ( 'NONE',  ( 25.64681081121879203, -91.10197563707990298, 66.70335573067838197 ) ) ;
#17228=CARTESIAN_POINT ( 'NONE',  ( 32.73300124599738581, 16.10546300444979195, -116.5274707358853163 ) ) ;
#17229=CARTESIAN_POINT ( 'NONE',  ( 109.1586059443104944, -0.006808232911146201889, -0.001921075557418339087 ) ) ;
#17230=CARTESIAN_POINT ( 'NONE',  ( 109.1586059443104944, -0.007058870754606105975, -0.0004635842312795806770 ) ) ;
#17231=CARTESIAN_POINT ( 'NONE',  ( 10.93730112725990011, -151.0983828010091656, -4.928439153521871674 ) ) ;
#17232=CARTESIAN_POINT ( 'NONE',  ( 1.833691583653551005, 117.1866391460185497, 85.58103979054524757 ) ) ;
#17233=VERTEX_POINT ( 'NONE', #4422 ) ;
#17235=CARTESIAN_POINT ( 'NONE',  ( 109.1587776205901577, 0.003057017121591207136, -0.006661366261224509200 ) ) ;
#17236=ORIENTED_EDGE ( 'NONE', *, *, #13806, .F. ) ;
#17237=CARTESIAN_POINT ( 'NONE',  ( 32.73300124599732186, 0.000000000000000000, 0.000000000000000000 ) ) ;
#17238=CARTESIAN_POINT ( 'NONE',  ( 13.36082413113061307, -56.35051087434871420, -142.1654513177093691 ) ) ;
#17242=CARTESIAN_POINT ( 'NONE',  ( 25.64681081121879203, 46.30456157731467925, -102.9795863647023850 ) ) ;
#17244=CARTESIAN_POINT ( 'NONE',  ( 32.73300124599735739, 20.69176323058628597, 115.8010721414084543 ) ) ;
#17245=CARTESIAN_POINT ( 'NONE',  ( 1.833603222531958288, -132.7445893798462180, 58.61467103263697709 ) ) ;
#17246=CARTESIAN_POINT ( 'NONE',  ( 25.64681081121879203, 110.5293738517608375, 23.06870491922360245 ) ) ;
#17249=CARTESIAN_POINT ( 'NONE',  ( 9.884929003653608603, -4.203795436553416920, 150.4771565009630194 ) ) ;
#17250=CARTESIAN_POINT ( 'NONE',  ( 94.22246935314088034, -151.1871800109700246, -12.50000000000000888 ) ) ;
#17253=ORIENTED_EDGE ( 'NONE', *, *, #16970, .F. ) ;
#17254=EDGE_LOOP ( 'NONE', ( #4815, #18661, #2206, #22839 ) ) ;
#17258=PLANE ( 'NONE',  #2308 ) ;
#17260=CARTESIAN_POINT ( 'NONE',  ( 109.1586059443104944, 0.006808232911146188011, 0.001921075557418385491 ) ) ;
#17261=VERTEX_POINT ( 'NONE', #15486 ) ;
#17265=CARTESIAN_POINT ( 'NONE',  ( 2.433796855181205476, 46.34326152018925171, -137.9325382748280333 ) ) ;
#17266=ORIENTED_EDGE ( 'NONE', *, *, #6226, .T. ) ;
#17267=CARTESIAN_POINT ( 'NONE',  ( 25.64681081121879203, -112.3352186517029878, -11.38886654529789233 ) ) ;
#17272=ORIENTED_EDGE ( 'NONE', *, *, #23071, .T. ) ;
#17273=CARTESIAN_POINT ( 'NONE',  ( 109.1589550718175161, -0.002126635388718581179, 0.007270618150635343134 ) ) ;
#17274=CARTESIAN_POINT ( 'NONE',  ( 32.73300124599737160, -116.5274707358854158, -16.10546300444944023 ) ) ;
#17278=CARTESIAN_POINT ( 'NONE',  ( 109.1592201516379674, -0.007845213074660005795, -0.0005146241775907089413 ) ) ;
#17279=ORIENTED_EDGE ( 'NONE', *, *, #27857, .T. ) ;
#17280=EDGE_CURVE ( 'NONE', #14288, #23510, #22416, .T. ) ;
#17281=B_SPLINE_CURVE_WITH_KNOTS ( 'NONE', 3,
 ( #1768, #23956, #25962, #5974 ),
 .UNSPECIFIED., .F., .F.,
 ( 4, 4 ),
 ( 6.118829799797332275E-16, 0.008383748772660060827 ),
 .UNSPECIFIED. ) ;
#17282=ORIENTED_EDGE ( 'NONE', *, *, #14422, .T. ) ;
#17284=CARTESIAN_POINT ( 'NONE',  ( 1.833485406944043827, -44.33323125129830089, -138.1714136985312962 ) ) ;
#17286=CARTESIAN_POINT ( 'NONE',  ( 26.11404676487257603, 110.5078194225164481, -24.64483677384740545 ) ) ;
#17289=CARTESIAN_POINT ( 'NONE',  ( 1.833838850093452599, 97.09738119087856489, -107.8375718686129687 ) ) ;
#17292=CARTESIAN_POINT ( 'NONE',  ( 9.884929003653626367, 71.59798461011516224, -132.4189379373563042 ) ) ;
#17293=DIRECTION ( 'NONE',  ( 0.5914120900931444380, 0.4804373588864810363, -0.6476200150380166942 ) ) ;
#17294=ORIENTED_EDGE ( 'NONE', *, *, #22339, .F. ) ;
#17296=CARTESIAN_POINT ( 'NONE',  ( 2.433796855181233454, -144.8571464219888298, -13.76554153471842312 ) ) ;
#17298=ORIENTED_EDGE ( 'NONE', *, *, #9688, .T. ) ;
#17299=ORIENTED_EDGE ( 'NONE', *, *, #10565, .T. ) ;
#17301=B_SPLINE_CURVE_WITH_KNOTS ( 'NONE', 3,
 ( #13267, #20178, #22052, #20321, #2474, #24095, #6963, #615 ),
 .UNSPECIFIED., .F., .F.,
 ( 4, 2, 2, 4 ),
 ( 6.938893903907228378E-18, 0.0002429588503611284506, 0.0004859177007222499622, 0.0009718354014444875646 ),
 .UNSPECIFIED. ) ;
#17302=( BOUNDED_SURFACE ( )  B_SPLINE_SURFACE ( 3, 1, ( 
 ( #21197, #17159 ),
 ( #16889, #4054 ),
 ( #23938, #21339 ),
 ( #19596, #6239 ) ),
 .UNSPECIFIED., .F., .F., .F. ) 
 B_SPLINE_SURFACE_WITH_KNOTS ( ( 4, 4 ),
 ( 2, 2 ),
 ( 0.000000000000000000, 1.000000000000000000 ),
 ( 0.000000000000000000, 1.000000000000000000 ),
 .UNSPECIFIED. ) 
 GEOMETRIC_REPRESENTATION_ITEM ( )  RATIONAL_B_SPLINE_SURFACE ( (
 ( 1.000000000000000000, 1.000000000000000000),
 ( 0.9960225298536222738, 0.9999952330161893110),
 ( 0.9960225298536222738, 0.9999952330161893110),
 ( 1.000000000000000000, 1.000000000000000000) ) ) 
 REPRESENTATION_ITEM ( '' )  SURFACE ( )  );
#17303=EDGE_CURVE ( 'NONE', #14688, #10266, #10914, .T. ) ;
#17305=CARTESIAN_POINT ( 'NONE',  ( 109.1586059443104944, -0.002622205828279790089, 0.006570129623063761248 ) ) ;
#17307=EDGE_CURVE ( 'NONE', #4802, #2974, #13474, .T. ) ;
#17308=CARTESIAN_POINT ( 'NONE',  ( 119.2224693531408946, -69.99999999999998579, -19.99999999999998934 ) ) ;
#17309=B_SPLINE_CURVE_WITH_KNOTS ( 'NONE', 3,
 ( #28335, #24468, #26052, #4733 ),
 .UNSPECIFIED., .F., .F.,
 ( 4, 4 ),
 ( 1.156367566894970741E-16, 0.008383748772659616738 ),
 .UNSPECIFIED. ) ;
#17313=CARTESIAN_POINT ( 'NONE',  ( 32.73300124599735739, -62.10906484417306928, 99.90245962373816724 ) ) ;
#17316=CARTESIAN_POINT ( 'NONE',  ( 2.430230287190581429, 109.1043569252027083, -96.28466919683992842 ) ) ;
#17317=CARTESIAN_POINT ( 'NONE',  ( 25.86096068574580187, -57.38862431273656739, 97.40497849554871834 ) ) ;
#17318=CARTESIAN_POINT ( 'NONE',  ( 25.64700659047697329, -103.0567718204599004, -46.13293552475893478 ) ) ;
#17322=CARTESIAN_POINT ( 'NONE',  ( 25.64670758986456534, 91.05338785329436746, 66.76959937251481847 ) ) ;
#17323=VERTEX_POINT ( 'NONE', #18088 ) ;
#17325=LINE ( 'NONE', #23705, #20252 ) ;
#17327=ORIENTED_EDGE ( 'NONE', *, *, #27023, .F. ) ;
#17331=ORIENTED_EDGE ( 'NONE', *, *, #19990, .T. ) ;
#17335=VERTEX_POINT ( 'NONE', #18222 ) ;
#17336=CARTESIAN_POINT ( 'NONE',  ( 109.1624594426973260, -0.005372302061310809534, 0.01503296564240495792 ) ) ;
#17339=EDGE_CURVE ( 'NONE', #25984, #25988, #24822, .T. ) ;
#17340=CARTESIAN_POINT ( 'NONE',  ( 32.73300124599732186, 0.000000000000000000, 0.000000000000000000 ) ) ;
#17343=CARTESIAN_POINT ( 'NONE',  ( 109.1592201516379674, 0.007780772729122757865, -0.001127733110588145750 ) ) ;
#17344=EDGE_CURVE ( 'NONE', #1421, #26154, #24741, .T. ) ;
#17345=CARTESIAN_POINT ( 'NONE',  ( 1.833485406944043827, 125.4007332306545379, 73.01664920993009389 ) ) ;
#17348=ORIENTED_EDGE ( 'NONE', *, *, #28129, .F. ) ;
#17351=CARTESIAN_POINT ( 'NONE',  ( 25.98552792386798771, 83.35136888841337566, -76.50165414343481984 ) ) ;
#17352=CARTESIAN_POINT ( 'NONE',  ( 1.832998868059890096, -15.69902610990469505, 144.2584710144579958 ) ) ;
#17355=CARTESIAN_POINT ( 'NONE',  ( 25.64660436782575204, -91.00479974714259868, 66.83584345385861525 ) ) ;
#17356=CARTESIAN_POINT ( 'NONE',  ( 25.81918753295378366, 90.88802830332049609, -67.18811037444338297 ) ) ;
#17357=ORIENTED_EDGE ( 'NONE', *, *, #26216, .F. ) ;
#17359=CARTESIAN_POINT ( 'NONE',  ( 1.832998868059858122, 30.69214149074210241, -141.8272129421605712 ) ) ;
#17360=CARTESIAN_POINT ( 'NONE',  ( 109.1589550718175161, -0.0002241941239326466313, -0.007571935245608773894 ) ) ;
#17361=CARTESIAN_POINT ( 'NONE',  ( 32.73300124599739291, 55.46353551262154014, -103.7392577722169875 ) ) ;
#17363=B_SPLINE_CURVE_WITH_KNOTS ( 'NONE', 3,
 ( #3739, #23626, #8353, #17113 ),
 .UNSPECIFIED., .F., .F.,
 ( 4, 4 ),
 ( 0.000000000000000000, 0.01077107196513866529 ),
 .UNSPECIFIED. ) ;
#17366=CIRCLE ( 'NONE', #15058, 117.6351876552689504 ) ;
#17367=CARTESIAN_POINT ( 'NONE',  ( 1.833838850855486591, 15.25659494068298550, -144.3055354793885101 ) ) ;
#17368=ORIENTED_EDGE ( 'NONE', *, *, #23215, .T. ) ;
#17369=CARTESIAN_POINT ( 'NONE',  ( 2.108985857320909929, -28.95357181520926204, 142.3791757917252312 ) ) ;
#17370=EDGE_LOOP ( 'NONE', ( #16025, #26438, #22773, #15939 ) ) ;
#17371=CARTESIAN_POINT ( 'NONE',  ( 109.1778270068192853, 0.004349865064721243624, -0.008236503545668650075 ) ) ;
#17372=CARTESIAN_POINT ( 'NONE',  ( 2.430230287190589422, -98.44218333480696970, -107.1617224697474313 ) ) ;
#17375=CARTESIAN_POINT ( 'NONE',  ( 25.64681081121879203, 11.38886654529823694, -112.3352186517029594 ) ) ;
#17376=CARTESIAN_POINT ( 'NONE',  ( 10.93730112725990367, -84.82621002473354110, -125.1380233598488019 ) ) ;
#17378=CARTESIAN_POINT ( 'NONE',  ( 25.65782528836481902, 46.45532072021325831, -102.9197507294671254 ) ) ;
#17379=CARTESIAN_POINT ( 'NONE',  ( 25.64699802086723324, 23.70809581152608558, 110.3941571196681650 ) ) ;
#17380=LINE ( 'NONE', #6604, #11992 ) ;
#17382=CARTESIAN_POINT ( 'NONE',  ( 25.69398547355839924, 110.6264597420659896, 22.75551036951965145 ) ) ;
#17383=VECTOR ( 'NONE', #19703, 1000.000000000000000 ) ;
#17384=( BOUNDED_SURFACE ( )  B_SPLINE_SURFACE ( 3, 1, ( 
 ( #3089, #924 ),
 ( #9710, #14295 ),
 ( #1074, #24295 ),
 ( #18482, #23113 ) ),
 .UNSPECIFIED., .F., .F., .F. ) 
 B_SPLINE_SURFACE_WITH_KNOTS ( ( 4, 4 ),
 ( 2, 2 ),
 ( 0.000000000000000000, 1.000000000000000000 ),
 ( 0.000000000000000000, 1.000000000000000000 ),
 .UNSPECIFIED. ) 
 GEOMETRIC_REPRESENTATION_ITEM ( )  RATIONAL_B_SPLINE_SURFACE ( (
 ( 1.000000000000000000, 1.000000000000000000),
 ( 0.9960225298536222738, 0.9999952330161893110),
 ( 0.9960225298536222738, 0.9999952330161893110),
 ( 1.000000000000000000, 1.000000000000000000) ) ) 
 REPRESENTATION_ITEM ( '' )  SURFACE ( )  );
#17385=CARTESIAN_POINT ( 'NONE',  ( 26.28373643307435614, 88.40064398364036435, 91.96212244992378260 ) ) ;
#17387=CONICAL_SURFACE ( 'NONE', #21062, 117.6351876552689504, 0.9945805576725580410 ) ;
#17390=ORIENTED_EDGE ( 'NONE', *, *, #11224, .T. ) ;
#17391=CARTESIAN_POINT ( 'NONE',  ( 25.64692232868535626, 103.2819624397967857, 45.62640214192299482 ) ) ;
#17392=CARTESIAN_POINT ( 'NONE',  ( 109.1586900883932856, 0.002995460350180808098, -0.006479576224403798407 ) ) ;
#17394=CARTESIAN_POINT ( 'NONE',  ( 32.73300124599732186, 0.000000000000000000, 0.000000000000000000 ) ) ;
#17395=CARTESIAN_POINT ( 'NONE',  ( 30.59138290137885718, -84.53179630244041221, 79.74792615266116513 ) ) ;
#17397=ORIENTED_EDGE ( 'NONE', *, *, #24094, .F. ) ;
#17398=CARTESIAN_POINT ( 'NONE',  ( 2.263178113027050742, 132.2496129425960021, 60.41552743271004999 ) ) ;
#17402=B_SPLINE_CURVE_WITH_KNOTS ( 'NONE', 3,
 ( #7259, #24246, #11139, #198 ),
 .UNSPECIFIED., .F., .F.,
 ( 4, 4 ),
 ( 0.000000000000000000, 0.01077107196513803732 ),
 .UNSPECIFIED. ) ;
#17403=ORIENTED_EDGE ( 'NONE', *, *, #8584, .T. ) ;
#17404=CARTESIAN_POINT ( 'NONE',  ( 25.64703792032470986, -112.3081285890369969, -11.65444440562296080 ) ) ;
#17405=FACE_OUTER_BOUND ( 'NONE', #2633, .T. ) ;
#17406=ORIENTED_EDGE ( 'NONE', *, *, #5904, .F. ) ;
#17407=VERTEX_POINT ( 'NONE', #4989 ) ;
#17409=VERTEX_POINT ( 'NONE', #26716 ) ;
#17410=EDGE_CURVE ( 'NONE', #28403, #16995, #11769, .T. ) ;
#17411=B_SPLINE_CURVE_WITH_KNOTS ( 'NONE', 3,
 ( #2983, #671, #7744, #16499 ),
 .UNSPECIFIED., .F., .F.,
 ( 4, 4 ),
 ( 0.000000000000000000, 0.01077107196513895152 ),
 .UNSPECIFIED. ) ;
#17413=B_SPLINE_CURVE_WITH_KNOTS ( 'NONE', 3,
 ( #10023, #26977, #22986, #7583, #27417, #24851, #14461, #5546 ),
 .UNSPECIFIED., .F., .F.,
 ( 4, 2, 2, 4 ),
 ( 6.938893903907228378E-18, 0.0002429588503611322453, 0.0004859177007222575517, 0.0009718354014444986234 ),
 .UNSPECIFIED. ) ;
#17414=CARTESIAN_POINT ( 'NONE',  ( 28.43349137099836099, -34.52178142065613287, 119.3601175884733010 ) ) ;
#17417=CARTESIAN_POINT ( 'NONE',  ( 1.833691583653550561, 72.24637705290489009, 125.8462703805701466 ) ) ;
#17418=( BOUNDED_SURFACE ( )  B_SPLINE_SURFACE ( 3, 1, ( 
 ( #18308, #16166 ),
 ( #24966, #3212 ),
 ( #13861, #14001 ),
 ( #7699, #25247 ) ),
 .UNSPECIFIED., .F., .F., .F. ) 
 B_SPLINE_SURFACE_WITH_KNOTS ( ( 4, 4 ),
 ( 2, 2 ),
 ( 0.000000000000000000, 1.000000000000000000 ),
 ( 0.000000000000000000, 1.000000000000000000 ),
 .UNSPECIFIED. ) 
 GEOMETRIC_REPRESENTATION_ITEM ( )  RATIONAL_B_SPLINE_SURFACE ( (
 ( 1.000000000000000000, 1.000000000000000000),
 ( 0.6386103224230302855, 0.9954351624131538845),
 ( 0.6386103224230302855, 0.9954351624131538845),
 ( 1.000000000000000000, 1.000000000000000000) ) ) 
 REPRESENTATION_ITEM ( '' )  SURFACE ( )  );
#17420=ORIENTED_EDGE ( 'NONE', *, *, #2728, .F. ) ;
#17424=LINE ( 'NONE', #8251, #521 ) ;
#17428=B_SPLINE_CURVE_WITH_KNOTS ( 'NONE', 3,
 ( #9582, #3108, #20219, #16338 ),
 .UNSPECIFIED., .F., .F.,
 ( 4, 4 ),
 ( 2.396682302503802907E-16, 0.008383748772659700005 ),
 .UNSPECIFIED. ) ;
#17429=CARTESIAN_POINT ( 'NONE',  ( 1.833485406944043827, 58.53321471326877656, 132.7804117027889674 ) ) ;
#17430=ORIENTED_EDGE ( 'NONE', *, *, #23096, .T. ) ;
#17431=EDGE_CURVE ( 'NONE', #16169, #26958, #7031, .T. ) ;
#17433=CARTESIAN_POINT ( 'NONE',  ( 25.69398547355839568, -24.20764173643324213, -110.3177996916217154 ) ) ;
#17434=CARTESIAN_POINT ( 'NONE',  ( 32.73300124599738581, 28.19767303745763698, -114.2056417606545153 ) ) ;
#17435=EDGE_LOOP ( 'NONE', ( #9069, #9882, #15964, #18284 ) ) ;
#17436=ORIENTED_EDGE ( 'NONE', *, *, #12510, .F. ) ;
#17439=CARTESIAN_POINT ( 'NONE',  ( 25.64681081121880624, -45.54494737132293380, 103.3177883989777825 ) ) ;
#17440=VECTOR ( 'NONE', #5972, 1000.000000000000227 ) ;
#17441=CARTESIAN_POINT ( 'NONE',  ( 2.430230287190581429, 125.2872625092162338, 74.01081053031141721 ) ) ;
#17442=CARTESIAN_POINT ( 'NONE',  ( 10.93730112725971360, 36.23586118136525158, 146.7718404940643211 ) ) ;
#17443=FACE_OUTER_BOUND ( 'NONE', #7342, .T. ) ;
#17445=CARTESIAN_POINT ( 'NONE',  ( 25.86096068574581963, 24.48003142199239690, -110.3716997142155947 ) ) ;
#17449=ORIENTED_EDGE ( 'NONE', *, *, #19306, .T. ) ;
#17450=( BOUNDED_SURFACE ( )  B_SPLINE_SURFACE ( 3, 1, ( 
 ( #23399, #27114 ),
 ( #7423, #22834 ),
 ( #3098, #22980 ),
 ( #10015, #25269 ) ),
 .UNSPECIFIED., .F., .F., .F. ) 
 B_SPLINE_SURFACE_WITH_KNOTS ( ( 4, 4 ),
 ( 2, 2 ),
 ( 0.000000000000000000, 1.000000000000000000 ),
 ( 0.000000000000000000, 1.000000000000000000 ),
 .UNSPECIFIED. ) 
 GEOMETRIC_REPRESENTATION_ITEM ( )  RATIONAL_B_SPLINE_SURFACE ( (
 ( 1.000000000000000000, 1.000000000000000000),
 ( 0.9960225298536222738, 0.9999952330161893110),
 ( 0.9960225298536222738, 0.9999952330161893110),
 ( 1.000000000000000000, 1.000000000000000000) ) ) 
 REPRESENTATION_ITEM ( '' )  SURFACE ( )  );
#17451=VERTEX_POINT ( 'NONE', #7456 ) ;
#17454=AXIS2_PLACEMENT_3D ( 'NONE', #19229, #28004, #14906 ) ;
#17455=CARTESIAN_POINT ( 'NONE',  ( 25.64692232868535626, -103.2819624397965015, -45.62640214192366983 ) ) ;
#17459=B_SPLINE_CURVE_WITH_KNOTS ( 'NONE', 3,
 ( #9805, #5030, #14094, #7219, #24920, #25196, #3034, #24781, #16268, #25065 ),
 .UNSPECIFIED., .F., .F.,
 ( 4, 3, 3, 4 ),
 ( 3.469446951953614805E-17, 0.0002669559177086245683, 0.0005339118354150954775, 0.001067817517169162948 ),
 .UNSPECIFIED. ) ;
#17461=CARTESIAN_POINT ( 'NONE',  ( 25.64708010899964208, 97.75667227735169718, -56.50300922386492175 ) ) ;
#17465=ORIENTED_EDGE ( 'NONE', *, *, #26603, .F. ) ;
#17466=ORIENTED_EDGE ( 'NONE', *, *, #7596, .F. ) ;
#17467=ADVANCED_FACE ( 'NONE', ( #7606 ), #17554, .F. ) ;
#17469=( BOUNDED_SURFACE ( )  B_SPLINE_SURFACE ( 3, 1, ( 
 ( #25797, #17150 ),
 ( #10279, #5806 ),
 ( #3771, #23371 ),
 ( #25937, #28217 ) ),
 .UNSPECIFIED., .F., .F., .F. ) 
 B_SPLINE_SURFACE_WITH_KNOTS ( ( 4, 4 ),
 ( 2, 2 ),
 ( 0.000000000000000000, 1.000000000000000000 ),
 ( 0.000000000000000000, 1.000000000000000000 ),
 .UNSPECIFIED. ) 
 GEOMETRIC_REPRESENTATION_ITEM ( )  RATIONAL_B_SPLINE_SURFACE ( (
 ( 1.000000000000000000, 1.000000000000000000),
 ( 0.6386103224230316178, 0.9954351624131538845),
 ( 0.6386103224230316178, 0.9954351624131538845),
 ( 1.000000000000000000, 1.000000000000000000) ) ) 
 REPRESENTATION_ITEM ( '' )  SURFACE ( )  );
#17471=FACE_OUTER_BOUND ( 'NONE', #19770, .T. ) ;
#17476=EDGE_LOOP ( 'NONE', ( #18002, #11190, #27986, #21794 ) ) ;
#17477=AXIS2_PLACEMENT_3D ( 'NONE', #13045, #26011, #6172 ) ;
#17478=CARTESIAN_POINT ( 'NONE',  ( 1.832998868059858122, 97.49378069860796359, 107.4798986104863303 ) ) ;
#17479=AXIS2_PLACEMENT_3D ( 'NONE', #28438, #4849, #9319 ) ;
#17481=CARTESIAN_POINT ( 'NONE',  ( 19.66333377628702195, -84.55762186019634896, 108.7423656420555886 ) ) ;
#17482=CARTESIAN_POINT ( 'NONE',  ( 13.36082413113061307, -53.25066407421903847, 143.3553710183987562 ) ) ;
#17486=CARTESIAN_POINT ( 'NONE',  ( 9.884929003653608603, 150.4771565009630478, 4.203795436552891118 ) ) ;
#17487=CARTESIAN_POINT ( 'NONE',  ( 1.832998868059858122, -132.3466930259789933, -59.50898020732644511 ) ) ;
#17488=CARTESIAN_POINT ( 'NONE',  ( 10.93730112725932635, 0.000000000000000000, 0.000000000000000000 ) ) ;
#17489=DIRECTION ( 'NONE',  ( -0.5946245182733607137, -0.8039981203473692828, 0.002950380665382086945 ) ) ;
#17490=CARTESIAN_POINT ( 'NONE',  ( 5.340103556456345046, 96.93942141426060743, 111.1041836730281034 ) ) ;
#17491=CARTESIAN_POINT ( 'NONE',  ( 2.433796855181233454, 98.43889364293860922, 107.1581411821788947 ) ) ;
#17493=EDGE_LOOP ( 'NONE', ( #19924, #9529, #3214, #27031 ) ) ;
#17494=CARTESIAN_POINT ( 'NONE',  ( 25.64708228042119842, 56.48974615489059659, -97.76433875577585297 ) ) ;
#17495=CARTESIAN_POINT ( 'NONE',  ( 55.49584447822657296, -66.38758986585135347, 29.26468316696749739 ) ) ;
#17498=CARTESIAN_POINT ( 'NONE',  ( 6.224689322667647851, 76.23997225729267768, 126.9212313063847120 ) ) ;
#17499=CARTESIAN_POINT ( 'NONE',  ( 1.833206308920099170, -137.7753864329222040, -45.54896581797600419 ) ) ;
#17501=VECTOR ( 'NONE', #21231, 999.9999999999998863 ) ;
#17505=EDGE_CURVE ( 'NONE', #4937, #28149, #6254, .T. ) ;
#17506=ORIENTED_EDGE ( 'NONE', *, *, #22395, .T. ) ;
#17507=CARTESIAN_POINT ( 'NONE',  ( 109.1721716018069657, -0.008708654716139515445, -0.01467989464939307293 ) ) ;
#17508=( BOUNDED_SURFACE ( )  B_SPLINE_SURFACE ( 3, 1, ( 
 ( #663, #3110 ),
 ( #7436, #11600 ),
 ( #16056, #9311 ),
 ( #26701, #18505 ) ),
 .UNSPECIFIED., .F., .F., .F. ) 
 B_SPLINE_SURFACE_WITH_KNOTS ( ( 4, 4 ),
 ( 2, 2 ),
 ( 0.000000000000000000, 1.000000000000000000 ),
 ( 0.000000000000000000, 1.000000000000000000 ),
 .UNSPECIFIED. ) 
 GEOMETRIC_REPRESENTATION_ITEM ( )  RATIONAL_B_SPLINE_SURFACE ( (
 ( 1.000000000000000000, 1.000000000000000000),
 ( 0.9956975270656955868, 0.8568959468854907557),
 ( 0.9956975270656955868, 0.8568959468854907557),
 ( 1.000000000000000000, 1.000000000000000000) ) ) 
 REPRESENTATION_ITEM ( '' )  SURFACE ( )  );
#17509=VECTOR ( 'NONE', #24889, 1000.000000000000000 ) ;
#17511=CARTESIAN_POINT ( 'NONE',  ( 1.833721034905652525, 14.81406766076126047, -144.3516387774750456 ) ) ;
#17512=EDGE_LOOP ( 'NONE', ( #6694, #23703, #8022, #13613 ) ) ;
#17514=CARTESIAN_POINT ( 'NONE',  ( 6.224689322667630975, -57.86870174583338411, -136.2818611715196653 ) ) ;
#17518=B_SPLINE_CURVE_WITH_KNOTS ( 'NONE', 3,
 ( #26848, #13896, #4974, #13747, #22706, #11750, #20517 ),
 .UNSPECIFIED., .F., .F.,
 ( 4, 3, 4 ),
 ( 0.000000000000000000, 0.02816610861753242670, 0.04000277880656208374 ),
 .UNSPECIFIED. ) ;
#17521=CARTESIAN_POINT ( 'NONE',  ( 55.79472521941426777, 48.13855120843883384, 54.55111121764100091 ) ) ;
#17522=CARTESIAN_POINT ( 'NONE',  ( 5.340103556456304190, 146.3832391989195116, 17.70136535449949022 ) ) ;
#17523=CARTESIAN_POINT ( 'NONE',  ( 9.884929003653626367, -146.3148513795968881, 35.39789245780281846 ) ) ;
#17524=CIRCLE ( 'NONE', #20284, 151.1787379149930359 ) ;
#17527=FACE_OUTER_BOUND ( 'NONE', #59, .T. ) ;
#17528=CARTESIAN_POINT ( 'NONE',  ( 25.64660436782584796, -98.07256794792245103, -55.95243482911472199 ) ) ;
#17529=ORIENTED_EDGE ( 'NONE', *, *, #17431, .F. ) ;
#17530=AXIS2_PLACEMENT_3D ( 'NONE', #12026, #16482, #5700 ) ;
#17531=ORIENTED_EDGE ( 'NONE', *, *, #10678, .F. ) ;
#17533=CARTESIAN_POINT ( 'NONE',  ( 10.93730112725990367, -149.7554878793147566, -20.69552240458495973 ) ) ;
#17534=CARTESIAN_POINT ( 'NONE',  ( 109.1587776205901577, -0.006661366261224517873, -0.003057017121591183717 ) ) ;
#17536=CARTESIAN_POINT ( 'NONE',  ( 28.43349137099833612, -42.22940898499130924, -116.8557575815932950 ) ) ;
#17537=CARTESIAN_POINT ( 'NONE',  ( 25.64660436782552466, 46.45435812945243015, 102.9120797476509779 ) ) ;
#17538=ORIENTED_EDGE ( 'NONE', *, *, #522, .F. ) ;
#17541=CARTESIAN_POINT ( 'NONE',  ( 1.833485406944043827, 117.0814567582556407, -85.72460230293573602 ) ) ;
#17543=EDGE_CURVE ( 'NONE', #12674, #7760, #16547, .T. ) ;
#17545=CARTESIAN_POINT ( 'NONE',  ( 21.16825799904897210, 9.757279788664570574, -135.0813719997368594 ) ) ;
#17546=EDGE_CURVE ( 'NONE', #207, #3333, #7269, .T. ) ;
#17547=CARTESIAN_POINT ( 'NONE',  ( 2.063896406836609909, 43.61045647697875438, -138.5688025270874562 ) ) ;
#17548=VERTEX_POINT ( 'NONE', #27870 ) ;
#17550=ORIENTED_EDGE ( 'NONE', *, *, #10706, .T. ) ;
#17551=ORIENTED_EDGE ( 'NONE', *, *, #18283, .F. ) ;
#17554=( BOUNDED_SURFACE ( )  B_SPLINE_SURFACE ( 3, 1, ( 
 ( #14625, #23154 ),
 ( #1112, #27576 ),
 ( #20825, #7895 ),
 ( #21096, #16806 ) ),
 .UNSPECIFIED., .F., .F., .F. ) 
 B_SPLINE_SURFACE_WITH_KNOTS ( ( 4, 4 ),
 ( 2, 2 ),
 ( 0.000000000000000000, 1.000000000000000000 ),
 ( 0.000000000000000000, 1.000000000000000000 ),
 .UNSPECIFIED. ) 
 GEOMETRIC_REPRESENTATION_ITEM ( )  RATIONAL_B_SPLINE_SURFACE ( (
 ( 1.000000000000000000, 1.000000000000000000),
 ( 0.9956975270656954757, 0.8568959468854893125),
 ( 0.9956975270656954757, 0.8568959468854893125),
 ( 1.000000000000000000, 1.000000000000000000) ) ) 
 REPRESENTATION_ITEM ( '' )  SURFACE ( )  );
#17555=CARTESIAN_POINT ( 'NONE',  ( 109.1586900883932856, -0.005715190711481754789, 0.004277182003227202392 ) ) ;
#17556=VERTEX_POINT ( 'NONE', #25154 ) ;
#17557=CARTESIAN_POINT ( 'NONE',  ( 1.833721034905633873, 72.86293192427493182, 125.4904194343087198 ) ) ;
#17559=ORIENTED_EDGE ( 'NONE', *, *, #2942, .T. ) ;
#17560=EDGE_LOOP ( 'NONE', ( #7210, #16289, #3362, #8858 ) ) ;
#17561=CARTESIAN_POINT ( 'NONE',  ( 1.833603222531957178, 142.0304769734132435, -29.73464781350118358 ) ) ;
#17564=CIRCLE ( 'NONE', #24954, 20.00000000000000000 ) ;
#17568=AXIS2_PLACEMENT_3D ( 'NONE', #24086, #19190, #4346 ) ;
#17569=EDGE_CURVE ( 'NONE', #24736, #531, #26108, .T. ) ;
#17570=CARTESIAN_POINT ( 'NONE',  ( 1.834118845439484335, -72.70910183320656017, 125.5799175751967454 ) ) ;
#17571=CARTESIAN_POINT ( 'NONE',  ( 1.833485406944043827, 14.63699153649359452, 144.3694338680885778 ) ) ;
#17573=EDGE_CURVE ( 'NONE', #8689, #21137, #22354, .T. ) ;
#17574=CARTESIAN_POINT ( 'NONE',  ( 26.11404676487257603, -110.9778746459745520, -22.43340081644882389 ) ) ;
#17576=VERTEX_POINT ( 'NONE', #3969 ) ;
#17578=LINE ( 'NONE', #8668, #9312 ) ;
#17581=ORIENTED_EDGE ( 'NONE', *, *, #19954, .T. ) ;
#17582=CARTESIAN_POINT ( 'NONE',  ( 28.37599760073042532, 84.05168479399091552, 78.09498850373434209 ) ) ;
#17584=CARTESIAN_POINT ( 'NONE',  ( 2.063896406836609909, -107.0521644432424040, 98.19887492195825018 ) ) ;
#17585=AXIS2_PLACEMENT_3D ( 'NONE', #16390, #10969, #10361 ) ;
#17586=( BOUNDED_SURFACE ( )  B_SPLINE_SURFACE ( 3, 1, ( 
 ( #24056, #9064 ),
 ( #15659, #21740 ),
 ( #17688, #26190 ),
 ( #26329, #15380 ) ),
 .UNSPECIFIED., .F., .F., .F. ) 
 B_SPLINE_SURFACE_WITH_KNOTS ( ( 4, 4 ),
 ( 2, 2 ),
 ( 0.000000000000000000, 1.000000000000000000 ),
 ( 0.000000000000000000, 1.000000000000000000 ),
 .UNSPECIFIED. ) 
 GEOMETRIC_REPRESENTATION_ITEM ( )  RATIONAL_B_SPLINE_SURFACE ( (
 ( 1.000000000000000000, 1.000000000000000000),
 ( 0.6386103224230302855, 0.9954351624131538845),
 ( 0.6386103224230302855, 0.9954351624131538845),
 ( 1.000000000000000000, 1.000000000000000000) ) ) 
 REPRESENTATION_ITEM ( '' )  SURFACE ( )  );
#17587=B_SPLINE_CURVE_WITH_KNOTS ( 'NONE', 3,
 ( #27037, #14228, #9801, #18570, #27338, #5466, #23050, #3313 ),
 .UNSPECIFIED., .F., .F.,
 ( 4, 2, 2, 4 ),
 ( 1.250926888277100303E-17, 0.0002429592666046748086, 0.0004859185332093370947, 0.0009718370664186629137 ),
 .UNSPECIFIED. ) ;
#17588=CARTESIAN_POINT ( 'NONE',  ( 2.263178607246715490, -144.4462811785177223, 16.59120332983095381 ) ) ;
#17591=CARTESIAN_POINT ( 'NONE',  ( 1.833485406944057594, 44.33323125130110043, -138.1714136985304151 ) ) ;
#17595=ADVANCED_FACE ( 'NONE', ( #21816 ), #6732, .F. ) ;
#17596=CARTESIAN_POINT ( 'NONE',  ( 26.28373643307404350, -108.3320567927994915, 67.34887744616746375 ) ) ;
#17599=EDGE_CURVE ( 'NONE', #13261, #21976, #13061, .T. ) ;
#17600=ORIENTED_EDGE ( 'NONE', *, *, #21580, .F. ) ;
#17603=CARTESIAN_POINT ( 'NONE',  ( 2.433796855181205476, 84.34988187690927930, 118.5671979538059730 ) ) ;
#17604=CARTESIAN_POINT ( 'NONE',  ( 25.98107933586720009, -22.45325949158398160, -110.8834224379716176 ) ) ;
#17607=CARTESIAN_POINT ( 'NONE',  ( 109.1586900883932856, 0.004701023939945712764, -0.005371970278528660422 ) ) ;
#17608=VECTOR ( 'NONE', #26075, 1000.000000000000114 ) ;
#17609=ORIENTED_EDGE ( 'NONE', *, *, #11300, .F. ) ;
#17610=CARTESIAN_POINT ( 'NONE',  ( 2.263178113027036087, 145.3892419963351017, 1.401567040888699101 ) ) ;
#17612=ORIENTED_EDGE ( 'NONE', *, *, #459, .F. ) ;
#17616=VERTEX_POINT ( 'NONE', #1662 ) ;
#17620=VERTEX_POINT ( 'NONE', #6417 ) ;
#17621=CARTESIAN_POINT ( 'NONE',  ( 1.833485406944043827, -125.4007332306540405, -73.01664920993097496 ) ) ;
#17622=CIRCLE ( 'NONE', #1989, 117.6351876552689504 ) ;
#17623=ORIENTED_EDGE ( 'NONE', *, *, #7010, .F. ) ;
#17624=CARTESIAN_POINT ( 'NONE',  ( 13.36082413113063083, -127.3428651193242445, -84.67697637120542709 ) ) ;
#17626=CARTESIAN_POINT ( 'NONE',  ( 10.93730112725932635, 0.000000000000000000, 0.000000000000000000 ) ) ;
#17627=EDGE_CURVE ( 'NONE', #19219, #12888, #24767, .T. ) ;
#17628=CARTESIAN_POINT ( 'NONE',  ( 26.04756280548354752, -110.9306483680201296, -22.44333019059113354 ) ) ;
#17631=EDGE_CURVE ( 'NONE', #23299, #26154, #13163, .T. ) ;
#17636=ORIENTED_EDGE ( 'NONE', *, *, #17794, .T. ) ;
#17640=CARTESIAN_POINT ( 'NONE',  ( 2.433796855181205476, -86.69855925934052721, 116.8607839509053434 ) ) ;
#17643=EDGE_CURVE ( 'NONE', #23985, #11536, #11694, .T. ) ;
#17644=VECTOR ( 'NONE', #3401, 1000.000000000000227 ) ;
#17645=EDGE_LOOP ( 'NONE', ( #9462, #19585, #2718, #1279 ) ) ;
#17646=CARTESIAN_POINT ( 'NONE',  ( 2.430230287190581429, 57.85706160874145354, 133.5180086894993110 ) ) ;
#17648=CARTESIAN_POINT ( 'NONE',  ( 28.37603512858456156, 55.80522682147411473, -100.2461737936624218 ) ) ;
#17649=CARTESIAN_POINT ( 'NONE',  ( 109.1586059443104944, -0.005067816690886790647, 0.004935564877224665227 ) ) ;
#17650=ORIENTED_EDGE ( 'NONE', *, *, #18486, .F. ) ;
#17653=ORIENTED_EDGE ( 'NONE', *, *, #15595, .T. ) ;
#17655=ORIENTED_EDGE ( 'NONE', *, *, #15448, .T. ) ;
#17656=CARTESIAN_POINT ( 'NONE',  ( 1.833206308920054539, 85.89457656604029978, -116.9567745381551163 ) ) ;
#17657=CARTESIAN_POINT ( 'NONE',  ( 1.894214914920945070, 108.5033568857724617, 96.41356089048316846 ) ) ;
#17658=B_SPLINE_CURVE_WITH_KNOTS ( 'NONE', 3,
 ( #3343, #18451, #27072, #12132, #18605, #7539 ),
 .UNSPECIFIED., .F., .F.,
 ( 4, 2, 4 ),
 ( 3.929062510380680860E-17, 0.0006311571484586211847, 0.001262314296917203338 ),
 .UNSPECIFIED. ) ;
#17659=ORIENTED_EDGE ( 'NONE', *, *, #24162, .T. ) ;
#17660=B_SPLINE_CURVE_WITH_KNOTS ( 'NONE', 3,
 ( #10574, #16914, #17040, #10166 ),
 .UNSPECIFIED., .F., .F.,
 ( 4, 4 ),
 ( 3.368494537013313651E-16, 0.01077107486149803464 ),
 .UNSPECIFIED. ) ;
#17662=CARTESIAN_POINT ( 'NONE',  ( 25.98107933586720719, 47.01057192495409254, -102.9042679418244290 ) ) ;
#17663=CARTESIAN_POINT ( 'NONE',  ( 1.833838850093452599, -138.0075868208083421, -44.84137955663364750 ) ) ;
#17665=DIRECTION ( 'NONE',  ( -0.5946245182733607137, 0.4749651461092252447, 0.6487139525627731995 ) ) ;
#17667=ORIENTED_EDGE ( 'NONE', *, *, #2186, .T. ) ;
#17671=ORIENTED_EDGE ( 'NONE', *, *, #23921, .F. ) ;
#17673=VERTEX_POINT ( 'NONE', #26127 ) ;
#17674=ORIENTED_EDGE ( 'NONE', *, *, #23992, .T. ) ;
#17676=CARTESIAN_POINT ( 'NONE',  ( 109.1592201516379674, 0.004368284148525261590, -0.006536841731962014269 ) ) ;
#17677=CARTESIAN_POINT ( 'NONE',  ( 25.64692872815574631, 75.31297890941272044, 84.12425003484072761 ) ) ;
#17678=CARTESIAN_POINT ( 'NONE',  ( 1.831572820252009626, 59.92262167723438182, 132.1614873090350954 ) ) ;
#17679=CARTESIAN_POINT ( 'NONE',  ( 1.833721034905635872, 72.24642519953950170, -125.8463597577919586 ) ) ;
#17680=CARTESIAN_POINT ( 'NONE',  ( 24.01988960052087307, -108.4726924928700527, 73.52806416354032137 ) ) ;
#17681=ORIENTED_EDGE ( 'NONE', *, *, #22128, .F. ) ;
#17684=( BOUNDED_SURFACE ( )  B_SPLINE_SURFACE ( 3, 1, ( 
 ( #10049, #1392 ),
 ( #23163, #16368 ),
 ( #22875, #14633 ),
 ( #3419, #16814 ) ),
 .UNSPECIFIED., .F., .F., .F. ) 
 B_SPLINE_SURFACE_WITH_KNOTS ( ( 4, 4 ),
 ( 2, 2 ),
 ( 0.000000000000000000, 1.000000000000000000 ),
 ( 0.000000000000000000, 1.000000000000000000 ),
 .UNSPECIFIED. ) 
 GEOMETRIC_REPRESENTATION_ITEM ( )  RATIONAL_B_SPLINE_SURFACE ( (
 ( 1.000000000000000000, 1.000000000000000000),
 ( 0.6386103224230302855, 0.9954351624131538845),
 ( 0.6386103224230302855, 0.9954351624131538845),
 ( 1.000000000000000000, 1.000000000000000000) ) ) 
 REPRESENTATION_ITEM ( '' )  SURFACE ( )  );
#17685=CARTESIAN_POINT ( 'NONE',  ( 25.64700659047697329, 11.57609179463959848, 112.3162501909140047 ) ) ;
#17686=CARTESIAN_POINT ( 'NONE',  ( 25.64670758986457955, -112.9099239813695732, -0.4979020485389182848 ) ) ;
#17687=CARTESIAN_POINT ( 'NONE',  ( 32.73300124599732186, 0.000000000000000000, 0.000000000000000000 ) ) ;
#17688=CARTESIAN_POINT ( 'NONE',  ( 109.1721716018069657, -0.01567407524362084484, -0.006757465437538735971 ) ) ;
#17689=VERTEX_POINT ( 'NONE', #13450 ) ;
#17691=CARTESIAN_POINT ( 'NONE',  ( 2.433796855181233454, -142.6247129145646397, -28.83182736670683610 ) ) ;
#17692=ORIENTED_EDGE ( 'NONE', *, *, #16700, .T. ) ;
#17695=B_SPLINE_CURVE_WITH_KNOTS ( 'NONE', 3,
 ( #1687, #23317, #17091, #23184 ),
 .UNSPECIFIED., .F., .F.,
 ( 4, 4 ),
 ( 3.495726066037707399E-16, 0.01077107486149809015 ),
 .UNSPECIFIED. ) ;
#17696=LINE ( 'NONE', #22169, #25219 ) ;
#17697=CARTESIAN_POINT ( 'NONE',  ( 109.1586900883932856, 0.006479576224398247292, -0.002995460350188419631 ) ) ;
#17698=VECTOR ( 'NONE', #9331, 1000.000000000000114 ) ;
#17699=CARTESIAN_POINT ( 'NONE',  ( 1.833485406944043827, 14.63699153649552365, -144.3694338680883789 ) ) ;
#17704=ORIENTED_EDGE ( 'NONE', *, *, #17792, .T. ) ;
#17706=ORIENTED_EDGE ( 'NONE', *, *, #27970, .F. ) ;
#17708=CARTESIAN_POINT ( 'NONE',  ( 2.433796855181205476, -1.451562450950653949, 145.5024947199069629 ) ) ;
#17709=CARTESIAN_POINT ( 'NONE',  ( 1.833485406944043827, 73.01664920992966756, 125.4007332306548221 ) ) ;
#17710=DIRECTION ( 'NONE',  ( 1.000000000000000000, -0.000000000000000000, -0.000000000000000000 ) ) ;
#17711=FACE_OUTER_BOUND ( 'NONE', #5644, .T. ) ;
#17715=CARTESIAN_POINT ( 'NONE',  ( 32.73300124599735739, -99.90245962373877830, 62.10906484417201767 ) ) ;
#17717=FACE_OUTER_BOUND ( 'NONE', #10440, .T. ) ;
#17719=VERTEX_POINT ( 'NONE', #2804 ) ;
#17722=CARTESIAN_POINT ( 'NONE',  ( 26.04756280548353686, 107.2904246402799799, -36.02883009343526766 ) ) ;
#17723=ORIENTED_EDGE ( 'NONE', *, *, #11122, .T. ) ;
#17726=ORIENTED_EDGE ( 'NONE', *, *, #4158, .F. ) ;
#17727=ORIENTED_EDGE ( 'NONE', *, *, #6909, .F. ) ;
#17728=EDGE_CURVE ( 'NONE', #9282, #26952, #22723, .T. ) ;
#17729=CARTESIAN_POINT ( 'NONE',  ( 2.108985857320939239, -145.2876352664462161, 1.281428372375244429 ) ) ;
#17731=CARTESIAN_POINT ( 'NONE',  ( 2.430230287190592531, 118.5711603495681459, 84.35270093935295677 ) ) ;
#17734=B_SPLINE_CURVE_WITH_KNOTS ( 'NONE', 3,
 ( #12351, #5892, #16954, #12081 ),
 .UNSPECIFIED., .F., .F.,
 ( 4, 4 ),
 ( 3.215760458551393353E-16, 0.01077107486149844404 ),
 .UNSPECIFIED. ) ;
#17738=DIRECTION ( 'NONE',  ( -1.000000000000000000, -0.000000000000000000, -0.000000000000000000 ) ) ;
#17739=CARTESIAN_POINT ( 'NONE',  ( 109.1778270068192853, -0.004958088776550157763, 0.007885345421907784952 ) ) ;
#17741=CARTESIAN_POINT ( 'NONE',  ( 109.1586900883932856, 0.0001010081143884156022, -0.007137750914552288065 ) ) ;
#17742=CARTESIAN_POINT ( 'NONE',  ( 1.833721034905632985, -117.1867194831484511, 85.58110185770060241 ) ) ;
#17743=ORIENTED_EDGE ( 'NONE', *, *, #1030, .T. ) ;
#17745=CARTESIAN_POINT ( 'NONE',  ( 55.49584447822657296, 69.08290406177579257, 22.16497542184429292 ) ) ;
#17746=CARTESIAN_POINT ( 'NONE',  ( 26.11404676487257603, 57.58742681967585497, -97.48350837663548418 ) ) ;
#17749=CARTESIAN_POINT ( 'NONE',  ( 25.64670758986457599, 0.4979020485393113038, -112.9099239813695448 ) ) ;
#17750=CARTESIAN_POINT ( 'NONE',  ( 10.93730112725982373, -142.1801301103788262, 51.37919228020236773 ) ) ;
#17752=CARTESIAN_POINT ( 'NONE',  ( 10.93730112726006354, 149.7554878793152966, -20.69552240458195413 ) ) ;
#17753=VERTEX_POINT ( 'NONE', #26833 ) ;
#17755=CARTESIAN_POINT ( 'NONE',  ( 2.108393763691197353, 141.8460676169243584, 31.45977531353340950 ) ) ;
#17756=ORIENTED_EDGE ( 'NONE', *, *, #28380, .T. ) ;
#17758=CARTESIAN_POINT ( 'NONE',  ( 10.93730112725932635, 0.000000000000000000, 0.000000000000000000 ) ) ;
#17760=CARTESIAN_POINT ( 'NONE',  ( 10.93730112725971715, 4.928439153520177030, 151.0983828010091372 ) ) ;
#17762=ORIENTED_EDGE ( 'NONE', *, *, #22501, .T. ) ;
#17763=CARTESIAN_POINT ( 'NONE',  ( 25.64681081121879203, -83.63051021305848565, -75.86069728269076506 ) ) ;
#17764=EDGE_CURVE ( 'NONE', #5605, #14867, #21204, .T. ) ;
#17765=ADVANCED_FACE ( 'NONE', ( #20359 ), #26379, .F. ) ;
#17767=CARTESIAN_POINT ( 'NONE',  ( 1.831572820252009626, 97.82994539998382777, 107.1759352627509543 ) ) ;
#17768=EDGE_CURVE ( 'NONE', #12739, #16696, #3125, .T. ) ;
#17770=CARTESIAN_POINT ( 'NONE',  ( 109.1586900883932856, -0.007088091345229661187, 0.0008465529156634868553 ) ) ;
#17772=CARTESIAN_POINT ( 'NONE',  ( 2.433796855181205476, 84.34988187690927930, 118.5671979538059730 ) ) ;
#17773=CARTESIAN_POINT ( 'NONE',  ( 109.1778270068192853, -0.007736698406808940019, -0.005186985107090110077 ) ) ;
#17774=CARTESIAN_POINT ( 'NONE',  ( 25.64681081121879203, -0.4157506337735756285, 112.9102952884414464 ) ) ;
#17777=CARTESIAN_POINT ( 'NONE',  ( 1.831572820252008738, 144.4165162501764996, -14.18623102066620412 ) ) ;
#17778=B_SPLINE_CURVE_WITH_KNOTS ( 'NONE', 3,
 ( #2321, #15418, #6815, #26370, #6674, #24234, #21918, #11124 ),
 .UNSPECIFIED., .F., .F.,
 ( 4, 2, 2, 4 ),
 ( 1.734723475976807094E-18, 0.0002429588503611276103, 0.0004859177007222534859, 0.0009718354014444998161 ),
 .UNSPECIFIED. ) ;
#17779=CARTESIAN_POINT ( 'NONE',  ( 1.833206310202343925, -30.89799345102857941, -141.7818020564281767 ) ) ;
#17780=CARTESIAN_POINT ( 'NONE',  ( 2.063896406836609909, -43.61045647697787331, 138.5688025270877120 ) ) ;
#17781=EDGE_CURVE ( 'NONE', #15925, #20443, #1438, .T. ) ;
#17782=CARTESIAN_POINT ( 'NONE',  ( 32.73300124599738581, -39.98094346392232268, -110.6325518752277759 ) ) ;
#17783=ORIENTED_EDGE ( 'NONE', *, *, #27857, .F. ) ;
#17784=CARTESIAN_POINT ( 'NONE',  ( 16.05277956358206737, -132.7473359121861449, -53.98852998724714780 ) ) ;
#17786=CARTESIAN_POINT ( 'NONE',  ( 30.59141879584284496, -38.47120193631536722, 109.6600586137411852 ) ) ;
#17787=ORIENTED_EDGE ( 'NONE', *, *, #8070, .T. ) ;
#17788=EDGE_CURVE ( 'NONE', #20235, #2885, #730, .T. ) ;
#17789=CARTESIAN_POINT ( 'NONE',  ( 1.833750490713725201, -97.29556423840206492, 107.6587173638742883 ) ) ;
#17790=ORIENTED_EDGE ( 'NONE', *, *, #19499, .T. ) ;
#17792=EDGE_CURVE ( 'NONE', #16650, #24385, #3480, .T. ) ;
#17794=EDGE_CURVE ( 'NONE', #9920, #4538, #19941, .T. ) ;
#17796=CARTESIAN_POINT ( 'NONE',  ( 1.832998868059890096, 117.7096351258398954, -84.86110816369486542 ) ) ;
#17799=VERTEX_POINT ( 'NONE', #22505 ) ;
#17810=CARTESIAN_POINT ( 'NONE',  ( 25.64670758986456889, -103.3508631837547682, 45.46974729533248194 ) ) ;
#17812=ORIENTED_EDGE ( 'NONE', *, *, #24439, .T. ) ;
#17813=CARTESIAN_POINT ( 'NONE',  ( 32.73300124599734318, 116.5274707358856006, 16.10546300444864443 ) ) ;
#17815=CARTESIAN_POINT ( 'NONE',  ( 2.063896406836609909, 145.2631347824382715, -1.344106060020873405 ) ) ;
#17817=B_SPLINE_CURVE_WITH_KNOTS ( 'NONE', 3,
 ( #24919, #15972, #18261, #11811, #7076, #24780, #432 ),
 .UNSPECIFIED., .F., .F.,
 ( 4, 3, 4 ),
 ( 6.272338867242750372E-16, 0.02816610861753246486, 0.04000277880656283314 ),
 .UNSPECIFIED. ) ;
#17819=CARTESIAN_POINT ( 'NONE',  ( 109.1586059443104944, -0.003127959656221041516, -0.006344953511159715648 ) ) ;
#17820=ADVANCED_FACE ( 'NONE', ( #5068 ), #837, .F. ) ;
#17821=ORIENTED_EDGE ( 'NONE', *, *, #15891, .T. ) ;
#17822=CARTESIAN_POINT ( 'NONE',  ( 10.93730112725996406, 10.89264110825190457, -150.7858122213661716 ) ) ;
#17823=CARTESIAN_POINT ( 'NONE',  ( 25.64681081121879203, -107.5125461021400355, -34.49579773461893950 ) ) ;
#17828=ADVANCED_FACE ( 'NONE', ( #27378 ), #22191, .F. ) ;
#17829=CARTESIAN_POINT ( 'NONE',  ( 26.11404676487257603, -36.06104232266525145, 107.3263591096429082 ) ) ;
#17830=CARTESIAN_POINT ( 'NONE',  ( 25.64704443564076897, -23.34498572103240832, -110.4715096490035364 ) ) ;
#17834=ORIENTED_EDGE ( 'NONE', *, *, #7292, .T. ) ;
#17836=B_SPLINE_CURVE_WITH_KNOTS ( 'NONE', 3,
 ( #8879, #15601, #17351, #6717, #26278, #8724, #22105, #6576 ),
 .UNSPECIFIED., .F., .F.,
 ( 4, 2, 2, 4 ),
 ( 1.962615573354718958E-17, 0.0002429592666046876293, 0.0004859185332093556345, 0.0009718370664186802609 ),
 .UNSPECIFIED. ) ;
#17837=LINE ( 'NONE', #434, #23643 ) ;
#17838=ORIENTED_EDGE ( 'NONE', *, *, #24976, .T. ) ;
#17839=( BOUNDED_SURFACE ( )  B_SPLINE_SURFACE ( 3, 1, ( 
 ( #28363, #10021 ),
 ( #27708, #23268 ),
 ( #14601, #16630 ),
 ( #8016, #25565 ) ),
 .UNSPECIFIED., .F., .F., .F. ) 
 B_SPLINE_SURFACE_WITH_KNOTS ( ( 4, 4 ),
 ( 2, 2 ),
 ( 0.000000000000000000, 1.000000000000000000 ),
 ( 0.000000000000000000, 1.000000000000000000 ),
 .UNSPECIFIED. ) 
 GEOMETRIC_REPRESENTATION_ITEM ( )  RATIONAL_B_SPLINE_SURFACE ( (
 ( 1.000000000000000000, 1.000000000000000000),
 ( 0.9956975270656955868, 0.8568959468854907557),
 ( 0.9956975270656955868, 0.8568959468854907557),
 ( 1.000000000000000000, 1.000000000000000000) ) ) 
 REPRESENTATION_ITEM ( '' )  SURFACE ( )  );
#17840=VERTEX_POINT ( 'NONE', #12401 ) ;
#17841=CARTESIAN_POINT ( 'NONE',  ( 1.894214914920955062, 126.1778046718836066, 71.74757687370502879 ) ) ;
#17844=CARTESIAN_POINT ( 'NONE',  ( 28.37644542392841984, 21.87158679436198483, 122.4011828058665543 ) ) ;
#17847=CARTESIAN_POINT ( 'NONE',  ( 9.884929003653608603, -85.04731144912427965, -124.2095058357586055 ) ) ;
#17849=CARTESIAN_POINT ( 'NONE',  ( 1.833691583653538348, 14.81406002961315949, 144.3515375443195694 ) ) ;
#17850=CARTESIAN_POINT ( 'NONE',  ( 2.108985857320896162, 141.8463279126005432, -31.46042399111103549 ) ) ;
#17852=VERTEX_POINT ( 'NONE', #3486 ) ;
#17854=CARTESIAN_POINT ( 'NONE',  ( 25.69398547355841345, 24.20764173643400952, 110.3177996916214596 ) ) ;
#17856=VERTEX_POINT ( 'NONE', #1744 ) ;
#17857=EDGE_CURVE ( 'NONE', #3538, #24090, #10681, .T. ) ;
#17858=ORIENTED_EDGE ( 'NONE', *, *, #11435, .T. ) ;
#17859=ORIENTED_EDGE ( 'NONE', *, *, #18700, .F. ) ;
#17860=CARTESIAN_POINT ( 'NONE',  ( 1.834118845439484335, -85.14950727125780361, -117.5010238212707065 ) ) ;
#17861=FACE_OUTER_BOUND ( 'NONE', #14359, .T. ) ;
#17862=EDGE_CURVE ( 'NONE', #22495, #7936, #8279, .T. ) ;
#17863=EDGE_CURVE ( 'NONE', #24126, #7024, #13406, .T. ) ;
#17864=CARTESIAN_POINT ( 'NONE',  ( 1.831572820252008738, 125.1738732943810106, 73.40899645746047497 ) ) ;
#17868=CARTESIAN_POINT ( 'NONE',  ( 2.108985857320913038, -144.6256801373125427, -13.91228467251966627 ) ) ;
#17872=CARTESIAN_POINT ( 'NONE',  ( 21.16825799904898986, 97.63815233965183893, -93.85612807858919382 ) ) ;
#17876=CARTESIAN_POINT ( 'NONE',  ( 55.49584447822657296, 29.26468316696863070, -66.38758986585085609 ) ) ;
#17878=CARTESIAN_POINT ( 'NONE',  ( 25.86096068574577700, 0.9975172952974178386, -113.0494979885903604 ) ) ;
#17879=CARTESIAN_POINT ( 'NONE',  ( 10.93730112725978287, -97.44200844886353252, 115.5857507957700250 ) ) ;
#17883=CARTESIAN_POINT ( 'NONE',  ( 1.833206308920081185, 117.8322276971147176, -84.68961866582884568 ) ) ;
#17884=CARTESIAN_POINT ( 'NONE',  ( 2.433796855181219243, 142.0211193075555798, 31.67151202413018396 ) ) ;
#17885=ORIENTED_EDGE ( 'NONE', *, *, #939, .T. ) ;
#17886=EDGE_LOOP ( 'NONE', ( #2980, #6004, #9875, #20150 ) ) ;
#17889=ORIENTED_EDGE ( 'NONE', *, *, #21056, .T. ) ;
#17890=CARTESIAN_POINT ( 'NONE',  ( 26.11404676487257603, 90.92995828888292920, -67.46175819463273626 ) ) ;
#17891=VERTEX_POINT ( 'NONE', #27948 ) ;
#17893=EDGE_CURVE ( 'NONE', #2443, #24769, #25113, .T. ) ;
#17894=CARTESIAN_POINT ( 'NONE',  ( 25.64681081121879203, 66.70335573067866619, 91.10197563707968982 ) ) ;
#17896=CARTESIAN_POINT ( 'NONE',  ( 1.834118845439484335, -96.96525081350071673, 107.9567937753789977 ) ) ;
#17898=CARTESIAN_POINT ( 'NONE',  ( 10.93730112725990367, -104.7670965581004054, -108.9902118373752842 ) ) ;
#17899=VECTOR ( 'NONE', #22859, 1000.000000000000114 ) ;
#17902=CARTESIAN_POINT ( 'NONE',  ( 26.11404676487257603, -84.89295829319442532, -74.91683232331061504 ) ) ;
#17905=VERTEX_POINT ( 'NONE', #12324 ) ;
#17906=CARTESIAN_POINT ( 'NONE',  ( 1.832998868059890096, -145.1092030902949830, -0.5339089137762871307 ) ) ;
#17909=LINE ( 'NONE', #22111, #13852 ) ;
#17910=ADVANCED_FACE ( 'NONE', ( #23859 ), #25145, .F. ) ;
#17911=CARTESIAN_POINT ( 'NONE',  ( 25.64681081121879203, -34.49579773461710630, -107.5125461021406181 ) ) ;
#17912=CARTESIAN_POINT ( 'NONE',  ( 21.16825799904900052, -125.4548537968710207, -51.02216409572695710 ) ) ;
#17914=VERTEX_POINT ( 'NONE', #19099 ) ;
#17915=CARTESIAN_POINT ( 'NONE',  ( 25.64703792032469920, 110.4127989088533184, -23.62108504469137671 ) ) ;
#17916=EDGE_CURVE ( 'NONE', #17673, #12674, #21098, .T. ) ;
#17917=ORIENTED_EDGE ( 'NONE', *, *, #20041, .F. ) ;
#17918=CIRCLE ( 'NONE', #12870, 151.1787379149930359 ) ;
#17925=AXIS2_PLACEMENT_3D ( 'NONE', #11092, #19861, #149 ) ;
#17926=ORIENTED_EDGE ( 'NONE', *, *, #5675, .T. ) ;
#17927=CARTESIAN_POINT ( 'NONE',  ( 2.263178113027036531, 86.59154384226330592, -116.7985471375923083 ) ) ;
#17934=CARTESIAN_POINT ( 'NONE',  ( 10.93730112726024117, 133.3192575531818136, -71.28103789254788580 ) ) ;
#17935=CARTESIAN_POINT ( 'NONE',  ( 28.37644542392835234, 124.2737818798215699, 4.054996728114629967 ) ) ;
#17936=CARTESIAN_POINT ( 'NONE',  ( 55.79472521941426777, -23.17337251492811490, 68.96476385670656839 ) ) ;
#17938=CARTESIAN_POINT ( 'NONE',  ( 2.433796855181205476, -31.67151202413066713, 142.0211193075554945 ) ) ;
#17939=CARTESIAN_POINT ( 'NONE',  ( 8.186469777910929224, -63.89871389959373005, -134.9918587298870705 ) ) ;
#17940=DIRECTION ( 'NONE',  ( -1.000000000000000000, -0.000000000000000000, -0.000000000000000000 ) ) ;
#17942=EDGE_CURVE ( 'NONE', #25430, #10776, #7954, .T. ) ;
#17944=ORIENTED_EDGE ( 'NONE', *, *, #12313, .T. ) ;
#17945=CARTESIAN_POINT ( 'NONE',  ( 25.98107933586721074, -90.88151529733741540, -67.37827847766610034 ) ) ;
#17948=VECTOR ( 'NONE', #14045, 1000.000000000000227 ) ;
#17950=CARTESIAN_POINT ( 'NONE',  ( 10.93730112725990011, -119.3442956573265974, -92.80059208661810999 ) ) ;
#17951=CARTESIAN_POINT ( 'NONE',  ( 25.86096068574579832, -103.6815822123522821, 45.07009591924524727 ) ) ;
#17952=CARTESIAN_POINT ( 'NONE',  ( 2.430230287190581429, 71.49654683843510838, 126.7388733285347229 ) ) ;
#17954=ORIENTED_EDGE ( 'NONE', *, *, #1341, .T. ) ;
#17955=CARTESIAN_POINT ( 'NONE',  ( 2.433796855181233454, -142.6247129145646397, -28.83182736670683610 ) ) ;
#17957=VECTOR ( 'NONE', #19677, 1000.000000000000114 ) ;
#17958=CARTESIAN_POINT ( 'NONE',  ( 2.063896406836605024, -1.344106060021375226, 145.2631347824382715 ) ) ;
#17959=CARTESIAN_POINT ( 'NONE',  ( 109.1624594426973118, -0.002863932759303199765, 0.01570508117120616304 ) ) ;
#17960=EDGE_CURVE ( 'NONE', #5605, #207, #13763, .T. ) ;
#17961=B_SPLINE_CURVE_WITH_KNOTS ( 'NONE', 3,
 ( #13065, #26298, #21562, #2107, #14933, #12912, #13190, #8606 ),
 .UNSPECIFIED., .F., .F.,
 ( 4, 2, 2, 4 ),
 ( 0.000000000000000000, 0.0002429592666046688455, 0.0004859185332093376910, 0.0009718370664186699610 ),
 .UNSPECIFIED. ) ;
#17962=CARTESIAN_POINT ( 'NONE',  ( 25.64681081121879203, 56.09509703373343115, 97.99105938547943140 ) ) ;
#17963=VERTEX_POINT ( 'NONE', #23290 ) ;
#17964=ORIENTED_EDGE ( 'NONE', *, *, #17728, .F. ) ;
#17965=CARTESIAN_POINT ( 'NONE',  ( 16.05277956358203539, 10.32496049470279154, -142.9335921074871294 ) ) ;
#17966=VERTEX_POINT ( 'NONE', #25587 ) ;
#17967=VERTEX_POINT ( 'NONE', #21391 ) ;
#17968=EDGE_LOOP ( 'NONE', ( #18537, #7759, #3808, #9940 ) ) ;
#17970=FACE_OUTER_BOUND ( 'NONE', #1181, .T. ) ;
#17971=CARTESIAN_POINT ( 'NONE',  ( 32.73300124599732186, 0.000000000000000000, 0.000000000000000000 ) ) ;
#17973=CARTESIAN_POINT ( 'NONE',  ( 109.1589550718174877, 0.002874971999843658425, 0.007008495014548480478 ) ) ;
#17974=ORIENTED_EDGE ( 'NONE', *, *, #17002, .F. ) ;
#17978=ORIENTED_EDGE ( 'NONE', *, *, #15448, .F. ) ;
#17979=EDGE_CURVE ( 'NONE', #18945, #16650, #6912, .T. ) ;
#17982=CARTESIAN_POINT ( 'NONE',  ( 2.263178113027063620, 31.59906256848478989, -141.9207360579558497 ) ) ;
#17984=CARTESIAN_POINT ( 'NONE',  ( 2.433796855181233454, 1.451562450949631211, 145.5024947199069913 ) ) ;
#17988=CARTESIAN_POINT ( 'NONE',  ( 6.224689322667647851, -48.18553814189932893, -139.9988794244337384 ) ) ;
#17992=CARTESIAN_POINT ( 'NONE',  ( 1.833721034905633429, 15.52204855105840409, 144.2772269874176629 ) ) ;
#17993=B_SPLINE_CURVE_WITH_KNOTS ( 'NONE', 3,
 ( #27719, #8026, #25710, #14610 ),
 .UNSPECIFIED., .F., .F.,
 ( 4, 4 ),
 ( 3.436022625892845483E-16, 0.01077107486149809015 ),
 .UNSPECIFIED. ) ;
#17995=CARTESIAN_POINT ( 'NONE',  ( 26.04756280548354752, -107.9769918539638098, -33.91579348271626770 ) ) ;
#17999=VERTEX_POINT ( 'NONE', #4249 ) ;
#18000=CARTESIAN_POINT ( 'NONE',  ( 30.59141879584312917, -21.51299111589962365, -114.2039975081484755 ) ) ;
#18002=ORIENTED_EDGE ( 'NONE', *, *, #6231, .T. ) ;
#18003=ORIENTED_EDGE ( 'NONE', *, *, #6290, .F. ) ;
#18006=CARTESIAN_POINT ( 'NONE',  ( 26.11404676487257603, 57.58742681967449784, 97.48350837663630841 ) ) ;
#18011=CIRCLE ( 'NONE', #14805, 12.50000000000000178 ) ;
#18013=CARTESIAN_POINT ( 'NONE',  ( 109.1592201516379674, 0.005631912476303814301, -0.005485778713202952607 ) ) ;
#18014=CARTESIAN_POINT ( 'NONE',  ( 25.64708228042118421, 66.33571787052811430, 91.37028996123288493 ) ) ;
#18016=CARTESIAN_POINT ( 'NONE',  ( 16.05277956358211355, 4.672229451527888600, 143.2298391883442719 ) ) ;
#18018=B_SPLINE_CURVE_WITH_KNOTS ( 'NONE', 3,
 ( #18373, #25033, #20835, #2701 ),
 .UNSPECIFIED., .F., .F.,
 ( 4, 4 ),
 ( 5.221978698409883944E-16, 0.008383748772659984499 ),
 .UNSPECIFIED. ) ;
#18019=CARTESIAN_POINT ( 'NONE',  ( 25.70243777736189017, 34.20488708978098913, 107.6443926015131325 ) ) ;
#18020=LINE ( 'NONE', #22507, #26683 ) ;
#18021=CARTESIAN_POINT ( 'NONE',  ( 1.833485406944043827, -72.09189602597619739, -125.9346397303442728 ) ) ;
#18022=CARTESIAN_POINT ( 'NONE',  ( 1.832998868059890096, -30.69214149074107922, 141.8272129421607985 ) ) ;
#18023=CARTESIAN_POINT ( 'NONE',  ( 1.833691583653495272, -117.6050685739175350, 85.00512109099220481 ) ) ;
#18024=EDGE_CURVE ( 'NONE', #21137, #20144, #26269, .T. ) ;
#18025=ORIENTED_EDGE ( 'NONE', *, *, #7824, .F. ) ;
#18028=FACE_OUTER_BOUND ( 'NONE', #18817, .T. ) ;
#18029=CARTESIAN_POINT ( 'NONE',  ( 109.1586059443104944, 0.006344953511164428892, 0.003127959656212888750 ) ) ;
#18030=CARTESIAN_POINT ( 'NONE',  ( 6.224689322667630975, -147.4941644018829265, 12.92299475786910712 ) ) ;
#18031=CARTESIAN_POINT ( 'NONE',  ( 25.64681081121879203, 83.63051021306002042, -75.86069728268907397 ) ) ;
#18034=ORIENTED_EDGE ( 'NONE', *, *, #4213, .T. ) ;
#18036=CARTESIAN_POINT ( 'NONE',  ( 25.70243777736188306, -12.53519966262558860, 112.2504268534933800 ) ) ;
#18037=VECTOR ( 'NONE', #11112, 1000.000000000000114 ) ;
#18038=ORIENTED_EDGE ( 'NONE', *, *, #23369, .T. ) ;
#18039=CARTESIAN_POINT ( 'NONE',  ( 26.11404676487259024, 24.64483677384848903, 110.5078194225162207 ) ) ;
#18042=EDGE_LOOP ( 'NONE', ( #18780, #15629, #16080, #16947 ) ) ;
#18043=CARTESIAN_POINT ( 'NONE',  ( 1.833838850093427730, -97.09738632348962994, -107.8375672471893125 ) ) ;
#18044=CONICAL_SURFACE ( 'NONE', #4740, 117.6351876552689504, 0.9945805576725580410 ) ;
#18045=ORIENTED_EDGE ( 'NONE', *, *, #3479, .T. ) ;
#18047=CARTESIAN_POINT ( 'NONE',  ( 13.36082413113063083, 22.28175172543560123, 151.2941478187908615 ) ) ;
#18050=VECTOR ( 'NONE', #12709, 1000.000000000000114 ) ;
#18052=CARTESIAN_POINT ( 'NONE',  ( 13.84597867724965070, 121.4327876424627988, -82.31427113894673653 ) ) ;
#18054=EDGE_CURVE ( 'NONE', #9521, #4937, #21676, .T. ) ;
#18055=CIRCLE ( 'NONE', #1530, 151.1787379149930359 ) ;
#18057=CARTESIAN_POINT ( 'NONE',  ( 32.73300124599735739, -110.6325518752276622, 39.98094346392273479 ) ) ;
#18058=CARTESIAN_POINT ( 'NONE',  ( 32.73300124599738581, 99.90245962373917621, -62.10906484417127871 ) ) ;
#18059=VECTOR ( 'NONE', #6602, 1000.000000000000000 ) ;
#18061=ORIENTED_EDGE ( 'NONE', *, *, #5397, .T. ) ;
#18062=CARTESIAN_POINT ( 'NONE',  ( 25.64681081121879203, 103.3177883989779531, 45.54494737132259274 ) ) ;
#18063=CIRCLE ( 'NONE', #4284, 151.1787379149930359 ) ;
#18064=CARTESIAN_POINT ( 'NONE',  ( 25.64681081121879203, 66.70335573067988832, -91.10197563707880875 ) ) ;
#18065=EDGE_CURVE ( 'NONE', #8156, #25619, #21819, .T. ) ;
#18066=CARTESIAN_POINT ( 'NONE',  ( 28.43349137099830415, -119.3601175884732868, -34.52178142065654498 ) ) ;
#18067=CARTESIAN_POINT ( 'NONE',  ( 1.894214914920948400, 86.08679174688076330, 116.8658096527525743 ) ) ;
#18070=CARTESIAN_POINT ( 'NONE',  ( 25.98107933586721074, 110.8834224379717313, -22.45325949158369738 ) ) ;
#18071=B_SPLINE_CURVE_WITH_KNOTS ( 'NONE', 3,
 ( #27792, #12517, #19149, #16561 ),
 .UNSPECIFIED., .F., .F.,
 ( 4, 4 ),
 ( 2.432574717070327228E-16, 0.008383748772659696535 ),
 .UNSPECIFIED. ) ;
#18072=CARTESIAN_POINT ( 'NONE',  ( 1.831572820252008738, 45.77972211429995752, -137.7011124121612795 ) ) ;
#18074=CARTESIAN_POINT ( 'NONE',  ( 32.73300124599740002, 66.00340565729470654, -97.37344512919790418 ) ) ;
#18076=B_SPLINE_CURVE_WITH_KNOTS ( 'NONE', 3,
 ( #18409, #25062, #27186, #2732, #9800, #15833 ),
 .UNSPECIFIED., .F., .F.,
 ( 4, 2, 4 ),
 ( 1.390486644391990834E-17, 0.0006311571484586102343, 0.001262314296917206808 ),
 .UNSPECIFIED. ) ;
#18077=B_SPLINE_CURVE_WITH_KNOTS ( 'NONE', 3,
 ( #3596, #1585, #20729, #18864, #3177, #23206, #16420 ),
 .UNSPECIFIED., .F., .F.,
 ( 4, 3, 4 ),
 ( 5.901834185273117976E-16, 0.02816610861753246139, 0.04000277880656281926 ),
 .UNSPECIFIED. ) ;
#18078=CARTESIAN_POINT ( 'NONE',  ( 16.05277956358202829, -141.9568301782830986, 19.61822947415926066 ) ) ;
#18081=ORIENTED_EDGE ( 'NONE', *, *, #23818, .F. ) ;
#18082=CARTESIAN_POINT ( 'NONE',  ( 109.1778270068192853, -0.007152128381194093436, 0.005967275455169858585 ) ) ;
#18083=EDGE_CURVE ( 'NONE', #18556, #23588, #11995, .T. ) ;
#18084=EDGE_LOOP ( 'NONE', ( #16082, #18913, #8110, #7353 ) ) ;
#18085=CARTESIAN_POINT ( 'NONE',  ( 24.01988960052063149, -117.9135177031533033, -57.17607523395325586 ) ) ;
#18087=DIRECTION ( 'NONE',  ( 0.000000000000000000, 0.000000000000000000, -1.000000000000000000 ) ) ;
#18088=CARTESIAN_POINT ( 'NONE',  ( 1.833485406944043827, 85.72460230293692973, 117.0814567582547596 ) ) ;
#18089=CARTESIAN_POINT ( 'NONE',  ( 25.64703792032468854, -34.74993974077031567, 107.4308312803557470 ) ) ;
#18092=ORIENTED_EDGE ( 'NONE', *, *, #10275, .F. ) ;
#18094=EDGE_CURVE ( 'NONE', #13886, #14457, #24315, .T. ) ;
#18095=CARTESIAN_POINT ( 'NONE',  ( 19.66333377628695089, -60.10102584214464372, 123.9466021833771947 ) ) ;
#18097=CARTESIAN_POINT ( 'NONE',  ( 10.93730112725990011, -146.7718404940640653, -36.23586118136687162 ) ) ;
#18098=EDGE_LOOP ( 'NONE', ( #18280, #20251, #6245, #14163 ) ) ;
#18099=ORIENTED_EDGE ( 'NONE', *, *, #21940, .F. ) ;
#18100=CARTESIAN_POINT ( 'NONE',  ( 25.64681081121879203, -91.10197563707900770, -66.70335573067958990 ) ) ;
#18101=CARTESIAN_POINT ( 'NONE',  ( 25.64692232868534560, 75.79483800045773023, 83.69035111837229124 ) ) ;
#18104=CARTESIAN_POINT ( 'NONE',  ( 25.64700659047694487, -84.06149911284495602, 75.38309044531857239 ) ) ;
#18105=CARTESIAN_POINT ( 'NONE',  ( 1.831572820252008738, 71.69925593429807975, 126.1609924456732159 ) ) ;
#18107=CARTESIAN_POINT ( 'NONE',  ( 26.11404676487257603, 102.9690087468801352, 47.08215554553553517 ) ) ;
#18109=CARTESIAN_POINT ( 'NONE',  ( 10.93730112725943471, 133.3192575531795683, 71.28103789254991796 ) ) ;
#18111=CARTESIAN_POINT ( 'NONE',  ( 32.73300124599735739, -51.32617430724984331, 105.8473486001049224 ) ) ;
#18112=CARTESIAN_POINT ( 'NONE',  ( 2.263178607246659091, 142.5035407554795199, 28.85718361840967461 ) ) ;
#18114=B_SPLINE_CURVE_WITH_KNOTS ( 'NONE', 3,
 ( #685, #16225, #9178, #20400 ),
 .UNSPECIFIED., .F., .F.,
 ( 4, 4 ),
 ( 1.211825722864169544E-16, 0.008383748772659583778 ),
 .UNSPECIFIED. ) ;
#18115=EDGE_CURVE ( 'NONE', #27090, #18454, #27633, .T. ) ;
#18116=CARTESIAN_POINT ( 'NONE',  ( 2.433796855181233454, 133.5135467655518369, 57.85512797797937168 ) ) ;
#18117=VERTEX_POINT ( 'NONE', #13208 ) ;
#18118=CARTESIAN_POINT ( 'NONE',  ( 32.73300124599734318, 116.5274707358856006, 16.10546300444864443 ) ) ;
#18120=EDGE_LOOP ( 'NONE', ( #1374, #1232, #20115, #8231 ) ) ;
#18125=CARTESIAN_POINT ( 'NONE',  ( 109.1587776205901861, -0.006388631651935916360, -0.003592288931003330757 ) ) ;
#18129=ORIENTED_EDGE ( 'NONE', *, *, #555, .F. ) ;
#18134=VERTEX_POINT ( 'NONE', #12934 ) ;
#18135=CARTESIAN_POINT ( 'NONE',  ( 109.1778270068192853, -0.008960903982066578330, -0.002542344697966412732 ) ) ;
#18136=CARTESIAN_POINT ( 'NONE',  ( 2.433796855181205476, 13.76554153471693454, 144.8571464219890004 ) ) ;
#18140=CARTESIAN_POINT ( 'NONE',  ( 109.1592201516379674, -0.001934867487012880598, 0.007620268632968135725 ) ) ;
#18142=DIRECTION ( 'NONE',  ( 0.000000000000000000, 0.000000000000000000, 1.000000000000000000 ) ) ;
#18144=CARTESIAN_POINT ( 'NONE',  ( 2.433796855181205476, 125.2830755159753977, 74.00833731765604284 ) ) ;
#18145=CARTESIAN_POINT ( 'NONE',  ( 2.433796855181205476, -142.6247129145649808, 28.83182736670489987 ) ) ;
#18146=ORIENTED_EDGE ( 'NONE', *, *, #14456, .F. ) ;
#18147=CARTESIAN_POINT ( 'NONE',  ( 2.263178113027049410, -96.24282436106540217, -108.9830942735803063 ) ) ;
#18148=ORIENTED_EDGE ( 'NONE', *, *, #1314, .T. ) ;
#18149=ORIENTED_EDGE ( 'NONE', *, *, #19778, .T. ) ;
#18150=VECTOR ( 'NONE', #112, 1000.000000000000341 ) ;
#18151=ORIENTED_EDGE ( 'NONE', *, *, #26899, .T. ) ;
#18157=CARTESIAN_POINT ( 'NONE',  ( 1.831572820252008738, -144.4165162501764144, 14.18623102066721664 ) ) ;
#18158=B_SPLINE_CURVE_WITH_KNOTS ( 'NONE', 3,
 ( #5950, #23930, #6232, #1884, #19173, #12821, #16883, #14852, #21608, #8111 ),
 .UNSPECIFIED., .F., .F.,
 ( 4, 3, 3, 4 ),
 ( 5.594315114139762021E-17, 0.0002669559177086202858, 0.0005339118354150952607, 0.001067817517169147769 ),
 .UNSPECIFIED. ) ;
#18159=FACE_OUTER_BOUND ( 'NONE', #26910, .T. ) ;
#18162=CARTESIAN_POINT ( 'NONE',  ( 1.833838848569444124, 132.6367525013577051, 58.85887272891235966 ) ) ;
#18163=CARTESIAN_POINT ( 'NONE',  ( 2.263178607246685736, -133.3897506477018169, -57.85473702627246695 ) ) ;
#18164=CARTESIAN_POINT ( 'NONE',  ( 1.894214914920938408, 59.90782071839196021, 132.2104617488239455 ) ) ;
#18167=VERTEX_POINT ( 'NONE', #7046 ) ;
#18169=DIRECTION ( 'NONE',  ( -1.000000000000000000, -0.000000000000000000, -0.000000000000000000 ) ) ;
#18170=CARTESIAN_POINT ( 'NONE',  ( 19.66333377628715340, 84.55762186019687476, -108.7423656420548213 ) ) ;
#18171=CARTESIAN_POINT ( 'NONE',  ( 2.430230287190572103, -144.8619874886007892, 13.76600171652595428 ) ) ;
#18172=CARTESIAN_POINT ( 'NONE',  ( 6.224689322667647851, 111.7293398381264922, 97.14981701196357733 ) ) ;
#18173=ORIENTED_EDGE ( 'NONE', *, *, #17410, .F. ) ;
#18174=CARTESIAN_POINT ( 'NONE',  ( 6.224689322667647851, 148.0369967195762797, -2.565137105444267540 ) ) ;
#18175=ORIENTED_EDGE ( 'NONE', *, *, #5165, .F. ) ;
#18177=CARTESIAN_POINT ( 'NONE',  ( 32.73300124599735739, -103.7392577722179823, 55.46353551261974957 ) ) ;
#18178=ORIENTED_EDGE ( 'NONE', *, *, #13947, .F. ) ;
#18181=ORIENTED_EDGE ( 'NONE', *, *, #27970, .T. ) ;
#18184=EDGE_CURVE ( 'NONE', #9343, #6084, #830, .T. ) ;
#18186=ORIENTED_EDGE ( 'NONE', *, *, #28040, .T. ) ;
#18187=CARTESIAN_POINT ( 'NONE',  ( 2.433796855181233454, 13.76554153471886366, -144.8571464219887730 ) ) ;
#18190=CARTESIAN_POINT ( 'NONE',  ( 2.108393763691160494, 137.7805780486507103, 46.11438684123211118 ) ) ;
#18191=CARTESIAN_POINT ( 'NONE',  ( 1.833838848569417257, 30.34409872482234860, 141.9017642089166600 ) ) ;
#18192=CARTESIAN_POINT ( 'NONE',  ( 1.833691583653550783, -72.24637705290399481, -125.8462703805706440 ) ) ;
#18193=CARTESIAN_POINT ( 'NONE',  ( 32.73300124599732186, 0.000000000000000000, 0.000000000000000000 ) ) ;
#18196=CARTESIAN_POINT ( 'NONE',  ( 26.11404676487257603, -1.130420376097928115, 113.2169081140373947 ) ) ;
#18197=CARTESIAN_POINT ( 'NONE',  ( 25.64681081121879203, 83.63051021305903987, 75.86069728269016821 ) ) ;
#18198=ORIENTED_EDGE ( 'NONE', *, *, #22245, .T. ) ;
#18201=CARTESIAN_POINT ( 'NONE',  ( 26.11404676487257603, 45.01677474591409833, 103.8885755249570906 ) ) ;
#18202=CARTESIAN_POINT ( 'NONE',  ( 1.894214914920928416, 0.9536781033360174353, 145.1469726764545385 ) ) ;
#18203=CARTESIAN_POINT ( 'NONE',  ( 10.93730112725932635, 0.000000000000000000, 0.000000000000000000 ) ) ;
#18205=EDGE_LOOP ( 'NONE', ( #23792, #8389, #13161, #8787 ) ) ;
#18206=CARTESIAN_POINT ( 'NONE',  ( 5.340103556456485379, -47.74933482044465194, 139.5040934094288616 ) ) ;
#18207=CARTESIAN_POINT ( 'NONE',  ( 109.1586059443104944, -0.007058870754606105975, 0.0004635842312890713491 ) ) ;
#18208=CARTESIAN_POINT ( 'NONE',  ( 30.58324630866342630, -87.19147450740413774, 83.81536267638921345 ) ) ;
#18210=CARTESIAN_POINT ( 'NONE',  ( 25.64692872815577473, 75.79105864157502026, -83.69378511050487646 ) ) ;
#18215=DIRECTION ( 'NONE',  ( 0.000000000000000000, 0.000000000000000000, 1.000000000000000000 ) ) ;
#18218=LINE ( 'NONE', #7452, #26262 ) ;
#18219=VERTEX_POINT ( 'NONE', #5436 ) ;
#18220=EDGE_CURVE ( 'NONE', #22412, #709, #21280, .T. ) ;
#18221=( BOUNDED_SURFACE ( )  B_SPLINE_SURFACE ( 3, 1, ( 
 ( #19951, #511 ),
 ( #20512, #17780 ),
 ( #15913, #15604 ),
 ( #4970, #24852 ) ),
 .UNSPECIFIED., .F., .F., .F. ) 
 B_SPLINE_SURFACE_WITH_KNOTS ( ( 4, 4 ),
 ( 2, 2 ),
 ( 0.000000000000000000, 1.000000000000000000 ),
 ( 0.000000000000000000, 1.000000000000000000 ),
 .UNSPECIFIED. ) 
 GEOMETRIC_REPRESENTATION_ITEM ( )  RATIONAL_B_SPLINE_SURFACE ( (
 ( 1.000000000000000000, 1.000000000000000000),
 ( 0.9956975270656954757, 0.8568959468854893125),
 ( 0.9956975270656954757, 0.8568959468854893125),
 ( 1.000000000000000000, 1.000000000000000000) ) ) 
 REPRESENTATION_ITEM ( '' )  SURFACE ( )  );
#18222=CARTESIAN_POINT ( 'NONE',  ( 32.73300124599734318, 81.52272205837205377, 84.80615050150403533 ) ) ;
#18224=DIRECTION ( 'NONE',  ( 0.5914120900931444380, 0.2567974902965144413, -0.7643865440136096145 ) ) ;
#18227=B_SPLINE_CURVE_WITH_KNOTS ( 'NONE', 3,
 ( #17879, #6832, #26392, #9122, #15296, #15575, #6693 ),
 .UNSPECIFIED., .F., .F.,
 ( 4, 3, 4 ),
 ( 5.185633697872110560E-16, 0.02816610861753246139, 0.04000277880656268048 ),
 .UNSPECIFIED. ) ;
#18230=DIRECTION ( 'NONE',  ( -1.000000000000000000, -0.000000000000000000, -0.000000000000000000 ) ) ;
#18235=CARTESIAN_POINT ( 'NONE',  ( 1.831572820252009626, 16.14965423926210519, 144.2101521542831222 ) ) ;
#18237=CARTESIAN_POINT ( 'NONE',  ( 24.01988960052073807, 44.53753990739662072, -123.2441023955610433 ) ) ;
#18238=CARTESIAN_POINT ( 'NONE',  ( 1.833750490713709880, 144.2866297127912958, 15.43355859895708093 ) ) ;
#18239=CARTESIAN_POINT ( 'NONE',  ( 1.833485406944057594, 108.1939177044926055, 96.69979900902202985 ) ) ;
#18242=CARTESIAN_POINT ( 'NONE',  ( 10.93730112725990367, -142.1801301103781157, -51.37919228020433593 ) ) ;
#18244=CARTESIAN_POINT ( 'NONE',  ( 109.1587776205901577, -0.006944419901758109442, -0.002343968083389333292 ) ) ;
#18245=FACE_OUTER_BOUND ( 'NONE', #17254, .T. ) ;
#18247=CARTESIAN_POINT ( 'NONE',  ( 109.1592201516379674, -0.0005146241775907877628, 0.007845213074660000591 ) ) ;
#18248=CARTESIAN_POINT ( 'NONE',  ( 13.36082413113063083, -37.97423473099187419, -148.1362653801006957 ) ) ;
#18252=EDGE_CURVE ( 'NONE', #15678, #23588, #26731, .T. ) ;
#18254=B_SPLINE_CURVE_WITH_KNOTS ( 'NONE', 3,
 ( #23033, #22895, #20858, #23319 ),
 .UNSPECIFIED., .F., .F.,
 ( 4, 4 ),
 ( 0.000000000000000000, 0.008383560773332696461 ),
 .UNSPECIFIED. ) ;
#18256=DIRECTION ( 'NONE',  ( -1.000000000000000000, -0.000000000000000000, -0.000000000000000000 ) ) ;
#18258=( BOUNDED_SURFACE ( )  B_SPLINE_SURFACE ( 3, 1, ( 
 ( #19226, #15459 ),
 ( #28140, #24130 ),
 ( #6420, #23721 ),
 ( #10464, #10597 ) ),
 .UNSPECIFIED., .F., .F., .F. ) 
 B_SPLINE_SURFACE_WITH_KNOTS ( ( 4, 4 ),
 ( 2, 2 ),
 ( 0.000000000000000000, 1.000000000000000000 ),
 ( 0.000000000000000000, 1.000000000000000000 ),
 .UNSPECIFIED. ) 
 GEOMETRIC_REPRESENTATION_ITEM ( )  RATIONAL_B_SPLINE_SURFACE ( (
 ( 1.000000000000000000, 1.000000000000000000),
 ( 0.6386103224230302855, 0.9954351624131538845),
 ( 0.6386103224230302855, 0.9954351624131538845),
 ( 1.000000000000000000, 1.000000000000000000) ) ) 
 REPRESENTATION_ITEM ( '' )  SURFACE ( )  );
#18260=CARTESIAN_POINT ( 'NONE',  ( 1.833721034905679392, 125.4904194343094446, -72.86293192427356757 ) ) ;
#18261=CARTESIAN_POINT ( 'NONE',  ( 21.16825799904898986, 115.0183107335399768, -71.50503315297764573 ) ) ;
#18263=CARTESIAN_POINT ( 'NONE',  ( 109.1587776205901577, 0.005390665547499365502, 0.004965871434389470748 ) ) ;
#18264=ORIENTED_EDGE ( 'NONE', *, *, #7093, .F. ) ;
#18265=ORIENTED_EDGE ( 'NONE', *, *, #22023, .F. ) ;
#18268=CARTESIAN_POINT ( 'NONE',  ( 10.93730112726006176, 146.7718404940648611, -36.23586118136403655 ) ) ;
#18270=CARTESIAN_POINT ( 'NONE',  ( 109.1587776205901861, -0.007328861771499511728, 8.330235398543782790E-05 ) ) ;
#18271=CARTESIAN_POINT ( 'NONE',  ( 1.833838848569429247, -137.9525894882060584, 45.01064392477885434 ) ) ;
#18272=ORIENTED_EDGE ( 'NONE', *, *, #26924, .T. ) ;
#18273=CARTESIAN_POINT ( 'NONE',  ( 25.64681081121880624, 35.28660243342550729, 107.2555980796242494 ) ) ;
#18274=CARTESIAN_POINT ( 'NONE',  ( 1.833206308920082739, 15.90849808442071023, -144.2348261777514153 ) ) ;
#18277=CARTESIAN_POINT ( 'NONE',  ( 25.87036335909427365, -107.8283083010001491, -33.99475147239120787 ) ) ;
#18278=EDGE_CURVE ( 'NONE', #10583, #3526, #26879, .T. ) ;
#18280=ORIENTED_EDGE ( 'NONE', *, *, #21932, .F. ) ;
#18281=CARTESIAN_POINT ( 'NONE',  ( 1.833691583653554336, 145.1092556475514073, 0.3559373310799965884 ) ) ;
#18282=ORIENTED_EDGE ( 'NONE', *, *, #24195, .F. ) ;
#18283=EDGE_CURVE ( 'NONE', #15966, #19470, #11323, .T. ) ;
#18284=ORIENTED_EDGE ( 'NONE', *, *, #25084, .F. ) ;
#18286=CARTESIAN_POINT ( 'NONE',  ( 109.1592201516379674, -0.0005146241775983334847, -0.007845213074654432128 ) ) ;
#18290=B_SPLINE_CURVE_WITH_KNOTS ( 'NONE', 3,
 ( #8588, #24140, #21685, #26007, #21402, #6169, #4262, #1955, #19521, #28426 ),
 .UNSPECIFIED., .F., .F.,
 ( 4, 3, 3, 4 ),
 ( 1.387778780781445676E-17, 0.0002669559177086201773, 0.0005339118354150702156, 0.001067817517169167285 ),
 .UNSPECIFIED. ) ;
#18291=CARTESIAN_POINT ( 'NONE',  ( 1.834118845439484335, -107.9567937753786708, -96.96525081350110042 ) ) ;
#18292=CARTESIAN_POINT ( 'NONE',  ( 32.73300124599735739, 32.68291970228236920, 113.0038235389603472 ) ) ;
#18293=CARTESIAN_POINT ( 'NONE',  ( 26.11404676487257603, -36.06104232266525145, 107.3263591096429082 ) ) ;
#18294=CARTESIAN_POINT ( 'NONE',  ( 25.64681081121879203, 112.9102952884414464, 0.4157506337731812773 ) ) ;
#18295=CARTESIAN_POINT ( 'NONE',  ( 1.832998868059890096, 132.7810136645738055, 58.53348008137691494 ) ) ;
#18296=CARTESIAN_POINT ( 'NONE',  ( 2.430230287190589422, 137.9371479820468949, -46.34481016236680517 ) ) ;
#18297=( BOUNDED_SURFACE ( )  B_SPLINE_SURFACE ( 3, 1, ( 
 ( #21955, #21392 ),
 ( #19511, #8576 ),
 ( #1664, #14905 ),
 ( #15172, #23993 ) ),
 .UNSPECIFIED., .F., .F., .F. ) 
 B_SPLINE_SURFACE_WITH_KNOTS ( ( 4, 4 ),
 ( 2, 2 ),
 ( 0.000000000000000000, 1.000000000000000000 ),
 ( 0.000000000000000000, 1.000000000000000000 ),
 .UNSPECIFIED. ) 
 GEOMETRIC_REPRESENTATION_ITEM ( )  RATIONAL_B_SPLINE_SURFACE ( (
 ( 1.000000000000000000, 1.000000000000000000),
 ( 0.9956975270656954757, 0.8568959468854893125),
 ( 0.9956975270656954757, 0.8568959468854893125),
 ( 1.000000000000000000, 1.000000000000000000) ) ) 
 REPRESENTATION_ITEM ( '' )  SURFACE ( )  );
#18300=CARTESIAN_POINT ( 'NONE',  ( 2.433796855181205476, -116.8607839509050734, -86.69855925934092511 ) ) ;
#18301=CIRCLE ( 'NONE', #858, 117.6351876552689504 ) ;
#18304=CARTESIAN_POINT ( 'NONE',  ( 109.1721716018069515, 0.01665253177025271744, 0.003746085893651872681 ) ) ;
#18307=CARTESIAN_POINT ( 'NONE',  ( 109.1721716018069515, 0.01127028715939371907, 0.01281875973823906091 ) ) ;
#18308=CARTESIAN_POINT ( 'NONE',  ( 109.1592201516379674, 0.001331853079201392653, -0.007748443302134886378 ) ) ;
#18309=CARTESIAN_POINT ( 'NONE',  ( 109.1592201516379674, -0.002134489919774417484, -0.007566779963318545632 ) ) ;
#18310=EDGE_CURVE ( 'NONE', #24736, #14545, #10474, .T. ) ;
#18315=CARTESIAN_POINT ( 'NONE',  ( 24.22246935314087324, 1.405874241570340095E-14, 111.9614997405030152 ) ) ;
#18317=B_SPLINE_CURVE_WITH_KNOTS ( 'NONE', 3,
 ( #22662, #2929, #11707, #18300 ),
 .UNSPECIFIED., .F., .F.,
 ( 4, 4 ),
 ( 0.000000000000000000, 0.01077107196513875549 ),
 .UNSPECIFIED. ) ;
#18319=ORIENTED_EDGE ( 'NONE', *, *, #19898, .T. ) ;
#18322=CARTESIAN_POINT ( 'NONE',  ( 9.884929003653626367, 91.84919534721940693, 119.2676479132376954 ) ) ;
#18324=CARTESIAN_POINT ( 'NONE',  ( 1.833750490713699444, 144.3424379351782534, -14.90257883162603925 ) ) ;
#18327=CARTESIAN_POINT ( 'NONE',  ( 1.833485406944043827, -72.09189602597619739, -125.9346397303442728 ) ) ;
#18329=CARTESIAN_POINT ( 'NONE',  ( 2.433796855181205476, -86.69855925934052721, 116.8607839509053434 ) ) ;
#18331=CARTESIAN_POINT ( 'NONE',  ( 1.833206308920039662, 58.34024961171237322, 132.8652726225755032 ) ) ;
#18332=CARTESIAN_POINT ( 'NONE',  ( 109.1586059443104944, 0.004378796245590010905, 0.005555961672773786220 ) ) ;
#18333=EDGE_CURVE ( 'NONE', #14920, #25928, #3555, .T. ) ;
#18334=VERTEX_POINT ( 'NONE', #8051 ) ;
#18335=EDGE_LOOP ( 'NONE', ( #24583, #27979, #12392, #26898 ) ) ;
#18336=CARTESIAN_POINT ( 'NONE',  ( 55.79472521941428198, -35.74479459808892301, 63.36760613016212318 ) ) ;
#18337=EDGE_CURVE ( 'NONE', #16763, #10758, #17078, .T. ) ;
#18339=CARTESIAN_POINT ( 'NONE',  ( 109.1592201516379674, -0.003661068210037343815, -0.006957642258146904887 ) ) ;
#18341=CARTESIAN_POINT ( 'NONE',  ( 24.01988960052067767, 31.41104197353493532, -127.2243989116370386 ) ) ;
#18345=DIRECTION ( 'NONE',  ( 0.000000000000000000, 0.000000000000000000, 1.000000000000000000 ) ) ;
#18347=CARTESIAN_POINT ( 'NONE',  ( 109.1587776205901577, 0.007186028091163433260, -0.001442274045003928652 ) ) ;
#18348=CARTESIAN_POINT ( 'NONE',  ( 32.73300124599737160, -84.80615050150427692, 81.52272205837169849 ) ) ;
#18353=DIRECTION ( 'NONE',  ( 0.000000000000000000, 1.000000000000000000, 3.122502256758243698E-15 ) ) ;
#18356=CARTESIAN_POINT ( 'NONE',  ( 2.433796855181219243, -132.3327394885235435, 60.50726454507858421 ) ) ;
#18357=ORIENTED_EDGE ( 'NONE', *, *, #12080, .T. ) ;
#18360=CARTESIAN_POINT ( 'NONE',  ( 10.93730112726005821, 140.0398180619120865, -56.95489579269602842 ) ) ;
#18361=ORIENTED_EDGE ( 'NONE', *, *, #4387, .F. ) ;
#18367=CARTESIAN_POINT ( 'NONE',  ( 25.64681081121879203, 112.3352186517032294, -11.38886654529559017 ) ) ;
#18369=B_SPLINE_CURVE_WITH_KNOTS ( 'NONE', 3,
 ( #2152, #157, #15680, #2444, #24493, #2590, #24345, #4464 ),
 .UNSPECIFIED., .F., .F.,
 ( 4, 2, 2, 4 ),
 ( 0.000000000000000000, 0.0002429592666046768957, 0.0004859185332093537914, 0.0009718370664186768999 ),
 .UNSPECIFIED. ) ;
#18370=VERTEX_POINT ( 'NONE', #16943 ) ;
#18371=CARTESIAN_POINT ( 'NONE',  ( 28.37644542392835945, -54.25112470585808211, 111.8804331835014239 ) ) ;
#18373=CARTESIAN_POINT ( 'NONE',  ( 32.73300124599739291, -3.836798148478013371, -117.5726003567929610 ) ) ;
#18374=ORIENTED_EDGE ( 'NONE', *, *, #7772, .F. ) ;
#18376=ORIENTED_EDGE ( 'NONE', *, *, #4387, .T. ) ;
#18380=CARTESIAN_POINT ( 'NONE',  ( 32.73300124599732186, 0.000000000000000000, 0.000000000000000000 ) ) ;
#18381=B_SPLINE_CURVE_WITH_KNOTS ( 'NONE', 3,
 ( #3037, #18414, #1160, #9649 ),
 .UNSPECIFIED., .F., .F.,
 ( 4, 4 ),
 ( 5.516747950212996126E-16, 0.008383748772659998377 ),
 .UNSPECIFIED. ) ;
#18382=CARTESIAN_POINT ( 'NONE',  ( 10.93730112726007775, 51.37919228020501805, -142.1801301103781725 ) ) ;
#18384=CARTESIAN_POINT ( 'NONE',  ( 1.833603222531973387, 107.5392551439154545, 97.42748212378315031 ) ) ;
#18385=CARTESIAN_POINT ( 'NONE',  ( 32.73300124599732186, 0.000000000000000000, 0.000000000000000000 ) ) ;
#18386=ORIENTED_EDGE ( 'NONE', *, *, #9347, .F. ) ;
#18387=CARTESIAN_POINT ( 'NONE',  ( 2.430230287190589422, -142.6294793592095687, -28.83279105684573551 ) ) ;
#18390=CARTESIAN_POINT ( 'NONE',  ( 6.224689322667630975, 147.4941644018829834, -12.92299475786806973 ) ) ;
#18392=( BOUNDED_SURFACE ( )  B_SPLINE_SURFACE ( 3, 1, ( 
 ( #13632, #19973 ),
 ( #22139, #22432 ),
 ( #2402, #24606 ),
 ( #20399, #11199 ) ),
 .UNSPECIFIED., .F., .F., .F. ) 
 B_SPLINE_SURFACE_WITH_KNOTS ( ( 4, 4 ),
 ( 2, 2 ),
 ( 0.000000000000000000, 1.000000000000000000 ),
 ( 0.000000000000000000, 1.000000000000000000 ),
 .UNSPECIFIED. ) 
 GEOMETRIC_REPRESENTATION_ITEM ( )  RATIONAL_B_SPLINE_SURFACE ( (
 ( 1.000000000000000000, 1.000000000000000000),
 ( 0.6386103224230316178, 0.9954351624131538845),
 ( 0.6386103224230316178, 0.9954351624131538845),
 ( 1.000000000000000000, 1.000000000000000000) ) ) 
 REPRESENTATION_ITEM ( '' )  SURFACE ( )  );
#18394=CARTESIAN_POINT ( 'NONE',  ( 26.11404676487257603, 110.5078194225164481, -24.64483677384740545 ) ) ;
#18398=CARTESIAN_POINT ( 'NONE',  ( 1.833838850855486591, -30.08297881069573521, -141.9572669680998160 ) ) ;
#18399=DIRECTION ( 'NONE',  ( -0.5914120900931443270, -0.8010740644654243958, 0.09226095020377671208 ) ) ;
#18400=ORIENTED_EDGE ( 'NONE', *, *, #16545, .F. ) ;
#18402=( BOUNDED_SURFACE ( )  B_SPLINE_SURFACE ( 3, 1, ( 
 ( #18840, #10226 ),
 ( #3722, #14652 ),
 ( #27899, #23457 ),
 ( #12633, #27766 ) ),
 .UNSPECIFIED., .F., .F., .F. ) 
 B_SPLINE_SURFACE_WITH_KNOTS ( ( 4, 4 ),
 ( 2, 2 ),
 ( 0.000000000000000000, 1.000000000000000000 ),
 ( 0.000000000000000000, 1.000000000000000000 ),
 .UNSPECIFIED. ) 
 GEOMETRIC_REPRESENTATION_ITEM ( )  RATIONAL_B_SPLINE_SURFACE ( (
 ( 1.000000000000000000, 1.000000000000000000),
 ( 0.6386103224230316178, 0.9954351624131538845),
 ( 0.6386103224230316178, 0.9954351624131538845),
 ( 1.000000000000000000, 1.000000000000000000) ) ) 
 REPRESENTATION_ITEM ( '' )  SURFACE ( )  );
#18403=ORIENTED_EDGE ( 'NONE', *, *, #1237, .T. ) ;
#18405=CARTESIAN_POINT ( 'NONE',  ( 109.1624594426973118, -0.01154818537151447444, 0.01102230012606822233 ) ) ;
#18406=CARTESIAN_POINT ( 'NONE',  ( 25.64708010899962787, -23.52908206539823155, -110.4325102642037564 ) ) ;
#18407=CARTESIAN_POINT ( 'NONE',  ( 109.1624594426973260, 0.0004639210235575793413, -0.01595733256931100227 ) ) ;
#18408=AXIS2_PLACEMENT_3D ( 'NONE', #22778, #14102, #869 ) ;
#18409=CARTESIAN_POINT ( 'NONE',  ( 1.833485406944057594, 58.53321471327059555, -132.7804117027882285 ) ) ;
#18410=CARTESIAN_POINT ( 'NONE',  ( 1.833603222531960286, 125.8904991419477142, -72.16916166673607336 ) ) ;
#18411=ORIENTED_EDGE ( 'NONE', *, *, #21879, .T. ) ;
#18412=AXIS2_PLACEMENT_3D ( 'NONE', #15207, #25899, #24028 ) ;
#18413=CARTESIAN_POINT ( 'NONE',  ( 109.1592201516379674, -0.003476928926125439582, 0.007051465909551701133 ) ) ;
#18414=CARTESIAN_POINT ( 'NONE',  ( 30.59138290137910943, 21.51300488027276003, -114.2039707400271595 ) ) ;
#18420=EDGE_CURVE ( 'NONE', #1094, #10623, #27113, .T. ) ;
#18421=CARTESIAN_POINT ( 'NONE',  ( 26.11404676487257603, 90.92995828888292920, -67.46175819463273626 ) ) ;
#18422=CARTESIAN_POINT ( 'NONE',  ( 55.49584447822657296, 62.69727227546400883, 36.50733923851220197 ) ) ;
#18423=LINE ( 'NONE', #22298, #12528 ) ;
#18424=CARTESIAN_POINT ( 'NONE',  ( 109.1586900883932856, 0.006130969560693664243, 0.003656351050324906093 ) ) ;
#18428=VERTEX_POINT ( 'NONE', #86 ) ;
#18429=CARTESIAN_POINT ( 'NONE',  ( 1.833750490713684345, 58.77746103890281404, 132.6726660571946184 ) ) ;
#18430=FACE_OUTER_BOUND ( 'NONE', #19108, .T. ) ;
#18431=EDGE_CURVE ( 'NONE', #3869, #16027, #14732, .T. ) ;
#18432=EDGE_CURVE ( 'NONE', #6423, #21210, #13713, .T. ) ;
#18434=CARTESIAN_POINT ( 'NONE',  ( 109.1624594426973118, -0.006066618937910808231, 0.01476644236456995697 ) ) ;
#18438=CARTESIAN_POINT ( 'NONE',  ( 25.64681081121879203, 23.06870491922322230, 110.5293738517609228 ) ) ;
#18443=B_SPLINE_CURVE_WITH_KNOTS ( 'NONE', 3,
 ( #5296, #9773, #10057, #20972, #20551, #27592, #833, #23020, #9917, #10211 ),
 .UNSPECIFIED., .F., .F.,
 ( 4, 3, 3, 4 ),
 ( 1.214306433183764966E-17, 0.0002669560319015731767, 0.0005492286108966349485, 0.0008315040496093412115 ),
 .UNSPECIFIED. ) ;
#18444=EDGE_LOOP ( 'NONE', ( #4818, #5828, #4865, #7618 ) ) ;
#18445=ORIENTED_EDGE ( 'NONE', *, *, #23096, .F. ) ;
#18448=EDGE_CURVE ( 'NONE', #5027, #16169, #9979, .T. ) ;
#18451=CARTESIAN_POINT ( 'NONE',  ( 1.833206310202340816, -126.0392056382537191, -71.90885922990283063 ) ) ;
#18454=VERTEX_POINT ( 'NONE', #4690 ) ;
#18455=CIRCLE ( 'NONE', #5584, 117.6351876552689504 ) ;
#18458=CARTESIAN_POINT ( 'NONE',  ( 1.893872463202046275, 108.5026245911431744, -96.41404152942830308 ) ) ;
#18459=ADVANCED_FACE ( 'NONE', ( #6857 ), #28077, .T. ) ;
#18461=EDGE_CURVE ( 'NONE', #26821, #19892, #17836, .T. ) ;
#18463=CARTESIAN_POINT ( 'NONE',  ( 32.73300124599738581, -28.19767303745521758, -114.2056417606550696 ) ) ;
#18467=CARTESIAN_POINT ( 'NONE',  ( 109.1778270068192853, 0.007152128381195953059, 0.005967275455179350992 ) ) ;
#18469=CARTESIAN_POINT ( 'NONE',  ( 2.433796855181205476, -84.34988187690851191, -118.5671979538065273 ) ) ;
#18470=CARTESIAN_POINT ( 'NONE',  ( 13.36082413113063083, -97.52406103376836199, 117.7941133658635238 ) ) ;
#18472=ORIENTED_EDGE ( 'NONE', *, *, #1529, .T. ) ;
#18473=CARTESIAN_POINT ( 'NONE',  ( 30.58324630866342630, 28.99049605145726360, 117.4177132550297387 ) ) ;
#18474=ORIENTED_EDGE ( 'NONE', *, *, #13404, .F. ) ;
#18477=ORIENTED_EDGE ( 'NONE', *, *, #15865, .F. ) ;
#18478=ORIENTED_EDGE ( 'NONE', *, *, #13806, .T. ) ;
#18480=AXIS2_PLACEMENT_3D ( 'NONE', #17340, #9142, #11730 ) ;
#18482=CARTESIAN_POINT ( 'NONE',  ( 109.1586900883932856, 0.005371970278523965393, -0.004701023939953875505 ) ) ;
#18483=CONICAL_SURFACE ( 'NONE', #9766, 117.6351876552689504, 0.9945805576725580410 ) ;
#18484=CARTESIAN_POINT ( 'NONE',  ( 32.73300124599732186, 0.000000000000000000, 0.000000000000000000 ) ) ;
#18486=EDGE_CURVE ( 'NONE', #19810, #10856, #24391, .T. ) ;
#18487=CARTESIAN_POINT ( 'NONE',  ( 1.833721034905633651, 30.51809396651017181, 141.8643653601971550 ) ) ;
#18488=EDGE_CURVE ( 'NONE', #24385, #23267, #3443, .T. ) ;
#18489=CARTESIAN_POINT ( 'NONE',  ( 1.833206310202321498, 71.90885922990329959, -126.0392056382534633 ) ) ;
#18490=CARTESIAN_POINT ( 'NONE',  ( 109.1586059443104944, -0.006344953511159748608, 0.003127959656220974296 ) ) ;
#18492=DIRECTION ( 'NONE',  ( -1.000000000000000000, -0.000000000000000000, -0.000000000000000000 ) ) ;
#18494=DIRECTION ( 'NONE',  ( -1.000000000000000000, -0.000000000000000000, -0.000000000000000000 ) ) ;
#18496=ORIENTED_EDGE ( 'NONE', *, *, #18283, .T. ) ;
#18498=CARTESIAN_POINT ( 'NONE',  ( 1.833838848569443014, 85.43736077718862987, 117.2916552720321448 ) ) ;
#18499=CARTESIAN_POINT ( 'NONE',  ( 25.64704443564076186, -91.42548471394241005, 66.25951665433258597 ) ) ;
#18500=CARTESIAN_POINT ( 'NONE',  ( 30.59138290137906324, -38.47117663195886195, -109.6600423140545786 ) ) ;
#18502=VERTEX_POINT ( 'NONE', #24139 ) ;
#18504=EDGE_LOOP ( 'NONE', ( #16203, #22046, #18509, #6088 ) ) ;
#18505=CARTESIAN_POINT ( 'NONE',  ( 2.430230287190581429, 126.7388733285354760, -71.49654683843377256 ) ) ;
#18506=AXIS2_PLACEMENT_3D ( 'NONE', #23531, #16896, #1206 ) ;
#18507=CARTESIAN_POINT ( 'NONE',  ( 2.430230287190581429, 144.5585181921885862, 16.65331920325786896 ) ) ;
#18508=DIRECTION ( 'NONE',  ( 0.5946245182733607137, 0.5955128528260739129, 0.5401723099040939280 ) ) ;
#18509=ORIENTED_EDGE ( 'NONE', *, *, #26281, .T. ) ;
#18510=CARTESIAN_POINT ( 'NONE',  ( 10.93730112725994275, -26.59437931460641025, -148.8212007290665042 ) ) ;
#18511=CARTESIAN_POINT ( 'NONE',  ( 1.833485406944043827, -144.3694338680886062, 14.63699153649312201 ) ) ;
#18512=CARTESIAN_POINT ( 'NONE',  ( 55.49584447822657296, -53.73688382046297818, 48.74506217377864203 ) ) ;
#18514=B_SPLINE_CURVE_WITH_KNOTS ( 'NONE', 3,
 ( #18643, #21072, #18932, #10832, #16783, #1357 ),
 .UNSPECIFIED., .F., .F.,
 ( 4, 2, 4 ),
 ( 6.071532165918824830E-18, 0.0006311636237756803203, 0.001262327247551354569 ),
 .UNSPECIFIED. ) ;
#18515=EDGE_LOOP ( 'NONE', ( #8178, #19277, #2430, #6730 ) ) ;
#18517=AXIS2_PLACEMENT_3D ( 'NONE', #8397, #6106, #19049 ) ;
#18518=EDGE_CURVE ( 'NONE', #26365, #21439, #8236, .T. ) ;
#18519=ORIENTED_EDGE ( 'NONE', *, *, #17979, .T. ) ;
#18523=ORIENTED_EDGE ( 'NONE', *, *, #20403, .F. ) ;
#18526=ADVANCED_FACE ( 'NONE', ( #19376 ), #15525, .F. ) ;
#18527=FACE_OUTER_BOUND ( 'NONE', #22490, .T. ) ;
#18528=FACE_OUTER_BOUND ( 'NONE', #19322, .T. ) ;
#18530=ORIENTED_EDGE ( 'NONE', *, *, #653, .F. ) ;
#18531=B_SPLINE_CURVE_WITH_KNOTS ( 'NONE', 3,
 ( #23338, #27629, #27783, #25634, #19273, #9952, #10505, #5773, #14530, #28045 ),
 .UNSPECIFIED., .F., .F.,
 ( 4, 3, 3, 4 ),
 ( 1.387778780781445676E-17, 0.0002669559177086277667, 0.0005339118354151018743, 0.001067817517169159262 ),
 .UNSPECIFIED. ) ;
#18532=EDGE_CURVE ( 'NONE', #21438, #22199, #20079, .T. ) ;
#18537=ORIENTED_EDGE ( 'NONE', *, *, #4777, .F. ) ;
#18542=DIRECTION ( 'NONE',  ( -1.000000000000000000, -0.000000000000000000, -0.000000000000000000 ) ) ;
#18545=CARTESIAN_POINT ( 'NONE',  ( 30.58324630866342986, -8.712468656081444607, 120.6294372749320161 ) ) ;
#18547=CARTESIAN_POINT ( 'NONE',  ( 32.73300124599735739, -39.98094346392385745, 110.6325518752272501 ) ) ;
#18549=CARTESIAN_POINT ( 'NONE',  ( 32.73300124599734318, 105.8473486001051072, 51.32617430724947383 ) ) ;
#18551=CARTESIAN_POINT ( 'NONE',  ( 25.70243777736188306, -66.98101477609066023, 90.94412140945929934 ) ) ;
#18552=PLANE ( 'NONE',  #4981 ) ;
#18553=DIRECTION ( 'NONE',  ( -0.5946245182733607137, -0.002950380665379280162, -0.8039981203473693938 ) ) ;
#18554=CARTESIAN_POINT ( 'NONE',  ( 1.833485406944057594, 15.69895494453384721, 144.2578170162063884 ) ) ;
#18555=CARTESIAN_POINT ( 'NONE',  ( 32.73300124599734318, 108.9684813982489118, 44.31599526637995012 ) ) ;
#18556=VERTEX_POINT ( 'NONE', #18062 ) ;
#18559=VECTOR ( 'NONE', #19751, 1000.000000000000000 ) ;
#18561=CARTESIAN_POINT ( 'NONE',  ( 26.28373643307435614, 55.65614982951275636, 114.7784771129672379 ) ) ;
#18562=ORIENTED_EDGE ( 'NONE', *, *, #3617, .T. ) ;
#18563=EDGE_LOOP ( 'NONE', ( #4082, #19671, #4718, #18975 ) ) ;
#18564=EDGE_CURVE ( 'NONE', #12372, #23363, #11446, .T. ) ;
#18570=CARTESIAN_POINT ( 'NONE',  ( 25.87036335909426654, 97.41424496619603701, -57.38512068812907074 ) ) ;
#18574=ADVANCED_FACE ( 'NONE', ( #2689 ), #20361, .T. ) ;
#18575=CARTESIAN_POINT ( 'NONE',  ( 26.11404676487259024, -45.01677474591480888, 103.8885755249567922 ) ) ;
#18576=ORIENTED_EDGE ( 'NONE', *, *, #23790, .F. ) ;
#18577=VERTEX_POINT ( 'NONE', #7428 ) ;
#18578=CARTESIAN_POINT ( 'NONE',  ( 10.93730112725972070, -26.59437931460858451, 148.8212007290659642 ) ) ;
#18580=CARTESIAN_POINT ( 'NONE',  ( 21.16825799904907512, -18.54093663547738302, -134.1581724640165305 ) ) ;
#18583=CARTESIAN_POINT ( 'NONE',  ( 1.833603222531969834, -138.1443021179084099, 44.41798579679493741 ) ) ;
#18584=B_SPLINE_CURVE_WITH_KNOTS ( 'NONE', 3,
 ( #20805, #5259, #13893, #12032, #25429, #1093 ),
 .UNSPECIFIED., .F., .F.,
 ( 4, 2, 4 ),
 ( 1.389302603484999005E-17, 0.0006311571484586140290, 0.001262314296917213963 ),
 .UNSPECIFIED. ) ;
#18585=CARTESIAN_POINT ( 'NONE',  ( 109.1592201516379674, -0.005631912476305732905, -0.005485778713193728215 ) ) ;
#18586=ORIENTED_EDGE ( 'NONE', *, *, #16868, .T. ) ;
#18587=CARTESIAN_POINT ( 'NONE',  ( 1.833485406944057594, 59.50871042846225834, 132.3460930279893262 ) ) ;
#18589=FACE_OUTER_BOUND ( 'NONE', #13519, .T. ) ;
#18590=CARTESIAN_POINT ( 'NONE',  ( 109.1589550718174877, 0.005777059646704591107, -0.004900004919105018994 ) ) ;
#18592=CARTESIAN_POINT ( 'NONE',  ( 25.98107933586718232, 65.61242423298442361, 92.16448350435750569 ) ) ;
#18594=CARTESIAN_POINT ( 'NONE',  ( 10.93730112725932635, 0.000000000000000000, 0.000000000000000000 ) ) ;
#18595=ORIENTED_EDGE ( 'NONE', *, *, #13369, .F. ) ;
#18597=VERTEX_POINT ( 'NONE', #938 ) ;
#18599=CARTESIAN_POINT ( 'NONE',  ( 25.86096068574578410, -107.8247115223744146, 33.98552076022159696 ) ) ;
#18600=CARTESIAN_POINT ( 'NONE',  ( 32.73300124599738581, 44.31599526638102304, -108.9684813982483860 ) ) ;
#18603=CARTESIAN_POINT ( 'NONE',  ( 109.1778270068192853, 0.0006237116683806083386, 0.009293669915253099933 ) ) ;
#18605=CARTESIAN_POINT ( 'NONE',  ( 2.263178607246673746, -126.6115608827432482, -71.48082837426134972 ) ) ;
#18608=B_SPLINE_CURVE_WITH_KNOTS ( 'NONE', 3,
 ( #2219, #19370, #24134, #10886, #21394, #8718, #14909, #26271 ),
 .UNSPECIFIED., .F., .F.,
 ( 4, 2, 2, 4 ),
 ( 1.734723475976807094E-17, 0.0002429592666046780883, 0.0004859185332093388294, 0.0009718370664186723462 ),
 .UNSPECIFIED. ) ;
#18609=CARTESIAN_POINT ( 'NONE',  ( 2.433796855181205476, -107.1581411821778858, -98.43889364293970345 ) ) ;
#18610=CARTESIAN_POINT ( 'NONE',  ( 1.833721034905648972, -85.58110185770016187, -117.1867194831487495 ) ) ;
#18611=CARTESIAN_POINT ( 'NONE',  ( 10.93730112725978287, -133.3192575531804209, 71.28103789254889477 ) ) ;
#18613=CARTESIAN_POINT ( 'NONE',  ( 10.93730112725999248, 42.00474393596446987, -145.2260730187398110 ) ) ;
#18614=CARTESIAN_POINT ( 'NONE',  ( 25.81918753295380498, -22.58534689649746596, 110.7464580477337108 ) ) ;
#18617=CARTESIAN_POINT ( 'NONE',  ( 25.64708010899966339, 83.87281825978713812, -75.59303792846540659 ) ) ;
#18619=DIRECTION ( 'NONE',  ( -1.000000000000000000, -0.000000000000000000, -0.000000000000000000 ) ) ;
#18624=ORIENTED_EDGE ( 'NONE', *, *, #17431, .T. ) ;
#18625=EDGE_CURVE ( 'NONE', #26606, #20029, #25417, .T. ) ;
#18626=ORIENTED_EDGE ( 'NONE', *, *, #16752, .F. ) ;
#18627=ORIENTED_EDGE ( 'NONE', *, *, #3127, .T. ) ;
#18628=B_SPLINE_CURVE_WITH_KNOTS ( 'NONE', 3,
 ( #17591, #6818, #15563, #2324, #11128, #9108 ),
 .UNSPECIFIED., .F., .F.,
 ( 4, 2, 4 ),
 ( 1.389302603484999005E-17, 0.0006311571484586018859, 0.001262314296917189894 ),
 .UNSPECIFIED. ) ;
#18629=ADVANCED_FACE ( 'NONE', ( #11879 ), #23782, .F. ) ;
#18630=CARTESIAN_POINT ( 'NONE',  ( 109.1721716018069515, 0.01706748904931388797, 0.0002019688922686267024 ) ) ;
#18631=CARTESIAN_POINT ( 'NONE',  ( 16.75465622695650225, -140.8868039942616122, -19.47041796022383053 ) ) ;
#18633=CARTESIAN_POINT ( 'NONE',  ( 30.59141879584288048, -111.3296561588015265, 33.33270905817553853 ) ) ;
#18634=FACE_OUTER_BOUND ( 'NONE', #12202, .T. ) ;
#18637=CARTESIAN_POINT ( 'NONE',  ( 109.1586059443104944, -0.005881369279875432732, 0.003930911098393195108 ) ) ;
#18639=CARTESIAN_POINT ( 'NONE',  ( 109.1592201516379674, -0.007376275279032879113, 0.002720803050370542309 ) ) ;
#18640=CARTESIAN_POINT ( 'NONE',  ( 6.224689322667630975, -134.1951906609234868, -62.55544044765383660 ) ) ;
#18641=ORIENTED_EDGE ( 'NONE', *, *, #21531, .T. ) ;
#18642=EDGE_LOOP ( 'NONE', ( #22178, #12867, #16930, #310 ) ) ;
#18643=CARTESIAN_POINT ( 'NONE',  ( 2.433796855181205476, -28.83182736670433499, -142.6247129145651229 ) ) ;
#18644=CARTESIAN_POINT ( 'NONE',  ( 24.22246935314087324, 0.000000000000000000, -111.9614997405030152 ) ) ;
#18645=CARTESIAN_POINT ( 'NONE',  ( 25.73574536432415272, 76.18908113044869879, -83.41179791497782503 ) ) ;
#18646=CARTESIAN_POINT ( 'NONE',  ( 1.833691583653494162, -85.58103979054574495, 117.1866391460183507 ) ) ;
#18648=ORIENTED_EDGE ( 'NONE', *, *, #9204, .F. ) ;
#18649=CARTESIAN_POINT ( 'NONE',  ( 26.11404676487259024, 36.06104232266452669, 107.3263591096431639 ) ) ;
#18653=CARTESIAN_POINT ( 'NONE',  ( 109.1589550718175161, 0.004632048724982901558, 0.005994046294305926253 ) ) ;
#18655=CONICAL_SURFACE ( 'NONE', #27837, 117.6351876552689504, 0.9945805576725580410 ) ;
#18657=EDGE_CURVE ( 'NONE', #6378, #11630, #18514, .T. ) ;
#18658=AXIS2_PLACEMENT_3D ( 'NONE', #7348, #20436, #22618 ) ;
#18659=ADVANCED_FACE ( 'NONE', ( #8146 ), #16622, .T. ) ;
#18661=ORIENTED_EDGE ( 'NONE', *, *, #223, .F. ) ;
#18662=VERTEX_POINT ( 'NONE', #20800 ) ;
#18663=CARTESIAN_POINT ( 'NONE',  ( 1.832998868059890096, -144.3700883710218363, 14.63705790013964680 ) ) ;
#18666=CARTESIAN_POINT ( 'NONE',  ( 2.433796855181205476, -60.50726454507993424, 132.3327394885229182 ) ) ;
#18668=FACE_OUTER_BOUND ( 'NONE', #2400, .T. ) ;
#18669=CARTESIAN_POINT ( 'NONE',  ( 1.833838850093452821, -107.8375718686133098, -97.09738119087818120 ) ) ;
#18671=B_SPLINE_CURVE_WITH_KNOTS ( 'NONE', 3,
 ( #13181, #24016, #26428, #19532, #26018, #2100, #23745, #236 ),
 .UNSPECIFIED., .F., .F.,
 ( 4, 2, 2, 4 ),
 ( 0.000000000000000000, 0.0002429588503611182591, 0.0004859177007222365181, 0.0009718354014444730363 ),
 .UNSPECIFIED. ) ;
#18672=FACE_OUTER_BOUND ( 'NONE', #26400, .T. ) ;
#18673=CARTESIAN_POINT ( 'NONE',  ( 21.16825799904900407, -135.0813719997368310, -9.757279788664144249 ) ) ;
#18675=CARTESIAN_POINT ( 'NONE',  ( 10.93730112725932635, 0.000000000000000000, 0.000000000000000000 ) ) ;
#18676=ORIENTED_EDGE ( 'NONE', *, *, #10421, .T. ) ;
#18680=DIRECTION ( 'NONE',  ( 0.7071067811865485719, 0.000000000000000000, -0.7071067811865465735 ) ) ;
#18681=CARTESIAN_POINT ( 'NONE',  ( 32.73300124599734318, 92.86301839380026024, 72.21147546950587071 ) ) ;
#18685=EDGE_LOOP ( 'NONE', ( #10684, #17294, #7194, #19314 ) ) ;
#18687=CARTESIAN_POINT ( 'NONE',  ( 28.43349137099831481, -124.1860347533534963, 4.052139611197981495 ) ) ;
#18690=CARTESIAN_POINT ( 'NONE',  ( 1.832998868059858122, 44.33343224355235890, 138.1720401012268553 ) ) ;
#18691=CARTESIAN_POINT ( 'NONE',  ( 26.11404676487257603, 45.01677474591409833, 103.8885755249570906 ) ) ;
#18692=ADVANCED_FACE ( 'NONE', ( #14311 ), #17839, .F. ) ;
#18693=CARTESIAN_POINT ( 'NONE',  ( 25.98552792386799126, -67.36997957637598233, -90.89136171349154836 ) ) ;
#18694=CARTESIAN_POINT ( 'NONE',  ( 1.832998868059858122, -72.09222286250995637, -125.9352106559991427 ) ) ;
#18695=CARTESIAN_POINT ( 'NONE',  ( 1.893872463202069811, -108.5026245911425207, 96.41404152942899941 ) ) ;
#18696=CARTESIAN_POINT ( 'NONE',  ( 9.884929003653626367, -139.1775604444700321, -57.36421526887299649 ) ) ;
#18698=CARTESIAN_POINT ( 'NONE',  ( 24.22246935314087324, 0.000000000000000000, 0.000000000000000000 ) ) ;
#18699=DIRECTION ( 'NONE',  ( 0.000000000000000000, 0.000000000000000000, 1.000000000000000000 ) ) ;
#18700=EDGE_CURVE ( 'NONE', #4838, #195, #12734, .T. ) ;
#18704=VERTEX_POINT ( 'NONE', #7871 ) ;
#18706=CARTESIAN_POINT ( 'NONE',  ( 2.430230287190572103, 125.2872625092162338, 74.01081053031143142 ) ) ;
#18708=CARTESIAN_POINT ( 'NONE',  ( 2.063896406836609909, 108.8509294491465198, 96.20114399516431547 ) ) ;
#18709=CARTESIAN_POINT ( 'NONE',  ( 1.832998868059890096, 144.2584710144582516, -15.69902610990226144 ) ) ;
#18712=CARTESIAN_POINT ( 'NONE',  ( 8.186469777911009160, 118.7566730872913752, -90.56875928602613612 ) ) ;
#18713=LINE ( 'NONE', #20873, #15245 ) ;
#18714=CARTESIAN_POINT ( 'NONE',  ( 2.108393763691183587, -116.7869873529603808, -86.43392821214699495 ) ) ;
#18715=VERTEX_POINT ( 'NONE', #25424 ) ;
#18716=VERTEX_POINT ( 'NONE', #5400 ) ;
#18718=CARTESIAN_POINT ( 'NONE',  ( 2.108393763691185363, 107.1124103264149738, 98.16799842733286141 ) ) ;
#18721=CARTESIAN_POINT ( 'NONE',  ( 1.832998868059858122, -107.4798986104853356, -97.49378069860905782 ) ) ;
#18723=CARTESIAN_POINT ( 'NONE',  ( 109.1589550718174877, -0.005994046294307837919, -0.004632048724973697983 ) ) ;
#18724=ORIENTED_EDGE ( 'NONE', *, *, #19589, .T. ) ;
#18727=LINE ( 'NONE', #11962, #5074 ) ;
#18728=EDGE_CURVE ( 'NONE', #14998, #17856, #14164, .T. ) ;
#18729=ADVANCED_FACE ( 'NONE', ( #3245 ), #9744, .T. ) ;
#18730=CARTESIAN_POINT ( 'NONE',  ( 32.73300124599735739, -44.31599526638029118, 108.9684813982487412 ) ) ;
#18731=VERTEX_POINT ( 'NONE', #25273 ) ;
#18732=VERTEX_POINT ( 'NONE', #3387 ) ;
#18733=CARTESIAN_POINT ( 'NONE',  ( 109.1586059443104944, 0.006637156007973981676, 0.002447596125905610390 ) ) ;
#18735=CARTESIAN_POINT ( 'NONE',  ( 109.1592201516379674, 0.005485778713193748164, -0.005631912476305715558 ) ) ;
#18736=ORIENTED_EDGE ( 'NONE', *, *, #20176, .T. ) ;
#18738=VERTEX_POINT ( 'NONE', #9391 ) ;
#18741=CARTESIAN_POINT ( 'NONE',  ( 28.37644542392835589, -98.15613422114043374, -76.32685750075110320 ) ) ;
#18746=CARTESIAN_POINT ( 'NONE',  ( 25.64703792032468854, 84.00887408969053638, 75.44170528134917220 ) ) ;
#18747=( BOUNDED_SURFACE ( )  B_SPLINE_SURFACE ( 3, 1, ( 
 ( #26745, #4589 ),
 ( #10940, #13222 ),
 ( #28472, #22011 ),
 ( #22309, #2572 ) ),
 .UNSPECIFIED., .F., .F., .F. ) 
 B_SPLINE_SURFACE_WITH_KNOTS ( ( 4, 4 ),
 ( 2, 2 ),
 ( 0.000000000000000000, 1.000000000000000000 ),
 ( 0.000000000000000000, 1.000000000000000000 ),
 .UNSPECIFIED. ) 
 GEOMETRIC_REPRESENTATION_ITEM ( )  RATIONAL_B_SPLINE_SURFACE ( (
 ( 1.000000000000000000, 1.000000000000000000),
 ( 0.6386103224230316178, 0.9954351624131538845),
 ( 0.6386103224230316178, 0.9954351624131538845),
 ( 1.000000000000000000, 1.000000000000000000) ) ) 
 REPRESENTATION_ITEM ( '' )  SURFACE ( )  );
#18751=CARTESIAN_POINT ( 'NONE',  ( 32.73300124599736449, -114.2056417606550127, 28.19767303745571496 ) ) ;
#18753=ADVANCED_FACE ( 'NONE', ( #20157 ), #4911, .F. ) ;
#18754=CARTESIAN_POINT ( 'NONE',  ( 1.833485406944057594, 15.69895494453384721, 144.2578170162063884 ) ) ;
#18755=CARTESIAN_POINT ( 'NONE',  ( 2.430230287190572103, -144.5585181921884725, -16.65331920325888149 ) ) ;
#18756=CARTESIAN_POINT ( 'NONE',  ( 55.79472521941426777, 53.57698701322215129, 49.22042574086442812 ) ) ;
#18757=LINE ( 'NONE', #5821, #10067 ) ;
#18761=ORIENTED_EDGE ( 'NONE', *, *, #19329, .T. ) ;
#18763=ADVANCED_FACE ( 'NONE', ( #593 ), #5599, .T. ) ;
#18767=ORIENTED_EDGE ( 'NONE', *, *, #9432, .T. ) ;
#18769=CARTESIAN_POINT ( 'NONE',  ( 32.73300124599735739, 44.31599526637956643, 108.9684813982490539 ) ) ;
#18774=CARTESIAN_POINT ( 'NONE',  ( 2.063896406836605024, 13.84738934186190917, 144.6078654718902214 ) ) ;
#18775=CARTESIAN_POINT ( 'NONE',  ( 109.1589550718174877, -0.001793588804091283831, 0.007359857714023712583 ) ) ;
#18777=CARTESIAN_POINT ( 'NONE',  ( 109.1592201516379674, 0.006649399203953463774, -0.004194960840990087647 ) ) ;
#18780=ORIENTED_EDGE ( 'NONE', *, *, #22905, .F. ) ;
#18782=CARTESIAN_POINT ( 'NONE',  ( 25.64708010899968116, -107.4019003251853377, -34.83947233573784530 ) ) ;
#18783=CARTESIAN_POINT ( 'NONE',  ( 1.834118845439484335, -30.34413640949595603, -141.9019470378990775 ) ) ;
#18784=CARTESIAN_POINT ( 'NONE',  ( 25.98107933586719653, 76.50887835172657958, -83.34070894055800238 ) ) ;
#18787=CARTESIAN_POINT ( 'NONE',  ( 25.64681081121879203, 11.38886654529823694, -112.3352186517029594 ) ) ;
#18791=CARTESIAN_POINT ( 'NONE',  ( 25.64692232868535626, 91.15460455808917573, -66.63160215461171276 ) ) ;
#18792=CARTESIAN_POINT ( 'NONE',  ( 109.1587776205901861, -0.007151389024635742414, 0.001605238040368439862 ) ) ;
#18794=CARTESIAN_POINT ( 'NONE',  ( 32.73300124599734318, 115.8010721414084117, 20.69176323058669809 ) ) ;
#18800=CARTESIAN_POINT ( 'NONE',  ( 2.433796855181233454, -86.69855925933894980, -116.8607839509065371 ) ) ;
#18803=DIRECTION ( 'NONE',  ( 0.5914120900931444380, 0.6942916636548107645, 0.4101107478122142935 ) ) ;
#18807=CARTESIAN_POINT ( 'NONE',  ( 25.64681081121879203, -107.2555980796243773, 35.28660243342513070 ) ) ;
#18808=LINE ( 'NONE', #27296, #10162 ) ;
#18810=ORIENTED_EDGE ( 'NONE', *, *, #22532, .T. ) ;
#18811=ADVANCED_FACE ( 'NONE', ( #2161 ), #6973, .T. ) ;
#18812=CARTESIAN_POINT ( 'NONE',  ( 10.93730112725990011, -146.7718404940640653, -36.23586118136687162 ) ) ;
#18814=CARTESIAN_POINT ( 'NONE',  ( 2.433796855181219243, -144.5536872373193376, 16.65276281464516828 ) ) ;
#18816=ORIENTED_EDGE ( 'NONE', *, *, #12267, .F. ) ;
#18817=EDGE_LOOP ( 'NONE', ( #18915, #4594, #1541, #17299 ) ) ;
#18820=LINE ( 'NONE', #27590, #2441 ) ;
#18821=CARTESIAN_POINT ( 'NONE',  ( 119.2224693531408803, 90.00000000000005684, -19.99999999999998934 ) ) ;
#18824=B_SPLINE_CURVE_WITH_KNOTS ( 'NONE', 3,
 ( #6070, #21585, #17124, #21447, #15091, #19286 ),
 .UNSPECIFIED., .F., .F.,
 ( 4, 2, 4 ),
 ( 2.394688213745465202E-17, 0.0006311636237756846571, 0.001262327247551345028 ),
 .UNSPECIFIED. ) ;
#18827=ORIENTED_EDGE ( 'NONE', *, *, #17303, .F. ) ;
#18828=CARTESIAN_POINT ( 'NONE',  ( 25.64681081121879203, -112.2483031020012589, -12.21581276189922427 ) ) ;
#18829=EDGE_CURVE ( 'NONE', #17799, #11098, #1427, .T. ) ;
#18830=DIRECTION ( 'NONE',  ( 0.000000000000000000, 0.000000000000000000, 1.000000000000000000 ) ) ;
#18831=VERTEX_POINT ( 'NONE', #20736 ) ;
#18835=CARTESIAN_POINT ( 'NONE',  ( 5.340103579038175674, -57.86178752084584431, 135.6222865281527277 ) ) ;
#18836=CARTESIAN_POINT ( 'NONE',  ( 25.70243777736187596, 75.03063812272054633, 84.42566495012475514 ) ) ;
#18837=CARTESIAN_POINT ( 'NONE',  ( 2.430230287190581429, -126.7388733285349787, 71.49654683843465364 ) ) ;
#18838=FACE_OUTER_BOUND ( 'NONE', #3221, .T. ) ;
#18839=ORIENTED_EDGE ( 'NONE', *, *, #15719, .F. ) ;
#18840=CARTESIAN_POINT ( 'NONE',  ( 109.1778270068192853, -0.006682187084639273911, -0.006489198140358696729 ) ) ;
#18841=( BOUNDED_SURFACE ( )  B_SPLINE_SURFACE ( 3, 1, ( 
 ( #8827, #6384 ),
 ( #9104, #17864 ),
 ( #19897, #13409 ),
 ( #13266, #17441 ) ),
 .UNSPECIFIED., .F., .F., .F. ) 
 B_SPLINE_SURFACE_WITH_KNOTS ( ( 4, 4 ),
 ( 2, 2 ),
 ( 0.000000000000000000, 1.000000000000000000 ),
 ( 0.000000000000000000, 1.000000000000000000 ),
 .UNSPECIFIED. ) 
 GEOMETRIC_REPRESENTATION_ITEM ( )  RATIONAL_B_SPLINE_SURFACE ( (
 ( 1.000000000000000000, 1.000000000000000000),
 ( 0.9956975270656955868, 0.8568959468854907557),
 ( 0.9956975270656955868, 0.8568959468854907557),
 ( 1.000000000000000000, 1.000000000000000000) ) ) 
 REPRESENTATION_ITEM ( '' )  SURFACE ( )  );
#18842=CARTESIAN_POINT ( 'NONE',  ( 25.69398547355837437, 110.3177996916217438, -24.20764173643295436 ) ) ;
#18843=B_SPLINE_CURVE_WITH_KNOTS ( 'NONE', 3,
 ( #2295, #17982, #11099, #26485, #7083, #15843 ),
 .UNSPECIFIED., .F., .F.,
 ( 4, 2, 4 ),
 ( 6.505213034913026604E-18, 0.0006311636237756838982, 0.001262327247551370615 ),
 .UNSPECIFIED. ) ;
#18849=CARTESIAN_POINT ( 'NONE',  ( 25.64681081121879203, -102.9795863647031666, 46.30456157731292421 ) ) ;
#18853=CARTESIAN_POINT ( 'NONE',  ( 1.832998868059858122, 145.1092030902949830, 0.5339089137753076919 ) ) ;
#18854=CARTESIAN_POINT ( 'NONE',  ( 1.833721034905619884, -125.8463597577922428, -72.24642519953907538 ) ) ;
#18855=ADVANCED_FACE ( 'NONE', ( #18430 ), #23083, .T. ) ;
#18856=CARTESIAN_POINT ( 'NONE',  ( 25.98107933586725338, -35.99661810150939090, 107.2544904356371092 ) ) ;
#18857=CARTESIAN_POINT ( 'NONE',  ( 55.49584447822657296, 53.73688382046329082, -48.74506217377828676 ) ) ;
#18860=EDGE_LOOP ( 'NONE', ( #11833, #7828, #10179, #6686 ) ) ;
#18861=CARTESIAN_POINT ( 'NONE',  ( 1.833691583653524804, -30.51806994139693785, 141.8642667235907311 ) ) ;
#18862=B_SPLINE_CURVE_WITH_KNOTS ( 'NONE', 3,
 ( #14657, #8604, #23887, #12638, #8474, #23463 ),
 .UNSPECIFIED., .F., .F.,
 ( 4, 2, 4 ),
 ( 5.637851296924623057E-18, 0.0006311636237756782604, 0.001262327247551351100 ),
 .UNSPECIFIED. ) ;
#18864=CARTESIAN_POINT ( 'NONE',  ( 26.28373643307404350, -78.30371666786325591, -100.6987277884692418 ) ) ;
#18865=VECTOR ( 'NONE', #12956, 1000.000000000000000 ) ;
#18866=CARTESIAN_POINT ( 'NONE',  ( 119.2224693531408803, 0.000000000000000000, 0.000000000000000000 ) ) ;
#18867=CARTESIAN_POINT ( 'NONE',  ( 1.833485406944057594, 107.4794113447422603, -97.49333871408586560 ) ) ;
#18870=CARTESIAN_POINT ( 'NONE',  ( 5.340103556456326395, 117.9209211572685518, 88.52145167812622617 ) ) ;
#18872=CARTESIAN_POINT ( 'NONE',  ( 25.64681081121879203, -11.38886654529598275, -112.3352186517031726 ) ) ;
#18874=CARTESIAN_POINT ( 'NONE',  ( 109.1589550718174877, 0.003284595046925658200, -0.006826119083824085977 ) ) ;
#18876=CARTESIAN_POINT ( 'NONE',  ( 25.81918753295377300, -57.31966094783135901, -97.41320410180144052 ) ) ;
#18877=CARTESIAN_POINT ( 'NONE',  ( 1.831572820252009626, -29.20415387690664133, 142.1425225354579140 ) ) ;
#18878=ORIENTED_EDGE ( 'NONE', *, *, #16867, .F. ) ;
#18879=B_SPLINE_CURVE_WITH_KNOTS ( 'NONE', 3,
 ( #12807, #3902, #6344, #1597, #21457, #14835, #23786, #23495, #25786, #10397 ),
 .UNSPECIFIED., .F., .F.,
 ( 4, 3, 3, 4 ),
 ( 1.387778780781445676E-17, 0.0002669560319015634731, 0.0005492286108966289854, 0.0008315040496093382841 ),
 .UNSPECIFIED. ) ;
#18880=EDGE_LOOP ( 'NONE', ( #18576, #2642, #11557, #6205 ) ) ;
#18883=AXIS2_PLACEMENT_3D ( 'NONE', #4142, #9139, #15750 ) ;
#18885=CARTESIAN_POINT ( 'NONE',  ( 25.64692232868535626, -110.5112661748243710, -23.15582834340398222 ) ) ;
#18886=CARTESIAN_POINT ( 'NONE',  ( 13.84597867724964004, -115.8103190066268837, -90.05293531772760218 ) ) ;
#18888=EDGE_CURVE ( 'NONE', #25030, #449, #24915, .T. ) ;
#18889=EDGE_CURVE ( 'NONE', #22240, #11755, #25375, .T. ) ;
#18890=CARTESIAN_POINT ( 'NONE',  ( 1.833721034905660296, 29.82176961967109818, -142.0123736691683973 ) ) ;
#18893=EDGE_CURVE ( 'NONE', #8964, #10429, #2832, .T. ) ;
#18894=CARTESIAN_POINT ( 'NONE',  ( 2.433796855181205476, -132.3327394885227477, -60.50726454508036056 ) ) ;
#18896=B_SPLINE_CURVE_WITH_KNOTS ( 'NONE', 3,
 ( #12505, #10242, #3455, #1707 ),
 .UNSPECIFIED., .F., .F.,
 ( 4, 4 ),
 ( 3.214625617059125298E-16, 0.01077107486149828444 ),
 .UNSPECIFIED. ) ;
#18897=CARTESIAN_POINT ( 'NONE',  ( 32.73300124599732186, 0.000000000000000000, 0.000000000000000000 ) ) ;
#18899=CARTESIAN_POINT ( 'NONE',  ( 28.37603512858449051, -25.60641750873823952, -111.8384105897144707 ) ) ;
#18900=CARTESIAN_POINT ( 'NONE',  ( 21.16825799904911776, 46.02882515936479280, 127.3716170292823477 ) ) ;
#18901=CARTESIAN_POINT ( 'NONE',  ( 25.64703792032471341, -11.65444440562256823, 112.3081285890370111 ) ) ;
#18903=CARTESIAN_POINT ( 'NONE',  ( 5.340103579038250281, -147.4316330314913159, 2.303180387974738341 ) ) ;
#18905=CARTESIAN_POINT ( 'NONE',  ( 25.64706015949225915, -0.09919735511113483839, -112.9111942614908060 ) ) ;
#18908=VERTEX_POINT ( 'NONE', #7668 ) ;
#18909=AXIS2_PLACEMENT_3D ( 'NONE', #17626, #7144, #11581 ) ;
#18910=EDGE_LOOP ( 'NONE', ( #1793, #26856, #11009, #15533 ) ) ;
#18912=CARTESIAN_POINT ( 'NONE',  ( 2.063896406836605024, 138.5688025270884793, -43.61045647697548588 ) ) ;
#18913=ORIENTED_EDGE ( 'NONE', *, *, #18054, .F. ) ;
#18914=ORIENTED_EDGE ( 'NONE', *, *, #19884, .F. ) ;
#18915=ORIENTED_EDGE ( 'NONE', *, *, #24348, .F. ) ;
#18916=EDGE_LOOP ( 'NONE', ( #23835, #28370, #23853, #26872 ) ) ;
#18919=ADVANCED_FACE ( 'NONE', ( #7519 ), #22670, .F. ) ;
#18920=AXIS2_PLACEMENT_3D ( 'NONE', #7731, #943, #22551 ) ;
#18922=CARTESIAN_POINT ( 'NONE',  ( 25.64681081121879203, 107.5125461021402486, 34.49579773461821475 ) ) ;
#18925=CARTESIAN_POINT ( 'NONE',  ( 2.433796855181233454, 60.50726454507903895, 132.3327394885233446 ) ) ;
#18926=CARTESIAN_POINT ( 'NONE',  ( 2.063896406836605024, 86.47093297169155335, -116.7302989755729072 ) ) ;
#18927=CARTESIAN_POINT ( 'NONE',  ( 1.833485406944043827, -85.72460230293772554, 117.0814567582541201 ) ) ;
#18928=CARTESIAN_POINT ( 'NONE',  ( 25.64681081121879203, 56.81519825470756047, 97.57530875170624540 ) ) ;
#18930=ORIENTED_EDGE ( 'NONE', *, *, #2247, .T. ) ;
#18931=EDGE_LOOP ( 'NONE', ( #3244, #13062, #14869, #26715 ) ) ;
#18932=CARTESIAN_POINT ( 'NONE',  ( 2.108393763691210676, -28.95405853987412570, -142.3786741588522773 ) ) ;
#18933=CARTESIAN_POINT ( 'NONE',  ( 25.64699802086724389, 112.9109702078780373, -0.2377811728601773311 ) ) ;
#18934=CARTESIAN_POINT ( 'NONE',  ( 55.79472521941428198, -15.83764557006218610, -71.00924468211174201 ) ) ;
#18935=CARTESIAN_POINT ( 'NONE',  ( 28.37603512858459709, -37.15644006762142482, -108.5491486026795087 ) ) ;
#18937=CARTESIAN_POINT ( 'NONE',  ( 25.64681081121879203, 91.10197563707947666, 66.70335573067896462 ) ) ;
#18938=ORIENTED_EDGE ( 'NONE', *, *, #20837, .F. ) ;
#18940=CARTESIAN_POINT ( 'NONE',  ( 10.93730112725990011, -128.3908183996585990, -79.81734490846054086 ) ) ;
#18941=CARTESIAN_POINT ( 'NONE',  ( 10.93730112725972958, -84.82621002473526062, 125.1380233598475229 ) ) ;
#18942=ORIENTED_EDGE ( 'NONE', *, *, #5260, .T. ) ;
#18943=ORIENTED_EDGE ( 'NONE', *, *, #9347, .T. ) ;
#18945=VERTEX_POINT ( 'NONE', #5336 ) ;
#18946=CONICAL_SURFACE ( 'NONE', #21242, 117.6351876552689504, 0.9945805576725580410 ) ;
#18947=ORIENTED_EDGE ( 'NONE', *, *, #16511, .T. ) ;
#18948=CARTESIAN_POINT ( 'NONE',  ( 28.43349137099831836, 98.08682467580888442, -76.27296957774029806 ) ) ;
#18949=ORIENTED_EDGE ( 'NONE', *, *, #16475, .T. ) ;
#18951=CARTESIAN_POINT ( 'NONE',  ( 25.81918753295377655, 112.5005889664128631, 10.88546493098895063 ) ) ;
#18952=EDGE_CURVE ( 'NONE', #21175, #14322, #14112, .T. ) ;
#18954=EDGE_CURVE ( 'NONE', #20493, #9181, #12488, .T. ) ;
#18961=VECTOR ( 'NONE', #17489, 1000.000000000000341 ) ;
#18963=CARTESIAN_POINT ( 'NONE',  ( 21.16825799904932381, 103.5479404090032602, 87.29264348877838131 ) ) ;
#18964=CARTESIAN_POINT ( 'NONE',  ( 26.11404676487257603, -102.9690087468798509, -47.08215554553621729 ) ) ;
#18965=EDGE_LOOP ( 'NONE', ( #3319, #7354, #2350, #17655 ) ) ;
#18968=EDGE_LOOP ( 'NONE', ( #13796, #13215, #6975, #19513 ) ) ;
#18970=DIRECTION ( 'NONE',  ( -1.000000000000000000, -0.000000000000000000, -0.000000000000000000 ) ) ;
#18971=CARTESIAN_POINT ( 'NONE',  ( 109.1721716018069657, 0.01616973485710950648, -0.005466227998629047229 ) ) ;
#18972=CARTESIAN_POINT ( 'NONE',  ( 109.1592201516379674, 0.007376275279032895593, -0.002720803050370492436 ) ) ;
#18975=ORIENTED_EDGE ( 'NONE', *, *, #23530, .F. ) ;
#18978=ORIENTED_EDGE ( 'NONE', *, *, #28212, .F. ) ;
#18979=CARTESIAN_POINT ( 'NONE',  ( 10.93730112725990189, -140.0398180619108075, -56.95489579269887059 ) ) ;
#18981=FACE_OUTER_BOUND ( 'NONE', #9736, .T. ) ;
#18982=CARTESIAN_POINT ( 'NONE',  ( 1.832998868059858122, 117.0819875546706896, -85.72499093307983742 ) ) ;
#18983=CARTESIAN_POINT ( 'NONE',  ( 25.64700659047696263, 107.3144208978484926, 35.10784848926700619 ) ) ;
#18986=ORIENTED_EDGE ( 'NONE', *, *, #9105, .F. ) ;
#18987=LINE ( 'NONE', #8472, #15799 ) ;
#18989=CARTESIAN_POINT ( 'NONE',  ( 9.884929003653626367, -42.50195158091132441, 144.4113244745770146 ) ) ;
#18990=CARTESIAN_POINT ( 'NONE',  ( 32.73300124599739291, 105.8473486001057466, -51.32617430724801721 ) ) ;
#18991=ORIENTED_EDGE ( 'NONE', *, *, #12383, .F. ) ;
#18994=CIRCLE ( 'NONE', #17585, 12.50000000000000178 ) ;
#18997=CARTESIAN_POINT ( 'NONE',  ( 1.893872463202066259, 73.39855082356820049, -125.2243573918626964 ) ) ;
#18998=EDGE_CURVE ( 'NONE', #17409, #6523, #15115, .T. ) ;
#19000=CARTESIAN_POINT ( 'NONE',  ( 8.186469777910561518, 131.0413692044509162, 71.65198614410246591 ) ) ;
#19002=CARTESIAN_POINT ( 'NONE',  ( 1.833603222531972721, 141.8454679205787272, 30.60504697399260721 ) ) ;
#19003=DIRECTION ( 'NONE',  ( -0.5946245182733606027, -0.7992853357633878941, 0.08697490616138658925 ) ) ;
#19006=ORIENTED_EDGE ( 'NONE', *, *, #25532, .F. ) ;
#19007=ORIENTED_EDGE ( 'NONE', *, *, #22711, .F. ) ;
#19010=CARTESIAN_POINT ( 'NONE',  ( 109.1592201516379674, -0.007780772729122749191, 0.001127733110588196924 ) ) ;
#19011=CARTESIAN_POINT ( 'NONE',  ( 25.64704443564076897, -83.82001435192574945, -75.65149037849849378 ) ) ;
#19012=CARTESIAN_POINT ( 'NONE',  ( 25.98552792386796995, -92.15963349013314598, -65.62435323276262977 ) ) ;
#19013=( BOUNDED_SURFACE ( )  B_SPLINE_SURFACE ( 3, 1, ( 
 ( #11161, #17624 ),
 ( #22089, #26266 ),
 ( #17336, #15315 ),
 ( #19935, #13162 ) ),
 .UNSPECIFIED., .F., .F., .F. ) 
 B_SPLINE_SURFACE_WITH_KNOTS ( ( 4, 4 ),
 ( 2, 2 ),
 ( 0.000000000000000000, 1.000000000000000000 ),
 ( 0.000000000000000000, 1.000000000000000000 ),
 .UNSPECIFIED. ) 
 GEOMETRIC_REPRESENTATION_ITEM ( )  RATIONAL_B_SPLINE_SURFACE ( (
 ( 1.000000000000000000, 1.000000000000000000),
 ( 0.6386103224230316178, 0.9954351624131538845),
 ( 0.6386103224230316178, 0.9954351624131538845),
 ( 1.000000000000000000, 1.000000000000000000) ) ) 
 REPRESENTATION_ITEM ( '' )  SURFACE ( )  );
#19014=CARTESIAN_POINT ( 'NONE',  ( 25.64699802086725455, -91.48665801621615401, -66.17503410043995871 ) ) ;
#19015=VERTEX_POINT ( 'NONE', #28200 ) ;
#19016=CARTESIAN_POINT ( 'NONE',  ( 1.833838850855438407, -144.3241377520101310, 15.07960613928581317 ) ) ;
#19017=CARTESIAN_POINT ( 'NONE',  ( 2.430230287190592531, 142.0258656395025980, -31.67257033707364400 ) ) ;
#19019=DIRECTION ( 'NONE',  ( 0.000000000000000000, 0.000000000000000000, 1.000000000000000000 ) ) ;
#19021=FACE_OUTER_BOUND ( 'NONE', #20422, .T. ) ;
#19025=FACE_OUTER_BOUND ( 'NONE', #14224, .T. ) ;
#19026=EDGE_LOOP ( 'NONE', ( #11909, #28339, #9202, #9651 ) ) ;
#19027=ORIENTED_EDGE ( 'NONE', *, *, #17631, .T. ) ;
#19029=ORIENTED_EDGE ( 'NONE', *, *, #4600, .F. ) ;
#19031=EDGE_CURVE ( 'NONE', #9431, #1130, #20998, .T. ) ;
#19032=CARTESIAN_POINT ( 'NONE',  ( 25.64681081121879203, 91.10197563708035773, -66.70335573067774249 ) ) ;
#19033=FACE_OUTER_BOUND ( 'NONE', #5313, .T. ) ;
#19034=CARTESIAN_POINT ( 'NONE',  ( 26.11404676487257603, 22.43340081644767636, 110.9778746459747794 ) ) ;
#19035=CARTESIAN_POINT ( 'NONE',  ( 26.11404676487257603, 110.9778746459746941, 22.43340081644806006 ) ) ;
#19036=B_SPLINE_CURVE_WITH_KNOTS ( 'NONE', 3,
 ( #14232, #25350, #14389, #19692, #8919, #9481 ),
 .UNSPECIFIED., .F., .F.,
 ( 4, 2, 4 ),
 ( 4.336808689942017255E-19, 0.0006311571484586044880, 0.001262314296917208542 ),
 .UNSPECIFIED. ) ;
#19037=CARTESIAN_POINT ( 'NONE',  ( 2.263178113027050742, -132.2496129425956042, -60.41552743271091686 ) ) ;
#19040=CARTESIAN_POINT ( 'NONE',  ( 1.833485406944057594, -59.50871042846138437, -132.3460930279897241 ) ) ;
#19041=CARTESIAN_POINT ( 'NONE',  ( 1.832998868059890096, 72.09222286251259959, -125.9352106559976363 ) ) ;
#19042=CARTESIAN_POINT ( 'NONE',  ( 1.833485406944057594, -142.0485807715644171, -29.64752363041688454 ) ) ;
#19043=( BOUNDED_SURFACE ( )  B_SPLINE_SURFACE ( 3, 1, ( 
 ( #1272, #16837 ),
 ( #3153, #18696 ),
 ( #10073, #27605 ),
 ( #22753, #16535 ) ),
 .UNSPECIFIED., .F., .F., .F. ) 
 B_SPLINE_SURFACE_WITH_KNOTS ( ( 4, 4 ),
 ( 2, 2 ),
 ( 0.000000000000000000, 1.000000000000000000 ),
 ( 0.000000000000000000, 1.000000000000000000 ),
 .UNSPECIFIED. ) 
 GEOMETRIC_REPRESENTATION_ITEM ( )  RATIONAL_B_SPLINE_SURFACE ( (
 ( 1.000000000000000000, 1.000000000000000000),
 ( 0.6386103224230316178, 0.9954351624131538845),
 ( 0.6386103224230316178, 0.9954351624131538845),
 ( 1.000000000000000000, 1.000000000000000000) ) ) 
 REPRESENTATION_ITEM ( '' )  SURFACE ( )  );
#19045=CARTESIAN_POINT ( 'NONE',  ( 10.93730112725943471, 125.1380233598475229, 84.82621002473483429 ) ) ;
#19046=CARTESIAN_POINT ( 'NONE',  ( 25.65782528836479770, 112.2379831684172302, 12.37768345530014358 ) ) ;
#19047=CARTESIAN_POINT ( 'NONE',  ( 109.1592201516379674, 0.002134489919774364575, 0.007566779963318560377 ) ) ;
#19048=CARTESIAN_POINT ( 'NONE',  ( 10.93730112726006354, 148.8212007290666747, -26.59437931460595905 ) ) ;
#19049=DIRECTION ( 'NONE',  ( 0.000000000000000000, 0.000000000000000000, 1.000000000000000000 ) ) ;
#19052=ADVANCED_FACE ( 'NONE', ( #12380 ), #23607, .F. ) ;
#19053=ORIENTED_EDGE ( 'NONE', *, *, #3742, .T. ) ;
#19056=ORIENTED_EDGE ( 'NONE', *, *, #16584, .T. ) ;
#19059=ORIENTED_EDGE ( 'NONE', *, *, #15000, .F. ) ;
#19060=ORIENTED_EDGE ( 'NONE', *, *, #17792, .F. ) ;
#19063=CARTESIAN_POINT ( 'NONE',  ( 5.340103579038266268, -120.6284720963480339, -84.79482754232395791 ) ) ;
#19064=B_SPLINE_CURVE_WITH_KNOTS ( 'NONE', 3,
 ( #18575, #14233, #22770, #3316, #25351, #5624, #579, #23200 ),
 .UNSPECIFIED., .F., .F.,
 ( 4, 2, 2, 4 ),
 ( 6.938893903907228378E-18, 0.0002429592666046844580, 0.0004859185332093619771, 0.0009718370664186995597 ),
 .UNSPECIFIED. ) ;
#19065=CARTESIAN_POINT ( 'NONE',  ( 1.833691583653522361, -142.0122737882510080, 29.82175144858052462 ) ) ;
#19068=DIRECTION ( 'NONE',  ( 0.000000000000000000, 0.000000000000000000, -1.000000000000000000 ) ) ;
#19069=CYLINDRICAL_SURFACE ( 'NONE', #25390, 20.00000000000000000 ) ;
#19070=DIRECTION ( 'NONE',  ( -1.000000000000000000, -0.000000000000000000, -0.000000000000000000 ) ) ;
#19074=CARTESIAN_POINT ( 'NONE',  ( 25.64681081121879203, -107.5125461021400355, -34.49579773461893950 ) ) ;
#19075=CARTESIAN_POINT ( 'NONE',  ( 2.108393763691206235, 133.2474712570801785, -57.92353377304154094 ) ) ;
#19076=CARTESIAN_POINT ( 'NONE',  ( 25.87036335909429852, 22.53739730344198833, -110.7910326764399542 ) ) ;
#19081=ADVANCED_FACE ( 'NONE', ( #22154 ), #20626, .F. ) ;
#19083=CARTESIAN_POINT ( 'NONE',  ( 1.833838850855474822, -15.25659494068204580, 144.3055354793886806 ) ) ;
#19084=ORIENTED_EDGE ( 'NONE', *, *, #25056, .T. ) ;
#19085=ORIENTED_EDGE ( 'NONE', *, *, #2628, .T. ) ;
#19088=EDGE_LOOP ( 'NONE', ( #21891, #519, #8015, #24636 ) ) ;
#19089=VERTEX_POINT ( 'NONE', #15509 ) ;
#19091=ORIENTED_EDGE ( 'NONE', *, *, #5128, .T. ) ;
#19092=CARTESIAN_POINT ( 'NONE',  ( 109.1592201516379674, 0.005631912476305695608, 0.005485778713193766379 ) ) ;
#19093=ORIENTED_EDGE ( 'NONE', *, *, #7756, .F. ) ;
#19099=CARTESIAN_POINT ( 'NONE',  ( 26.11404676487257603, 112.7148551500680469, 10.71016160607605627 ) ) ;
#19100=CARTESIAN_POINT ( 'NONE',  ( 1.833485406944043827, 0.5339064996905048543, -145.1085452359073145 ) ) ;
#19103=CARTESIAN_POINT ( 'NONE',  ( 30.58324630866341565, -3.944468862006814458, -120.8793175557613893 ) ) ;
#19108=EDGE_LOOP ( 'NONE', ( #16028, #1741, #3113, #25715 ) ) ;
#19110=B_SPLINE_CURVE_WITH_KNOTS ( 'NONE', 3,
 ( #5175, #2436, #20001, #24775, #15671, #20285, #13804, #13950 ),
 .UNSPECIFIED., .F., .F.,
 ( 4, 2, 2, 4 ),
 ( 6.938893903907228378E-18, 0.0002429592666046851085, 0.0004859185332093632782, 0.0009718370664186818872 ),
 .UNSPECIFIED. ) ;
#19112=CARTESIAN_POINT ( 'NONE',  ( 109.1592201516379674, -0.007051465909551689858, -0.003476928926125464302 ) ) ;
#19113=B_SPLINE_CURVE_WITH_KNOTS ( 'NONE', 3,
 ( #27624, #27780, #25496, #9948, #1285, #3451, #12096, #12365, #14667, #5465 ),
 .UNSPECIFIED., .F., .F.,
 ( 4, 3, 3, 4 ),
 ( 1.040834085586084257E-17, 0.0002669560319015703035, 0.0005492286108966372253, 0.0008315040496093471746 ),
 .UNSPECIFIED. ) ;
#19114=CARTESIAN_POINT ( 'NONE',  ( 2.263178607246643104, 133.3897506477022148, 57.85473702627159298 ) ) ;
#19115=CARTESIAN_POINT ( 'NONE',  ( 21.16825799904909289, -9.757279788663675291, 135.0813719997368878 ) ) ;
#19116=ORIENTED_EDGE ( 'NONE', *, *, #2619, .T. ) ;
#19117=CARTESIAN_POINT ( 'NONE',  ( 2.433796855181205476, 71.49415740225076377, 126.7346379669258312 ) ) ;
#19119=EDGE_LOOP ( 'NONE', ( #18530, #23134, #11959, #25338 ) ) ;
#19120=LINE ( 'NONE', #27759, #4675 ) ;
#19121=CARTESIAN_POINT ( 'NONE',  ( 109.1586900883932856, -0.006479576224398268976, 0.002995460350188374095 ) ) ;
#19122=CARTESIAN_POINT ( 'NONE',  ( 109.1587776205901861, 0.005502145856762305151, 0.004842060007769406239 ) ) ;
#19124=CARTESIAN_POINT ( 'NONE',  ( 26.11404676487259024, -55.62948129436313849, 98.61392875273344316 ) ) ;
#19125=EDGE_CURVE ( 'NONE', #22997, #771, #15855, .T. ) ;
#19126=ORIENTED_EDGE ( 'NONE', *, *, #17053, .T. ) ;
#19127=CARTESIAN_POINT ( 'NONE',  ( 109.1721716018069657, -0.01616973485710946484, 0.005466227998629163455 ) ) ;
#19128=ADVANCED_FACE ( 'NONE', ( #13089 ), #1877, .F. ) ;
#19129=B_SPLINE_CURVE_WITH_KNOTS ( 'NONE', 3,
 ( #14654, #3577, #12358, #25891, #10228, #12496, #18990 ),
 .UNSPECIFIED., .F., .F.,
 ( 4, 3, 4 ),
 ( 6.687668363004596812E-16, 0.02816610861753246139, 0.04000277880656288865 ),
 .UNSPECIFIED. ) ;
#19130=CARTESIAN_POINT ( 'NONE',  ( 109.1721716018069657, -0.001984900887706511109, -0.01695288006057378907 ) ) ;
#19132=ORIENTED_EDGE ( 'NONE', *, *, #21445, .T. ) ;
#19133=CARTESIAN_POINT ( 'NONE',  ( 2.433796855181219243, -28.83182736670634583, 142.6247129145647534 ) ) ;
#19134=CARTESIAN_POINT ( 'NONE',  ( 1.894214914920939075, -116.8658096527528443, 86.08679174688037961 ) ) ;
#19135=B_SPLINE_CURVE_WITH_KNOTS ( 'NONE', 3,
 ( #10694, #6105, #14708, #19459 ),
 .UNSPECIFIED., .F., .F.,
 ( 4, 4 ),
 ( 3.469446951953614189E-18, 0.008383560773332719013 ),
 .UNSPECIFIED. ) ;
#19136=CARTESIAN_POINT ( 'NONE',  ( 26.04756280548352265, -102.9366382251196228, 47.04636360340792578 ) ) ;
#19139=CARTESIAN_POINT ( 'NONE',  ( 26.28373643307405771, 60.14387450369989097, -112.4918671811453663 ) ) ;
#19140=CARTESIAN_POINT ( 'NONE',  ( 8.186469829614221538, 42.84118568057207455, 143.0750865143068040 ) ) ;
#19141=CARTESIAN_POINT ( 'NONE',  ( 55.79472521941428198, 21.78881894124796403, -69.41463258328491293 ) ) ;
#19142=CARTESIAN_POINT ( 'NONE',  ( 25.64692232868533139, 112.2580042965358871, -12.12735788170695805 ) ) ;
#19143=CARTESIAN_POINT ( 'NONE',  ( 2.108985857320902824, -57.92316197981750747, 133.2480631238191791 ) ) ;
#19145=ORIENTED_EDGE ( 'NONE', *, *, #25609, .T. ) ;
#19148=CARTESIAN_POINT ( 'NONE',  ( 109.1589550718174877, -0.006445391216542599791, -0.003980125429499862914 ) ) ;
#19149=CARTESIAN_POINT ( 'NONE',  ( 28.37603512858447985, -104.0705994281840105, 48.29936889363920471 ) ) ;
#19150=CARTESIAN_POINT ( 'NONE',  ( 32.73300124599732186, 0.000000000000000000, 0.000000000000000000 ) ) ;
#19151=CARTESIAN_POINT ( 'NONE',  ( 109.1586900883932856, 0.006561743627145262027, 0.002810909342002427570 ) ) ;
#19152=CARTESIAN_POINT ( 'NONE',  ( 55.79472521941426777, 66.16469064668298472, 30.25520714117929444 ) ) ;
#19153=ORIENTED_EDGE ( 'NONE', *, *, #10196, .F. ) ;
#19154=DIRECTION ( 'NONE',  ( 0.000000000000000000, 0.000000000000000000, 1.000000000000000000 ) ) ;
#19158=LINE ( 'NONE', #3606, #9828 ) ;
#19159=ORIENTED_EDGE ( 'NONE', *, *, #26567, .T. ) ;
#19160=CARTESIAN_POINT ( 'NONE',  ( 25.64692872815577473, -112.2585610031152328, -12.12228186621173975 ) ) ;
#19161=CARTESIAN_POINT ( 'NONE',  ( 26.11404676487259024, -97.48350837663652158, 57.58742681967414256 ) ) ;
#19162=VERTEX_POINT ( 'NONE', #25320 ) ;
#19164=ORIENTED_EDGE ( 'NONE', *, *, #6974, .F. ) ;
#19165=B_SPLINE_CURVE_WITH_KNOTS ( 'NONE', 3,
 ( #21092, #1378, #8034, #23421, #16802, #25579, #5858, #14619, #13299, #73 ),
 .UNSPECIFIED., .F., .F.,
 ( 4, 3, 3, 4 ),
 ( 3.925231146709437917E-17, 0.0002669559177086215868, 0.0005339118354151091385, 0.001067817517169165117 ),
 .UNSPECIFIED. ) ;
#19167=CARTESIAN_POINT ( 'NONE',  ( 10.93730112725994275, -36.23586118136433498, -146.7718404940647190 ) ) ;
#19169=( BOUNDED_SURFACE ( )  B_SPLINE_SURFACE ( 3, 1, ( 
 ( #2376, #21550 ),
 ( #17090, #24015 ),
 ( #4269, #13317 ),
 ( #21972, #8887 ) ),
 .UNSPECIFIED., .F., .F., .F. ) 
 B_SPLINE_SURFACE_WITH_KNOTS ( ( 4, 4 ),
 ( 2, 2 ),
 ( 0.000000000000000000, 1.000000000000000000 ),
 ( 0.000000000000000000, 1.000000000000000000 ),
 .UNSPECIFIED. ) 
 GEOMETRIC_REPRESENTATION_ITEM ( )  RATIONAL_B_SPLINE_SURFACE ( (
 ( 1.000000000000000000, 1.000000000000000000),
 ( 0.9956975270656954757, 0.8568959468854893125),
 ( 0.9956975270656954757, 0.8568959468854893125),
 ( 1.000000000000000000, 1.000000000000000000) ) ) 
 REPRESENTATION_ITEM ( '' )  SURFACE ( )  );
#19171=VERTEX_POINT ( 'NONE', #2863 ) ;
#19173=CARTESIAN_POINT ( 'NONE',  ( 1.833809397773902283, 59.18399778167309933, -132.4918864201821407 ) ) ;
#19175=B_SPLINE_CURVE_WITH_KNOTS ( 'NONE', 3,
 ( #26229, #24093, #4356, #7246 ),
 .UNSPECIFIED., .F., .F.,
 ( 4, 4 ),
 ( 3.503851573261294794E-16, 0.01077107486149824281 ),
 .UNSPECIFIED. ) ;
#19180=CARTESIAN_POINT ( 'NONE',  ( 1.833838850093440165, -141.9387673160884162, -30.17001281793505996 ) ) ;
#19182=CARTESIAN_POINT ( 'NONE',  ( 2.063896406836605024, 73.79559738457928120, -125.1295119249431309 ) ) ;
#19183=ADVANCED_FACE ( 'NONE', ( #24898 ), #27609, .F. ) ;
#19184=CARTESIAN_POINT ( 'NONE',  ( 26.28373643307440233, 105.5888781856746732, 71.57300207276388448 ) ) ;
#19185=DIRECTION ( 'NONE',  ( 0.000000000000000000, 0.000000000000000000, 1.000000000000000000 ) ) ;
#19187=ORIENTED_EDGE ( 'NONE', *, *, #21359, .F. ) ;
#19190=DIRECTION ( 'NONE',  ( -1.000000000000000000, -0.000000000000000000, -0.000000000000000000 ) ) ;
#19191=ORIENTED_EDGE ( 'NONE', *, *, #28102, .F. ) ;
#19192=ORIENTED_EDGE ( 'NONE', *, *, #3162, .F. ) ;
#19194=B_SPLINE_CURVE_WITH_KNOTS ( 'NONE', 3,
 ( #19280, #1583, #27788, #23630, #14538, #16979, #10247, #28190 ),
 .UNSPECIFIED., .F., .F.,
 ( 4, 2, 2, 4 ),
 ( 0.000000000000000000, 0.0002429588503611307274, 0.0004859177007222614548, 0.0009718354014445039360 ),
 .UNSPECIFIED. ) ;
#19195=CARTESIAN_POINT ( 'NONE',  ( 1.833485406944043827, 97.49333871408838093, -107.4794113447399297 ) ) ;
#19196=CARTESIAN_POINT ( 'NONE',  ( 109.1586059443104944, 0.002447596125914170816, 0.006637156007970161815 ) ) ;
#19197=( BOUNDED_SURFACE ( )  B_SPLINE_SURFACE ( 3, 1, ( 
 ( #3297, #28025 ),
 ( #5756, #10224 ),
 ( #14513, #23603 ),
 ( #3862, #18837 ) ),
 .UNSPECIFIED., .F., .F., .F. ) 
 B_SPLINE_SURFACE_WITH_KNOTS ( ( 4, 4 ),
 ( 2, 2 ),
 ( 0.000000000000000000, 1.000000000000000000 ),
 ( 0.000000000000000000, 1.000000000000000000 ),
 .UNSPECIFIED. ) 
 GEOMETRIC_REPRESENTATION_ITEM ( )  RATIONAL_B_SPLINE_SURFACE ( (
 ( 1.000000000000000000, 1.000000000000000000),
 ( 0.9956975270656955868, 0.8568959468854907557),
 ( 0.9956975270656955868, 0.8568959468854907557),
 ( 1.000000000000000000, 1.000000000000000000) ) ) 
 REPRESENTATION_ITEM ( '' )  SURFACE ( )  );
#19200=CARTESIAN_POINT ( 'NONE',  ( 25.64681081121879203, 66.70335573067866619, 91.10197563707968982 ) ) ;
#19201=CARTESIAN_POINT ( 'NONE',  ( 119.2224693531408946, -90.00000000000005684, -19.99999999999999645 ) ) ;
#19202=EDGE_CURVE ( 'NONE', #16069, #27652, #24799, .T. ) ;
#19203=CARTESIAN_POINT ( 'NONE',  ( 9.884929003653608603, 146.3148513795966608, 35.39789245780380611 ) ) ;
#19204=EDGE_CURVE ( 'NONE', #24734, #13159, #11928, .T. ) ;
#19205=EDGE_LOOP ( 'NONE', ( #14682, #12513, #17944, #17140 ) ) ;
#19206=ORIENTED_EDGE ( 'NONE', *, *, #17028, .T. ) ;
#19208=CARTESIAN_POINT ( 'NONE',  ( 55.79472521941428198, 37.00555938668259870, 62.63970324008273849 ) ) ;
#19209=CARTESIAN_POINT ( 'NONE',  ( 55.49584447822657296, -66.16986612640756960, -29.75369869231020914 ) ) ;
#19212=CARTESIAN_POINT ( 'NONE',  ( 25.64708228042122329, 91.37028996123351021, -66.33571787052716218 ) ) ;
#19214=CARTESIAN_POINT ( 'NONE',  ( 28.37644542392838432, -120.7150203538607087, -29.80435743554073724 ) ) ;
#19216=VERTEX_POINT ( 'NONE', #22747 ) ;
#19218=ORIENTED_EDGE ( 'NONE', *, *, #7729, .T. ) ;
#19219=VERTEX_POINT ( 'NONE', #24760 ) ;
#19220=CARTESIAN_POINT ( 'NONE',  ( 30.59141879584280943, -2.701465575440527012, 116.1811685142589567 ) ) ;
#19221=ORIENTED_EDGE ( 'NONE', *, *, #3029, .F. ) ;
#19222=CARTESIAN_POINT ( 'NONE',  ( 1.832998868059858122, 29.64765804470268407, -142.0492247521719946 ) ) ;
#19224=CARTESIAN_POINT ( 'NONE',  ( 2.108393763691185363, 126.4628696952929374, -71.53437599919685397 ) ) ;
#19225=EDGE_CURVE ( 'NONE', #14349, #174, #22018, .T. ) ;
#19226=CARTESIAN_POINT ( 'NONE',  ( 109.1592201516379674, -0.006957642258155097119, -0.003661068210032647052 ) ) ;
#19229=CARTESIAN_POINT ( 'NONE',  ( 32.73300124599732186, 0.000000000000000000, 0.000000000000000000 ) ) ;
#19231=CARTESIAN_POINT ( 'NONE',  ( 55.79472521941426777, -71.31192372336683150, 14.41365263906529748 ) ) ;
#19232=CARTESIAN_POINT ( 'NONE',  ( 1.833485406944043827, 84.86072343962726450, -117.7091014914941809 ) ) ;
#19235=EDGE_CURVE ( 'NONE', #2712, #13376, #1266, .T. ) ;
#19236=VERTEX_POINT ( 'NONE', #19251 ) ;
#19237=VERTEX_POINT ( 'NONE', #26015 ) ;
#19240=DIRECTION ( 'NONE',  ( 0.5914120900931444380, 0.4674599267565303085, 0.6570486713847291105 ) ) ;
#19241=CARTESIAN_POINT ( 'NONE',  ( 1.833206310202331712, 45.54896489827154937, 137.7753867363979623 ) ) ;
#19242=CARTESIAN_POINT ( 'NONE',  ( 26.04756280548355107, -76.55292122839982483, -83.36043467252099504 ) ) ;
#19243=CARTESIAN_POINT ( 'NONE',  ( 109.1592201516379674, 0.0003082430541934987381, -0.007856029051018018419 ) ) ;
#19244=ORIENTED_EDGE ( 'NONE', *, *, #7937, .T. ) ;
#19249=EDGE_CURVE ( 'NONE', #27430, #21234, #19120, .T. ) ;
#19250=EDGE_LOOP ( 'NONE', ( #25215, #17114, #19006, #19885 ) ) ;
#19251=CARTESIAN_POINT ( 'NONE',  ( 10.93730112725978287, -140.0398180619114896, 56.95489579269701608 ) ) ;
#19252=AXIS2_PLACEMENT_3D ( 'NONE', #21650, #5706, #12443 ) ;
#19253=CARTESIAN_POINT ( 'NONE',  ( 2.430230287190581429, 31.67257033707698710, -142.0258656395018591 ) ) ;
#19254=FACE_OUTER_BOUND ( 'NONE', #10509, .T. ) ;
#19256=CARTESIAN_POINT ( 'NONE',  ( 1.833485406944043827, 117.0814567582544612, 85.72460230293732764 ) ) ;
#19257=ORIENTED_EDGE ( 'NONE', *, *, #6351, .F. ) ;
#19259=FACE_OUTER_BOUND ( 'NONE', #13907, .T. ) ;
#19263=ORIENTED_EDGE ( 'NONE', *, *, #15416, .F. ) ;
#19265=CARTESIAN_POINT ( 'NONE',  ( 25.64692232868534560, 97.94691534265433575, 56.17236075411980067 ) ) ;
#19267=CARTESIAN_POINT ( 'NONE',  ( 2.433796855181219243, -142.0211193075558356, 31.67151202412923894 ) ) ;
#19270=FACE_OUTER_BOUND ( 'NONE', #13234, .T. ) ;
#19271=CARTESIAN_POINT ( 'NONE',  ( 2.433796855181219243, -144.8571464219890004, 13.76554153471645847 ) ) ;
#19272=EDGE_CURVE ( 'NONE', #2848, #8996, #12215, .T. ) ;
#19273=CARTESIAN_POINT ( 'NONE',  ( 1.833809397773829675, -59.18399778167225378, 132.4918864201826523 ) ) ;
#19274=CARTESIAN_POINT ( 'NONE',  ( 109.1589550718175161, -0.007571935245608773894, 0.0002241941239326721372 ) ) ;
#19275=LINE ( 'NONE', #13202, #19877 ) ;
#19276=CARTESIAN_POINT ( 'NONE',  ( 1.894214914920953730, -58.16536411968030507, 132.9862534094754665 ) ) ;
#19277=ORIENTED_EDGE ( 'NONE', *, *, #26640, .F. ) ;
#19278=EDGE_CURVE ( 'NONE', #8700, #20108, #11363, .T. ) ;
#19280=CARTESIAN_POINT ( 'NONE',  ( 25.64681081121879203, -97.57530875170564855, -56.81519825470856944 ) ) ;
#19281=LINE ( 'NONE', #19558, #1951 ) ;
#19282=CARTESIAN_POINT ( 'NONE',  ( 32.73300124599738581, -97.37344512919901263, 66.00340565729310072 ) ) ;
#19283=CARTESIAN_POINT ( 'NONE',  ( 109.1592201516379674, 0.001127733110579580769, -0.007780772729118883360 ) ) ;
#19284=DIRECTION ( 'NONE',  ( 0.000000000000000000, 0.000000000000000000, 1.000000000000000000 ) ) ;
#19285=CARTESIAN_POINT ( 'NONE',  ( 24.01988960052036148, 69.18817751538470873, -111.2910478357996453 ) ) ;
#19286=CARTESIAN_POINT ( 'NONE',  ( 1.833485406944043827, 97.49333871408838093, -107.4794113447399297 ) ) ;
#19287=ORIENTED_EDGE ( 'NONE', *, *, #20019, .F. ) ;
#19290=CARTESIAN_POINT ( 'NONE',  ( 109.1586900883932856, -0.001385221016536898869, -0.007002774699553655259 ) ) ;
#19292=B_SPLINE_CURVE_WITH_KNOTS ( 'NONE', 3,
 ( #16689, #3298, #11932, #23185 ),
 .UNSPECIFIED., .F., .F.,
 ( 4, 4 ),
 ( 0.000000000000000000, 0.01077107196513861845 ),
 .UNSPECIFIED. ) ;
#19294=CARTESIAN_POINT ( 'NONE',  ( 2.433796855181205476, 43.58222566461644476, 138.8296532063089614 ) ) ;
#19295=DIRECTION ( 'NONE',  ( -1.000000000000000000, -0.000000000000000000, -0.000000000000000000 ) ) ;
#19299=APPLICATION_CONTEXT ( 'automotive_design' ) ;
#19300=CARTESIAN_POINT ( 'NONE',  ( 1.831572820252009626, 96.36280042116079869, -108.4969585352545209 ) ) ;
#19302=B_SPLINE_CURVE_WITH_KNOTS ( 'NONE', 3,
 ( #21430, #10501, #16548, #19139, #3452, #25630, #23470 ),
 .UNSPECIFIED., .F., .F.,
 ( 4, 3, 4 ),
 ( 6.012562578665078486E-16, 0.02816610861753242670, 0.04000277880656282620 ),
 .UNSPECIFIED. ) ;
#19304=ORIENTED_EDGE ( 'NONE', *, *, #26351, .F. ) ;
#19306=EDGE_CURVE ( 'NONE', #391, #945, #16513, .T. ) ;
#19307=EDGE_CURVE ( 'NONE', #15221, #14195, #23791, .T. ) ;
#19308=DIRECTION ( 'NONE',  ( -1.000000000000000000, -0.000000000000000000, -0.000000000000000000 ) ) ;
#19309=CARTESIAN_POINT ( 'NONE',  ( 26.11404676487259024, 113.2169081140373947, -1.130420376097525326 ) ) ;
#19310=CARTESIAN_POINT ( 'NONE',  ( 25.64692872815574276, -12.12228186621135428, 112.2585610031153180 ) ) ;
#19311=CARTESIAN_POINT ( 'NONE',  ( 32.73300124599734318, 97.37344512919861472, 66.00340565729376863 ) ) ;
#19312=CARTESIAN_POINT ( 'NONE',  ( 109.1624594426973260, -0.01551217196236916694, -0.003771499231549737489 ) ) ;
#19313=ORIENTED_EDGE ( 'NONE', *, *, #20267, .T. ) ;
#19314=ORIENTED_EDGE ( 'NONE', *, *, #2283, .F. ) ;
#19315=CARTESIAN_POINT ( 'NONE',  ( 1.834118845439484335, -141.9759513273466780, 29.99597360113025246 ) ) ;
#19316=VECTOR ( 'NONE', #7226, 1000.000000000000114 ) ;
#19318=CARTESIAN_POINT ( 'NONE',  ( 25.98552792386799837, 35.98568266743512112, 107.2612904323490284 ) ) ;
#19321=ORIENTED_EDGE ( 'NONE', *, *, #24725, .T. ) ;
#19322=EDGE_LOOP ( 'NONE', ( #12663, #9050, #3399, #16214 ) ) ;
#19323=ORIENTED_EDGE ( 'NONE', *, *, #19398, .F. ) ;
#19325=( BOUNDED_SURFACE ( )  B_SPLINE_SURFACE ( 3, 1, ( 
 ( #23854, #8711 ),
 ( #25992, #4525 ),
 ( #8571, #17767 ),
 ( #19365, #17478 ) ),
 .UNSPECIFIED., .F., .F., .F. ) 
 B_SPLINE_SURFACE_WITH_KNOTS ( ( 4, 4 ),
 ( 2, 2 ),
 ( 0.000000000000000000, 1.000000000000000000 ),
 ( 0.000000000000000000, 1.000000000000000000 ),
 .UNSPECIFIED. ) 
 GEOMETRIC_REPRESENTATION_ITEM ( )  RATIONAL_B_SPLINE_SURFACE ( (
 ( 1.000000000000000000, 1.000000000000000000),
 ( 0.9956975270656954757, 0.8568959468854893125),
 ( 0.9956975270656954757, 0.8568959468854893125),
 ( 1.000000000000000000, 1.000000000000000000) ) ) 
 REPRESENTATION_ITEM ( '' )  SURFACE ( )  );
#19327=CONICAL_SURFACE ( 'NONE', #16133, 117.6351876552689504, 0.9945805576725580410 ) ;
#19329=EDGE_CURVE ( 'NONE', #823, #27505, #14771, .T. ) ;
#19330=EDGE_CURVE ( 'NONE', #2536, #20059, #1728, .T. ) ;
#19331=CARTESIAN_POINT ( 'NONE',  ( 94.22246935314088034, -69.99999999999998579, -12.50000000000000888 ) ) ;
#19332=CARTESIAN_POINT ( 'NONE',  ( 28.37599760073042887, -84.05168479399036130, -78.09498850373492473 ) ) ;
#19334=FACE_OUTER_BOUND ( 'NONE', #23293, .T. ) ;
#19335=CIRCLE ( 'NONE', #22564, 117.6351876552689504 ) ;
#19337=CARTESIAN_POINT ( 'NONE',  ( 109.1592201516379674, 0.007780772729118878156, 0.001127733110579607657 ) ) ;
#19339=VECTOR ( 'NONE', #8311, 1000.000000000000227 ) ;
#19340=EDGE_LOOP ( 'NONE', ( #5163, #25713, #20991, #11616 ) ) ;
#19342=B_SPLINE_CURVE_WITH_KNOTS ( 'NONE', 3,
 ( #19100, #1386, #27873, #11907, #20675, #9755, #23291 ),
 .UNSPECIFIED., .F., .F.,
 ( 4, 3, 4 ),
 ( 3.404394821604483923E-17, 0.0002669559177086210989, 0.0005339083821128836910 ),
 .UNSPECIFIED. ) ;
#19343=CARTESIAN_POINT ( 'NONE',  ( 25.64704443564078673, 112.9111375659905292, 0.1334765861207808380 ) ) ;
#19344=DIRECTION ( 'NONE',  ( -0.5914120900931443270, 0.4101107478122070771, 0.6942916636548150944 ) ) ;
#19347=CARTESIAN_POINT ( 'NONE',  ( 25.98107933586726759, 112.6229961579375924, -10.73978443746618439 ) ) ;
#19348=ORIENTED_EDGE ( 'NONE', *, *, #780, .F. ) ;
#19349=CARTESIAN_POINT ( 'NONE',  ( 25.64704443564079739, 97.85065179540836766, -56.33997466860298431 ) ) ;
#19350=CARTESIAN_POINT ( 'NONE',  ( 24.01988960052045741, 90.81495976423938998, -94.47404045191558453 ) ) ;
#19353=ORIENTED_EDGE ( 'NONE', *, *, #17643, .F. ) ;
#19355=DIRECTION ( 'NONE',  ( -1.000000000000000000, -0.000000000000000000, -0.000000000000000000 ) ) ;
#19356=VERTEX_POINT ( 'NONE', #24013 ) ;
#19357=EDGE_LOOP ( 'NONE', ( #26960, #19978, #18173, #9849 ) ) ;
#19360=CARTESIAN_POINT ( 'NONE',  ( 32.73300124599735739, -3.836798148479648507, 117.5726003567929610 ) ) ;
#19361=ADVANCED_FACE ( 'NONE', ( #2526 ), #26504, .F. ) ;
#19363=EDGE_CURVE ( 'NONE', #20199, #21696, #24370, .T. ) ;
#19364=ORIENTED_EDGE ( 'NONE', *, *, #12705, .T. ) ;
#19365=CARTESIAN_POINT ( 'NONE',  ( 109.1586900883932856, -0.003656351050331892692, -0.006130969560687349849 ) ) ;
#19366=CARTESIAN_POINT ( 'NONE',  ( 2.433796855181233454, -125.2830755159759519, 74.00833731765517598 ) ) ;
#19370=CARTESIAN_POINT ( 'NONE',  ( 26.04756280548352265, 103.8403168215175754, 45.01666824410803258 ) ) ;
#19371=CARTESIAN_POINT ( 'NONE',  ( 2.433796855181205476, 96.28145139437683042, 109.1007109081229345 ) ) ;
#19372=CARTESIAN_POINT ( 'NONE',  ( 25.64660436782540387, 98.07256794792336052, 55.95243482911432409 ) ) ;
#19373=ORIENTED_EDGE ( 'NONE', *, *, #7333, .F. ) ;
#19374=B_SPLINE_CURVE_WITH_KNOTS ( 'NONE', 3,
 ( #13602, #17779, #21829, #11310, #24141, #362 ),
 .UNSPECIFIED., .F., .F.,
 ( 4, 2, 4 ),
 ( 6.952433221959954168E-18, 0.0006311571484586070901, 0.001262314296917207458 ),
 .UNSPECIFIED. ) ;
#19375=ORIENTED_EDGE ( 'NONE', *, *, #24563, .T. ) ;
#19376=FACE_OUTER_BOUND ( 'NONE', #1247, .T. ) ;
#19378=CARTESIAN_POINT ( 'NONE',  ( 9.884929003653608603, -27.17402761732236627, -148.0628878137283380 ) ) ;
#19379=CARTESIAN_POINT ( 'NONE',  ( 21.16825799904893302, 18.54093663547828896, 134.1581724640165021 ) ) ;
#19380=VECTOR ( 'NONE', #1720, 1000.000000000000000 ) ;
#19387=CARTESIAN_POINT ( 'NONE',  ( 32.73300124599734318, 99.90245962373836619, 62.10906484417276374 ) ) ;
#19388=CYLINDRICAL_SURFACE ( 'NONE', #22582, 37.50000000000001421 ) ;
#19389=CARTESIAN_POINT ( 'NONE',  ( 25.64700659047694487, 112.2686754657455168, 12.02873506870207443 ) ) ;
#19394=CARTESIAN_POINT ( 'NONE',  ( 2.063896406836609909, -13.84738934186288084, 144.6078654718901362 ) ) ;
#19395=EDGE_CURVE ( 'NONE', #18219, #14717, #14790, .T. ) ;
#19396=ORIENTED_EDGE ( 'NONE', *, *, #2533, .T. ) ;
#19397=CARTESIAN_POINT ( 'NONE',  ( 13.84597867724966669, -94.55652763153750584, -112.1633818588836107 ) ) ;
#19398=EDGE_CURVE ( 'NONE', #28326, #10330, #4200, .T. ) ;
#19400=B_SPLINE_CURVE_WITH_KNOTS ( 'NONE', 3,
 ( #25604, #20973, #25172, #9918 ),
 .UNSPECIFIED., .F., .F.,
 ( 4, 4 ),
 ( 3.105545673626859933E-16, 0.01077107486149834689 ),
 .UNSPECIFIED. ) ;
#19403=CARTESIAN_POINT ( 'NONE',  ( 1.833485406944057594, -72.09189602597798796, 125.9346397303433065 ) ) ;
#19408=CARTESIAN_POINT ( 'NONE',  ( 1.833485406944043827, -132.7804117027891948, 58.53321471326832182 ) ) ;
#19409=CARTESIAN_POINT ( 'NONE',  ( 1.833750490713655479, -137.9248034078894989, -45.09517546033787738 ) ) ;
#19410=PLANE ( 'NONE',  #9690 ) ;
#19413=( BOUNDED_SURFACE ( )  B_SPLINE_SURFACE ( 3, 1, ( 
 ( #4353, #8826 ),
 ( #19895, #17584 ),
 ( #21628, #8968 ),
 ( #26369, #6672 ) ),
 .UNSPECIFIED., .F., .F., .F. ) 
 B_SPLINE_SURFACE_WITH_KNOTS ( ( 4, 4 ),
 ( 2, 2 ),
 ( 0.000000000000000000, 1.000000000000000000 ),
 ( 0.000000000000000000, 1.000000000000000000 ),
 .UNSPECIFIED. ) 
 GEOMETRIC_REPRESENTATION_ITEM ( )  RATIONAL_B_SPLINE_SURFACE ( (
 ( 1.000000000000000000, 1.000000000000000000),
 ( 0.9956975270656954757, 0.8568959468854893125),
 ( 0.9956975270656954757, 0.8568959468854893125),
 ( 1.000000000000000000, 1.000000000000000000) ) ) 
 REPRESENTATION_ITEM ( '' )  SURFACE ( )  );
#19415=CARTESIAN_POINT ( 'NONE',  ( 5.340103579038259163, -17.70136536264566729, -146.3832392131353402 ) ) ;
#19418=B_SPLINE_CURVE_WITH_KNOTS ( 'NONE', 3,
 ( #6657, #15404, #6796, #443 ),
 .UNSPECIFIED., .F., .F.,
 ( 4, 4 ),
 ( 0.000000000000000000, 0.008383560773332705135 ),
 .UNSPECIFIED. ) ;
#19419=ORIENTED_EDGE ( 'NONE', *, *, #21419, .T. ) ;
#19420=CARTESIAN_POINT ( 'NONE',  ( 109.1586059443104944, 0.0002768082440288753641, 0.007068659269321312354 ) ) ;
#19423=FACE_OUTER_BOUND ( 'NONE', #6662, .T. ) ;
#19424=CARTESIAN_POINT ( 'NONE',  ( 10.93730112726005999, 136.0306644680993600, -65.95960219662998725 ) ) ;
#19428=DIRECTION ( 'NONE',  ( 0.000000000000000000, 0.000000000000000000, 1.000000000000000000 ) ) ;
#19429=CARTESIAN_POINT ( 'NONE',  ( 109.1778270068192853, 0.004106684808172231596, -0.008360410075186628168 ) ) ;
#19431=CARTESIAN_POINT ( 'NONE',  ( 25.64681081121879203, 0.4157506337727869816, 112.9102952884414464 ) ) ;
#19433=AXIS2_PLACEMENT_3D ( 'NONE', #6306, #28161, #1820 ) ;
#19434=ORIENTED_EDGE ( 'NONE', *, *, #1696, .F. ) ;
#19436=DIRECTION ( 'NONE',  ( 0.000000000000000000, 0.000000000000000000, 1.000000000000000000 ) ) ;
#19438=EDGE_CURVE ( 'NONE', #26175, #12942, #26981, .T. ) ;
#19440=ORIENTED_EDGE ( 'NONE', *, *, #11499, .F. ) ;
#19441=EDGE_CURVE ( 'NONE', #24512, #1061, #2746, .T. ) ;
#19444=FACE_OUTER_BOUND ( 'NONE', #17476, .T. ) ;
#19445=CONICAL_SURFACE ( 'NONE', #7053, 117.6351876552689504, 0.9945805576725580410 ) ;
#19447=VECTOR ( 'NONE', #17293, 1000.000000000000000 ) ;
#19451=CARTESIAN_POINT ( 'NONE',  ( 2.433796855181219243, -43.58222566461740399, 138.8296532063086772 ) ) ;
#19455=CARTESIAN_POINT ( 'NONE',  ( 109.1721716018069657, 0.01695288006057379254, -0.001984900887706451695 ) ) ;
#19456=DIRECTION ( 'NONE',  ( 0.000000000000000000, 0.000000000000000000, 1.000000000000000000 ) ) ;
#19458=B_SPLINE_CURVE_WITH_KNOTS ( 'NONE', 3,
 ( #20730, #17844, #587, #22334, #2596, #26915, #11380 ),
 .UNSPECIFIED., .F., .F.,
 ( 4, 3, 4 ),
 ( 0.000000000000000000, 0.02398743853561338679, 0.04000277880656215312 ),
 .UNSPECIFIED. ) ;
#19459=CARTESIAN_POINT ( 'NONE',  ( 32.73300124599735028, 110.6325518752274206, 39.98094346392350218 ) ) ;
#19460=B_SPLINE_CURVE_WITH_KNOTS ( 'NONE', 3,
 ( #22908, #22467, #3168, #11945, #20717, #27036, #22322 ),
 .UNSPECIFIED., .F., .F.,
 ( 4, 3, 4 ),
 ( 0.000000000000000000, 0.02398743853561350475, 0.04000277880656220864 ),
 .UNSPECIFIED. ) ;
#19461=CARTESIAN_POINT ( 'NONE',  ( 6.224689322667647851, -111.7293398381258243, -97.14981701196437314 ) ) ;
#19463=CARTESIAN_POINT ( 'NONE',  ( 2.430230287190572103, 118.5711603495692827, -84.35270093935136515 ) ) ;
#19464=ORIENTED_EDGE ( 'NONE', *, *, #11837, .T. ) ;
#19465=ORIENTED_EDGE ( 'NONE', *, *, #4130, .T. ) ;
#19466=CARTESIAN_POINT ( 'NONE',  ( 1.834118845439484335, 14.99112450600438429, -144.3336252355295528 ) ) ;
#19467=CARTESIAN_POINT ( 'NONE',  ( 25.87036335909427365, 35.87755773825718109, 107.2165474610295490 ) ) ;
#19469=ADVANCED_FACE ( 'NONE', ( #14037 ), #17508, .F. ) ;
#19470=VERTEX_POINT ( 'NONE', #11452 ) ;
#19471=ORIENTED_EDGE ( 'NONE', *, *, #14854, .F. ) ;
#19472=EDGE_CURVE ( 'NONE', #9093, #14545, #2363, .T. ) ;
#19474=CARTESIAN_POINT ( 'NONE',  ( 2.263178607246656426, -145.3892423243864584, 1.401567185705964169 ) ) ;
#19476=FACE_OUTER_BOUND ( 'NONE', #1939, .T. ) ;
#19479=CARTESIAN_POINT ( 'NONE',  ( 5.340103579038033565, 147.4316330314911738, -2.303180387975705123 ) ) ;
#19480=CARTESIAN_POINT ( 'NONE',  ( 28.37603512858450117, 84.05169593519829618, -78.09501335733503424 ) ) ;
#19481=CARTESIAN_POINT ( 'NONE',  ( 2.263178113027048521, 108.9830942735805905, -96.24282436106508953 ) ) ;
#19484=VERTEX_POINT ( 'NONE', #24856 ) ;
#19486=CARTESIAN_POINT ( 'NONE',  ( 109.1587776205901861, -0.003592288931003392340, 0.006388631651935879063 ) ) ;
#19487=CARTESIAN_POINT ( 'NONE',  ( 25.65782528836480836, -56.95887699624806544, 97.50004228081037638 ) ) ;
#19488=CARTESIAN_POINT ( 'NONE',  ( 25.64703792032466367, -103.2099561461821793, -45.78915563622668117 ) ) ;
#19489=B_SPLINE_CURVE_WITH_KNOTS ( 'NONE', 3,
 ( #15801, #2549, #17939, #9475 ),
 .UNSPECIFIED., .F., .F.,
 ( 4, 4 ),
 ( 3.313460909250643119E-16, 0.01077107486149829832 ),
 .UNSPECIFIED. ) ;
#19492=CARTESIAN_POINT ( 'NONE',  ( 25.64670758986457955, 91.63870681572909405, -65.96397693491071834 ) ) ;
#19493=EDGE_CURVE ( 'NONE', #9341, #11691, #15789, .T. ) ;
#19494=VERTEX_POINT ( 'NONE', #2670 ) ;
#19497=ORIENTED_EDGE ( 'NONE', *, *, #1905, .T. ) ;
#19498=EDGE_LOOP ( 'NONE', ( #11782, #1808, #4096, #13983 ) ) ;
#19499=EDGE_CURVE ( 'NONE', #16228, #17548, #17518, .T. ) ;
#19500=FACE_OUTER_BOUND ( 'NONE', #23770, .T. ) ;
#19503=VERTEX_POINT ( 'NONE', #803 ) ;
#19505=VERTEX_POINT ( 'NONE', #23275 ) ;
#19507=CARTESIAN_POINT ( 'NONE',  ( 2.430230287190572103, -16.65331920325837345, 144.5585181921885294 ) ) ;
#19508=CARTESIAN_POINT ( 'NONE',  ( 109.1592201516379674, 0.003661068210032671338, -0.006957642258155084976 ) ) ;
#19511=CARTESIAN_POINT ( 'NONE',  ( 109.1589550718174877, 0.007453082872776639785, -0.001354998915261358293 ) ) ;
#19512=DIRECTION ( 'NONE',  ( 0.5914120900931444380, 0.1754905759872898430, -0.7870418015781041055 ) ) ;
#19513=ORIENTED_EDGE ( 'NONE', *, *, #27619, .F. ) ;
#19517=ORIENTED_EDGE ( 'NONE', *, *, #20738, .F. ) ;
#19518=VERTEX_POINT ( 'NONE', #27856 ) ;
#19519=CARTESIAN_POINT ( 'NONE',  ( 2.433796855181233454, -96.28145139437756939, 109.1007109081222666 ) ) ;
#19520=B_SPLINE_CURVE_WITH_KNOTS ( 'NONE', 3,
 ( #26896, #24059, #13095, #21881, #11080, #24192, #13224, #22012, #2274, #139 ),
 .UNSPECIFIED., .F., .F.,
 ( 4, 3, 3, 4 ),
 ( 7.850462293418877066E-17, 0.0002669559177086319409, 0.0005339118354151246425, 0.001067817517169165117 ),
 .UNSPECIFIED. ) ;
#19521=CARTESIAN_POINT ( 'NONE',  ( 1.833721034905666958, -72.24642519953862063, 125.8463597577924276 ) ) ;
#19522=CARTESIAN_POINT ( 'NONE',  ( 10.93730112725969938, 79.81734490845904872, 128.3908183996593948 ) ) ;
#19523=CARTESIAN_POINT ( 'NONE',  ( 1.833485406944043827, -117.0814567582538501, -85.72460230293812344 ) ) ;
#19525=CARTESIAN_POINT ( 'NONE',  ( 25.73574536432415272, 97.42965068311228549, 57.18187897120832019 ) ) ;
#19526=CARTESIAN_POINT ( 'NONE',  ( 30.59141879584273482, 113.0806649571965465, 26.79785525806430968 ) ) ;
#19528=EDGE_LOOP ( 'NONE', ( #16459, #12064, #22496, #14010 ) ) ;
#19529=CARTESIAN_POINT ( 'NONE',  ( 1.833750490713653480, -45.09517546033740842, 137.9248034078896410 ) ) ;
#19530=ADVANCED_FACE ( 'NONE', ( #25570 ), #7799, .F. ) ;
#19531=CARTESIAN_POINT ( 'NONE',  ( 1.833485406944057594, -144.3694338680884073, -14.63699153649508311 ) ) ;
#19532=CARTESIAN_POINT ( 'NONE',  ( 25.70243777736188662, -91.80600962488439620, 65.79472741891235898 ) ) ;
#19534=ORIENTED_EDGE ( 'NONE', *, *, #3196, .F. ) ;
#19535=EDGE_CURVE ( 'NONE', #7680, #21385, #4653, .T. ) ;
#19536=CARTESIAN_POINT ( 'NONE',  ( 2.430230287190581429, 28.83279105684427535, 142.6294793592098813 ) ) ;
#19538=CARTESIAN_POINT ( 'NONE',  ( 109.1721716018069515, 0.01368917435590588996, 0.01019541462303041185 ) ) ;
#19539=EDGE_LOOP ( 'NONE', ( #23476, #3682, #16341, #16172 ) ) ;
#19543=CARTESIAN_POINT ( 'NONE',  ( 25.64699802086723679, 97.90265915240027539, 56.24956056770054147 ) ) ;
#19544=DIRECTION ( 'NONE',  ( -1.000000000000000000, -0.000000000000000000, -0.000000000000000000 ) ) ;
#19546=CARTESIAN_POINT ( 'NONE',  ( 26.11404676487257603, -10.71016160607490875, -112.7148551500681606 ) ) ;
#19549=CARTESIAN_POINT ( 'NONE',  ( 1.833721034905622549, -132.4192200895886629, 59.34646046113731899 ) ) ;
#19550=CARTESIAN_POINT ( 'NONE',  ( 25.81918753295379076, 110.7464580477338245, 22.58534689649710003 ) ) ;
#19551=FACE_OUTER_BOUND ( 'NONE', #20380, .T. ) ;
#19552=DIRECTION ( 'NONE',  ( -0.5946245182733607137, 0.1642747008466300118, -0.7870422510449638365 ) ) ;
#19554=VERTEX_POINT ( 'NONE', #18649 ) ;
#19556=ORIENTED_EDGE ( 'NONE', *, *, #11904, .T. ) ;
#19558=CARTESIAN_POINT ( 'NONE',  ( 55.49584447822657296, 58.53775398922257978, 42.86099773636560428 ) ) ;
#19559=CARTESIAN_POINT ( 'NONE',  ( 1.832998868059858122, 144.3700883710216942, 14.63705790014056163 ) ) ;
#19560=CARTESIAN_POINT ( 'NONE',  ( 109.1589550718174877, 0.0002241941239240469565, -0.007571935245604908930 ) ) ;
#19561=CARTESIAN_POINT ( 'NONE',  ( 25.87036335909424878, -92.04585932622728706, -65.65170964736225301 ) ) ;
#19562=DIRECTION ( 'NONE',  ( -0.5914120900931443270, 0.4804373588864766509, 0.6476200150380201359 ) ) ;
#19564=ORIENTED_EDGE ( 'NONE', *, *, #27579, .F. ) ;
#19565=CARTESIAN_POINT ( 'NONE',  ( 1.833485406944043827, 132.3460930279890704, 59.50871042846269177 ) ) ;
#19570=B_SPLINE_CURVE_WITH_KNOTS ( 'NONE', 3,
 ( #4287, #8477, #19134, #4003, #12643, #1833 ),
 .UNSPECIFIED., .F., .F.,
 ( 4, 2, 4 ),
 ( 0.000000000000000000, 0.0006311571484586011270, 0.001262314296917202037 ),
 .UNSPECIFIED. ) ;
#19571=CARTESIAN_POINT ( 'NONE',  ( 26.11404676487257603, 47.08215554553657256, -102.9690087468796662 ) ) ;
#19574=EDGE_LOOP ( 'NONE', ( #4455, #13836, #17282, #19791 ) ) ;
#19575=CARTESIAN_POINT ( 'NONE',  ( 1.833485406944057594, -45.34878176254139248, -137.8414413349090637 ) ) ;
#19576=ORIENTED_EDGE ( 'NONE', *, *, #4993, .T. ) ;
#19579=B_SPLINE_CURVE_WITH_KNOTS ( 'NONE', 3,
 ( #23676, #3792, #8667, #24085, #21486, #21910 ),
 .UNSPECIFIED., .F., .F.,
 ( 4, 2, 4 ),
 ( 1.965608005753612659E-17, 0.0006311571484586143543, 0.001262314296917209193 ),
 .UNSPECIFIED. ) ;
#19580=DIRECTION ( 'NONE',  ( -0.5914120900931443270, -0.09226095020377388101, -0.8010740644654246179 ) ) ;
#19583=CARTESIAN_POINT ( 'NONE',  ( 109.1624594426973118, -0.009004164758064462162, 0.01318243916935004680 ) ) ;
#19585=ORIENTED_EDGE ( 'NONE', *, *, #26378, .F. ) ;
#19587=ORIENTED_EDGE ( 'NONE', *, *, #4816, .F. ) ;
#19589=EDGE_CURVE ( 'NONE', #142, #21070, #9284, .T. ) ;
#19591=CARTESIAN_POINT ( 'NONE',  ( 109.1778270068192853, 0.007323887274081532055, -0.005755170886745342509 ) ) ;
#19593=CARTESIAN_POINT ( 'NONE',  ( 2.430230287190572103, -84.35270093935176305, -118.5711603495689985 ) ) ;
#19595=EDGE_CURVE ( 'NONE', #17548, #16728, #9264, .T. ) ;
#19596=CARTESIAN_POINT ( 'NONE',  ( 109.1586900883932856, -0.005236795036868193212, -0.004851151255031836522 ) ) ;
#19597=DIRECTION ( 'NONE',  ( 0.000000000000000000, 0.000000000000000000, -1.000000000000000000 ) ) ;
#19598=CARTESIAN_POINT ( 'NONE',  ( 2.430230287190592531, 71.49654683843687053, -126.7388733285337281 ) ) ;
#19599=EDGE_CURVE ( 'NONE', #14920, #18597, #23728, .T. ) ;
#19602=CARTESIAN_POINT ( 'NONE',  ( 109.1586900883932856, 0.0006456433529162510171, 0.007109207791181754860 ) ) ;
#19603=VERTEX_POINT ( 'NONE', #23704 ) ;
#19604=EDGE_LOOP ( 'NONE', ( #16736, #24885, #16641, #14721 ) ) ;
#19606=CARTESIAN_POINT ( 'NONE',  ( 32.73300124599732186, 0.000000000000000000, 0.000000000000000000 ) ) ;
#19607=CARTESIAN_POINT ( 'NONE',  ( -90.83090735639699176, 0.000000000000000000, 0.000000000000000000 ) ) ;
#19608=( BOUNDED_SURFACE ( )  B_SPLINE_SURFACE ( 3, 1, ( 
 ( #20017, #19593 ),
 ( #15689, #26210 ),
 ( #11245, #17847 ),
 ( #2299, #26628 ) ),
 .UNSPECIFIED., .F., .F., .F. ) 
 B_SPLINE_SURFACE_WITH_KNOTS ( ( 4, 4 ),
 ( 2, 2 ),
 ( 0.000000000000000000, 1.000000000000000000 ),
 ( 0.000000000000000000, 1.000000000000000000 ),
 .UNSPECIFIED. ) 
 GEOMETRIC_REPRESENTATION_ITEM ( )  RATIONAL_B_SPLINE_SURFACE ( (
 ( 1.000000000000000000, 1.000000000000000000),
 ( 0.6386103224230302855, 0.9954351624131538845),
 ( 0.6386103224230302855, 0.9954351624131538845),
 ( 1.000000000000000000, 1.000000000000000000) ) ) 
 REPRESENTATION_ITEM ( '' )  SURFACE ( )  );
#19609=CARTESIAN_POINT ( 'NONE',  ( 25.65782528836481546, -83.52701600504825308, -75.98558751977860481 ) ) ;
#19611=B_SPLINE_CURVE_WITH_KNOTS ( 'NONE', 3,
 ( #8836, #190, #20042, #17596, #6682, #4495, #1195 ),
 .UNSPECIFIED., .F., .F.,
 ( 4, 3, 4 ),
 ( 5.852680391678861476E-16, 0.02816610861753249262, 0.04000277880656273599 ),
 .UNSPECIFIED. ) ;
#19613=CARTESIAN_POINT ( 'NONE',  ( 55.79472521941428198, 30.25520714117905996, 66.16469064668309841 ) ) ;
#19616=CARTESIAN_POINT ( 'NONE',  ( 25.64708228042118421, -110.4520805602537337, 23.43704872438724962 ) ) ;
#19619=ORIENTED_EDGE ( 'NONE', *, *, #16694, .T. ) ;
#19622=DIRECTION ( 'NONE',  ( 0.000000000000000000, 0.000000000000000000, 1.000000000000000000 ) ) ;
#19626=ORIENTED_EDGE ( 'NONE', *, *, #5810, .T. ) ;
#19628=CARTESIAN_POINT ( 'NONE',  ( 1.833206308920080740, -144.2348261777515006, -15.90849808442029101 ) ) ;
#19630=ORIENTED_EDGE ( 'NONE', *, *, #14828, .F. ) ;
#19634=ORIENTED_EDGE ( 'NONE', *, *, #16799, .F. ) ;
#19636=FACE_OUTER_BOUND ( 'NONE', #16678, .T. ) ;
#19637=EDGE_LOOP ( 'NONE', ( #26450, #6930, #8470, #5884 ) ) ;
#19638=CARTESIAN_POINT ( 'NONE',  ( 8.186469829614237526, -77.65916164626425200, 127.5731248499974129 ) ) ;
#19639=CARTESIAN_POINT ( 'NONE',  ( 6.224689322667630975, -48.18553814190126872, 139.9988794244330563 ) ) ;
#19640=CARTESIAN_POINT ( 'NONE',  ( 13.36082413113061307, -70.90215303572030336, -135.4964217943314679 ) ) ;
#19642=CARTESIAN_POINT ( 'NONE',  ( 25.64670758986457599, 56.02376616805423026, 98.03181353150503696 ) ) ;
#19643=CARTESIAN_POINT ( 'NONE',  ( 16.75465622695657686, -10.24707101927944031, -141.8562168210794994 ) ) ;
#19644=B_SPLINE_CURVE_WITH_KNOTS ( 'NONE', 3,
 ( #19914, #11001, #6396, #8846 ),
 .UNSPECIFIED., .F., .F.,
 ( 4, 4 ),
 ( 0.000000000000000000, 0.01077107196513851436 ),
 .UNSPECIFIED. ) ;
#19645=EDGE_CURVE ( 'NONE', #25619, #17840, #12033, .T. ) ;
#19646=CARTESIAN_POINT ( 'NONE',  ( 25.98552792386801613, -103.7897946223262693, -45.02923844025588096 ) ) ;
#19647=CARTESIAN_POINT ( 'NONE',  ( 1.833838850093517658, 1.769966374633376447E-14, 145.1097630783160923 ) ) ;
#19648=CARTESIAN_POINT ( 'NONE',  ( 2.108393763691148948, -118.2927144690665102, 84.36147263237538141 ) ) ;
#19649=DIRECTION ( 'NONE',  ( -1.000000000000000000, -0.000000000000000000, -0.000000000000000000 ) ) ;
#19650=ADVANCED_FACE ( 'NONE', ( #57 ), #27656, .T. ) ;
#19651=ORIENTED_EDGE ( 'NONE', *, *, #5803, .T. ) ;
#19652=CARTESIAN_POINT ( 'NONE',  ( 8.186469829614399174, -12.15801983495520133, -148.8557359502364079 ) ) ;
#19653=CARTESIAN_POINT ( 'NONE',  ( 2.430230287190589422, -86.70145658344578976, -116.8646894862420993 ) ) ;
#19656=CARTESIAN_POINT ( 'NONE',  ( 10.93730112725969938, 71.28103789254939215, 133.3192575531800799 ) ) ;
#19657=CARTESIAN_POINT ( 'NONE',  ( 28.37644542392850511, 122.4011828058666538, -21.87158679436075204 ) ) ;
#19659=( BOUNDED_SURFACE ( )  B_SPLINE_SURFACE ( 3, 1, ( 
 ( #13322, #19667 ),
 ( #21841, #4412 ),
 ( #15199, #26155 ),
 ( #373, #19536 ) ),
 .UNSPECIFIED., .F., .F., .F. ) 
 B_SPLINE_SURFACE_WITH_KNOTS ( ( 4, 4 ),
 ( 2, 2 ),
 ( 0.000000000000000000, 1.000000000000000000 ),
 ( 0.000000000000000000, 1.000000000000000000 ),
 .UNSPECIFIED. ) 
 GEOMETRIC_REPRESENTATION_ITEM ( )  RATIONAL_B_SPLINE_SURFACE ( (
 ( 1.000000000000000000, 1.000000000000000000),
 ( 0.9956975270656955868, 0.8568959468854907557),
 ( 0.9956975270656955868, 0.8568959468854907557),
 ( 1.000000000000000000, 1.000000000000000000) ) ) 
 REPRESENTATION_ITEM ( '' )  SURFACE ( )  );
#19660=ORIENTED_EDGE ( 'NONE', *, *, #23655, .F. ) ;
#19665=CARTESIAN_POINT ( 'NONE',  ( 1.833838850093452599, 117.3962664098823439, 85.29337590730578711 ) ) ;
#19666=ORIENTED_EDGE ( 'NONE', *, *, #20094, .F. ) ;
#19667=CARTESIAN_POINT ( 'NONE',  ( 1.832998868059858122, 29.64765804470072652, 142.0492247521723925 ) ) ;
#19668=CARTESIAN_POINT ( 'NONE',  ( 109.1592201516379674, 0.007566779963325568660, 0.002134489919768169444 ) ) ;
#19671=ORIENTED_EDGE ( 'NONE', *, *, #1572, .F. ) ;
#19673=CARTESIAN_POINT ( 'NONE',  ( 10.93730112725996229, -20.69552240458240888, -149.7554878793151545 ) ) ;
#19676=EDGE_CURVE ( 'NONE', #14235, #9093, #4113, .T. ) ;
#19677=DIRECTION ( 'NONE',  ( -0.5914120900931443270, 0.008020494142996235920, 0.8063295922669343474 ) ) ;
#19678=DIRECTION ( 'NONE',  ( 0.000000000000000000, 6.938893903907228378E-16, 1.000000000000000000 ) ) ;
#19679=CARTESIAN_POINT ( 'NONE',  ( 25.64681081121879203, 23.06870491922322230, 110.5293738517609228 ) ) ;
#19680=FACE_OUTER_BOUND ( 'NONE', #11329, .T. ) ;
#19681=EDGE_CURVE ( 'NONE', #27586, #28027, #11676, .T. ) ;
#19684=CARTESIAN_POINT ( 'NONE',  ( 32.73300124599732186, 0.000000000000000000, 0.000000000000000000 ) ) ;
#19686=CARTESIAN_POINT ( 'NONE',  ( 28.37644542392829194, -105.5967537682339525, -65.64862111872180606 ) ) ;
#19688=ORIENTED_EDGE ( 'NONE', *, *, #2151, .T. ) ;
#19690=CARTESIAN_POINT ( 'NONE',  ( 25.64700659047695552, 103.0567718204601846, 46.13293552475826687 ) ) ;
#19692=CARTESIAN_POINT ( 'NONE',  ( 2.108985857320929025, 98.16869034643305270, 107.1123114102931595 ) ) ;
#19694=CARTESIAN_POINT ( 'NONE',  ( 2.430230287190592531, -138.8342928068217077, -43.58368230469531568 ) ) ;
#19696=CARTESIAN_POINT ( 'NONE',  ( 8.186469829614374305, -42.84118568057105847, -143.0750865143072588 ) ) ;
#19699=CARTESIAN_POINT ( 'NONE',  ( 1.894214914920919757, 31.11059045489134789, 141.7768822502887929 ) ) ;
#19703=DIRECTION ( 'NONE',  ( -0.5914120900931443270, -0.5335794202785262286, 0.6045864222316693626 ) ) ;
#19706=ORIENTED_EDGE ( 'NONE', *, *, #18220, .T. ) ;
#19708=CARTESIAN_POINT ( 'NONE',  ( 2.430230287190589422, 43.58368230469574911, -138.8342928068215656 ) ) ;
#19709=ORIENTED_EDGE ( 'NONE', *, *, #10988, .F. ) ;
#19710=B_SPLINE_CURVE_WITH_KNOTS ( 'NONE', 3,
 ( #24846, #9441, #13738, #27116, #2812, #15908, #11588 ),
 .UNSPECIFIED., .F., .F.,
 ( 4, 3, 4 ),
 ( 0.000000000000000000, 0.02398743853561358455, 0.04000277880656216700 ),
 .UNSPECIFIED. ) ;
#19712=ORIENTED_EDGE ( 'NONE', *, *, #15067, .F. ) ;
#19714=CARTESIAN_POINT ( 'NONE',  ( 109.1587776205901861, -0.002904816147412016356, 0.006729130500864200642 ) ) ;
#19717=EDGE_CURVE ( 'NONE', #10457, #9181, #344, .T. ) ;
#19719=LINE ( 'NONE', #21892, #10203 ) ;
#19721=ORIENTED_EDGE ( 'NONE', *, *, #7823, .F. ) ;
#19723=CARTESIAN_POINT ( 'NONE',  ( 1.833809397773840777, 141.9756687985006636, -29.99591688576947845 ) ) ;
#19725=CARTESIAN_POINT ( 'NONE',  ( 5.340103556456518241, -96.93942141425988268, -111.1041836730288708 ) ) ;
#19726=FACE_OUTER_BOUND ( 'NONE', #21107, .T. ) ;
#19728=DIRECTION ( 'NONE',  ( -0.000000000000000000, 1.000000000000000000, -0.000000000000000000 ) ) ;
#19730=CYLINDRICAL_SURFACE ( 'NONE', #21286, 80.00000000000000000 ) ;
#19731=CARTESIAN_POINT ( 'NONE',  ( 1.834118845439484335, 97.22976650547425947, 107.7186227765457858 ) ) ;
#19733=ORIENTED_EDGE ( 'NONE', *, *, #22395, .F. ) ;
#19734=CARTESIAN_POINT ( 'NONE',  ( 1.833485406944057594, -142.0485807715644171, -29.64752363041688454 ) ) ;
#19735=CARTESIAN_POINT ( 'NONE',  ( 2.433796855181233454, -84.34988187691011774, 118.5671979538053904 ) ) ;
#19736=ORIENTED_EDGE ( 'NONE', *, *, #20786, .F. ) ;
#19737=( BOUNDED_SURFACE ( )  B_SPLINE_SURFACE ( 3, 1, ( 
 ( #10738, #19931 ),
 ( #21132, #15162 ),
 ( #13296, #28404 ),
 ( #24121, #4238 ) ),
 .UNSPECIFIED., .F., .F., .F. ) 
 B_SPLINE_SURFACE_WITH_KNOTS ( ( 4, 4 ),
 ( 2, 2 ),
 ( 0.000000000000000000, 1.000000000000000000 ),
 ( 0.000000000000000000, 1.000000000000000000 ),
 .UNSPECIFIED. ) 
 GEOMETRIC_REPRESENTATION_ITEM ( )  RATIONAL_B_SPLINE_SURFACE ( (
 ( 1.000000000000000000, 1.000000000000000000),
 ( 0.9956975270656954757, 0.8568959468854893125),
 ( 0.9956975270656954757, 0.8568959468854893125),
 ( 1.000000000000000000, 1.000000000000000000) ) ) 
 REPRESENTATION_ITEM ( '' )  SURFACE ( )  );
#19738=VERTEX_POINT ( 'NONE', #24547 ) ;
#19740=EDGE_CURVE ( 'NONE', #17200, #9116, #526, .T. ) ;
#19741=EDGE_CURVE ( 'NONE', #6430, #6599, #7249, .T. ) ;
#19742=CARTESIAN_POINT ( 'NONE',  ( 1.833485406944043827, 144.2578170162065021, -15.69895494453236395 ) ) ;
#19743=EDGE_CURVE ( 'NONE', #4329, #20108, #11716, .T. ) ;
#19744=B_SPLINE_CURVE_WITH_KNOTS ( 'NONE', 3,
 ( #21405, #19242, #4263, #28015, #10612, #10478, #21965, #15186 ),
 .UNSPECIFIED., .F., .F.,
 ( 4, 2, 2, 4 ),
 ( 0.000000000000000000, 0.0002429592666046696586, 0.0004859185332093393173, 0.0009718370664186723462 ),
 .UNSPECIFIED. ) ;
#19748=CARTESIAN_POINT ( 'NONE',  ( 1.832998868059858122, -142.0492247521724778, 29.64765804470026467 ) ) ;
#19751=DIRECTION ( 'NONE',  ( 0.8320502949607718746, 6.793118186493350437E-17, 0.5547001952908368061 ) ) ;
#19752=CARTESIAN_POINT ( 'NONE',  ( 1.833485406944043827, 145.1085452359073145, 0.5339064996889848480 ) ) ;
#19754=CARTESIAN_POINT ( 'NONE',  ( 1.833838848569429913, -117.2916552720324432, 85.43736077718830302 ) ) ;
#19756=ORIENTED_EDGE ( 'NONE', *, *, #19235, .F. ) ;
#19758=CARTESIAN_POINT ( 'NONE',  ( 2.433796855181205476, 132.3327394885231456, 60.50726454507948660 ) ) ;
#19759=VECTOR ( 'NONE', #19512, 1000.000000000000114 ) ;
#19764=ORIENTED_EDGE ( 'NONE', *, *, #9436, .F. ) ;
#19769=ORIENTED_EDGE ( 'NONE', *, *, #10128, .F. ) ;
#19770=EDGE_LOOP ( 'NONE', ( #12588, #22152, #23727, #5676 ) ) ;
#19771=CARTESIAN_POINT ( 'NONE',  ( 109.1586059443104944, -0.0004635842312890466835, -0.007058870754606107710 ) ) ;
#19772=ORIENTED_EDGE ( 'NONE', *, *, #22969, .F. ) ;
#19776=CARTESIAN_POINT ( 'NONE',  ( 32.73300124599735028, 72.21147546950551543, 92.86301839380053025 ) ) ;
#19777=ORIENTED_EDGE ( 'NONE', *, *, #16820, .F. ) ;
#19778=EDGE_CURVE ( 'NONE', #28093, #11774, #16168, .T. ) ;
#19783=CIRCLE ( 'NONE', #28064, 37.50000000000001421 ) ;
#19784=CARTESIAN_POINT ( 'NONE',  ( 109.1721716018069657, 0.01368917435591433980, -0.01019541462303498285 ) ) ;
#19785=CARTESIAN_POINT ( 'NONE',  ( 1.833206310202335265, 144.2348262833783963, -15.90849712171590902 ) ) ;
#19786=CARTESIAN_POINT ( 'NONE',  ( 28.37599760073042532, 45.02094138570584647, 105.5302221302108165 ) ) ;
#19788=CARTESIAN_POINT ( 'NONE',  ( 25.69398547355838502, -103.4778695380286138, -45.25878216557533307 ) ) ;
#19790=CYLINDRICAL_SURFACE ( 'NONE', #17058, 12.50000000000000178 ) ;
#19791=ORIENTED_EDGE ( 'NONE', *, *, #20573, .F. ) ;
#19792=CARTESIAN_POINT ( 'NONE',  ( 25.64704443564077252, 56.57116289738743120, -97.71717520928621070 ) ) ;
#19794=CARTESIAN_POINT ( 'NONE',  ( 25.98107933586719298, 45.01656174308578784, 103.7920584735895346 ) ) ;
#19795=CARTESIAN_POINT ( 'NONE',  ( 26.11404676487257603, 65.63269960453364149, -92.25884714080342519 ) ) ;
#19796=CARTESIAN_POINT ( 'NONE',  ( 32.73300124599738581, 108.9684813982494092, -44.31599526637845798 ) ) ;
#19798=CARTESIAN_POINT ( 'NONE',  ( 25.64700659047694487, -34.67498789830372630, -107.4550658295754886 ) ) ;
#19800=CARTESIAN_POINT ( 'NONE',  ( 2.063896406836605024, -60.31174178979897960, 132.1577797566303900 ) ) ;
#19801=CARTESIAN_POINT ( 'NONE',  ( 32.73300124599732186, 0.000000000000000000, 0.000000000000000000 ) ) ;
#19802=CARTESIAN_POINT ( 'NONE',  ( 21.16825799904902894, 75.99073816868455822, -112.1052598354958008 ) ) ;
#19804=VERTEX_POINT ( 'NONE', #4944 ) ;
#19805=B_SPLINE_CURVE_WITH_KNOTS ( 'NONE', 3,
 ( #3494, #25393, #10135, #27532, #18905, #7990, #16755 ),
 .UNSPECIFIED., .F., .F.,
 ( 4, 3, 4 ),
 ( 8.890457814381136359E-18, 0.0002669560319015655330, 0.0004157520161266013833 ),
 .UNSPECIFIED. ) ;
#19809=ADVANCED_FACE ( 'NONE', ( #3081 ), #16606, .F. ) ;
#19810=VERTEX_POINT ( 'NONE', #7555 ) ;
#19811=CARTESIAN_POINT ( 'NONE',  ( -40.00000000000000000, 0.000000000000000000, 0.000000000000000000 ) ) ;
#19812=EDGE_CURVE ( 'NONE', #23901, #17967, #24740, .T. ) ;
#19813=CARTESIAN_POINT ( 'NONE',  ( 30.59138290137872929, 95.58039132682516481, 66.10404757334093517 ) ) ;
#19821=CARTESIAN_POINT ( 'NONE',  ( 25.64670758986457955, 46.37945960492014308, -102.9458331681480843 ) ) ;
#19822=CARTESIAN_POINT ( 'NONE',  ( 2.108985857320901047, -138.5727354014054811, -43.67763756616795945 ) ) ;
#19823=CARTESIAN_POINT ( 'NONE',  ( 10.93730112725982373, -142.1801301103788262, 51.37919228020236773 ) ) ;
#19824=CARTESIAN_POINT ( 'NONE',  ( 109.1624594426973260, 0.007576898892904877086, 0.01405141589343896456 ) ) ;
#19826=ORIENTED_EDGE ( 'NONE', *, *, #13577, .F. ) ;
#19827=CARTESIAN_POINT ( 'NONE',  ( 13.36082413113063083, -106.9547846563628042, -109.3026516754243431 ) ) ;
#19831=VERTEX_POINT ( 'NONE', #22378 ) ;
#19835=ORIENTED_EDGE ( 'NONE', *, *, #23491, .T. ) ;
#19837=CARTESIAN_POINT ( 'NONE',  ( 10.93730112725978287, -136.0306644680987915, 65.95960219663069779 ) ) ;
#19840=DIRECTION ( 'NONE',  ( -1.000000000000000000, -0.000000000000000000, -0.000000000000000000 ) ) ;
#19841=EDGE_CURVE ( 'NONE', #3526, #21162, #22638, .T. ) ;
#19843=ORIENTED_EDGE ( 'NONE', *, *, #25438, .T. ) ;
#19846=CARTESIAN_POINT ( 'NONE',  ( 5.340103556456495149, 75.71042922800717179, -126.5279493230351875 ) ) ;
#19847=DIRECTION ( 'NONE',  ( 0.5946245182733607137, -0.8039981203473692828, -0.002950380665387635458 ) ) ;
#19848=B_SPLINE_CURVE_WITH_KNOTS ( 'NONE', 3,
 ( #26448, #8352, #6751, #15495, #1843, #15078, #25908, #6200 ),
 .UNSPECIFIED., .F., .F.,
 ( 4, 2, 2, 4 ),
 ( 0.000000000000000000, 0.0002429592666046706344, 0.0004859185332093412689, 0.0009718370664186825377 ),
 .UNSPECIFIED. ) ;
#19849=CARTESIAN_POINT ( 'NONE',  ( 1.833206308920097394, 45.54896581797642341, -137.7753864329220619 ) ) ;
#19851=CARTESIAN_POINT ( 'NONE',  ( 26.28373643307403285, 9.189598927293648245, -127.2291519022770956 ) ) ;
#19854=ADVANCED_FACE ( 'NONE', ( #16458 ), #92, .T. ) ;
#19855=AXIS2_PLACEMENT_3D ( 'NONE', #11510, #27337, #9507 ) ;
#19858=EDGE_LOOP ( 'NONE', ( #24206, #2589, #16519, #27613 ) ) ;
#19859=CIRCLE ( 'NONE', #23566, 151.1787379149930359 ) ;
#19861=DIRECTION ( 'NONE',  ( -1.000000000000000000, -0.000000000000000000, -0.000000000000000000 ) ) ;
#19863=ORIENTED_EDGE ( 'NONE', *, *, #11541, .T. ) ;
#19866=ORIENTED_EDGE ( 'NONE', *, *, #24913, .F. ) ;
#19869=CARTESIAN_POINT ( 'NONE',  ( 1.833750490713681458, 141.9939712933758642, -29.90883416717475640 ) ) ;
#19872=LINE ( 'NONE', #26074, #5173 ) ;
#19874=VECTOR ( 'NONE', #4562, 1000.000000000000114 ) ;
#19877=VECTOR ( 'NONE', #1991, 1000.000000000000000 ) ;
#19879=CARTESIAN_POINT ( 'NONE',  ( 1.832998868059890096, 107.4798986104873109, -97.49378069860691198 ) ) ;
#19881=FACE_OUTER_BOUND ( 'NONE', #1355, .T. ) ;
#19883=CARTESIAN_POINT ( 'NONE',  ( 26.11404676487259024, -1.130420376096339385, -113.2169081140374232 ) ) ;
#19884=EDGE_CURVE ( 'NONE', #24940, #17233, #27536, .T. ) ;
#19885=ORIENTED_EDGE ( 'NONE', *, *, #18625, .F. ) ;
#19886=ADVANCED_FACE ( 'NONE', ( #25397 ), #23422, .F. ) ;
#19891=EDGE_CURVE ( 'NONE', #20281, #15583, #11013, .T. ) ;
#19892=VERTEX_POINT ( 'NONE', #7505 ) ;
#19895=CARTESIAN_POINT ( 'NONE',  ( 109.1589550718174877, 0.007270618150629033077, -0.002126635388725490582 ) ) ;
#19896=VECTOR ( 'NONE', #4699, 1000.000000000000000 ) ;
#19897=CARTESIAN_POINT ( 'NONE',  ( 109.1589550718175161, -0.007553890059316987690, -0.0005685167901217184081 ) ) ;
#19898=EDGE_CURVE ( 'NONE', #11599, #10661, #17459, .T. ) ;
#19903=CARTESIAN_POINT ( 'NONE',  ( 6.224689322667647851, -146.9579047224770818, 18.02516478984095372 ) ) ;
#19905=CARTESIAN_POINT ( 'NONE',  ( 13.36082413113061307, -129.1512766091115623, -81.89226687792222492 ) ) ;
#19908=EDGE_CURVE ( 'NONE', #10454, #16841, #649, .T. ) ;
#19909=ORIENTED_EDGE ( 'NONE', *, *, #17794, .F. ) ;
#19911=CARTESIAN_POINT ( 'NONE',  ( 30.59141879584289825, -115.2623358717302295, -14.83090566979546487 ) ) ;
#19912=CARTESIAN_POINT ( 'NONE',  ( 25.65782528836479770, -22.91156770660721520, -110.5695798068305606 ) ) ;
#19914=CARTESIAN_POINT ( 'NONE',  ( 10.93730112725971715, -20.69552240458431314, 149.7554878793147282 ) ) ;
#19915=CARTESIAN_POINT ( 'NONE',  ( 25.64681081121879203, -107.2555980796238657, -35.28660243342658731 ) ) ;
#19916=VECTOR ( 'NONE', #7118, 1000.000000000000000 ) ;
#19918=EDGE_LOOP ( 'NONE', ( #12039, #28031 ) ) ;
#19920=AXIS2_PLACEMENT_3D ( 'NONE', #14204, #27168, #5748 ) ;
#19921=ADVANCED_FACE ( 'NONE', ( #20581 ), #11643, .F. ) ;
#19923=CARTESIAN_POINT ( 'NONE',  ( 2.063896406836605024, 84.29612368209153317, 118.3103904147684631 ) ) ;
#19924=ORIENTED_EDGE ( 'NONE', *, *, #12549, .F. ) ;
#19925=B_SPLINE_CURVE_WITH_KNOTS ( 'NONE', 3,
 ( #12367, #23471, #25195, #20871 ),
 .UNSPECIFIED., .F., .F.,
 ( 4, 4 ),
 ( 1.729163450533575901E-16, 0.008383748772659649698 ),
 .UNSPECIFIED. ) ;
#19926=VERTEX_POINT ( 'NONE', #20146 ) ;
#19928=DIRECTION ( 'NONE',  ( 0.7071067811865465735, 0.000000000000000000, 0.7071067811865485719 ) ) ;
#19929=EDGE_CURVE ( 'NONE', #2978, #1180, #11303, .T. ) ;
#19930=ORIENTED_EDGE ( 'NONE', *, *, #12160, .T. ) ;
#19931=CARTESIAN_POINT ( 'NONE',  ( 2.430230287190589422, 118.5711603495681459, 84.35270093935295677 ) ) ;
#19933=CARTESIAN_POINT ( 'NONE',  ( 109.1592201516379674, 0.005027640251764384401, -0.006044422199831492315 ) ) ;
#19935=CARTESIAN_POINT ( 'NONE',  ( 109.1592201516379674, 0.002913740842108636896, 0.007302213399779935825 ) ) ;
#19937=CARTESIAN_POINT ( 'NONE',  ( 9.884929003653608603, -50.49804566712222709, 141.8132360130356062 ) ) ;
#19940=CARTESIAN_POINT ( 'NONE',  ( 1.832998868059890096, 108.1944082009157455, 96.70023740551157232 ) ) ;
#19941=B_SPLINE_CURVE_WITH_KNOTS ( 'NONE', 3,
 ( #7253, #18016, #26805, #7115, #11704, #20475, #15872 ),
 .UNSPECIFIED., .F., .F.,
 ( 4, 3, 4 ),
 ( 5.285450785082491170E-16, 0.02816610861753246486, 0.04000277880656266660 ),
 .UNSPECIFIED. ) ;
#19942=B_SPLINE_CURVE_WITH_KNOTS ( 'NONE', 3,
 ( #26466, #11355, #2869, #6768, #9357, #15515, #24328, #13358 ),
 .UNSPECIFIED., .F., .F.,
 ( 4, 2, 2, 4 ),
 ( 0.000000000000000000, 0.0002429588503611265532, 0.0004859177007222531064, 0.0009718354014444913593 ),
 .UNSPECIFIED. ) ;
#19943=DIRECTION ( 'NONE',  ( -0.000000000000000000, 1.000000000000000000, 0.000000000000000000 ) ) ;
#19945=CARTESIAN_POINT ( 'NONE',  ( 25.64681081121880624, -56.09509703373412748, 97.99105938547904771 ) ) ;
#19948=CARTESIAN_POINT ( 'NONE',  ( 1.832998868059858122, 144.3700883710219216, -14.63705790013859875 ) ) ;
#19951=CARTESIAN_POINT ( 'NONE',  ( 109.1592201516379674, 0.006044422199822535938, -0.005027640251767235419 ) ) ;
#19952=CARTESIAN_POINT ( 'NONE',  ( 25.98552792386799837, 90.89136171349180415, -67.36997957637572654 ) ) ;
#19953=CARTESIAN_POINT ( 'NONE',  ( 1.833838850855462388, -44.92600961247758562, 137.9800888515322299 ) ) ;
#19954=EDGE_CURVE ( 'NONE', #4838, #26195, #18713, .T. ) ;
#19955=CARTESIAN_POINT ( 'NONE',  ( 1.834118845439484335, 145.1099497418795750, -0.1779704863075349530 ) ) ;
#19957=CARTESIAN_POINT ( 'NONE',  ( 55.79472521941428198, -66.16469064668319788, 30.25520714117883259 ) ) ;
#19958=ORIENTED_EDGE ( 'NONE', *, *, #3773, .F. ) ;
#19960=CARTESIAN_POINT ( 'NONE',  ( 109.1778270068192853, 0.003465086990427089769, 0.008646067828078128972 ) ) ;
#19963=CARTESIAN_POINT ( 'NONE',  ( 25.64692872815577473, -112.9107203549055498, -0.3216598674795657642 ) ) ;
#19965=ORIENTED_EDGE ( 'NONE', *, *, #12440, .T. ) ;
#19968=CARTESIAN_POINT ( 'NONE',  ( 2.433796855181219243, 144.5536872373191670, 16.65276281464612396 ) ) ;
#19970=CARTESIAN_POINT ( 'NONE',  ( 25.87036335909427365, -113.0557711752706211, 0.9898498320583746235 ) ) ;
#19971=VERTEX_POINT ( 'NONE', #23764 ) ;
#19972=CARTESIAN_POINT ( 'NONE',  ( 25.64681081121879203, -34.49579773461710630, -107.5125461021406181 ) ) ;
#19973=CARTESIAN_POINT ( 'NONE',  ( 13.36082413113063083, 152.6206443696328563, 9.660980093455210138 ) ) ;
#19975=CARTESIAN_POINT ( 'NONE',  ( 26.11404676487257603, -98.61392875273325842, -55.62948129436350087 ) ) ;
#19978=ORIENTED_EDGE ( 'NONE', *, *, #13305, .F. ) ;
#19980=FACE_OUTER_BOUND ( 'NONE', #18880, .T. ) ;
#19985=DIRECTION ( 'NONE',  ( -0.5914120900931443270, -0.8027508043202530308, -0.07630783613001643206 ) ) ;
#19987=CARTESIAN_POINT ( 'NONE',  ( 2.263178607246655982, 31.59906277834222266, 141.9207363487295481 ) ) ;
#19990=EDGE_CURVE ( 'NONE', #106, #16635, #16708, .T. ) ;
#19997=ORIENTED_EDGE ( 'NONE', *, *, #27615, .F. ) ;
#19999=ORIENTED_EDGE ( 'NONE', *, *, #10334, .F. ) ;
#20000=LINE ( 'NONE', #11365, #7771 ) ;
#20001=CARTESIAN_POINT ( 'NONE',  ( 25.98552792386801968, 84.79516057869876988, 74.89816102339737824 ) ) ;
#20002=CARTESIAN_POINT ( 'NONE',  ( 8.186469777910533097, 146.7694294853781116, 27.65107827750139435 ) ) ;
#20006=ORIENTED_EDGE ( 'NONE', *, *, #15856, .T. ) ;
#20010=B_SPLINE_CURVE_WITH_KNOTS ( 'NONE', 3,
 ( #11419, #3078, #631, #5370 ),
 .UNSPECIFIED., .F., .F.,
 ( 4, 4 ),
 ( 1.734723475976807094E-17, 0.008383560773332731156 ),
 .UNSPECIFIED. ) ;
#20011=CARTESIAN_POINT ( 'NONE',  ( 25.64704443564079739, -45.80316013050762791, -103.2037466592378507 ) ) ;
#20012=EDGE_CURVE ( 'NONE', #23708, #25105, #18896, .T. ) ;
#20015=CARTESIAN_POINT ( 'NONE',  ( 109.1592201516379674, 0.006174480289200316024, 0.004867031887010233454 ) ) ;
#20016=CARTESIAN_POINT ( 'NONE',  ( 109.1586900883932856, 0.0008465529156635116835, 0.007088091345229658585 ) ) ;
#20017=CARTESIAN_POINT ( 'NONE',  ( 109.1592201516379674, 0.007302213399787552996, 0.002913740842103208079 ) ) ;
#20019=EDGE_CURVE ( 'NONE', #8700, #10668, #8082, .T. ) ;
#20020=CARTESIAN_POINT ( 'NONE',  ( -40.00000000000000000, 0.000000000000000000, 0.000000000000000000 ) ) ;
#20021=CARTESIAN_POINT ( 'NONE',  ( 25.73574536432414561, -65.74844932374591622, -91.86645484851379706 ) ) ;
#20023=CARTESIAN_POINT ( 'NONE',  ( 26.11404676487257603, -10.71016160607644174, 112.7148551500680185 ) ) ;
#20025=ORIENTED_EDGE ( 'NONE', *, *, #525, .F. ) ;
#20027=ORIENTED_EDGE ( 'NONE', *, *, #17222, .F. ) ;
#20029=VERTEX_POINT ( 'NONE', #10380 ) ;
#20030=DIRECTION ( 'NONE',  ( 0.5946245182733608248, -0.7858154137795719807, -0.1700465163848226269 ) ) ;
#20032=B_SPLINE_CURVE_WITH_KNOTS ( 'NONE', 3,
 ( #540, #18371, #9338, #18095, #26873, #27153, #24747 ),
 .UNSPECIFIED., .F., .F.,
 ( 4, 3, 4 ),
 ( 0.000000000000000000, 0.02398743853561372680, 0.04000277880656215312 ),
 .UNSPECIFIED. ) ;
#20035=EDGE_CURVE ( 'NONE', #28149, #19505, #18531, .T. ) ;
#20038=CARTESIAN_POINT ( 'NONE',  ( 1.833206310202335265, -144.3905118062893109, -14.42724831649501560 ) ) ;
#20039=CARTESIAN_POINT ( 'NONE',  ( 24.01988960052050359, -44.53753990739600255, 123.2441023955617254 ) ) ;
#20040=CARTESIAN_POINT ( 'NONE',  ( 1.833485406944043827, 108.1939177044938560, -96.69979900902059455 ) ) ;
#20041=EDGE_CURVE ( 'NONE', #13623, #17999, #13694, .T. ) ;
#20042=CARTESIAN_POINT ( 'NONE',  ( 21.16825799904898631, -115.0183107335394368, 71.50503315297841311 ) ) ;
#20043=FACE_OUTER_BOUND ( 'NONE', #18504, .T. ) ;
#20046=CARTESIAN_POINT ( 'NONE',  ( 30.59141879584322510, 115.8270959620731873, -9.457572341075218603 ) ) ;
#20047=CARTESIAN_POINT ( 'NONE',  ( 28.37599760073042532, -113.9023239246301955, -13.77583212279449398 ) ) ;
#20048=CARTESIAN_POINT ( 'NONE',  ( 109.1778270068192853, -0.008646067828078141115, 0.003465086990427058110 ) ) ;
#20049=CARTESIAN_POINT ( 'NONE',  ( 13.84597867724971998, 90.05293531772780113, -115.8103190066264006 ) ) ;
#20051=CARTESIAN_POINT ( 'NONE',  ( 25.64681081121880624, -56.09509703373412748, 97.99105938547904771 ) ) ;
#20052=ORIENTED_EDGE ( 'NONE', *, *, #22681, .T. ) ;
#20053=CARTESIAN_POINT ( 'NONE',  ( 1.833838850093465700, -15.16810397409683198, -144.3148362521193633 ) ) ;
#20054=ORIENTED_EDGE ( 'NONE', *, *, #525, .T. ) ;
#20056=CARTESIAN_POINT ( 'NONE',  ( 1.833206308920068306, 141.7818018507502416, 30.89799439741674192 ) ) ;
#20058=B_SPLINE_CURVE_WITH_KNOTS ( 'NONE', 3,
 ( #2923, #4425, #24033, #17244 ),
 .UNSPECIFIED., .F., .F.,
 ( 4, 4 ),
 ( 0.000000000000000000, 0.008383560773332705135 ),
 .UNSPECIFIED. ) ;
#20059=VERTEX_POINT ( 'NONE', #19972 ) ;
#20060=CARTESIAN_POINT ( 'NONE',  ( 28.37603512858445853, 25.60641750873904954, 111.8384105897142859 ) ) ;
#20061=ORIENTED_EDGE ( 'NONE', *, *, #25296, .T. ) ;
#20062=CARTESIAN_POINT ( 'NONE',  ( 109.1592201516379674, 0.007566779963325568660, 0.002134489919768169444 ) ) ;
#20063=ORIENTED_EDGE ( 'NONE', *, *, #25291, .T. ) ;
#20064=B_SPLINE_CURVE_WITH_KNOTS ( 'NONE', 3,
 ( #19945, #8875, #15464, #24137, #4398, #9015, #21825, #11030, #26551, #4257 ),
 .UNSPECIFIED., .F., .F.,
 ( 4, 3, 3, 4 ),
 ( 6.938893903907228378E-18, 0.0002669560319015819587, 0.0005492286108966481758, 0.0008315040496093573661 ),
 .UNSPECIFIED. ) ;
#20065=CARTESIAN_POINT ( 'NONE',  ( 109.1586900883932856, 0.006231977675082106191, -0.003481399864227394114 ) ) ;
#20066=ADVANCED_FACE ( 'NONE', ( #15630 ), #4697, .T. ) ;
#20067=CARTESIAN_POINT ( 'NONE',  ( 8.186469829614351212, -84.95702201190461267, -122.8338389144555549 ) ) ;
#20071=ADVANCED_FACE ( 'NONE', ( #1988 ), #9982, .F. ) ;
#20072=CARTESIAN_POINT ( 'NONE',  ( 1.833721034905634539, -72.86293192427403653, -125.4904194343092172 ) ) ;
#20073=CARTESIAN_POINT ( 'NONE',  ( 5.340103556456447187, -62.06990747183774459, 133.7487107983441490 ) ) ;
#20074=CARTESIAN_POINT ( 'NONE',  ( 30.58324630866351512, 63.85566901681615093, 102.7123253644116829 ) ) ;
#20075=( BOUNDED_SURFACE ( )  B_SPLINE_SURFACE ( 3, 1, ( 
 ( #5569, #16502 ),
 ( #3408, #14334 ),
 ( #16931, #3832 ),
 ( #27731, #19222 ) ),
 .UNSPECIFIED., .F., .F., .F. ) 
 B_SPLINE_SURFACE_WITH_KNOTS ( ( 4, 4 ),
 ( 2, 2 ),
 ( 0.000000000000000000, 1.000000000000000000 ),
 ( 0.000000000000000000, 1.000000000000000000 ),
 .UNSPECIFIED. ) 
 GEOMETRIC_REPRESENTATION_ITEM ( )  RATIONAL_B_SPLINE_SURFACE ( (
 ( 1.000000000000000000, 1.000000000000000000),
 ( 0.9956975270656954757, 0.8568959468854893125),
 ( 0.9956975270656954757, 0.8568959468854893125),
 ( 1.000000000000000000, 1.000000000000000000) ) ) 
 REPRESENTATION_ITEM ( '' )  SURFACE ( )  );
#20079=LINE ( 'NONE', #796, #23056 ) ;
#20081=CARTESIAN_POINT ( 'NONE',  ( 25.64681081121879203, -84.18689316040098447, 75.24277141833462679 ) ) ;
#20082=CARTESIAN_POINT ( 'NONE',  ( 1.834118845439484335, -45.01070051384685655, 137.9527673765103941 ) ) ;
#20083=CARTESIAN_POINT ( 'NONE',  ( 2.263178607246674190, -125.2099936970372767, 73.90841395012540715 ) ) ;
#20084=CARTESIAN_POINT ( 'NONE',  ( 1.833485406944043827, -107.4794113447402566, -97.49333871408801144 ) ) ;
#20085=CARTESIAN_POINT ( 'NONE',  ( 2.063896406836609909, -125.1295119249444241, 73.79559738457707851 ) ) ;
#20086=DIRECTION ( 'NONE',  ( 0.5946245182733607137, 0.2456431038754758323, 0.7655593692109030624 ) ) ;
#20087=CARTESIAN_POINT ( 'NONE',  ( 25.64708228042121263, 75.58165863986150157, -83.88307475435979654 ) ) ;
#20092=ORIENTED_EDGE ( 'NONE', *, *, #6646, .F. ) ;
#20093=CARTESIAN_POINT ( 'NONE',  ( 5.340103556456524458, 32.90561046456912919, -143.7310399800114737 ) ) ;
#20094=EDGE_CURVE ( 'NONE', #4882, #18134, #28182, .T. ) ;
#20098=EDGE_CURVE ( 'NONE', #11372, #21365, #23005, .T. ) ;
#20099=VERTEX_POINT ( 'NONE', #6607 ) ;
#20100=CARTESIAN_POINT ( 'NONE',  ( 2.433796855181219243, -144.8571464219890004, 13.76554153471645847 ) ) ;
#20101=DIRECTION ( 'NONE',  ( -0.000000000000000000, -1.000000000000000000, -3.122502256758243304E-15 ) ) ;
#20103=DIRECTION ( 'NONE',  ( -0.5946245182733607137, 0.7858154137795742011, -0.1700465163848121908 ) ) ;
#20105=CARTESIAN_POINT ( 'NONE',  ( 55.79472521941426777, -28.92526238350430390, -66.75682020267559835 ) ) ;
#20107=CARTESIAN_POINT ( 'NONE',  ( 109.1586900883932856, 0.001582822706024251871, -0.006960773163856037206 ) ) ;
#20108=VERTEX_POINT ( 'NONE', #4427 ) ;
#20110=CARTESIAN_POINT ( 'NONE',  ( 25.64706015949228046, 0.09919735511166506703, 112.9111942614907491 ) ) ;
#20111=CARTESIAN_POINT ( 'NONE',  ( 1.833485406944043827, -96.69979900902241354, 108.1939177044922786 ) ) ;
#20114=( BOUNDED_SURFACE ( )  B_SPLINE_SURFACE ( 3, 1, ( 
 ( #28282, #8719 ),
 ( #8581, #26135 ),
 ( #6425, #21823 ),
 ( #2084, #10887 ) ),
 .UNSPECIFIED., .F., .F., .F. ) 
 B_SPLINE_SURFACE_WITH_KNOTS ( ( 4, 4 ),
 ( 2, 2 ),
 ( 0.000000000000000000, 1.000000000000000000 ),
 ( 0.000000000000000000, 1.000000000000000000 ),
 .UNSPECIFIED. ) 
 GEOMETRIC_REPRESENTATION_ITEM ( )  RATIONAL_B_SPLINE_SURFACE ( (
 ( 1.000000000000000000, 1.000000000000000000),
 ( 0.9956975270656955868, 0.8568959468854907557),
 ( 0.9956975270656955868, 0.8568959468854907557),
 ( 1.000000000000000000, 1.000000000000000000) ) ) 
 REPRESENTATION_ITEM ( '' )  SURFACE ( )  );
#20115=ORIENTED_EDGE ( 'NONE', *, *, #22095, .T. ) ;
#20120=CARTESIAN_POINT ( 'NONE',  ( 94.22246935314088034, -69.99999999999998579, -6.938893903907228378E-15 ) ) ;
#20122=CARTESIAN_POINT ( 'NONE',  ( 25.64708228042120908, -91.32398912286983261, -66.39944550735367557 ) ) ;
#20124=CARTESIAN_POINT ( 'NONE',  ( 10.93730112725977932, -108.9902118373748863, 104.7670965581006755 ) ) ;
#20125=CARTESIAN_POINT ( 'NONE',  ( 2.430230287190589422, 132.3371620660959138, -60.50928654924622663 ) ) ;
#20126=CARTESIAN_POINT ( 'NONE',  ( 24.22246935314087324, 0.000000000000000000, -111.9614997405030152 ) ) ;
#20128=B_SPLINE_CURVE_WITH_KNOTS ( 'NONE', 3,
 ( #9662, #7667, #2901, #11960, #27205, #9818, #23067, #7518 ),
 .UNSPECIFIED., .F., .F.,
 ( 4, 2, 2, 4 ),
 ( 0.000000000000000000, 0.0002429588503611202919, 0.0004859177007222405839, 0.0009718354014444863720 ),
 .UNSPECIFIED. ) ;
#20129=CARTESIAN_POINT ( 'NONE',  ( 25.98107933586707219, 102.9042679418251964, 47.01057192495316883 ) ) ;
#20130=CARTESIAN_POINT ( 'NONE',  ( 2.433796855181219243, 118.5671979538068257, -84.34988187690807138 ) ) ;
#20131=CARTESIAN_POINT ( 'NONE',  ( 109.1586059443104944, -0.002622205828288729987, -0.006570129623060863393 ) ) ;
#20132=CARTESIAN_POINT ( 'NONE',  ( 1.894214914920970605, -142.1734439042095630, -29.24491455759085667 ) ) ;
#20133=ORIENTED_EDGE ( 'NONE', *, *, #19595, .F. ) ;
#20134=B_SPLINE_CURVE_WITH_KNOTS ( 'NONE', 3,
 ( #26078, #2301, #10968, #14079 ),
 .UNSPECIFIED., .F., .F.,
 ( 4, 4 ),
 ( 0.000000000000000000, 0.01077107196513851610 ),
 .UNSPECIFIED. ) ;
#20137=EDGE_CURVE ( 'NONE', #19171, #17689, #16134, .T. ) ;
#20140=CARTESIAN_POINT ( 'NONE',  ( 6.224689322667647851, 141.5842213414013600, 43.30635742325425497 ) ) ;
#20141=AXIS2_PLACEMENT_3D ( 'NONE', #7261, #2937, #13715 ) ;
#20142=ADVANCED_FACE ( 'NONE', ( #26445 ), #24516, .F. ) ;
#20143=CARTESIAN_POINT ( 'NONE',  ( 109.1592201516379674, 0.002134489919774364575, 0.007566779963318560377 ) ) ;
#20144=VERTEX_POINT ( 'NONE', #10645 ) ;
#20146=CARTESIAN_POINT ( 'NONE',  ( 26.11404676487257603, 74.91683232330973397, 84.89295829319517850 ) ) ;
#20150=ORIENTED_EDGE ( 'NONE', *, *, #11120, .F. ) ;
#20151=CARTESIAN_POINT ( 'NONE',  ( 1.833721034905586800, 141.8643653601974961, -30.51809396650877559 ) ) ;
#20152=CARTESIAN_POINT ( 'NONE',  ( 32.73300124599738581, -55.46353551261936587, -103.7392577722181812 ) ) ;
#20153=CARTESIAN_POINT ( 'NONE',  ( 109.1586900883932856, 0.007137750914550311347, -0.0001010081143976270922 ) ) ;
#20155=CARTESIAN_POINT ( 'NONE',  ( 1.833838848569429469, 132.4919773286277405, -59.18404309081229542 ) ) ;
#20157=FACE_OUTER_BOUND ( 'NONE', #26622, .T. ) ;
#20159=CARTESIAN_POINT ( 'NONE',  ( 2.063896406836605024, 107.0521644432417503, 98.19887492195893230 ) ) ;
#20161=VECTOR ( 'NONE', #24959, 1000.000000000000000 ) ;
#20162=CARTESIAN_POINT ( 'NONE',  ( 25.64681081121879203, -107.2555980796243773, 35.28660243342513070 ) ) ;
#20164=VECTOR ( 'NONE', #19847, 1000.000000000000341 ) ;
#20165=VERTEX_POINT ( 'NONE', #21717 ) ;
#20166=CARTESIAN_POINT ( 'NONE',  ( 1.893872463202055378, -96.41404152942862993, -108.5026245911428475 ) ) ;
#20169=B_SPLINE_CURVE_WITH_KNOTS ( 'NONE', 3,
 ( #7472, #1127, #7765, #5881, #14353, #16523, #1257 ),
 .UNSPECIFIED., .F., .F.,
 ( 4, 3, 4 ),
 ( 0.000000000000000000, 0.02398743853561364700, 0.04000277880656215312 ),
 .UNSPECIFIED. ) ;
#20170=ORIENTED_EDGE ( 'NONE', *, *, #2658, .F. ) ;
#20171=ORIENTED_EDGE ( 'NONE', *, *, #27400, .F. ) ;
#20172=CARTESIAN_POINT ( 'NONE',  ( 2.063896406836609909, 86.47093297169000436, 116.7302989755740725 ) ) ;
#20173=CARTESIAN_POINT ( 'NONE',  ( 2.433796855181233454, -126.7346379669250780, -71.49415740225209959 ) ) ;
#20176=EDGE_CURVE ( 'NONE', #23697, #26503, #5103, .T. ) ;
#20177=ADVANCED_FACE ( 'NONE', ( #25122 ), #8687, .F. ) ;
#20178=CARTESIAN_POINT ( 'NONE',  ( 25.64670758986459376, -107.2298587623393047, -35.36461833156630519 ) ) ;
#20179=CARTESIAN_POINT ( 'NONE',  ( 32.73300124599735739, -39.98094346392385745, 110.6325518752272501 ) ) ;
#20180=CARTESIAN_POINT ( 'NONE',  ( 32.73300124599735739, -72.21147546950616913, 92.86301839379999024 ) ) ;
#20181=CARTESIAN_POINT ( 'NONE',  ( 55.49584447822657296, -42.42793568432998086, 58.85239198729172472 ) ) ;
#20182=CARTESIAN_POINT ( 'NONE',  ( 24.22246935314087324, 1.371132922849442231E-14, 111.9614997405030152 ) ) ;
#20183=CARTESIAN_POINT ( 'NONE',  ( 109.1589550718175161, 0.002126635388718530872, -0.007270618150635357012 ) ) ;
#20184=CARTESIAN_POINT ( 'NONE',  ( 26.28373643307403640, 91.96212244992503315, -88.40064398363983855 ) ) ;
#20186=CARTESIAN_POINT ( 'NONE',  ( 26.11404676487257603, -112.4785329405481065, -12.95861723607569438 ) ) ;
#20187=CARTESIAN_POINT ( 'NONE',  ( 1.833838848569417701, -144.3334397096298005, -14.99110384899675807 ) ) ;
#20188=DIRECTION ( 'NONE',  ( -0.5946245182733608248, -0.6521823330502958260, -0.4701913299128841484 ) ) ;
#20192=CARTESIAN_POINT ( 'NONE',  ( 32.73300124599735739, -16.10546300444903167, 116.5274707358854869 ) ) ;
#20193=ORIENTED_EDGE ( 'NONE', *, *, #25079, .T. ) ;
#20195=CARTESIAN_POINT ( 'NONE',  ( 26.11404676487257603, -98.61392875273402581, 55.62948129436210110 ) ) ;
#20196=EDGE_LOOP ( 'NONE', ( #724, #24772, #3635, #27541 ) ) ;
#20198=EDGE_CURVE ( 'NONE', #24626, #19219, #21066, .T. ) ;
#20199=VERTEX_POINT ( 'NONE', #14303 ) ;
#20201=ORIENTED_EDGE ( 'NONE', *, *, #22784, .T. ) ;
#20202=ADVANCED_FACE ( 'NONE', ( #7421 ), #8867, .F. ) ;
#20205=CARTESIAN_POINT ( 'NONE',  ( 1.893872463202042500, 125.2243573918634638, 73.39855082356687888 ) ) ;
#20206=CARTESIAN_POINT ( 'NONE',  ( 1.833206308920111827, 137.7753864329225166, 45.54896581797505917 ) ) ;
#20207=CARTESIAN_POINT ( 'NONE',  ( 25.64699802086726521, -66.17503410043964607, 91.48665801621639559 ) ) ;
#20208=CARTESIAN_POINT ( 'NONE',  ( 1.833485406944043827, -73.01664920992880070, -125.4007332306553195 ) ) ;
#20209=CARTESIAN_POINT ( 'NONE',  ( 55.49584447822657296, 7.849835876628332265, 72.12568090333346049 ) ) ;
#20210=CIRCLE ( 'NONE', #11491, 151.1787379149930359 ) ;
#20211=CARTESIAN_POINT ( 'NONE',  ( 6.224689322667630975, -141.5842213414016157, 43.30635742325330284 ) ) ;
#20212=CARTESIAN_POINT ( 'NONE',  ( 28.37603512858452959, -86.45299531409403926, -75.42810021528178765 ) ) ;
#20214=ORIENTED_EDGE ( 'NONE', *, *, #16587, .F. ) ;
#20219=CARTESIAN_POINT ( 'NONE',  ( 28.37603512858447274, -109.6581134439365570, -33.74339723237898880 ) ) ;
#20221=CARTESIAN_POINT ( 'NONE',  ( 10.93730112725990189, -140.0398180619108075, -56.95489579269887059 ) ) ;
#20222=CARTESIAN_POINT ( 'NONE',  ( 109.1586900883932856, -0.0008465529156546314172, 0.007088091345232576390 ) ) ;
#20223=ORIENTED_EDGE ( 'NONE', *, *, #4713, .F. ) ;
#20224=CARTESIAN_POINT ( 'NONE',  ( 25.64708228042117355, 110.4520805602538758, -23.43704872438652131 ) ) ;
#20225=ORIENTED_EDGE ( 'NONE', *, *, #6162, .F. ) ;
#20227=ADVANCED_FACE ( 'NONE', ( #9569 ), #11815, .F. ) ;
#20229=AXIS2_PLACEMENT_3D ( 'NONE', #441, #22920, #3178 ) ;
#20234=AXIS2_PLACEMENT_3D ( 'NONE', #2767, #6526, #11547 ) ;
#20235=VERTEX_POINT ( 'NONE', #14157 ) ;
#20236=CARTESIAN_POINT ( 'NONE',  ( 1.834118845439484335, 138.0627591860429959, 44.67218053242439879 ) ) ;
#20237=ORIENTED_EDGE ( 'NONE', *, *, #7896, .T. ) ;
#20238=( NAMED_UNIT ( * ) SI_UNIT ( $, .STERADIAN. ) SOLID_ANGLE_UNIT ( ) );
#20239=( BOUNDED_SURFACE ( )  B_SPLINE_SURFACE ( 3, 1, ( 
 ( #25968, #25206 ),
 ( #3179, #14103 ),
 ( #3322, #870 ),
 ( #27350, #24928 ) ),
 .UNSPECIFIED., .F., .F., .F. ) 
 B_SPLINE_SURFACE_WITH_KNOTS ( ( 4, 4 ),
 ( 2, 2 ),
 ( 0.000000000000000000, 1.000000000000000000 ),
 ( 0.000000000000000000, 1.000000000000000000 ),
 .UNSPECIFIED. ) 
 GEOMETRIC_REPRESENTATION_ITEM ( )  RATIONAL_B_SPLINE_SURFACE ( (
 ( 1.000000000000000000, 1.000000000000000000),
 ( 0.9960225298536222738, 0.9999952330161893110),
 ( 0.9960225298536222738, 0.9999952330161893110),
 ( 1.000000000000000000, 1.000000000000000000) ) ) 
 REPRESENTATION_ITEM ( '' )  SURFACE ( )  );
#20241=CONICAL_SURFACE ( 'NONE', #6488, 117.6351876552689504, 0.9945805576725580410 ) ;
#20242=CARTESIAN_POINT ( 'NONE',  ( 25.64692872815576408, 107.4838747185725651, -34.58541472378539794 ) ) ;
#20244=CARTESIAN_POINT ( 'NONE',  ( 30.59141879584290891, -75.73279557183244037, -88.14706749784132001 ) ) ;
#20245=CARTESIAN_POINT ( 'NONE',  ( 25.69398547355838147, -112.9401428107247654, 0.7422864227361197775 ) ) ;
#20246=VERTEX_POINT ( 'NONE', #27702 ) ;
#20248=DIRECTION ( 'NONE',  ( 0.000000000000000000, 0.000000000000000000, 1.000000000000000000 ) ) ;
#20250=FACE_OUTER_BOUND ( 'NONE', #22460, .T. ) ;
#20251=ORIENTED_EDGE ( 'NONE', *, *, #3936, .F. ) ;
#20252=VECTOR ( 'NONE', #26114, 999.9999999999998863 ) ;
#20253=VERTEX_POINT ( 'NONE', #5248 ) ;
#20254=VECTOR ( 'NONE', #27600, 999.9999999999998863 ) ;
#20255=CARTESIAN_POINT ( 'NONE',  ( 94.22246935314088034, -151.1871800109700246, 12.49999999999999467 ) ) ;
#20257=CARTESIAN_POINT ( 'NONE',  ( 25.65782528836481902, -24.04194111108942522, 110.3293115225706202 ) ) ;
#20260=CARTESIAN_POINT ( 'NONE',  ( 10.93730112725994097, -51.37919228020192008, -142.1801301103790536 ) ) ;
#20262=VERTEX_POINT ( 'NONE', #14019 ) ;
#20263=CARTESIAN_POINT ( 'NONE',  ( 109.1587776205901577, 0.006305329297952418956, 0.003736572840486965252 ) ) ;
#20266=CARTESIAN_POINT ( 'NONE',  ( 1.833750490713744297, -145.1094586213657465, -0.2669522761660584886 ) ) ;
#20267=EDGE_CURVE ( 'NONE', #8144, #17963, #5853, .T. ) ;
#20269=EDGE_CURVE ( 'NONE', #12529, #3847, #10567, .T. ) ;
#20270=CARTESIAN_POINT ( 'NONE',  ( 109.1592201516379674, 0.0003082430542015802727, 0.007856029051022768092 ) ) ;
#20271=ORIENTED_EDGE ( 'NONE', *, *, #1774, .F. ) ;
#20272=CARTESIAN_POINT ( 'NONE',  ( 25.87036335909427009, -12.80197335559886085, -112.3329723497412544 ) ) ;
#20274=EDGE_LOOP ( 'NONE', ( #1228, #1015, #25639, #26026 ) ) ;
#20275=DIRECTION ( 'NONE',  ( 0.5946245182733607137, -0.002950380665396057540, 0.8039981203473692828 ) ) ;
#20276=EDGE_CURVE ( 'NONE', #27090, #26821, #21288, .T. ) ;
#20277=CARTESIAN_POINT ( 'NONE',  ( 25.64708228042119487, -56.42152786924437180, -97.80372460135731671 ) ) ;
#20278=ORIENTED_EDGE ( 'NONE', *, *, #16340, .F. ) ;
#20280=EDGE_CURVE ( 'NONE', #5960, #17673, #2046, .T. ) ;
#20281=VERTEX_POINT ( 'NONE', #25830 ) ;
#20282=VERTEX_POINT ( 'NONE', #10436 ) ;
#20283=CIRCLE ( 'NONE', #21660, 151.1787379149930359 ) ;
#20284=AXIS2_PLACEMENT_3D ( 'NONE', #13328, #22127, #21850 ) ;
#20285=CARTESIAN_POINT ( 'NONE',  ( 25.69398547355839568, 84.42756928260575933, 75.02007992711736506 ) ) ;
#20287=( BOUNDED_SURFACE ( )  B_SPLINE_SURFACE ( 3, 1, ( 
 ( #12515, #1442 ),
 ( #5920, #1165 ),
 ( #23059, #21009 ),
 ( #27636, #20879 ) ),
 .UNSPECIFIED., .F., .F., .F. ) 
 B_SPLINE_SURFACE_WITH_KNOTS ( ( 4, 4 ),
 ( 2, 2 ),
 ( 0.000000000000000000, 1.000000000000000000 ),
 ( 0.000000000000000000, 1.000000000000000000 ),
 .UNSPECIFIED. ) 
 GEOMETRIC_REPRESENTATION_ITEM ( )  RATIONAL_B_SPLINE_SURFACE ( (
 ( 1.000000000000000000, 1.000000000000000000),
 ( 0.6386103224230302855, 0.9954351624131538845),
 ( 0.6386103224230302855, 0.9954351624131538845),
 ( 1.000000000000000000, 1.000000000000000000) ) ) 
 REPRESENTATION_ITEM ( '' )  SURFACE ( )  );
#20288=FACE_OUTER_BOUND ( 'NONE', #7601, .T. ) ;
#20292=CARTESIAN_POINT ( 'NONE',  ( 25.64681081121879203, -102.9795863647031666, 46.30456157731292421 ) ) ;
#20293=CARTESIAN_POINT ( 'NONE',  ( 2.263178113027022764, -142.5035404044876088, 28.85718369185665821 ) ) ;
#20294=VERTEX_POINT ( 'NONE', #12845 ) ;
#20295=ORIENTED_EDGE ( 'NONE', *, *, #21324, .T. ) ;
#20297=CARTESIAN_POINT ( 'NONE',  ( 1.833206308920058536, 14.42724735286848947, 144.3905119031280719 ) ) ;
#20300=CARTESIAN_POINT ( 'NONE',  ( -40.00000000000000000, 0.000000000000000000, -80.00000000000000000 ) ) ;
#20304=EDGE_CURVE ( 'NONE', #17196, #6453, #23691, .T. ) ;
#20306=CARTESIAN_POINT ( 'NONE',  ( 109.1587776205901861, -0.006729130500864231000, -0.002904816147411946967 ) ) ;
#20308=VECTOR ( 'NONE', #12163, 1000.000000000000000 ) ;
#20309=ORIENTED_EDGE ( 'NONE', *, *, #28135, .T. ) ;
#20312=CARTESIAN_POINT ( 'NONE',  ( 8.186469829614216209, 71.65198613712979636, 131.0413692472655214 ) ) ;
#20314=ORIENTED_EDGE ( 'NONE', *, *, #313, .F. ) ;
#20315=ORIENTED_EDGE ( 'NONE', *, *, #12923, .F. ) ;
#20317=B_SPLINE_CURVE_WITH_KNOTS ( 'NONE', 3,
 ( #4563, #26306, #17522, #19968 ),
 .UNSPECIFIED., .F., .F.,
 ( 4, 4 ),
 ( 0.000000000000000000, 0.01077107196513799221 ),
 .UNSPECIFIED. ) ;
#20318=CARTESIAN_POINT ( 'NONE',  ( 109.1586900883932856, 0.004277182003220953051, -0.005715190711488734449 ) ) ;
#20321=CARTESIAN_POINT ( 'NONE',  ( 25.70243777736189017, -107.1912711514952576, -35.59945151684184594 ) ) ;
#20322=VECTOR ( 'NONE', #16367, 1000.000000000000000 ) ;
#20323=AXIS2_PLACEMENT_3D ( 'NONE', #1294, #25771, #5627 ) ;
#20324=CARTESIAN_POINT ( 'NONE',  ( 32.73300124599732186, 0.000000000000000000, 0.000000000000000000 ) ) ;
#20327=CARTESIAN_POINT ( 'NONE',  ( 1.833485406944057594, -132.7804117027884274, -58.53321471327013370 ) ) ;
#20328=CARTESIAN_POINT ( 'NONE',  ( 26.11404676487257603, 33.91085499298377925, 108.0249973236468577 ) ) ;
#20333=ORIENTED_EDGE ( 'NONE', *, *, #13544, .T. ) ;
#20335=CARTESIAN_POINT ( 'NONE',  ( 109.1624594426973118, -0.001206615835669557933, 0.01591840958353239049 ) ) ;
#20338=CARTESIAN_POINT ( 'NONE',  ( 10.93730112726002979, 92.80059208661855052, -119.3442956573263558 ) ) ;
#20343=ORIENTED_EDGE ( 'NONE', *, *, #7110, .F. ) ;
#20345=EDGE_CURVE ( 'NONE', #17200, #3161, #8220, .T. ) ;
#20347=CARTESIAN_POINT ( 'NONE',  ( 25.64681081121880624, 12.21581276189807497, 112.2483031020013868 ) ) ;
#20349=ADVANCED_FACE ( 'NONE', ( #19334 ), #19069, .F. ) ;
#20351=CIRCLE ( 'NONE', #10277, 117.6351876552689504 ) ;
#20352=ORIENTED_EDGE ( 'NONE', *, *, #17599, .T. ) ;
#20354=VECTOR ( 'NONE', #5586, 1000.000000000000114 ) ;
#20355=EDGE_LOOP ( 'NONE', ( #11465, #9779, #8399, #3593 ) ) ;
#20357=CARTESIAN_POINT ( 'NONE',  ( 109.1592201516379674, 0.001127733110588118211, 0.007780772729122761334 ) ) ;
#20359=FACE_OUTER_BOUND ( 'NONE', #21645, .T. ) ;
#20360=CARTESIAN_POINT ( 'NONE',  ( 109.1721716018069515, 0.01392660302850057957, -0.009868622090669602540 ) ) ;
#20361=CONICAL_SURFACE ( 'NONE', #3835, 117.6351876552689504, 0.9945805576725580410 ) ;
#20362=CARTESIAN_POINT ( 'NONE',  ( 5.340103579038068204, 135.6222865281528414, 57.86178752084538246 ) ) ;
#20364=CARTESIAN_POINT ( 'NONE',  ( 1.834118845439484335, -97.22976650547352051, -107.7186227765464395 ) ) ;
#20366=( BOUNDED_SURFACE ( )  B_SPLINE_SURFACE ( 3, 1, ( 
 ( #6828, #26386 ),
 ( #22223, #21931 ),
 ( #2190, #24387 ),
 ( #4656, #26659 ) ),
 .UNSPECIFIED., .F., .F., .F. ) 
 B_SPLINE_SURFACE_WITH_KNOTS ( ( 4, 4 ),
 ( 2, 2 ),
 ( 0.000000000000000000, 1.000000000000000000 ),
 ( 0.000000000000000000, 1.000000000000000000 ),
 .UNSPECIFIED. ) 
 GEOMETRIC_REPRESENTATION_ITEM ( )  RATIONAL_B_SPLINE_SURFACE ( (
 ( 1.000000000000000000, 1.000000000000000000),
 ( 0.6386103224230316178, 0.9954351624131538845),
 ( 0.6386103224230316178, 0.9954351624131538845),
 ( 1.000000000000000000, 1.000000000000000000) ) ) 
 REPRESENTATION_ITEM ( '' )  SURFACE ( )  );
#20368=DIRECTION ( 'NONE',  ( -0.5914120900931442160, -0.3962188444547289912, 0.7023121577978114205 ) ) ;
#20370=CARTESIAN_POINT ( 'NONE',  ( 25.86096068574581963, 45.07009591924560254, 103.6815822123520263 ) ) ;
#20371=B_SPLINE_CURVE_WITH_KNOTS ( 'NONE', 3,
 ( #20560, #24325, #22598, #16095, #11354, #3013, #9490, #17685, #8928, #2864 ),
 .UNSPECIFIED., .F., .F.,
 ( 4, 3, 3, 4 ),
 ( 6.938893903907228378E-18, 0.0002669560319015760498, 0.0005492286108966415621, 0.0008315040496093473914 ),
 .UNSPECIFIED. ) ;
#20373=CARTESIAN_POINT ( 'NONE',  ( 55.79472521941428198, 72.42790650415572884, 6.880567342319954705 ) ) ;
#20374=CARTESIAN_POINT ( 'NONE',  ( 2.263178607246656870, 86.59154415224598722, 116.7985473178705860 ) ) ;
#20375=ORIENTED_EDGE ( 'NONE', *, *, #11837, .F. ) ;
#20376=ORIENTED_EDGE ( 'NONE', *, *, #24283, .T. ) ;
#20377=CARTESIAN_POINT ( 'NONE',  ( 26.11404676487257603, 98.61392875273440950, -55.62948129436141897 ) ) ;
#20379=CARTESIAN_POINT ( 'NONE',  ( 55.49584447822657296, -53.73688382046231737, -48.74506217377937389 ) ) ;
#20380=EDGE_LOOP ( 'NONE', ( #23072, #26559, #5088, #6753 ) ) ;
#20381=CARTESIAN_POINT ( 'NONE',  ( 26.11404676487257603, -36.06104232266525145, 107.3263591096429082 ) ) ;
#20382=ORIENTED_EDGE ( 'NONE', *, *, #7705, .T. ) ;
#20384=VECTOR ( 'NONE', #27025, 1000.000000000000114 ) ;
#20386=ORIENTED_EDGE ( 'NONE', *, *, #3617, .F. ) ;
#20387=DIRECTION ( 'NONE',  ( 0.000000000000000000, 0.000000000000000000, 1.000000000000000000 ) ) ;
#20389=CARTESIAN_POINT ( 'NONE',  ( 109.1778270068192853, -0.0003511581237512927567, -0.009307953841270274684 ) ) ;
#20390=EDGE_LOOP ( 'NONE', ( #4066, #9274, #24480, #13716 ) ) ;
#20392=CARTESIAN_POINT ( 'NONE',  ( 25.64681081121879203, -97.57530875170644435, 56.81519825470720519 ) ) ;
#20394=CARTESIAN_POINT ( 'NONE',  ( 1.833721034905621661, -125.4904194343090182, 72.86293192427449128 ) ) ;
#20396=B_SPLINE_CURVE_WITH_KNOTS ( 'NONE', 3,
 ( #21376, #12178, #14751, #18941 ),
 .UNSPECIFIED., .F., .F.,
 ( 4, 4 ),
 ( 3.332884739788762247E-16, 0.01077107486149806760 ),
 .UNSPECIFIED. ) ;
#20397=EDGE_CURVE ( 'NONE', #6178, #1609, #27673, .T. ) ;
#20399=CARTESIAN_POINT ( 'NONE',  ( 109.1592201516379674, -0.006174480289200349852, -0.004867031887010190086 ) ) ;
#20400=CARTESIAN_POINT ( 'NONE',  ( 26.11404676487257603, 47.08215554553518700, 102.9690087468803341 ) ) ;
#20401=CARTESIAN_POINT ( 'NONE',  ( 16.75465622695666923, -19.47041796022332605, 140.8868039942614985 ) ) ;
#20403=EDGE_CURVE ( 'NONE', #24442, #16227, #2049, .T. ) ;
#20404=ORIENTED_EDGE ( 'NONE', *, *, #24067, .F. ) ;
#20405=ORIENTED_EDGE ( 'NONE', *, *, #20198, .T. ) ;
#20408=CARTESIAN_POINT ( 'NONE',  ( 28.37599760073041821, 10.20682761621932499, 114.2774414139535253 ) ) ;
#20415=CARTESIAN_POINT ( 'NONE',  ( 10.93730112726003156, 125.1380233598492140, -84.82621002473311478 ) ) ;
#20416=CARTESIAN_POINT ( 'NONE',  ( 55.79472521941426777, 14.41365263906553196, 71.31192372336680307 ) ) ;
#20418=CARTESIAN_POINT ( 'NONE',  ( 9.884929003653608603, 150.0922431698406285, -11.54837932062876860 ) ) ;
#20420=CARTESIAN_POINT ( 'NONE',  ( 1.833485406944043827, 73.01664920993141550, -125.4007332306537563 ) ) ;
#20421=CARTESIAN_POINT ( 'NONE',  ( 1.833206310202331935, 142.0914673790820757, 29.44113265020980919 ) ) ;
#20422=EDGE_LOOP ( 'NONE', ( #964, #4781, #27152, #14242 ) ) ;
#20423=DIRECTION ( 'NONE',  ( 0.000000000000000000, 0.000000000000000000, 1.000000000000000000 ) ) ;
#20424=ORIENTED_EDGE ( 'NONE', *, *, #5528, .F. ) ;
#20425=CARTESIAN_POINT ( 'NONE',  ( 1.833603222531957400, -29.73464781350154595, -142.0304769734131867 ) ) ;
#20426=B_SPLINE_CURVE_WITH_KNOTS ( 'NONE', 3,
 ( #13187, #11185, #11461, #17789, #6735, #15480, #15345, #15778, #9027, #22273 ),
 .UNSPECIFIED., .F., .F.,
 ( 4, 3, 3, 4 ),
 ( 3.925231146709437917E-17, 0.0002669559177086255441, 0.0005339118354151083795, 0.001067817517169174875 ),
 .UNSPECIFIED. ) ;
#20428=ORIENTED_EDGE ( 'NONE', *, *, #24157, .F. ) ;
#20429=( BOUNDED_SURFACE ( )  B_SPLINE_SURFACE ( 3, 1, ( 
 ( #26174, #26725 ),
 ( #28323, #8621 ),
 ( #6466, #8759 ),
 ( #26586, #24171 ) ),
 .UNSPECIFIED., .F., .F., .F. ) 
 B_SPLINE_SURFACE_WITH_KNOTS ( ( 4, 4 ),
 ( 2, 2 ),
 ( 0.000000000000000000, 1.000000000000000000 ),
 ( 0.000000000000000000, 1.000000000000000000 ),
 .UNSPECIFIED. ) 
 GEOMETRIC_REPRESENTATION_ITEM ( )  RATIONAL_B_SPLINE_SURFACE ( (
 ( 1.000000000000000000, 1.000000000000000000),
 ( 0.6386103224230302855, 0.9954351624131538845),
 ( 0.6386103224230302855, 0.9954351624131538845),
 ( 1.000000000000000000, 1.000000000000000000) ) ) 
 REPRESENTATION_ITEM ( '' )  SURFACE ( )  );
#20430=ORIENTED_EDGE ( 'NONE', *, *, #13617, .F. ) ;
#20436=DIRECTION ( 'NONE',  ( -1.000000000000000000, -0.000000000000000000, -0.000000000000000000 ) ) ;
#20437=VERTEX_POINT ( 'NONE', #24100 ) ;
#20439=CARTESIAN_POINT ( 'NONE',  ( 2.063896406836609909, -16.52087515463681200, -144.3268707900448931 ) ) ;
#20441=VERTEX_POINT ( 'NONE', #22504 ) ;
#20442=EDGE_CURVE ( 'NONE', #16465, #5899, #9963, .T. ) ;
#20443=VERTEX_POINT ( 'NONE', #2326 ) ;
#20446=CARTESIAN_POINT ( 'NONE',  ( 2.063896406836609909, -141.8093313989362798, 31.51663808384510546 ) ) ;
#20448=CARTESIAN_POINT ( 'NONE',  ( 1.894214914920950843, 107.2270864706603248, -97.83100278581306952 ) ) ;
#20451=CARTESIAN_POINT ( 'NONE',  ( 32.73300124599732186, 0.000000000000000000, 0.000000000000000000 ) ) ;
#20453=CARTESIAN_POINT ( 'NONE',  ( 32.73300124599732186, 0.000000000000000000, 0.000000000000000000 ) ) ;
#20454=CARTESIAN_POINT ( 'NONE',  ( 6.224689322667647851, 108.2965163446087615, -100.9623537450640924 ) ) ;
#20455=ORIENTED_EDGE ( 'NONE', *, *, #26089, .F. ) ;
#20456=CARTESIAN_POINT ( 'NONE',  ( 1.833485406944043827, 145.1085452359073145, 0.5339064996889848480 ) ) ;
#20460=ORIENTED_EDGE ( 'NONE', *, *, #25385, .F. ) ;
#20461=( BOUNDED_SURFACE ( )  B_SPLINE_SURFACE ( 3, 1, ( 
 ( #14716, #12285 ),
 ( #25548, #1065 ),
 ( #9700, #27243 ),
 ( #14444, #20773 ) ),
 .UNSPECIFIED., .F., .F., .F. ) 
 B_SPLINE_SURFACE_WITH_KNOTS ( ( 4, 4 ),
 ( 2, 2 ),
 ( 0.000000000000000000, 1.000000000000000000 ),
 ( 0.000000000000000000, 1.000000000000000000 ),
 .UNSPECIFIED. ) 
 GEOMETRIC_REPRESENTATION_ITEM ( )  RATIONAL_B_SPLINE_SURFACE ( (
 ( 1.000000000000000000, 1.000000000000000000),
 ( 0.6386103224230302855, 0.9954351624131538845),
 ( 0.6386103224230302855, 0.9954351624131538845),
 ( 1.000000000000000000, 1.000000000000000000) ) ) 
 REPRESENTATION_ITEM ( '' )  SURFACE ( )  );
#20464=CARTESIAN_POINT ( 'NONE',  ( 109.1592201516379674, 0.002134489919768143857, -0.007566779963325576466 ) ) ;
#20465=CARTESIAN_POINT ( 'NONE',  ( 32.73300124599734318, 105.8473486001051072, 51.32617430724947383 ) ) ;
#20466=EDGE_CURVE ( 'NONE', #15825, #4812, #1023, .T. ) ;
#20467=EDGE_CURVE ( 'NONE', #16400, #14717, #3410, .T. ) ;
#20468=CARTESIAN_POINT ( 'NONE',  ( 2.430230287190592531, 126.7388733285345097, 71.49654683843552050 ) ) ;
#20469=LINE ( 'NONE', #16586, #8765 ) ;
#20470=CARTESIAN_POINT ( 'NONE',  ( 10.93730112725932813, 150.7858122213658305, 10.89264110825069132 ) ) ;
#20471=EDGE_CURVE ( 'NONE', #18577, #6221, #7942, .T. ) ;
#20472=CARTESIAN_POINT ( 'NONE',  ( 25.65782528836481546, -35.44279022896562026, 107.2118488517899664 ) ) ;
#20473=B_SPLINE_CURVE_WITH_KNOTS ( 'NONE', 3,
 ( #3027, #11804, #20575, #856, #18406, #27183, #17830, #26615, #4750, #13525 ),
 .UNSPECIFIED., .F., .F.,
 ( 4, 3, 3, 4 ),
 ( 1.040834085586084257E-17, 0.0002669560319015708998, 0.0005492286108966411284, 0.0008315040496093379589 ),
 .UNSPECIFIED. ) ;
#20474=LINE ( 'NONE', #25383, #14328 ) ;
#20475=CARTESIAN_POINT ( 'NONE',  ( 30.58324630866341565, 3.944468862007675103, 120.8793175557614745 ) ) ;
#20476=CARTESIAN_POINT ( 'NONE',  ( 1.833206308920085181, 108.3342547309378006, -96.54250175814011925 ) ) ;
#20479=CARTESIAN_POINT ( 'NONE',  ( 32.73300124599732186, 0.000000000000000000, 0.000000000000000000 ) ) ;
#20481=CARTESIAN_POINT ( 'NONE',  ( 26.04756280548352265, -83.36043467252073924, 76.55292122840010904 ) ) ;
#20483=CARTESIAN_POINT ( 'NONE',  ( 28.37599760073041466, -78.09498850373461210, 84.05168479399063131 ) ) ;
#20484=CARTESIAN_POINT ( 'NONE',  ( 109.1778270068192853, 0.001591747944959422253, 0.009177562596826683780 ) ) ;
#20485=CARTESIAN_POINT ( 'NONE',  ( 2.433796855181233454, -107.1581411821792216, 98.43889364293823974 ) ) ;
#20486=ORIENTED_EDGE ( 'NONE', *, *, #3305, .F. ) ;
#20487=CARTESIAN_POINT ( 'NONE',  ( 26.28373643307413232, 30.57614217577458149, 123.8418562193897543 ) ) ;
#20489=CARTESIAN_POINT ( 'NONE',  ( 1.833485406944057594, -84.86072343962649711, 117.7091014914947209 ) ) ;
#20490=CARTESIAN_POINT ( 'NONE',  ( 2.433796855181205476, 1.451562450951669803, -145.5024947199069345 ) ) ;
#20492=ORIENTED_EDGE ( 'NONE', *, *, #4327, .F. ) ;
#20493=VERTEX_POINT ( 'NONE', #21922 ) ;
#20494=CARTESIAN_POINT ( 'NONE',  ( 6.224689322667647851, 18.02516478984143333, 146.9579047224770250 ) ) ;
#20496=( BOUNDED_SURFACE ( )  B_SPLINE_SURFACE ( 3, 1, ( 
 ( #6637, #6498 ),
 ( #19714, #6782 ),
 ( #17273, #4457 ),
 ( #25934, #12816 ) ),
 .UNSPECIFIED., .F., .F., .F. ) 
 B_SPLINE_SURFACE_WITH_KNOTS ( ( 4, 4 ),
 ( 2, 2 ),
 ( 0.000000000000000000, 1.000000000000000000 ),
 ( 0.000000000000000000, 1.000000000000000000 ),
 .UNSPECIFIED. ) 
 GEOMETRIC_REPRESENTATION_ITEM ( )  RATIONAL_B_SPLINE_SURFACE ( (
 ( 1.000000000000000000, 1.000000000000000000),
 ( 0.9956975270656955868, 0.8568959468854907557),
 ( 0.9956975270656955868, 0.8568959468854907557),
 ( 1.000000000000000000, 1.000000000000000000) ) ) 
 REPRESENTATION_ITEM ( '' )  SURFACE ( )  );
#20499=EDGE_CURVE ( 'NONE', #24314, #24512, #20569, .T. ) ;
#20500=CARTESIAN_POINT ( 'NONE',  ( 9.884929003653626367, 65.04493172071478568, 135.7578851563887952 ) ) ;
#20501=CARTESIAN_POINT ( 'NONE',  ( 19.66333377628681944, 114.0223162644916215, -77.29039328249528751 ) ) ;
#20502=DIRECTION ( 'NONE',  ( 0.000000000000000000, 1.000000000000000000, 0.000000000000000000 ) ) ;
#20503=CARTESIAN_POINT ( 'NONE',  ( 28.43349137099851021, 65.60227321965575698, 105.5221910860617527 ) ) ;
#20504=FACE_OUTER_BOUND ( 'NONE', #18515, .T. ) ;
#20506=CARTESIAN_POINT ( 'NONE',  ( 25.81918753295379432, -34.03777907511991430, 107.7789657594973676 ) ) ;
#20510=CARTESIAN_POINT ( 'NONE',  ( 2.430230287190581429, 144.8619874886008461, -13.76600171652495241 ) ) ;
#20511=CARTESIAN_POINT ( 'NONE',  ( 25.64699802086721547, -91.20712948285704158, 66.55977212001133125 ) ) ;
#20512=CARTESIAN_POINT ( 'NONE',  ( 109.1589550718174877, 0.005233222325298225036, -0.005477029346537791096 ) ) ;
#20517=CARTESIAN_POINT ( 'NONE',  ( 32.73300124599731475, 117.5726003567930036, -3.836798148479248827 ) ) ;
#20518=CARTESIAN_POINT ( 'NONE',  ( 28.37644542392842695, -46.84227702240702484, -115.1790646972553986 ) ) ;
#20522=ORIENTED_EDGE ( 'NONE', *, *, #10833, .T. ) ;
#20523=CARTESIAN_POINT ( 'NONE',  ( 25.65782528836481902, -112.3587790429871518, 11.22838748007579568 ) ) ;
#20524=B_SPLINE_CURVE_WITH_KNOTS ( 'NONE', 3,
 ( #12263, #1463, #23504, #14840, #1605, #5941 ),
 .UNSPECIFIED., .F., .F.,
 ( 4, 2, 4 ),
 ( 2.168404344971008868E-18, 0.0006311636237756670931, 0.001262327247551332018 ),
 .UNSPECIFIED. ) ;
#20526=B_SPLINE_CURVE_WITH_KNOTS ( 'NONE', 3,
 ( #17746, #8843, #15292, #474 ),
 .UNSPECIFIED., .F., .F.,
 ( 4, 4 ),
 ( 0.000000000000000000, 0.008383560773332729421 ),
 .UNSPECIFIED. ) ;
#20528=CARTESIAN_POINT ( 'NONE',  ( 55.79472521941426777, 69.41463258328542452, -21.78881894124631913 ) ) ;
#20534=( BOUNDED_SURFACE ( )  B_SPLINE_SURFACE ( 3, 1, ( 
 ( #2422, #275 ),
 ( #17819, #26605 ),
 ( #6913, #24474 ),
 ( #4739, #13513 ) ),
 .UNSPECIFIED., .F., .F., .F. ) 
 B_SPLINE_SURFACE_WITH_KNOTS ( ( 4, 4 ),
 ( 2, 2 ),
 ( 0.000000000000000000, 1.000000000000000000 ),
 ( 0.000000000000000000, 1.000000000000000000 ),
 .UNSPECIFIED. ) 
 GEOMETRIC_REPRESENTATION_ITEM ( )  RATIONAL_B_SPLINE_SURFACE ( (
 ( 1.000000000000000000, 1.000000000000000000),
 ( 0.9960225298536222738, 0.9999952330161893110),
 ( 0.9960225298536222738, 0.9999952330161893110),
 ( 1.000000000000000000, 1.000000000000000000) ) ) 
 REPRESENTATION_ITEM ( '' )  SURFACE ( )  );
#20536=CARTESIAN_POINT ( 'NONE',  ( 109.1586059443104944, -0.005983234375914175257, 0.003774052605966610619 ) ) ;
#20537=CARTESIAN_POINT ( 'NONE',  ( 32.73300124599731475, 117.5726003567930178, 3.836798148479249715 ) ) ;
#20539=EDGE_CURVE ( 'NONE', #119, #12354, #321, .T. ) ;
#20540=ORIENTED_EDGE ( 'NONE', *, *, #27775, .F. ) ;
#20541=CARTESIAN_POINT ( 'NONE',  ( 109.1721716018069657, 0.01673651515803009984, 0.003350975118864233521 ) ) ;
#20542=CARTESIAN_POINT ( 'NONE',  ( 26.04756280548352620, 33.91579348271660876, -107.9769918539636677 ) ) ;
#20543=VECTOR ( 'NONE', #8048, 1000.000000000000000 ) ;
#20544=CARTESIAN_POINT ( 'NONE',  ( 13.84597867724983367, -20.08297016719483352, 145.3211459389822267 ) ) ;
#20545=VERTEX_POINT ( 'NONE', #13851 ) ;
#20546=ORIENTED_EDGE ( 'NONE', *, *, #2134, .F. ) ;
#20550=CARTESIAN_POINT ( 'NONE',  ( 32.73300124599735739, 39.98094346392311138, 110.6325518752275485 ) ) ;
#20551=CARTESIAN_POINT ( 'NONE',  ( 25.64708010899963142, 11.74803558238434853, -112.2984447178532434 ) ) ;
#20553=CARTESIAN_POINT ( 'NONE',  ( 25.64681081121879203, -102.9795863647031666, 46.30456157731292421 ) ) ;
#20555=CARTESIAN_POINT ( 'NONE',  ( 26.11404676487259024, 10.71016160607717538, -112.7148551500679332 ) ) ;
#20556=CARTESIAN_POINT ( 'NONE',  ( 10.93730112725990011, -151.0983828010092225, 4.928439153519769356 ) ) ;
#20558=CARTESIAN_POINT ( 'NONE',  ( 32.73300124599740002, -110.6325518752271080, -39.98094346392423404 ) ) ;
#20559=CARTESIAN_POINT ( 'NONE',  ( 1.831572820252008738, 43.90210991190623702, 138.3111855986062437 ) ) ;
#20560=CARTESIAN_POINT ( 'NONE',  ( 25.64681081121880624, 12.21581276189807497, 112.2483031020013868 ) ) ;
#20561=CARTESIAN_POINT ( 'NONE',  ( 1.831572820252008738, -73.40899645746092972, 125.1738732943807690 ) ) ;
#20563=CARTESIAN_POINT ( 'NONE',  ( 10.93730112725939030, 140.0398180619108075, 56.95489579269806057 ) ) ;
#20565=CARTESIAN_POINT ( 'NONE',  ( 109.1624594426973260, -0.01405141589343899405, 0.007576898892904823310 ) ) ;
#20566=CARTESIAN_POINT ( 'NONE',  ( 1.833838848569443014, -30.34409872482129344, -141.9017642089167737 ) ) ;
#20568=VERTEX_POINT ( 'NONE', #24815 ) ;
#20569=B_SPLINE_CURVE_WITH_KNOTS ( 'NONE', 3,
 ( #20179, #24238, #20039, #11130, #11551, #15871, #13701 ),
 .UNSPECIFIED., .F., .F.,
 ( 4, 3, 4 ),
 ( 0.000000000000000000, 0.02398743853561383088, 0.04000277880656213925 ),
 .UNSPECIFIED. ) ;
#20570=ORIENTED_EDGE ( 'NONE', *, *, #13704, .T. ) ;
#20571=EDGE_CURVE ( 'NONE', #14717, #20645, #9938, .T. ) ;
#20572=ORIENTED_EDGE ( 'NONE', *, *, #10774, .F. ) ;
#20573=EDGE_CURVE ( 'NONE', #18502, #13492, #26073, .T. ) ;
#20575=CARTESIAN_POINT ( 'NONE',  ( 25.64699802086723324, -23.70809581152530043, -110.3941571196683640 ) ) ;
#20576=CARTESIAN_POINT ( 'NONE',  ( 109.1778270068192853, 0.007736698406806029153, -0.005186985107080967217 ) ) ;
#20577=CARTESIAN_POINT ( 'NONE',  ( 25.98107933586756246, 112.3948402207508650, 12.91054317625147796 ) ) ;
#20580=CARTESIAN_POINT ( 'NONE',  ( 25.98107933586720719, 67.37827847766638456, -90.88151529733718803 ) ) ;
#20581=FACE_OUTER_BOUND ( 'NONE', #2023, .T. ) ;
#20582=CARTESIAN_POINT ( 'NONE',  ( 10.93730112725932635, 0.000000000000000000, 0.000000000000000000 ) ) ;
#20585=CARTESIAN_POINT ( 'NONE',  ( 13.36082413113061307, -127.3428651193253813, 84.67697637120370757 ) ) ;
#20586=CARTESIAN_POINT ( 'NONE',  ( 10.93730112725991432, -71.28103789254845424, -133.3192575531807620 ) ) ;
#20587=CARTESIAN_POINT ( 'NONE',  ( 109.1586900883932856, 0.007109207791181753125, -0.0006456433529162725928 ) ) ;
#20588=DIRECTION ( 'NONE',  ( 0.5946245182733608248, -0.6948076064830658316, -0.4045541647807455732 ) ) ;
#20589=CARTESIAN_POINT ( 'NONE',  ( 2.063896406836605024, 137.7380992975102743, 46.16709813092669634 ) ) ;
#20590=CARTESIAN_POINT ( 'NONE',  ( 2.433796855181205476, -145.5024947199069629, -1.451562450951161987 ) ) ;
#20591=ORIENTED_EDGE ( 'NONE', *, *, #721, .T. ) ;
#20592=CARTESIAN_POINT ( 'NONE',  ( 1.833485406944043827, -132.3460930279895535, 59.50871042846178938 ) ) ;
#20594=CARTESIAN_POINT ( 'NONE',  ( 25.86096068574579832, -65.64181925268263740, -92.04529103340848906 ) ) ;
#20595=LINE ( 'NONE', #27502, #14413 ) ;
#20598=ORIENTED_EDGE ( 'NONE', *, *, #20796, .F. ) ;
#20599=CARTESIAN_POINT ( 'NONE',  ( 1.832998868059890096, -132.7810136645734360, -58.53348008137779601 ) ) ;
#20601=ORIENTED_EDGE ( 'NONE', *, *, #6868, .T. ) ;
#20602=EDGE_CURVE ( 'NONE', #12090, #9124, #16443, .T. ) ;
#20603=ORIENTED_EDGE ( 'NONE', *, *, #7756, .T. ) ;
#20606=CARTESIAN_POINT ( 'NONE',  ( 1.831572820252008738, -108.4969585352561410, 96.36280042115893707 ) ) ;
#20608=CARTESIAN_POINT ( 'NONE',  ( 6.224689322667647851, -108.2965163446081078, 100.9623537450648172 ) ) ;
#20609=CARTESIAN_POINT ( 'NONE',  ( 2.433796855181219243, -13.76554153471791864, 144.8571464219888583 ) ) ;
#20613=FACE_OUTER_BOUND ( 'NONE', #12260, .T. ) ;
#20617=CIRCLE ( 'NONE', #22951, 117.6351876552689504 ) ;
#20618=CARTESIAN_POINT ( 'NONE',  ( 25.86096068574578766, -55.66087367585338797, -98.40249579084571963 ) ) ;
#20619=CARTESIAN_POINT ( 'NONE',  ( 25.81918753295378366, -83.36706424720497921, 76.32043280377783390 ) ) ;
#20621=CARTESIAN_POINT ( 'NONE',  ( 55.49584447822657296, -58.85239198729157550, -42.42793568433017981 ) ) ;
#20623=CARTESIAN_POINT ( 'NONE',  ( 10.93730112725990189, -148.8212007290660495, -26.59437931460901439 ) ) ;
#20624=ORIENTED_EDGE ( 'NONE', *, *, #20198, .F. ) ;
#20626=( BOUNDED_SURFACE ( )  B_SPLINE_SURFACE ( 3, 1, ( 
 ( #22303, #20125 ),
 ( #2565, #8772 ),
 ( #7056, #13355 ),
 ( #410, #9192 ) ),
 .UNSPECIFIED., .F., .F., .F. ) 
 B_SPLINE_SURFACE_WITH_KNOTS ( ( 4, 4 ),
 ( 2, 2 ),
 ( 0.000000000000000000, 1.000000000000000000 ),
 ( 0.000000000000000000, 1.000000000000000000 ),
 .UNSPECIFIED. ) 
 GEOMETRIC_REPRESENTATION_ITEM ( )  RATIONAL_B_SPLINE_SURFACE ( (
 ( 1.000000000000000000, 1.000000000000000000),
 ( 0.9956975270656954757, 0.8568959468854893125),
 ( 0.9956975270656954757, 0.8568959468854893125),
 ( 1.000000000000000000, 1.000000000000000000) ) ) 
 REPRESENTATION_ITEM ( '' )  SURFACE ( )  );
#20627=EDGE_CURVE ( 'NONE', #7617, #13959, #20474, .T. ) ;
#20628=ORIENTED_EDGE ( 'NONE', *, *, #14655, .F. ) ;
#20629=FACE_OUTER_BOUND ( 'NONE', #5398, .T. ) ;
#20630=CARTESIAN_POINT ( 'NONE',  ( 109.1592201516379674, -0.005027640251764426034, 0.006044422199831456753 ) ) ;
#20631=ORIENTED_EDGE ( 'NONE', *, *, #12317, .F. ) ;
#20633=VERTEX_POINT ( 'NONE', #7542 ) ;
#20634=ORIENTED_EDGE ( 'NONE', *, *, #746, .F. ) ;
#20635=EDGE_CURVE ( 'NONE', #15678, #4919, #6161, .T. ) ;
#20636=CARTESIAN_POINT ( 'NONE',  ( 109.1587776205901861, -0.0006832286435017355386, 0.007297420966932444478 ) ) ;
#20637=EDGE_CURVE ( 'NONE', #7936, #23571, #26940, .T. ) ;
#20639=DIRECTION ( 'NONE',  ( -1.000000000000000000, -0.000000000000000000, -0.000000000000000000 ) ) ;
#20641=CARTESIAN_POINT ( 'NONE',  ( 55.49584447822657296, -22.16497542184453451, 69.08290406177572152 ) ) ;
#20643=CARTESIAN_POINT ( 'NONE',  ( 1.833721034905660741, -59.34646046113689977, -132.4192200895888050 ) ) ;
#20644=CARTESIAN_POINT ( 'NONE',  ( 25.64670758986456889, 83.57526425215496602, 75.92149922855223565 ) ) ;
#20645=VERTEX_POINT ( 'NONE', #8246 ) ;
#20646=EDGE_LOOP ( 'NONE', ( #11814, #22794, #12203, #1655 ) ) ;
#20648=CARTESIAN_POINT ( 'NONE',  ( 25.64699802086725811, 66.17503410044022871, -91.48665801621594085 ) ) ;
#20649=CARTESIAN_POINT ( 'NONE',  ( 5.340103579038300019, 57.86178752084676091, -135.6222865281523582 ) ) ;
#20651=LINE ( 'NONE', #24722, #25825 ) ;
#20652=CARTESIAN_POINT ( 'NONE',  ( 2.263178113027022764, -71.48082833564976113, -126.6115605262345980 ) ) ;
#20653=ORIENTED_EDGE ( 'NONE', *, *, #347, .T. ) ;
#20654=CARTESIAN_POINT ( 'NONE',  ( 25.64681081121879203, 97.99105938548001404, -56.09509703373240797 ) ) ;
#20657=VERTEX_POINT ( 'NONE', #5808 ) ;
#20658=CARTESIAN_POINT ( 'NONE',  ( 55.49584447822657296, -36.04376091928588721, 62.96491934285981529 ) ) ;
#20659=ADVANCED_FACE ( 'NONE', ( #25671 ), #18946, .T. ) ;
#20661=CARTESIAN_POINT ( 'NONE',  ( 1.833206310202331935, 116.9567751109830596, -85.89457578512693203 ) ) ;
#20662=EDGE_CURVE ( 'NONE', #6495, #25074, #8381, .T. ) ;
#20664=( BOUNDED_SURFACE ( )  B_SPLINE_SURFACE ( 3, 1, ( 
 ( #9756, #20829 ),
 ( #14340, #10045 ),
 ( #7900, #3414 ),
 ( #25456, #5730 ) ),
 .UNSPECIFIED., .F., .F., .F. ) 
 B_SPLINE_SURFACE_WITH_KNOTS ( ( 4, 4 ),
 ( 2, 2 ),
 ( 0.000000000000000000, 1.000000000000000000 ),
 ( 0.000000000000000000, 1.000000000000000000 ),
 .UNSPECIFIED. ) 
 GEOMETRIC_REPRESENTATION_ITEM ( )  RATIONAL_B_SPLINE_SURFACE ( (
 ( 1.000000000000000000, 1.000000000000000000),
 ( 0.9956975270656954757, 0.8568959468854893125),
 ( 0.9956975270656954757, 0.8568959468854893125),
 ( 1.000000000000000000, 1.000000000000000000) ) ) 
 REPRESENTATION_ITEM ( '' )  SURFACE ( )  );
#20665=ORIENTED_EDGE ( 'NONE', *, *, #21996, .T. ) ;
#20667=ORIENTED_EDGE ( 'NONE', *, *, #22034, .F. ) ;
#20670=B_SPLINE_CURVE_WITH_KNOTS ( 'NONE', 3,
 ( #5319, #575, #15971, #5026, #11662, #22909, #25193 ),
 .UNSPECIFIED., .F., .F.,
 ( 4, 3, 4 ),
 ( 0.000000000000000000, 0.02398743853561357067, 0.04000277880656220864 ),
 .UNSPECIFIED. ) ;
#20674=CARTESIAN_POINT ( 'NONE',  ( 9.884929003653608603, -91.84919534722023116, 119.2676479132370702 ) ) ;
#20675=CARTESIAN_POINT ( 'NONE',  ( 1.833809397011890940, 0.1779683723495601722, -145.1096615925544882 ) ) ;
#20676=CARTESIAN_POINT ( 'NONE',  ( 2.433796855181219243, -142.0211193075558356, 31.67151202412923894 ) ) ;
#20679=CARTESIAN_POINT ( 'NONE',  ( 99.22246935314079508, -90.00000000000005684, -40.00000000000002842 ) ) ;
#20684=ORIENTED_EDGE ( 'NONE', *, *, #20019, .T. ) ;
#20686=DIRECTION ( 'NONE',  ( -1.000000000000000000, -0.000000000000000000, -0.000000000000000000 ) ) ;
#20687=CARTESIAN_POINT ( 'NONE',  ( 2.430230287190592531, -74.01081053031012402, -125.2872625092170153 ) ) ;
#20688=CARTESIAN_POINT ( 'NONE',  ( 8.186469829614452465, 49.43817854882515661, -140.9315935955036423 ) ) ;
#20691=CARTESIAN_POINT ( 'NONE',  ( 30.59138290137910587, 9.457588828076605836, -115.8270707793591185 ) ) ;
#20692=CARTESIAN_POINT ( 'NONE',  ( 5.340103556456419653, -88.52145167812672355, 117.9209211572682818 ) ) ;
#20696=DIRECTION ( 'NONE',  ( 0.000000000000000000, 0.000000000000000000, 1.000000000000000000 ) ) ;
#20697=CARTESIAN_POINT ( 'NONE',  ( 25.87036335909426299, -67.25332031939082356, -90.88222105969130382 ) ) ;
#20699=CARTESIAN_POINT ( 'NONE',  ( 1.834118845439484335, 107.7186227765467237, -97.22976650547319366 ) ) ;
#20700=CARTESIAN_POINT ( 'NONE',  ( 109.1592201516379674, 0.007051465909552763651, -0.003476928926134732496 ) ) ;
#20701=EDGE_CURVE ( 'NONE', #28132, #17753, #24456, .T. ) ;
#20702=CIRCLE ( 'NONE', #17454, 117.6351876552689504 ) ;
#20704=CARTESIAN_POINT ( 'NONE',  ( 109.1592201516379674, 0.007620268632968142664, 0.001934867487012853927 ) ) ;
#20707=ADVANCED_FACE ( 'NONE', ( #10685 ), #12875, .F. ) ;
#20709=CARTESIAN_POINT ( 'NONE',  ( 109.1592201516379674, 0.0005146241775907373474, -0.007845213074660002325 ) ) ;
#20710=EDGE_CURVE ( 'NONE', #23443, #3658, #18158, .T. ) ;
#20713=( BOUNDED_SURFACE ( )  B_SPLINE_SURFACE ( 3, 1, ( 
 ( #5757, #25182 ),
 ( #16245, #7781 ),
 ( #14212, #9931 ),
 ( #20700, #7928 ) ),
 .UNSPECIFIED., .F., .F., .F. ) 
 B_SPLINE_SURFACE_WITH_KNOTS ( ( 4, 4 ),
 ( 2, 2 ),
 ( 0.000000000000000000, 1.000000000000000000 ),
 ( 0.000000000000000000, 1.000000000000000000 ),
 .UNSPECIFIED. ) 
 GEOMETRIC_REPRESENTATION_ITEM ( )  RATIONAL_B_SPLINE_SURFACE ( (
 ( 1.000000000000000000, 1.000000000000000000),
 ( 0.9956975270656955868, 0.8568959468854907557),
 ( 0.9956975270656955868, 0.8568959468854907557),
 ( 1.000000000000000000, 1.000000000000000000) ) ) 
 REPRESENTATION_ITEM ( '' )  SURFACE ( )  );
#20715=CARTESIAN_POINT ( 'NONE',  ( 26.11404676487257603, -102.9690087468804762, 47.08215554553482463 ) ) ;
#20717=CARTESIAN_POINT ( 'NONE',  ( 16.75465622695656265, -79.80233222761923173, -117.7275519421685459 ) ) ;
#20718=CARTESIAN_POINT ( 'NONE',  ( 1.833691583653538126, 125.8462703805709140, -72.24637705290355427 ) ) ;
#20719=ORIENTED_EDGE ( 'NONE', *, *, #2868, .F. ) ;
#20720=CARTESIAN_POINT ( 'NONE',  ( 8.186469777910991397, 84.95702201436577639, -122.8338388711454314 ) ) ;
#20723=CARTESIAN_POINT ( 'NONE',  ( 1.833206308920100724, -116.9567745381553436, -85.89457656603988767 ) ) ;
#20724=VERTEX_POINT ( 'NONE', #28220 ) ;
#20728=CARTESIAN_POINT ( 'NONE',  ( 10.93730112725972958, -84.82621002473526062, 125.1380233598475229 ) ) ;
#20729=CARTESIAN_POINT ( 'NONE',  ( 21.16825799904899341, -83.13600836828936735, -106.9139171613934849 ) ) ;
#20730=CARTESIAN_POINT ( 'NONE',  ( 32.73300124599735739, 20.69176323058628597, 115.8010721414084543 ) ) ;
#20731=CARTESIAN_POINT ( 'NONE',  ( 2.263178113027046301, -84.32376073259139559, -118.4461880110611958 ) ) ;
#20732=EDGE_CURVE ( 'NONE', #19518, #11913, #19859, .T. ) ;
#20735=CARTESIAN_POINT ( 'NONE',  ( 8.186469777910986068, 42.84118569629532658, -143.0750864738772918 ) ) ;
#20736=CARTESIAN_POINT ( 'NONE',  ( 32.73300124599737870, 20.69176323058787759, -115.8010721414081132 ) ) ;
#20738=EDGE_CURVE ( 'NONE', #4343, #17054, #11656, .T. ) ;
#20739=CARTESIAN_POINT ( 'NONE',  ( 2.430230287190589422, -60.50928654924667427, -132.3371620660956864 ) ) ;
#20741=ORIENTED_EDGE ( 'NONE', *, *, #12962, .T. ) ;
#20743=CARTESIAN_POINT ( 'NONE',  ( 26.11404676487257603, 22.43340081644767636, 110.9778746459747794 ) ) ;
#20744=VERTEX_POINT ( 'NONE', #14701 ) ;
#20746=ORIENTED_EDGE ( 'NONE', *, *, #7141, .T. ) ;
#20747=ORIENTED_EDGE ( 'NONE', *, *, #14886, .F. ) ;
#20749=FACE_OUTER_BOUND ( 'NONE', #7681, .T. ) ;
#20751=FACE_OUTER_BOUND ( 'NONE', #11914, .T. ) ;
#20752=CARTESIAN_POINT ( 'NONE',  ( 10.93730112725990367, -145.2260730187398678, -42.00474393596407197 ) ) ;
#20753=CARTESIAN_POINT ( 'NONE',  ( 2.063896406836605024, 142.3682421260911326, -28.88716984836180401 ) ) ;
#20754=B_SPLINE_CURVE_WITH_KNOTS ( 'NONE', 3,
 ( #24275, #6578, #22403, #22107 ),
 .UNSPECIFIED., .F., .F.,
 ( 4, 4 ),
 ( 3.389420616900455111E-16, 0.01077107486149848047 ),
 .UNSPECIFIED. ) ;
#20756=CARTESIAN_POINT ( 'NONE',  ( 2.433796855181233454, -133.5135467655514390, -57.85512797798025275 ) ) ;
#20757=VECTOR ( 'NONE', #23308, 1000.000000000000114 ) ;
#20758=B_SPLINE_CURVE_WITH_KNOTS ( 'NONE', 3,
 ( #10031, #23276, #3529, #23557, #7591, #19083, #25435, #5712, #22993, #25141 ),
 .UNSPECIFIED., .F., .F.,
 ( 4, 3, 3, 4 ),
 ( 3.122502256758252770E-17, 0.0002669559177086242431, 0.0005339118354151079458, 0.001067817517169163816 ),
 .UNSPECIFIED. ) ;
#20761=CARTESIAN_POINT ( 'NONE',  ( 109.1586900883932856, -0.002301750759599821821, 0.006757191295060836940 ) ) ;
#20762=CARTESIAN_POINT ( 'NONE',  ( 25.64681081121879203, -56.09509703373275613, -97.99105938547980088 ) ) ;
#20763=ADVANCED_FACE ( 'NONE', ( #27814 ), #18483, .T. ) ;
#20765=EDGE_CURVE ( 'NONE', #18556, #4919, #4762, .T. ) ;
#20767=CARTESIAN_POINT ( 'NONE',  ( 9.884929003653626367, -97.56484214660700616, 114.6392083957114494 ) ) ;
#20768=CARTESIAN_POINT ( 'NONE',  ( 2.430230287190592531, 109.1043569252014436, 96.28466919684133529 ) ) ;
#20769=ORIENTED_EDGE ( 'NONE', *, *, #19202, .T. ) ;
#20773=CARTESIAN_POINT ( 'NONE',  ( 13.36082413113061307, -67.94366799842909188, 137.0038452127797939 ) ) ;
#20775=ORIENTED_EDGE ( 'NONE', *, *, #6845, .T. ) ;
#20776=ORIENTED_EDGE ( 'NONE', *, *, #19398, .T. ) ;
#20777=B_SPLINE_CURVE_WITH_KNOTS ( 'NONE', 3,
 ( #13197, #4147, #15074, #4292, #26442, #25904, #26307 ),
 .UNSPECIFIED., .F., .F.,
 ( 4, 3, 4 ),
 ( 5.762311684337388436E-16, 0.02816610861753244405, 0.04000277880656280538 ),
 .UNSPECIFIED. ) ;
#20778=B_SPLINE_CURVE_WITH_KNOTS ( 'NONE', 3,
 ( #11470, #27000, #26717, #821, #7034, #22427, #9604, #11906, #20242, #5282 ),
 .UNSPECIFIED., .F., .F.,
 ( 4, 3, 3, 4 ),
 ( 6.938893903907228378E-18, 0.0002669560319015712793, 0.0005492286108966321296, 0.0008315040496093543303 ),
 .UNSPECIFIED. ) ;
#20780=EDGE_LOOP ( 'NONE', ( #26748, #24784, #19434, #15326 ) ) ;
#20781=CARTESIAN_POINT ( 'NONE',  ( 9.884929003653626367, 19.90991253123246452, 149.2134106160916929 ) ) ;
#20785=CARTESIAN_POINT ( 'NONE',  ( 2.433796855181205476, -28.83182736670433499, -142.6247129145651229 ) ) ;
#20786=EDGE_CURVE ( 'NONE', #4626, #8623, #17154, .T. ) ;
#20789=CARTESIAN_POINT ( 'NONE',  ( 1.831572820252008738, 14.18623102066768915, 144.4165162501763575 ) ) ;
#20790=CARTESIAN_POINT ( 'NONE',  ( 1.832998868059858122, -44.33343224355138545, -138.1720401012271680 ) ) ;
#20791=CARTESIAN_POINT ( 'NONE',  ( 1.833206308920097616, -85.89457656603950397, 116.9567745381556563 ) ) ;
#20793=LINE ( 'NONE', #27704, #6555 ) ;
#20796=EDGE_CURVE ( 'NONE', #24974, #8000, #5115, .T. ) ;
#20797=EDGE_LOOP ( 'NONE', ( #3795, #18949, #4689, #3022 ) ) ;
#20800=CARTESIAN_POINT ( 'NONE',  ( 25.64681081121879203, -11.38886654529750331, 112.3352186517030447 ) ) ;
#20802=CARTESIAN_POINT ( 'NONE',  ( 25.65782528836481902, 75.98558751977886061, -83.52701600504799728 ) ) ;
#20803=CARTESIAN_POINT ( 'NONE',  ( 28.37603512858459354, -108.5491486026793808, 37.15644006762180851 ) ) ;
#20805=CARTESIAN_POINT ( 'NONE',  ( 1.833485406944043827, 144.3694338680884925, 14.63699153649408480 ) ) ;
#20808=ORIENTED_EDGE ( 'NONE', *, *, #12080, .F. ) ;
#20809=CARTESIAN_POINT ( 'NONE',  ( 1.833809397773888517, 44.67209459545068029, 138.0624841332889332 ) ) ;
#20810=VECTOR ( 'NONE', #3099, 1000.000000000000227 ) ;
#20813=EDGE_LOOP ( 'NONE', ( #20540, #1699, #5998, #4369 ) ) ;
#20814=DIRECTION ( 'NONE',  ( -0.000000000000000000, 1.000000000000000000, -0.000000000000000000 ) ) ;
#20815=CARTESIAN_POINT ( 'NONE',  ( 26.28373643307402574, -126.3595147275198514, 17.46364395087421073 ) ) ;
#20816=AXIS2_PLACEMENT_3D ( 'NONE', #22977, #25263, #9865 ) ;
#20817=ORIENTED_EDGE ( 'NONE', *, *, #6203, .T. ) ;
#20819=ORIENTED_EDGE ( 'NONE', *, *, #13936, .T. ) ;
#20825=CARTESIAN_POINT ( 'NONE',  ( 109.1587776205901577, -0.004965871434389489830, 0.005390665547499349022 ) ) ;
#20826=VECTOR ( 'NONE', #1715, 1000.000000000000114 ) ;
#20828=CARTESIAN_POINT ( 'NONE',  ( 16.75465622695659462, 142.1502242093125687, 4.637075857201994111 ) ) ;
#20829=CARTESIAN_POINT ( 'NONE',  ( 2.430230287190589422, 31.67257033707502600, 142.0258656395022570 ) ) ;
#20832=CARTESIAN_POINT ( 'NONE',  ( 109.1592201516379674, 0.004867031887019543715, 0.006174480289199423509 ) ) ;
#20834=CARTESIAN_POINT ( 'NONE',  ( 32.73300124599731475, 117.5726003567930178, 3.836798148479249715 ) ) ;
#20835=CARTESIAN_POINT ( 'NONE',  ( 28.37603512858355970, -1.794342805482070258, -114.7183465482400351 ) ) ;
#20837=EDGE_CURVE ( 'NONE', #25686, #16400, #3311, .T. ) ;
#20839=VERTEX_POINT ( 'NONE', #438 ) ;
#20840=CARTESIAN_POINT ( 'NONE',  ( 55.79472521941426777, -0.7279028900798781843, 72.75035398477136539 ) ) ;
#20842=CARTESIAN_POINT ( 'NONE',  ( 109.1592201516379674, -0.0003082430541935533277, 0.007856029051018016685 ) ) ;
#20843=CARTESIAN_POINT ( 'NONE',  ( 2.063896406836605024, -141.8093313989358251, -31.51663808384702037 ) ) ;
#20844=B_SPLINE_CURVE_WITH_KNOTS ( 'NONE', 3,
 ( #22919, #7512, #18580, #16715, #1019, #25070, #27492 ),
 .UNSPECIFIED., .F., .F.,
 ( 4, 3, 4 ),
 ( 5.297613739687102098E-16, 0.02816610861753238160, 0.04000277880656268742 ),
 .UNSPECIFIED. ) ;
#20845=CARTESIAN_POINT ( 'NONE',  ( 1.833485406944057594, 132.7804117027888253, 58.53321471326925263 ) ) ;
#20846=LINE ( 'NONE', #14503, #3332 ) ;
#20847=ORIENTED_EDGE ( 'NONE', *, *, #7209, .T. ) ;
#20848=CARTESIAN_POINT ( 'NONE',  ( 1.833838848569441682, 107.9566558236576554, 96.96512505224261247 ) ) ;
#20851=ORIENTED_EDGE ( 'NONE', *, *, #13272, .T. ) ;
#20852=CARTESIAN_POINT ( 'NONE',  ( 2.108985857320947233, -1.281428372374745273, -145.2876352664462445 ) ) ;
#20853=CARTESIAN_POINT ( 'NONE',  ( 10.93730112725977932, -104.7670965581018123, 108.9902118373738062 ) ) ;
#20854=CARTESIAN_POINT ( 'NONE',  ( 32.73300124599738581, 39.98094346392455378, -110.6325518752269517 ) ) ;
#20857=CARTESIAN_POINT ( 'NONE',  ( 2.263178113027039196, -108.9830942735799511, 96.24282436106580008 ) ) ;
#20858=CARTESIAN_POINT ( 'NONE',  ( 30.59141879584291246, -105.0379937202710892, -49.72305007553554645 ) ) ;
#20860=CARTESIAN_POINT ( 'NONE',  ( 25.64681081121879203, -66.70335573067806934, -91.10197563708015878 ) ) ;
#20861=( BOUNDED_SURFACE ( )  B_SPLINE_SURFACE ( 3, 1, ( 
 ( #782, #16175 ),
 ( #923, #18322 ),
 ( #9563, #9709 ),
 ( #5091, #7566 ) ),
 .UNSPECIFIED., .F., .F., .F. ) 
 B_SPLINE_SURFACE_WITH_KNOTS ( ( 4, 4 ),
 ( 2, 2 ),
 ( 0.000000000000000000, 1.000000000000000000 ),
 ( 0.000000000000000000, 1.000000000000000000 ),
 .UNSPECIFIED. ) 
 GEOMETRIC_REPRESENTATION_ITEM ( )  RATIONAL_B_SPLINE_SURFACE ( (
 ( 1.000000000000000000, 1.000000000000000000),
 ( 0.6386103224230316178, 0.9954351624131538845),
 ( 0.6386103224230316178, 0.9954351624131538845),
 ( 1.000000000000000000, 1.000000000000000000) ) ) 
 REPRESENTATION_ITEM ( '' )  SURFACE ( )  );
#20862=VECTOR ( 'NONE', #22058, 999.9999999999998863 ) ;
#20863=CARTESIAN_POINT ( 'NONE',  ( 32.73300124599738581, -44.31599526637883457, -108.9684813982493097 ) ) ;
#20864=CARTESIAN_POINT ( 'NONE',  ( 1.831572820252009626, 43.90210991190804179, -138.3111855986056753 ) ) ;
#20865=EDGE_LOOP ( 'NONE', ( #23841, #13206, #17978, #20271 ) ) ;
#20866=ORIENTED_EDGE ( 'NONE', *, *, #8343, .T. ) ;
#20867=CARTESIAN_POINT ( 'NONE',  ( 0.000000000000000000, 0.000000000000000000, 0.000000000000000000 ) ) ;
#20869=CARTESIAN_POINT ( 'NONE',  ( 25.64681081121879203, -46.30456157731261868, -102.9795863647033229 ) ) ;
#20871=CARTESIAN_POINT ( 'NONE',  ( 26.11404676487259024, -55.62948129436313849, 98.61392875273344316 ) ) ;
#20872=EDGE_CURVE ( 'NONE', #9793, #28263, #18843, .T. ) ;
#20873=CARTESIAN_POINT ( 'NONE',  ( 55.49584447822657296, -69.08290406177565046, -22.16497542184476188 ) ) ;
#20874=CARTESIAN_POINT ( 'NONE',  ( 2.430230287190589422, -133.5180086894987710, -57.85706160874279647 ) ) ;
#20877=ORIENTED_EDGE ( 'NONE', *, *, #24868, .F. ) ;
#20878=CARTESIAN_POINT ( 'NONE',  ( 109.1624594426973118, -0.005372302061316169830, -0.01503296564241275897 ) ) ;
#20879=CARTESIAN_POINT ( 'NONE',  ( 13.36082413113061307, -117.7941133658645043, 97.52406103376718249 ) ) ;
#20881=DIRECTION ( 'NONE',  ( 1.000000000000000000, 0.000000000000000000, 0.000000000000000000 ) ) ;
#20882=B_SPLINE_CURVE_WITH_KNOTS ( 'NONE', 3,
 ( #22, #25956, #26363, #23677, #12699, #10840, #8818 ),
 .UNSPECIFIED., .F., .F.,
 ( 4, 3, 4 ),
 ( 0.000000000000000000, 0.02398743853561324454, 0.04000277880656220864 ),
 .UNSPECIFIED. ) ;
#20884=FACE_OUTER_BOUND ( 'NONE', #28388, .T. ) ;
#20887=CARTESIAN_POINT ( 'NONE',  ( 2.063896406836605024, -137.7380992975099332, -46.16709813092763426 ) ) ;
#20891=CARTESIAN_POINT ( 'NONE',  ( 109.1586900883932856, 0.005833932871491316619, 0.004113747440992344268 ) ) ;
#20893=ORIENTED_EDGE ( 'NONE', *, *, #6352, .F. ) ;
#20895=ORIENTED_EDGE ( 'NONE', *, *, #5267, .T. ) ;
#20897=CARTESIAN_POINT ( 'NONE',  ( 10.93730112725990011, -119.3442956573265974, -92.80059208661810999 ) ) ;
#20898=CARTESIAN_POINT ( 'NONE',  ( 109.1624594426973260, -0.009754804742273366636, 0.01263706729758978797 ) ) ;
#20901=CARTESIAN_POINT ( 'NONE',  ( 26.28373643307435614, 127.2291519022767403, 9.189598927292342623 ) ) ;
#20903=CARTESIAN_POINT ( 'NONE',  ( 5.340103556456460510, 2.303180381360306228, -147.4316330165021043 ) ) ;
#20904=CARTESIAN_POINT ( 'NONE',  ( 2.433796855181205476, 86.69855925934130880, -116.8607839509047892 ) ) ;
#20907=FACE_OUTER_BOUND ( 'NONE', #6494, .T. ) ;
#20909=CARTESIAN_POINT ( 'NONE',  ( 30.58324630866341920, -21.27395054437324262, 119.0579156359858359 ) ) ;
#20910=CARTESIAN_POINT ( 'NONE',  ( 2.108985857320929469, 16.46110181986684395, 144.3577886602084845 ) ) ;
#20911=B_SPLINE_CURVE_WITH_KNOTS ( 'NONE', 3,
 ( #695, #20691, #25042, #20555 ),
 .UNSPECIFIED., .F., .F.,
 ( 4, 4 ),
 ( 5.539203223666104022E-16, 0.008383748772660015725 ),
 .UNSPECIFIED. ) ;
#20912=CARTESIAN_POINT ( 'NONE',  ( 28.37599760073042177, -114.2774414139535679, 10.20682761621895018 ) ) ;
#20913=CARTESIAN_POINT ( 'NONE',  ( 32.73300124599732186, 0.000000000000000000, 0.000000000000000000 ) ) ;
#20917=VERTEX_POINT ( 'NONE', #18578 ) ;
#20919=ORIENTED_EDGE ( 'NONE', *, *, #290, .F. ) ;
#20921=ORIENTED_EDGE ( 'NONE', *, *, #8292, .F. ) ;
#20922=B_SPLINE_CURVE_WITH_KNOTS ( 'NONE', 3,
 ( #6064, #3889, #23771, #4020 ),
 .UNSPECIFIED., .F., .F.,
 ( 4, 4 ),
 ( 3.469446951953614189E-18, 0.008383560773332731156 ),
 .UNSPECIFIED. ) ;
#20923=ADVANCED_FACE ( 'NONE', ( #11817 ), #10881, .F. ) ;
#20928=CARTESIAN_POINT ( 'NONE',  ( 2.430230287190592531, 60.50928654924753403, 132.3371620660953170 ) ) ;
#20929=CARTESIAN_POINT ( 'NONE',  ( 1.832998868059890096, 125.9352106559993842, -72.09222286250953005 ) ) ;
#20930=CARTESIAN_POINT ( 'NONE',  ( 1.832998868059858122, -30.69214149073912523, -141.8272129421612249 ) ) ;
#20931=CARTESIAN_POINT ( 'NONE',  ( 1.832998868059858122, -145.1092030902949830, -0.5339089137763209925 ) ) ;
#20932=CARTESIAN_POINT ( 'NONE',  ( 5.340103556456468503, -128.8311297043950674, 71.72120378849564304 ) ) ;
#20934=ORIENTED_EDGE ( 'NONE', *, *, #17916, .F. ) ;
#20935=CARTESIAN_POINT ( 'NONE',  ( 25.64700659047694842, -107.3144208978482794, -35.10784848926773805 ) ) ;
#20936=CARTESIAN_POINT ( 'NONE',  ( 25.64692872815575342, 66.62748454953282362, -91.15762468787677619 ) ) ;
#20939=B_SPLINE_CURVE_WITH_KNOTS ( 'NONE', 3,
 ( #19403, #24026, #1980, #8751, #3730, #10781 ),
 .UNSPECIFIED., .F., .F.,
 ( 4, 2, 4 ),
 ( 1.392007502815792650E-17, 0.0006311571484586009102, 0.001262314296917188159 ),
 .UNSPECIFIED. ) ;
#20940=CARTESIAN_POINT ( 'NONE',  ( 5.340103579038232517, -111.1041836885941052, -96.93942141937414192 ) ) ;
#20943=CARTESIAN_POINT ( 'NONE',  ( 25.64699802086722968, 91.20712948285751054, -66.55977212001069176 ) ) ;
#20945=VERTEX_POINT ( 'NONE', #24785 ) ;
#20951=CARTESIAN_POINT ( 'NONE',  ( 10.93730112725971360, 26.59437931460756488, 148.8212007290661916 ) ) ;
#20952=ADVANCED_FACE ( 'NONE', ( #12656 ), #2041, .F. ) ;
#20954=ORIENTED_EDGE ( 'NONE', *, *, #14009, .T. ) ;
#20959=FACE_OUTER_BOUND ( 'NONE', #9531, .T. ) ;
#20963=CARTESIAN_POINT ( 'NONE',  ( 30.58324630866348670, -120.6294372749320445, -8.712468656081851393 ) ) ;
#20966=VERTEX_POINT ( 'NONE', #21578 ) ;
#20969=CARTESIAN_POINT ( 'NONE',  ( 55.49584447822657296, 58.53775398922314821, -42.86099773636481558 ) ) ;
#20971=CARTESIAN_POINT ( 'NONE',  ( 13.36082413113063083, -81.89226687791996540, -129.1512766091129834 ) ) ;
#20972=CARTESIAN_POINT ( 'NONE',  ( 25.64703792032468854, 11.65444440562330719, -112.3081285890369827 ) ) ;
#20973=CARTESIAN_POINT ( 'NONE',  ( 5.340103579038262716, -2.303180387974230303, -147.4316330314913444 ) ) ;
#20974=CARTESIAN_POINT ( 'NONE',  ( 1.833603222531970056, -132.3826570575579069, -59.42758433816098318 ) ) ;
#20976=CARTESIAN_POINT ( 'NONE',  ( 94.22246935314088034, 70.00000000000002842, -6.938893903907228378E-15 ) ) ;
#20982=CARTESIAN_POINT ( 'NONE',  ( 8.186469777910764023, -57.56191611950399079, 137.8131828745824237 ) ) ;
#20983=CARTESIAN_POINT ( 'NONE',  ( 2.063896406836605024, -71.46753739785927451, -126.4736179849655144 ) ) ;
#20984=CARTESIAN_POINT ( 'NONE',  ( 30.59141879584279522, 75.73279557183299460, 88.14706749784066631 ) ) ;
#20987=EDGE_CURVE ( 'NONE', #3154, #14763, #19194, .T. ) ;
#20988=CARTESIAN_POINT ( 'NONE',  ( 26.11404676487257603, 110.9778746459749641, -22.43340081644658213 ) ) ;
#20990=EDGE_CURVE ( 'NONE', #14585, #26642, #7538, .T. ) ;
#20991=ORIENTED_EDGE ( 'NONE', *, *, #22028, .T. ) ;
#20992=LINE ( 'NONE', #5057, #8297 ) ;
#20993=ADVANCED_FACE ( 'NONE', ( #10385 ), #5777, .F. ) ;
#20995=B_SPLINE_CURVE_WITH_KNOTS ( 'NONE', 3,
 ( #24413, #20362, #22692, #13457 ),
 .UNSPECIFIED., .F., .F.,
 ( 4, 4 ),
 ( 3.206611828262218431E-16, 0.01077107486149763219 ),
 .UNSPECIFIED. ) ;
#20996=CARTESIAN_POINT ( 'NONE',  ( 6.224689322667647851, -62.55544044765161260, -134.1951906609245384 ) ) ;
#20997=EDGE_CURVE ( 'NONE', #10838, #5291, #20922, .T. ) ;
#20998=B_SPLINE_CURVE_WITH_KNOTS ( 'NONE', 3,
 ( #10392, #12944, #21734, #10103 ),
 .UNSPECIFIED., .F., .F.,
 ( 4, 4 ),
 ( 2.593745175800364344E-16, 0.008383748772659713883 ),
 .UNSPECIFIED. ) ;
#21000=CARTESIAN_POINT ( 'NONE',  ( 109.1592201516379674, 0.006649399203953390916, 0.004194960840980714069 ) ) ;
#21001=CARTESIAN_POINT ( 'NONE',  ( 1.833809397773862537, 138.0624841332893880, -44.67209459544923078 ) ) ;
#21003=CARTESIAN_POINT ( 'NONE',  ( 32.73300124599735028, 84.80615050150375112, 81.52272205837232377 ) ) ;
#21004=CARTESIAN_POINT ( 'NONE',  ( 1.833838850093465700, -125.6687428896154159, -72.55487854850817087 ) ) ;
#21006=ORIENTED_EDGE ( 'NONE', *, *, #4618, .F. ) ;
#21008=CARTESIAN_POINT ( 'NONE',  ( 109.1624594426973260, -0.01582142368018300480, -0.002129375066970793252 ) ) ;
#21009=CARTESIAN_POINT ( 'NONE',  ( 9.884929003653608603, -114.6392083957124441, 97.56484214660585508 ) ) ;
#21011=CARTESIAN_POINT ( 'NONE',  ( 25.64681081121879203, -83.63051021305848565, -75.86069728269076506 ) ) ;
#21012=EDGE_CURVE ( 'NONE', #9366, #945, #10262, .T. ) ;
#21014=( BOUNDED_SURFACE ( )  B_SPLINE_SURFACE ( 3, 1, ( 
 ( #2075, #10880 ),
 ( #22094, #19639 ),
 ( #2359, #19937 ),
 ( #218, #17482 ) ),
 .UNSPECIFIED., .F., .F., .F. ) 
 B_SPLINE_SURFACE_WITH_KNOTS ( ( 4, 4 ),
 ( 2, 2 ),
 ( 0.000000000000000000, 1.000000000000000000 ),
 ( 0.000000000000000000, 1.000000000000000000 ),
 .UNSPECIFIED. ) 
 GEOMETRIC_REPRESENTATION_ITEM ( )  RATIONAL_B_SPLINE_SURFACE ( (
 ( 1.000000000000000000, 1.000000000000000000),
 ( 0.6386103224230302855, 0.9954351624131538845),
 ( 0.6386103224230302855, 0.9954351624131538845),
 ( 1.000000000000000000, 1.000000000000000000) ) ) 
 REPRESENTATION_ITEM ( '' )  SURFACE ( )  );
#21017=ORIENTED_EDGE ( 'NONE', *, *, #25969, .F. ) ;
#21018=CARTESIAN_POINT ( 'NONE',  ( 1.833691583653570101, -144.3515375443195978, 14.81406002961268342 ) ) ;
#21019=DIRECTION ( 'NONE',  ( -1.000000000000000000, -0.000000000000000000, -0.000000000000000000 ) ) ;
#21020=CARTESIAN_POINT ( 'NONE',  ( 109.1587776205901577, 0.006388631651928893332, -0.003592288931009626502 ) ) ;
#21023=EDGE_LOOP ( 'NONE', ( #27449, #11933, #3961, #17327 ) ) ;
#21026=VERTEX_POINT ( 'NONE', #14393 ) ;
#21027=EDGE_CURVE ( 'NONE', #27866, #1025, #24352, .T. ) ;
#21032=DIRECTION ( 'NONE',  ( -1.000000000000000000, -0.000000000000000000, -0.000000000000000000 ) ) ;
#21033=CARTESIAN_POINT ( 'NONE',  ( 109.1589550718175161, 0.005777059646713184060, 0.004900004919101252042 ) ) ;
#21034=CARTESIAN_POINT ( 'NONE',  ( 2.433796855181233454, -138.8296532063085351, -43.58222566461785163 ) ) ;
#21036=CARTESIAN_POINT ( 'NONE',  ( 2.108393763691208456, -132.2055356348357691, -60.26375949664320331 ) ) ;
#21037=CARTESIAN_POINT ( 'NONE',  ( 109.1592201516379674, 0.007748443302134881173, 0.001331853079201419324 ) ) ;
#21038=FACE_OUTER_BOUND ( 'NONE', #4187, .T. ) ;
#21040=CARTESIAN_POINT ( 'NONE',  ( 26.11404676487257603, -33.91085499298301897, -108.0249973236470993 ) ) ;
#21041=FACE_OUTER_BOUND ( 'NONE', #13870, .T. ) ;
#21046=CARTESIAN_POINT ( 'NONE',  ( 24.01988960052066702, 125.8850824254504630, -36.40943914739766285 ) ) ;
#21047=ORIENTED_EDGE ( 'NONE', *, *, #3220, .T. ) ;
#21048=CARTESIAN_POINT ( 'NONE',  ( 109.1592201516379674, 0.002720803050361310545, -0.007376275279030886783 ) ) ;
#21053=EDGE_CURVE ( 'NONE', #20645, #16536, #12667, .T. ) ;
#21055=ORIENTED_EDGE ( 'NONE', *, *, #19438, .F. ) ;
#21056=EDGE_CURVE ( 'NONE', #1292, #10573, #14007, .T. ) ;
#21057=EDGE_CURVE ( 'NONE', #27330, #21644, #4239, .T. ) ;
#21060=CARTESIAN_POINT ( 'NONE',  ( 1.832998868059890096, -58.53348008137562175, -132.7810136645743739 ) ) ;
#21061=CIRCLE ( 'NONE', #13765, 117.6351876552689504 ) ;
#21062=AXIS2_PLACEMENT_3D ( 'NONE', #11456, #370, #13751 ) ;
#21064=CARTESIAN_POINT ( 'NONE',  ( 109.1778270068192853, 0.007736698406808902723, 0.005186985107090163853 ) ) ;
#21065=CARTESIAN_POINT ( 'NONE',  ( 26.11404676487257603, -107.3263591096432776, 36.06104232266415721 ) ) ;
#21066=LINE ( 'NONE', #11873, #20308 ) ;
#21068=DIRECTION ( 'NONE',  ( 0.000000000000000000, 0.000000000000000000, 1.000000000000000000 ) ) ;
#21069=CARTESIAN_POINT ( 'NONE',  ( 1.833750490713756731, 132.6726660571951300, -58.77746103890142138 ) ) ;
#21070=VERTEX_POINT ( 'NONE', #2645 ) ;
#21072=CARTESIAN_POINT ( 'NONE',  ( 2.263178113027048521, -28.85718369185609333, -142.5035404044876941 ) ) ;
#21073=CARTESIAN_POINT ( 'NONE',  ( 1.833485406944057594, -138.1714136985305572, -44.33323125130066700 ) ) ;
#21074=CARTESIAN_POINT ( 'NONE',  ( 2.433796855181233454, 57.85512797798071460, -133.5135467655512400 ) ) ;
#21076=CARTESIAN_POINT ( 'NONE',  ( 1.833750490713655479, -85.50916867388886544, 117.2391074582370578 ) ) ;
#21079=EDGE_CURVE ( 'NONE', #20029, #2039, #6450, .T. ) ;
#21083=CARTESIAN_POINT ( 'NONE',  ( 2.430230287190581429, 46.34481016237006656, -137.9371479820457864 ) ) ;
#21084=ORIENTED_EDGE ( 'NONE', *, *, #6045, .F. ) ;
#21086=EDGE_CURVE ( 'NONE', #26751, #25984, #16767, .T. ) ;
#21087=CARTESIAN_POINT ( 'NONE',  ( 109.1587776205901861, 0.003736572840496128929, 0.006305329297950517699 ) ) ;
#21088=EDGE_CURVE ( 'NONE', #21864, #10457, #28392, .T. ) ;
#21090=ORIENTED_EDGE ( 'NONE', *, *, #14451, .T. ) ;
#21092=CARTESIAN_POINT ( 'NONE',  ( 1.833485406944043827, 96.69979900902167458, 108.1939177044929323 ) ) ;
#21093=ORIENTED_EDGE ( 'NONE', *, *, #7791, .T. ) ;
#21095=CARTESIAN_POINT ( 'NONE',  ( 25.87036335909425588, 112.5399073133628605, 10.83311869338108302 ) ) ;
#21096=CARTESIAN_POINT ( 'NONE',  ( 109.1586900883932856, -0.004113747440992365084, 0.005833932871491302741 ) ) ;
#21098=LINE ( 'NONE', #15037, #14762 ) ;
#21099=CARTESIAN_POINT ( 'NONE',  ( 32.73300124599732186, 0.000000000000000000, 0.000000000000000000 ) ) ;
#21101=ORIENTED_EDGE ( 'NONE', *, *, #14324, .F. ) ;
#21102=CARTESIAN_POINT ( 'NONE',  ( 26.11404676487257603, -103.8885755249572469, 45.01677474591374306 ) ) ;
#21104=FACE_OUTER_BOUND ( 'NONE', #11160, .T. ) ;
#21105=DIRECTION ( 'NONE',  ( 0.000000000000000000, 1.110223024625156343E-15, 1.000000000000000000 ) ) ;
#21107=EDGE_LOOP ( 'NONE', ( #13636, #7844, #1458, #19721 ) ) ;
#21108=VERTEX_POINT ( 'NONE', #18315 ) ;
#21110=CARTESIAN_POINT ( 'NONE',  ( 1.834118845439484335, -138.0627591860427117, -44.67218053242533671 ) ) ;
#21111=CARTESIAN_POINT ( 'NONE',  ( 109.1778270068192853, 0.005967275455179332777, -0.007152128381195968672 ) ) ;
#21114=B_SPLINE_CURVE_WITH_KNOTS ( 'NONE', 3,
 ( #15333, #10613, #24143, #15187, #19525, #28429, #8459, #2093 ),
 .UNSPECIFIED., .F., .F.,
 ( 4, 2, 2, 4 ),
 ( 6.938893903907228378E-18, 0.0002429588503611247914, 0.0004859177007222426439, 0.0009718354014444878898 ),
 .UNSPECIFIED. ) ;
#21115=DIRECTION ( 'NONE',  ( 0.000000000000000000, 0.000000000000000000, 1.000000000000000000 ) ) ;
#21116=ORIENTED_EDGE ( 'NONE', *, *, #12447, .F. ) ;
#21119=EDGE_CURVE ( 'NONE', #14178, #25292, #23658, .T. ) ;
#21120=EDGE_LOOP ( 'NONE', ( #24364, #7402, #26433, #4118 ) ) ;
#21121=DIRECTION ( 'NONE',  ( 0.000000000000000000, 0.000000000000000000, 1.000000000000000000 ) ) ;
#21123=CARTESIAN_POINT ( 'NONE',  ( 6.224689322667647851, 139.9988794244339090, -48.18553814189883866 ) ) ;
#21124=CARTESIAN_POINT ( 'NONE',  ( 26.11404676487259024, -67.46175819463304890, -90.92995828888270182 ) ) ;
#21125=EDGE_CURVE ( 'NONE', #2053, #8211, #27771, .T. ) ;
#21127=CARTESIAN_POINT ( 'NONE',  ( 26.11404676487257603, 74.91683232330973397, 84.89295829319517850 ) ) ;
#21128=CARTESIAN_POINT ( 'NONE',  ( 28.43349137099852797, 115.0977416143054199, 46.80919715692925820 ) ) ;
#21129=EDGE_CURVE ( 'NONE', #21239, #2577, #7706, .T. ) ;
#21130=ORIENTED_EDGE ( 'NONE', *, *, #8951, .F. ) ;
#21132=CARTESIAN_POINT ( 'NONE',  ( 109.1589550718174877, -0.003591809816105041679, -0.006669585340466632761 ) ) ;
#21135=CARTESIAN_POINT ( 'NONE',  ( 2.433796855181219243, 142.0211193075555798, 31.67151202413018396 ) ) ;
#21137=VERTEX_POINT ( 'NONE', #9853 ) ;
#21138=B_SPLINE_CURVE_WITH_KNOTS ( 'NONE', 3,
 ( #9348, #26882, #18237, #16234, #3006, #15946, #18382 ),
 .UNSPECIFIED., .F., .F.,
 ( 4, 3, 4 ),
 ( 0.000000000000000000, 0.02398743853561317516, 0.04000277880656230578 ),
 .UNSPECIFIED. ) ;
#21139=B_SPLINE_CURVE_WITH_KNOTS ( 'NONE', 3,
 ( #3648, #12424, #27836, #21213, #1764, #10708 ),
 .UNSPECIFIED., .F., .F.,
 ( 4, 2, 4 ),
 ( 8.673617379884035472E-18, 0.0006311636237756842235, 0.001262327247551359773 ),
 .UNSPECIFIED. ) ;
#21140=B_SPLINE_CURVE_WITH_KNOTS ( 'NONE', 3,
 ( #18327, #9294, #18192, #24568, #4682, #2807, #11301, #27109, #20072, #20208 ),
 .UNSPECIFIED., .F., .F.,
 ( 4, 3, 3, 4 ),
 ( 5.003707553108401214E-17, 0.0002669559177086182258, 0.0005339118354151107648, 0.001067817517169164900 ),
 .UNSPECIFIED. ) ;
#21145=CARTESIAN_POINT ( 'NONE',  ( 1.832998868059890096, 29.64765804470076205, 142.0492247521723641 ) ) ;
#21146=CARTESIAN_POINT ( 'NONE',  ( 32.73300124599734318, 116.5274707358856006, 16.10546300444864443 ) ) ;
#21148=CARTESIAN_POINT ( 'NONE',  ( 1.833485406944043827, -125.4007332306540405, -73.01664920993097496 ) ) ;
#21149=CARTESIAN_POINT ( 'NONE',  ( 25.64700659047696973, 112.3162501909140900, -11.57609179463844207 ) ) ;
#21150=CARTESIAN_POINT ( 'NONE',  ( 1.833206308920077632, -15.90849808441977942, 144.2348261777515290 ) ) ;
#21151=ORIENTED_EDGE ( 'NONE', *, *, #2684, .T. ) ;
#21157=CARTESIAN_POINT ( 'NONE',  ( 2.433796855181205476, -43.58222566461547132, -138.8296532063092457 ) ) ;
#21160=CARTESIAN_POINT ( 'NONE',  ( 25.81918753295378011, -91.98563552012987543, -65.67738364544824492 ) ) ;
#21161=DIRECTION ( 'NONE',  ( 0.5914120900931445490, -0.8010740644654237297, -0.09226095020378197176 ) ) ;
#21162=VERTEX_POINT ( 'NONE', #16610 ) ;
#21164=CARTESIAN_POINT ( 'NONE',  ( 9.884929003653626367, 146.3148513795970871, -35.39789245780186633 ) ) ;
#21166=ADVANCED_FACE ( 'NONE', ( #27685 ), #6850, .F. ) ;
#21168=CARTESIAN_POINT ( 'NONE',  ( 25.86096068574582674, 65.64181925268327689, 92.04529103340799168 ) ) ;
#21170=EDGE_LOOP ( 'NONE', ( #9001, #4223, #24944, #20295 ) ) ;
#21171=FACE_OUTER_BOUND ( 'NONE', #11226, .T. ) ;
#21172=CYLINDRICAL_SURFACE ( 'NONE', #14338, 12.50000000000000178 ) ;
#21174=ORIENTED_EDGE ( 'NONE', *, *, #21419, .F. ) ;
#21175=VERTEX_POINT ( 'NONE', #27830 ) ;
#21177=AXIS2_PLACEMENT_3D ( 'NONE', #5362, #899, #9683 ) ;
#21178=CARTESIAN_POINT ( 'NONE',  ( 25.64681081121879203, -110.5293738517606954, -23.06870491922435207 ) ) ;
#21179=CARTESIAN_POINT ( 'NONE',  ( 109.1586900883932856, 0.001385221016536852898, 0.007002774699553664800 ) ) ;
#21181=( BOUNDED_SURFACE ( )  B_SPLINE_SURFACE ( 3, 1, ( 
 ( #13083, #2125 ),
 ( #6474, #21869 ),
 ( #26319, #12937 ),
 ( #8766, #19694 ) ),
 .UNSPECIFIED., .F., .F., .F. ) 
 B_SPLINE_SURFACE_WITH_KNOTS ( ( 4, 4 ),
 ( 2, 2 ),
 ( 0.000000000000000000, 1.000000000000000000 ),
 ( 0.000000000000000000, 1.000000000000000000 ),
 .UNSPECIFIED. ) 
 GEOMETRIC_REPRESENTATION_ITEM ( )  RATIONAL_B_SPLINE_SURFACE ( (
 ( 1.000000000000000000, 1.000000000000000000),
 ( 0.6386103224230316178, 0.9954351624131538845),
 ( 0.6386103224230316178, 0.9954351624131538845),
 ( 1.000000000000000000, 1.000000000000000000) ) ) 
 REPRESENTATION_ITEM ( '' )  SURFACE ( )  );
#21183=CARTESIAN_POINT ( 'NONE',  ( 19.66333377628664181, 116.9853418557814280, 72.72773398758276642 ) ) ;
#21184=VERTEX_POINT ( 'NONE', #27539 ) ;
#21185=ADVANCED_FACE ( 'NONE', ( #25110 ), #13897, .T. ) ;
#21186=CARTESIAN_POINT ( 'NONE',  ( 32.73300124599732186, 0.000000000000000000, 0.000000000000000000 ) ) ;
#21188=EDGE_CURVE ( 'NONE', #18334, #24971, #10000, .T. ) ;
#21190=CARTESIAN_POINT ( 'NONE',  ( 25.64708010899968116, -75.59303792846567660, -83.87281825978691074 ) ) ;
#21191=CARTESIAN_POINT ( 'NONE',  ( 1.833809397773832783, -141.9016658667394495, -30.34407330672331682 ) ) ;
#21192=ADVANCED_FACE ( 'NONE', ( #5963 ), #20461, .F. ) ;
#21193=VECTOR ( 'NONE', #18553, 1000.000000000000227 ) ;
#21194=B_SPLINE_CURVE_WITH_KNOTS ( 'NONE', 3,
 ( #1242, #12461, #7746, #23001, #23572, #21247, #5723 ),
 .UNSPECIFIED., .F., .F.,
 ( 4, 3, 4 ),
 ( 7.852014599531142026E-16, 0.02816610861753242323, 0.04000277880656292334 ),
 .UNSPECIFIED. ) ;
#21196=CARTESIAN_POINT ( 'NONE',  ( 55.79472521941428198, -48.13855120843920332, 54.55111121764066695 ) ) ;
#21197=CARTESIAN_POINT ( 'NONE',  ( 109.1586900883932856, -0.002995460350188440014, -0.006479576224398238618 ) ) ;
#21199=CARTESIAN_POINT ( 'NONE',  ( 25.64681081121879203, 112.2483031020013442, 12.21581276189844800 ) ) ;
#21201=FACE_OUTER_BOUND ( 'NONE', #16526, .T. ) ;
#21202=CARTESIAN_POINT ( 'NONE',  ( 25.64681081121879203, 102.9795863647028682, 46.30456157731362765 ) ) ;
#21203=ORIENTED_EDGE ( 'NONE', *, *, #10768, .F. ) ;
#21204=CIRCLE ( 'NONE', #18909, 151.1787379149930359 ) ;
#21205=ORIENTED_EDGE ( 'NONE', *, *, #27421, .F. ) ;
#21206=CARTESIAN_POINT ( 'NONE',  ( 109.1592201516379674, -0.007376275279030860763, -0.002720803050361382969 ) ) ;
#21207=CARTESIAN_POINT ( 'NONE',  ( 109.1586900883932856, -0.006231977675082132212, 0.003481399864227350312 ) ) ;
#21209=ORIENTED_EDGE ( 'NONE', *, *, #6283, .T. ) ;
#21210=VERTEX_POINT ( 'NONE', #5376 ) ;
#21212=CIRCLE ( 'NONE', #8806, 117.6351876552689504 ) ;
#21213=CARTESIAN_POINT ( 'NONE',  ( 1.893872463202031620, -73.39855082356734783, 125.2243573918632507 ) ) ;
#21214=B_SPLINE_CURVE_WITH_KNOTS ( 'NONE', 3,
 ( #2604, #4624, #11249, #11827, #20021, #20594, #302, #877 ),
 .UNSPECIFIED., .F., .F.,
 ( 4, 2, 2, 4 ),
 ( 0.000000000000000000, 0.0002429588503611201022, 0.0004859177007222402044, 0.0009718354014444856130 ),
 .UNSPECIFIED. ) ;
#21215=( BOUNDED_SURFACE ( )  B_SPLINE_SURFACE ( 3, 1, ( 
 ( #5507, #19041 ),
 ( #27818, #1196 ),
 ( #25387, #16887 ),
 ( #20761, #1054 ) ),
 .UNSPECIFIED., .F., .F., .F. ) 
 B_SPLINE_SURFACE_WITH_KNOTS ( ( 4, 4 ),
 ( 2, 2 ),
 ( 0.000000000000000000, 1.000000000000000000 ),
 ( 0.000000000000000000, 1.000000000000000000 ),
 .UNSPECIFIED. ) 
 GEOMETRIC_REPRESENTATION_ITEM ( )  RATIONAL_B_SPLINE_SURFACE ( (
 ( 1.000000000000000000, 1.000000000000000000),
 ( 0.9960225298536222738, 0.9999952330161893110),
 ( 0.9960225298536222738, 0.9999952330161893110),
 ( 1.000000000000000000, 1.000000000000000000) ) ) 
 REPRESENTATION_ITEM ( '' )  SURFACE ( )  );
#21216=VECTOR ( 'NONE', #8189, 1000.000000000000000 ) ;
#21217=CARTESIAN_POINT ( 'NONE',  ( 55.79472521941426777, 72.42790650415584253, -6.880567342318959945 ) ) ;
#21218=CARTESIAN_POINT ( 'NONE',  ( 32.73300124599741423, -84.80615050150312584, -81.52272205837286378 ) ) ;
#21219=CARTESIAN_POINT ( 'NONE',  ( 1.833485406944057594, 72.09189602597886903, -125.9346397303427665 ) ) ;
#21220=DIRECTION ( 'NONE',  ( 1.000000000000000000, -0.000000000000000000, -0.000000000000000000 ) ) ;
#21221=EDGE_CURVE ( 'NONE', #3847, #10427, #1342, .T. ) ;
#21223=CARTESIAN_POINT ( 'NONE',  ( 25.98552792386798771, -112.6247604222998291, -10.75254026142917674 ) ) ;
#21224=EDGE_CURVE ( 'NONE', #19554, #2978, #11585, .T. ) ;
#21226=ORIENTED_EDGE ( 'NONE', *, *, #2151, .F. ) ;
#21228=CARTESIAN_POINT ( 'NONE',  ( 1.893872463202068923, 132.9857054814988260, -58.16604752596591510 ) ) ;
#21229=CARTESIAN_POINT ( 'NONE',  ( 109.1721716018069515, 0.006757465437533756447, 0.01567407524361263613 ) ) ;
#21231=DIRECTION ( 'NONE',  ( -0.5946245182733608248, 0.5401723099040878218, 0.5955128528260794640 ) ) ;
#21233=CARTESIAN_POINT ( 'NONE',  ( 1.894214914920956172, 96.41356089048431954, -108.5033568857715096 ) ) ;
#21234=VERTEX_POINT ( 'NONE', #3930 ) ;
#21237=CARTESIAN_POINT ( 'NONE',  ( 26.11404676487257603, 90.92995828888199128, 67.46175819463394419 ) ) ;
#21238=VERTEX_POINT ( 'NONE', #19735 ) ;
#21239=VERTEX_POINT ( 'NONE', #28369 ) ;
#21241=ORIENTED_EDGE ( 'NONE', *, *, #14255, .T. ) ;
#21242=AXIS2_PLACEMENT_3D ( 'NONE', #25800, #8390, #6098 ) ;
#21243=ORIENTED_EDGE ( 'NONE', *, *, #6290, .T. ) ;
#21244=CARTESIAN_POINT ( 'NONE',  ( 26.11404676487257603, 76.59696442953305962, -83.38016054979703995 ) ) ;
#21245=ORIENTED_EDGE ( 'NONE', *, *, #9804, .T. ) ;
#21247=CARTESIAN_POINT ( 'NONE',  ( 30.58324630866334104, -57.02364853894557228, 106.6567942264195352 ) ) ;
#21248=B_SPLINE_CURVE_WITH_KNOTS ( 'NONE', 3,
 ( #1535, #16510, #3274, #25589, #5574, #23429, #3545 ),
 .UNSPECIFIED., .F., .F.,
 ( 4, 3, 4 ),
 ( 0.000000000000000000, 0.02398743853561422640, 0.04000277880656209761 ),
 .UNSPECIFIED. ) ;
#21251=CARTESIAN_POINT ( 'NONE',  ( 25.64704443564077252, 83.82001435192627525, 75.65149037849788272 ) ) ;
#21252=LINE ( 'NONE', #9904, #23052 ) ;
#21254=EDGE_CURVE ( 'NONE', #14469, #14145, #17578, .T. ) ;
#21255=AXIS2_PLACEMENT_3D ( 'NONE', #24992, #1498, #19068 ) ;
#21257=CARTESIAN_POINT ( 'NONE',  ( 25.64708010899964918, -97.81137751680957138, -56.40825696968362735 ) ) ;
#21259=CARTESIAN_POINT ( 'NONE',  ( 32.73300124599732186, 0.000000000000000000, 0.000000000000000000 ) ) ;
#21260=VECTOR ( 'NONE', #15982, 1000.000000000000000 ) ;
#21261=VERTEX_POINT ( 'NONE', #28097 ) ;
#21263=DIRECTION ( 'NONE',  ( 0.5914120900931444380, -0.7023121577978181929, 0.3962188444547167232 ) ) ;
#21265=CARTESIAN_POINT ( 'NONE',  ( 32.73300124599732186, 0.000000000000000000, 0.000000000000000000 ) ) ;
#21266=CARTESIAN_POINT ( 'NONE',  ( 2.108985857320904156, 46.11505917359444595, 137.7807691131289403 ) ) ;
#21267=CARTESIAN_POINT ( 'NONE',  ( 94.22246935314088034, 70.00000000000004263, 12.49999999999999467 ) ) ;
#21269=ORIENTED_EDGE ( 'NONE', *, *, #815, .F. ) ;
#21273=VERTEX_POINT ( 'NONE', #17434 ) ;
#21276=CARTESIAN_POINT ( 'NONE',  ( 2.433796855181233454, -57.85512797797981932, 133.5135467655516095 ) ) ;
#21277=LINE ( 'NONE', #27466, #39 ) ;
#21279=ORIENTED_EDGE ( 'NONE', *, *, #9403, .T. ) ;
#21280=B_SPLINE_CURVE_WITH_KNOTS ( 'NONE', 3,
 ( #18100, #13638, #24751, #27009, #7620, #16230, #17945, #7321 ),
 .UNSPECIFIED., .F., .F.,
 ( 4, 2, 2, 4 ),
 ( 1.993045536433795054E-17, 0.0002429588503611324350, 0.0004859177007222449749, 0.0009718354014444726026 ),
 .UNSPECIFIED. ) ;
#21281=FACE_OUTER_BOUND ( 'NONE', #3118, .T. ) ;
#21282=CARTESIAN_POINT ( 'NONE',  ( 109.1592201516379674, 0.006649399203953463774, -0.004194960840990087647 ) ) ;
#21283=CIRCLE ( 'NONE', #12990, 151.1787379149930359 ) ;
#21284=ORIENTED_EDGE ( 'NONE', *, *, #16081, .T. ) ;
#21286=AXIS2_PLACEMENT_3D ( 'NONE', #20020, #22189, #2456 ) ;
#21288=B_SPLINE_CURVE_WITH_KNOTS ( 'NONE', 3,
 ( #25963, #17034, #19480, #23823 ),
 .UNSPECIFIED., .F., .F.,
 ( 4, 4 ),
 ( 6.258866915731342927E-16, 0.008383748772660081644 ),
 .UNSPECIFIED. ) ;
#21290=EDGE_CURVE ( 'NONE', #19216, #19831, #25867, .T. ) ;
#21293=CARTESIAN_POINT ( 'NONE',  ( 109.1624594426973260, 0.004489871836309092604, 0.01531968460305925539 ) ) ;
#21294=CARTESIAN_POINT ( 'NONE',  ( 25.87036335909425944, 74.91347493818375369, -84.67915015758781294 ) ) ;
#21295=EDGE_CURVE ( 'NONE', #422, #4630, #25411, .T. ) ;
#21299=ORIENTED_EDGE ( 'NONE', *, *, #15595, .F. ) ;
#21300=ORIENTED_EDGE ( 'NONE', *, *, #8750, .T. ) ;
#21301=CARTESIAN_POINT ( 'NONE',  ( 1.834118845439484335, -14.99112450600151369, -144.3336252355298370 ) ) ;
#21302=CARTESIAN_POINT ( 'NONE',  ( 99.22246935314075245, -90.00000000000005684, 39.99999999999997158 ) ) ;
#21303=CARTESIAN_POINT ( 'NONE',  ( 109.1586900883932856, -0.005833932871487542728, 0.004113747441000899924 ) ) ;
#21304=LINE ( 'NONE', #25205, #15614 ) ;
#21308=ORIENTED_EDGE ( 'NONE', *, *, #8768, .T. ) ;
#21309=FACE_OUTER_BOUND ( 'NONE', #13338, .T. ) ;
#21311=VECTOR ( 'NONE', #27794, 1000.000000000000000 ) ;
#21312=CARTESIAN_POINT ( 'NONE',  ( 10.93730112725932635, 0.000000000000000000, 0.000000000000000000 ) ) ;
#21313=CARTESIAN_POINT ( 'NONE',  ( 109.1586059443104944, -0.0002768082440289232316, -0.007068659269321312354 ) ) ;
#21319=VERTEX_POINT ( 'NONE', #4203 ) ;
#21320=EDGE_CURVE ( 'NONE', #1896, #12511, #23286, .T. ) ;
#21321=B_SPLINE_CURVE_WITH_KNOTS ( 'NONE', 3,
 ( #6402, #15155, #23978, #13015, #17883, #4813 ),
 .UNSPECIFIED., .F., .F.,
 ( 4, 2, 4 ),
 ( 1.734723475976807094E-18, 0.0006311636237756867171, 0.001262327247551371916 ),
 .UNSPECIFIED. ) ;
#21324=EDGE_CURVE ( 'NONE', #10869, #10817, #20882, .T. ) ;
#21325=CARTESIAN_POINT ( 'NONE',  ( 109.1586059443104944, 0.0004635842312889974066, 0.007058870754606111179 ) ) ;
#21326=EDGE_CURVE ( 'NONE', #19503, #22199, #6665, .T. ) ;
#21328=B_SPLINE_CURVE_WITH_KNOTS ( 'NONE', 3,
 ( #9158, #22413, #2234, #13182 ),
 .UNSPECIFIED., .F., .F.,
 ( 4, 4 ),
 ( 3.527177457865194202E-16, 0.01077107486149824801 ),
 .UNSPECIFIED. ) ;
#21329=CARTESIAN_POINT ( 'NONE',  ( 10.93730112725943293, 128.3908183996590537, 79.81734490845931873 ) ) ;
#21330=ORIENTED_EDGE ( 'NONE', *, *, #22336, .T. ) ;
#21332=CARTESIAN_POINT ( 'NONE',  ( 1.833206308920118932, -132.2594750499821430, -59.70089323729867914 ) ) ;
#21333=CARTESIAN_POINT ( 'NONE',  ( 109.1778270068192853, 0.0006237116683871330673, -0.009293669915260188014 ) ) ;
#21337=CARTESIAN_POINT ( 'NONE',  ( 109.1778270068192853, 0.008743876326153509834, 0.003210287141656787899 ) ) ;
#21338=CARTESIAN_POINT ( 'NONE',  ( 26.11404676487259024, 10.71016160607717538, -112.7148551500679332 ) ) ;
#21339=CARTESIAN_POINT ( 'NONE',  ( 1.834118845439484335, 85.14950727125857100, 117.5010238212701381 ) ) ;
#21340=CARTESIAN_POINT ( 'NONE',  ( 1.833485406944057594, -117.0814567582550154, 85.72460230293657446 ) ) ;
#21341=CARTESIAN_POINT ( 'NONE',  ( 55.79472521941428198, -14.41365263906602401, 71.31192372336670360 ) ) ;
#21343=ORIENTED_EDGE ( 'NONE', *, *, #9635, .F. ) ;
#21348=ORIENTED_EDGE ( 'NONE', *, *, #15279, .F. ) ;
#21349=ORIENTED_EDGE ( 'NONE', *, *, #26251, .T. ) ;
#21350=ORIENTED_EDGE ( 'NONE', *, *, #26065, .T. ) ;
#21351=ORIENTED_EDGE ( 'NONE', *, *, #9859, .T. ) ;
#21354=( BOUNDED_SURFACE ( )  B_SPLINE_SURFACE ( 3, 1, ( 
 ( #19290, #8368 ),
 ( #23913, #17128 ),
 ( #10804, #17958 ),
 ( #5012, #9355 ) ),
 .UNSPECIFIED., .F., .F., .F. ) 
 B_SPLINE_SURFACE_WITH_KNOTS ( ( 4, 4 ),
 ( 2, 2 ),
 ( 0.000000000000000000, 1.000000000000000000 ),
 ( 0.000000000000000000, 1.000000000000000000 ),
 .UNSPECIFIED. ) 
 GEOMETRIC_REPRESENTATION_ITEM ( )  RATIONAL_B_SPLINE_SURFACE ( (
 ( 1.000000000000000000, 1.000000000000000000),
 ( 0.9956975270656955868, 0.8568959468854907557),
 ( 0.9956975270656955868, 0.8568959468854907557),
 ( 1.000000000000000000, 1.000000000000000000) ) ) 
 REPRESENTATION_ITEM ( '' )  SURFACE ( )  );
#21355=CARTESIAN_POINT ( 'NONE',  ( 28.37644542392839853, 80.14194118792715926, 95.06674036596241706 ) ) ;
#21358=LINE ( 'NONE', #9254, #14262 ) ;
#21359=EDGE_CURVE ( 'NONE', #25814, #431, #9200, .T. ) ;
#21360=CARTESIAN_POINT ( 'NONE',  ( 32.73300124599769134, -51.32617430724849328, -105.8473486001054198 ) ) ;
#21361=CARTESIAN_POINT ( 'NONE',  ( 109.1592201516379674, -0.007845213074660005795, -0.0005146241775907089413 ) ) ;
#21363=CARTESIAN_POINT ( 'NONE',  ( 26.11404676487257603, 65.63269960453241936, 92.25884714080432047 ) ) ;
#21364=LINE ( 'NONE', #1354, #24433 ) ;
#21365=VERTEX_POINT ( 'NONE', #22196 ) ;
#21366=EDGE_LOOP ( 'NONE', ( #23014, #10720, #13026, #6028 ) ) ;
#21367=CARTESIAN_POINT ( 'NONE',  ( 119.2224693531408803, 70.00000000000004263, 39.99999999999999289 ) ) ;
#21370=CARTESIAN_POINT ( 'NONE',  ( 26.11404676487259024, 10.71016160607717538, -112.7148551500679332 ) ) ;
#21372=ORIENTED_EDGE ( 'NONE', *, *, #1633, .F. ) ;
#21376=CARTESIAN_POINT ( 'NONE',  ( 2.433796855181233454, -84.34988187691011774, 118.5671979538053904 ) ) ;
#21378=EDGE_LOOP ( 'NONE', ( #23876, #11031, #13154, #20428 ) ) ;
#21382=EDGE_CURVE ( 'NONE', #17891, #3139, #11956, .T. ) ;
#21383=CARTESIAN_POINT ( 'NONE',  ( 13.36082413113063083, -22.28175172543457450, -151.2941478187909752 ) ) ;
#21385=VERTEX_POINT ( 'NONE', #4482 ) ;
#21386=ADVANCED_FACE ( 'NONE', ( #4780 ), #26669, .F. ) ;
#21387=CARTESIAN_POINT ( 'NONE',  ( 26.11404676487257603, -45.01677474591340911, -103.8885755249573606 ) ) ;
#21388=CARTESIAN_POINT ( 'NONE',  ( 2.433796855181205476, -118.5671979538062146, 84.34988187690890982 ) ) ;
#21389=CARTESIAN_POINT ( 'NONE',  ( 5.340103579038186332, -126.5279493327089995, 75.71042924123000262 ) ) ;
#21390=CARTESIAN_POINT ( 'NONE',  ( 6.224689322667630975, -71.79702446228212409, -129.4863684118294884 ) ) ;
#21391=CARTESIAN_POINT ( 'NONE',  ( 1.833485406944057594, -15.69895494453287021, -144.2578170162064737 ) ) ;
#21392=CARTESIAN_POINT ( 'NONE',  ( 2.430230287190589422, -116.8646894862417867, 86.70145658344620188 ) ) ;
#21393=CARTESIAN_POINT ( 'NONE',  ( 26.11404676487257603, -103.8885755249572469, 45.01677474591374306 ) ) ;
#21394=CARTESIAN_POINT ( 'NONE',  ( 25.81918753295376945, 103.6306245682015117, 45.11728622333180283 ) ) ;
#21395=CARTESIAN_POINT ( 'NONE',  ( 25.64681081121879203, -97.57530875170564855, -56.81519825470856944 ) ) ;
#21396=CARTESIAN_POINT ( 'NONE',  ( 26.11404676487257603, -10.71016160607644174, 112.7148551500680185 ) ) ;
#21399=ORIENTED_EDGE ( 'NONE', *, *, #1937, .T. ) ;
#21400=ORIENTED_EDGE ( 'NONE', *, *, #8531, .F. ) ;
#21402=CARTESIAN_POINT ( 'NONE',  ( 1.833809397773847882, -72.70895493223461870, 125.5796696653635678 ) ) ;
#21403=CARTESIAN_POINT ( 'NONE',  ( 2.430230287190572103, -28.83279105684323440, -142.6294793592101087 ) ) ;
#21404=CARTESIAN_POINT ( 'NONE',  ( 25.73574536432414916, -98.23578516674997729, 55.78561308781451089 ) ) ;
#21405=CARTESIAN_POINT ( 'NONE',  ( 26.11404676487257603, -76.59696442953135431, -83.38016054979861735 ) ) ;
#21407=ORIENTED_EDGE ( 'NONE', *, *, #6406, .T. ) ;
#21410=ORIENTED_EDGE ( 'NONE', *, *, #10237, .T. ) ;
#21411=CARTESIAN_POINT ( 'NONE',  ( 28.37644542392842695, -21.87158679436108955, -122.4011828058667106 ) ) ;
#21412=CARTESIAN_POINT ( 'NONE',  ( 32.73300124599732186, 0.000000000000000000, 0.000000000000000000 ) ) ;
#21413=CARTESIAN_POINT ( 'NONE',  ( 25.64704443564078318, 107.3436266109713273, 35.01840413910168337 ) ) ;
#21419=EDGE_CURVE ( 'NONE', #11307, #16438, #15217, .T. ) ;
#21420=VERTEX_POINT ( 'NONE', #118 ) ;
#21421=CARTESIAN_POINT ( 'NONE',  ( 1.833485406944057594, -29.64752363041639782, 142.0485807715645024 ) ) ;
#21423=ADVANCED_FACE ( 'NONE', ( #6465 ), #4067, .F. ) ;
#21429=CARTESIAN_POINT ( 'NONE',  ( 28.37603512858461485, 108.5491486026796224, -37.15644006762103402 ) ) ;
#21430=CARTESIAN_POINT ( 'NONE',  ( 10.93730112726003156, 71.28103789255123957, -133.3192575531793693 ) ) ;
#21431=CARTESIAN_POINT ( 'NONE',  ( 2.063896406836605024, 145.2631347824382715, 1.344106060020868076 ) ) ;
#21433=( BOUNDED_SURFACE ( )  B_SPLINE_SURFACE ( 3, 1, ( 
 ( #1152, #25759 ),
 ( #10375, #22904 ),
 ( #7648, #20996 ),
 ( #25627, #27478 ) ),
 .UNSPECIFIED., .F., .F., .F. ) 
 B_SPLINE_SURFACE_WITH_KNOTS ( ( 4, 4 ),
 ( 2, 2 ),
 ( 0.000000000000000000, 1.000000000000000000 ),
 ( 0.000000000000000000, 1.000000000000000000 ),
 .UNSPECIFIED. ) 
 GEOMETRIC_REPRESENTATION_ITEM ( )  RATIONAL_B_SPLINE_SURFACE ( (
 ( 1.000000000000000000, 1.000000000000000000),
 ( 0.6386103224230316178, 0.9954351624131538845),
 ( 0.6386103224230316178, 0.9954351624131538845),
 ( 1.000000000000000000, 1.000000000000000000) ) ) 
 REPRESENTATION_ITEM ( '' )  SURFACE ( )  );
#21436=CARTESIAN_POINT ( 'NONE',  ( 25.64681081121879203, 35.28660243342691416, -107.2555980796237804 ) ) ;
#21437=EDGE_LOOP ( 'NONE', ( #26277, #2276, #22014, #17357 ) ) ;
#21438=VERTEX_POINT ( 'NONE', #6610 ) ;
#21439=VERTEX_POINT ( 'NONE', #28322 ) ;
#21443=CARTESIAN_POINT ( 'NONE',  ( 25.64708010899964208, -83.94602815988619682, -75.51173009720608320 ) ) ;
#21445=EDGE_CURVE ( 'NONE', #6599, #6748, #23587, .T. ) ;
#21446=CARTESIAN_POINT ( 'NONE',  ( 109.1586900883932856, 0.007137750914552287197, 0.0001010081143884401729 ) ) ;
#21447=CARTESIAN_POINT ( 'NONE',  ( 1.893872463202038947, 97.83022426232111002, -107.2274879309817806 ) ) ;
#21448=ORIENTED_EDGE ( 'NONE', *, *, #5742, .T. ) ;
#21452=B_SPLINE_CURVE_WITH_KNOTS ( 'NONE', 3,
 ( #21034, #11839, #5499, #20752 ),
 .UNSPECIFIED., .F., .F.,
 ( 4, 4 ),
 ( 3.364033176744297164E-16, 0.01077107486149825669 ),
 .UNSPECIFIED. ) ;
#21453=CARTESIAN_POINT ( 'NONE',  ( 25.81918753295379076, 0.9336804662327143900, 113.0221398901142607 ) ) ;
#21454=CARTESIAN_POINT ( 'NONE',  ( 25.70243777736190438, 65.79472741891264320, 91.80600962488421146 ) ) ;
#21455=ADVANCED_FACE ( 'NONE', ( #17527 ), #10648, .F. ) ;
#21456=ORIENTED_EDGE ( 'NONE', *, *, #14319, .F. ) ;
#21457=CARTESIAN_POINT ( 'NONE',  ( 25.64708010899960300, -45.87517365398556279, 103.1718249732473538 ) ) ;
#21458=DIRECTION ( 'NONE',  ( -1.000000000000000000, -0.000000000000000000, -0.000000000000000000 ) ) ;
#21459=ORIENTED_EDGE ( 'NONE', *, *, #15419, .T. ) ;
#21461=EDGE_CURVE ( 'NONE', #13553, #26751, #24170, .T. ) ;
#21463=VERTEX_POINT ( 'NONE', #2118 ) ;
#21465=CARTESIAN_POINT ( 'NONE',  ( 1.833809397773857430, 30.34407330672380709, -141.9016658667393074 ) ) ;
#21466=EDGE_CURVE ( 'NONE', #19804, #24626, #26023, .T. ) ;
#21467=( BOUNDED_SURFACE ( )  B_SPLINE_SURFACE ( 3, 1, ( 
 ( #5076, #5366 ),
 ( #18304, #7694 ),
 ( #27084, #16453 ),
 ( #7393, #27530 ) ),
 .UNSPECIFIED., .F., .F., .F. ) 
 B_SPLINE_SURFACE_WITH_KNOTS ( ( 4, 4 ),
 ( 2, 2 ),
 ( 0.000000000000000000, 1.000000000000000000 ),
 ( 0.000000000000000000, 1.000000000000000000 ),
 .UNSPECIFIED. ) 
 GEOMETRIC_REPRESENTATION_ITEM ( )  RATIONAL_B_SPLINE_SURFACE ( (
 ( 1.000000000000000000, 1.000000000000000000),
 ( 0.6386103224230316178, 0.9954351624131538845),
 ( 0.6386103224230316178, 0.9954351624131538845),
 ( 1.000000000000000000, 1.000000000000000000) ) ) 
 REPRESENTATION_ITEM ( '' )  SURFACE ( )  );
#21472=CARTESIAN_POINT ( 'NONE',  ( 1.833485406944043827, -132.3460930279887293, -59.50871042846357994 ) ) ;
#21473=CARTESIAN_POINT ( 'NONE',  ( 1.834118845439484335, 132.4921483272728153, 59.18411796427096050 ) ) ;
#21474=DIRECTION ( 'NONE',  ( -0.5914120900931443270, 0.1754905759872845417, 0.7870418015781053267 ) ) ;
#21477=CARTESIAN_POINT ( 'NONE',  ( 13.36082413113061307, 135.4964217943317237, -70.90215303571982020 ) ) ;
#21478=CARTESIAN_POINT ( 'NONE',  ( 30.58324630866347960, 100.1119227962719265, 67.85993782330791646 ) ) ;
#21481=CARTESIAN_POINT ( 'NONE',  ( 2.433796855181205476, 71.49415740225076377, 126.7346379669258312 ) ) ;
#21482=EDGE_CURVE ( 'NONE', #9399, #19503, #19275, .T. ) ;
#21483=ORIENTED_EDGE ( 'NONE', *, *, #6401, .F. ) ;
#21484=EDGE_CURVE ( 'NONE', #7441, #8520, #21993, .T. ) ;
#21486=CARTESIAN_POINT ( 'NONE',  ( 2.263178607246684404, -108.9830946142707262, -96.24282447295553311 ) ) ;
#21489=VERTEX_POINT ( 'NONE', #2257 ) ;
#21492=CARTESIAN_POINT ( 'NONE',  ( 32.73300124599734318, 115.8010721414084117, 20.69176323058669809 ) ) ;
#21493=B_SPLINE_CURVE_WITH_KNOTS ( 'NONE', 3,
 ( #17708, #2157, #12968, #12822, #296, #6653 ),
 .UNSPECIFIED., .F., .F.,
 ( 4, 2, 4 ),
 ( 1.852685484479510670E-17, 0.0006311636237756912708, 0.001262327247551363676 ),
 .UNSPECIFIED. ) ;
#21496=CARTESIAN_POINT ( 'NONE',  ( 10.93730112725932813, 151.0983828010088246, -4.928439153520510985 ) ) ;
#21498=CARTESIAN_POINT ( 'NONE',  ( 109.1778270068192853, 0.004106684808170127376, 0.008360410075196028634 ) ) ;
#21500=CARTESIAN_POINT ( 'NONE',  ( 28.43349137099835389, -65.60227321965514591, -105.5221910860624064 ) ) ;
#21502=ORIENTED_EDGE ( 'NONE', *, *, #21221, .T. ) ;
#21503=ORIENTED_EDGE ( 'NONE', *, *, #8674, .T. ) ;
#21504=EDGE_CURVE ( 'NONE', #1292, #6108, #19848, .T. ) ;
#21505=CARTESIAN_POINT ( 'NONE',  ( 19.66333377628685142, 38.27269871461067652, 132.3257119126255077 ) ) ;
#21507=LINE ( 'NONE', #23551, #15691 ) ;
#21508=CARTESIAN_POINT ( 'NONE',  ( 25.64681081121879203, 112.3352186517032294, -11.38886654529559017 ) ) ;
#21511=EDGE_CURVE ( 'NONE', #24477, #9366, #27396, .T. ) ;
#21512=CARTESIAN_POINT ( 'NONE',  ( 10.93730112726003156, 125.1380233598492140, -84.82621002473311478 ) ) ;
#21513=ORIENTED_EDGE ( 'NONE', *, *, #1377, .F. ) ;
#21520=ORIENTED_EDGE ( 'NONE', *, *, #11144, .T. ) ;
#21521=CARTESIAN_POINT ( 'NONE',  ( 28.37599760073042532, -1.794331790580228736, 114.7183216384031397 ) ) ;
#21522=ORIENTED_EDGE ( 'NONE', *, *, #22996, .T. ) ;
#21524=CARTESIAN_POINT ( 'NONE',  ( 1.833206310202324607, -73.19872434058702027, -125.2945016693818587 ) ) ;
#21525=CARTESIAN_POINT ( 'NONE',  ( 2.433796855181219243, -74.00833731765649759, 125.2830755159751703 ) ) ;
#21528=CARTESIAN_POINT ( 'NONE',  ( 25.64681081121879203, -112.2483031020012589, -12.21581276189922427 ) ) ;
#21530=CARTESIAN_POINT ( 'NONE',  ( 32.73300124599741423, 113.0038235389606314, -32.68291970228113996 ) ) ;
#21531=EDGE_CURVE ( 'NONE', #10573, #17409, #19489, .T. ) ;
#21532=CARTESIAN_POINT ( 'NONE',  ( 1.831572820252008738, -31.13525033585589341, 141.7320553118905195 ) ) ;
#21533=CARTESIAN_POINT ( 'NONE',  ( 25.64670758986458665, -102.9458331681482406, -46.37945960491978070 ) ) ;
#21535=CARTESIAN_POINT ( 'NONE',  ( 16.05277956358235159, 137.6634701901226094, 39.81690014528699351 ) ) ;
#21536=CARTESIAN_POINT ( 'NONE',  ( 109.1586059443104944, 0.0002768082440195323061, -0.007068659269322301146 ) ) ;
#21538=DIRECTION ( 'NONE',  ( -0.5946245182733607137, 0.6521823330502990457, 0.4701913299128794854 ) ) ;
#21539=CARTESIAN_POINT ( 'NONE',  ( 26.11404676487257603, -98.61392875273402581, 55.62948129436210110 ) ) ;
#21543=CIRCLE ( 'NONE', #393, 117.6351876552689504 ) ;
#21550=CARTESIAN_POINT ( 'NONE',  ( 2.430230287190589422, 138.8342928068220203, 43.58368230469437776 ) ) ;
#21551=CARTESIAN_POINT ( 'NONE',  ( 25.64692232868533139, 112.3263170481597371, 11.47740546588672750 ) ) ;
#21552=B_SPLINE_CURVE_WITH_KNOTS ( 'NONE', 3,
 ( #24156, #28441, #4554, #9321, #11463, #102, #21980, #8895, #19963, #4706 ),
 .UNSPECIFIED., .F., .F.,
 ( 4, 3, 3, 4 ),
 ( 8.944667923005411581E-18, 0.0002669560319015738272, 0.0005492286108966411284, 0.0008315040496093442472 ),
 .UNSPECIFIED. ) ;
#21553=CARTESIAN_POINT ( 'NONE',  ( 1.893872463202041168, -45.75900850850099033, 137.7483215415846871 ) ) ;
#21554=ORIENTED_EDGE ( 'NONE', *, *, #12002, .T. ) ;
#21556=B_SPLINE_CURVE_WITH_KNOTS ( 'NONE', 3,
 ( #8929, #6483, #19846, #12406 ),
 .UNSPECIFIED., .F., .F.,
 ( 4, 4 ),
 ( 0.000000000000000000, 0.01077107196513890988 ),
 .UNSPECIFIED. ) ;
#21562=CARTESIAN_POINT ( 'NONE',  ( 25.98552792386799482, 65.62435323276291399, -92.15963349013291861 ) ) ;
#21563=ORIENTED_EDGE ( 'NONE', *, *, #20872, .F. ) ;
#21565=CARTESIAN_POINT ( 'NONE',  ( 24.22246935314087324, 0.000000000000000000, -20.00000000000000000 ) ) ;
#21567=DIRECTION ( 'NONE',  ( -0.5914120900931443270, 0.6045864222316711389, 0.5335794202785242302 ) ) ;
#21568=CARTESIAN_POINT ( 'NONE',  ( 1.833485406944043827, -137.8414413349082110, -45.34878176254374438 ) ) ;
#21569=CARTESIAN_POINT ( 'NONE',  ( -40.00000000000000000, 9.797174393178826052E-15, 80.00000000000000000 ) ) ;
#21571=CARTESIAN_POINT ( 'NONE',  ( 25.98552792386798771, 110.8838436908327481, 22.46612985365010573 ) ) ;
#21573=CARTESIAN_POINT ( 'NONE',  ( 2.433796855181233454, -16.65276281464466024, -144.5536872373193660 ) ) ;
#21575=VERTEX_POINT ( 'NONE', #11778 ) ;
#21577=ORIENTED_EDGE ( 'NONE', *, *, #23183, .T. ) ;
#21578=CARTESIAN_POINT ( 'NONE',  ( 26.11404676487257603, -102.9690087468804762, 47.08215554553482463 ) ) ;
#21579=DIRECTION ( 'NONE',  ( 0.5946245182733607137, -0.6487139525627716452, -0.4749651461092272986 ) ) ;
#21580=EDGE_CURVE ( 'NONE', #4784, #8439, #18114, .T. ) ;
#21581=CARTESIAN_POINT ( 'NONE',  ( 2.063896406836605024, 16.52087515463969680, -144.3268707900445520 ) ) ;
#21584=CARTESIAN_POINT ( 'NONE',  ( 109.1587776205901861, -0.005390665547495615897, 0.004965871434398026404 ) ) ;
#21585=CARTESIAN_POINT ( 'NONE',  ( 2.263178113027052518, 98.32595894905985290, -107.1074314657334554 ) ) ;
#21587=DIRECTION ( 'NONE',  ( -1.000000000000000000, -0.000000000000000000, -0.000000000000000000 ) ) ;
#21590=EDGE_CURVE ( 'NONE', #106, #27364, #7485, .T. ) ;
#21591=EDGE_CURVE ( 'NONE', #8288, #27586, #12600, .T. ) ;
#21596=DIRECTION ( 'NONE',  ( 0.000000000000000000, 0.000000000000000000, 1.000000000000000000 ) ) ;
#21597=EDGE_LOOP ( 'NONE', ( #17253, #11667, #10814, #10383 ) ) ;
#21598=ORIENTED_EDGE ( 'NONE', *, *, #4844, .T. ) ;
#21599=VERTEX_POINT ( 'NONE', #13493 ) ;
#21600=( BOUNDED_SURFACE ( )  B_SPLINE_SURFACE ( 3, 1, ( 
 ( #2349, #11154 ),
 ( #5761, #1419 ),
 ( #10227, #27768 ),
 ( #8069, #6277 ) ),
 .UNSPECIFIED., .F., .F., .F. ) 
 B_SPLINE_SURFACE_WITH_KNOTS ( ( 4, 4 ),
 ( 2, 2 ),
 ( 0.000000000000000000, 1.000000000000000000 ),
 ( 0.000000000000000000, 1.000000000000000000 ),
 .UNSPECIFIED. ) 
 GEOMETRIC_REPRESENTATION_ITEM ( )  RATIONAL_B_SPLINE_SURFACE ( (
 ( 1.000000000000000000, 1.000000000000000000),
 ( 0.9960225298536222738, 0.9999952330161893110),
 ( 0.9960225298536222738, 0.9999952330161893110),
 ( 1.000000000000000000, 1.000000000000000000) ) ) 
 REPRESENTATION_ITEM ( '' )  SURFACE ( )  );
#21601=CARTESIAN_POINT ( 'NONE',  ( 109.1586900883932856, 0.004851151255031853869, -0.005236795036868178467 ) ) ;
#21603=CARTESIAN_POINT ( 'NONE',  ( 1.833838848569442570, 72.70900949568773797, 125.5797553397071624 ) ) ;
#21606=CARTESIAN_POINT ( 'NONE',  ( 28.43349137099833968, 80.08535015164038384, -94.99961975860179564 ) ) ;
#21607=EDGE_LOOP ( 'NONE', ( #9247, #3086, #23149, #8664 ) ) ;
#21608=CARTESIAN_POINT ( 'NONE',  ( 1.833721034905646308, 58.69612512971785634, -132.7087680342062015 ) ) ;
#21609=EDGE_CURVE ( 'NONE', #16670, #19810, #22629, .T. ) ;
#21612=CARTESIAN_POINT ( 'NONE',  ( 1.834118845439484335, 144.2964192726481940, 15.34511559672728964 ) ) ;
#21614=CARTESIAN_POINT ( 'NONE',  ( 26.11404676487259024, 97.48350837663691948, -57.58742681967348176 ) ) ;
#21616=CARTESIAN_POINT ( 'NONE',  ( 2.430230287190589422, 74.01081053031099088, 125.2872625092165180 ) ) ;
#21617=CARTESIAN_POINT ( 'NONE',  ( 109.1721716018069657, 0.001583175916620053981, -0.01699510305644695227 ) ) ;
#21622=CARTESIAN_POINT ( 'NONE',  ( 16.05277956358202474, 39.81690014528850696, -137.6634701901227231 ) ) ;
#21624=CIRCLE ( 'NONE', #10622, 151.1787379149930359 ) ;
#21626=EDGE_LOOP ( 'NONE', ( #20776, #25300 ) ) ;
#21628=CARTESIAN_POINT ( 'NONE',  ( 109.1587776205901577, 0.006729130500857901862, -0.002904816147418943541 ) ) ;
#21629=( BOUNDED_SURFACE ( )  B_SPLINE_SURFACE ( 3, 1, ( 
 ( #10417, #1616 ),
 ( #24054, #14707 ),
 ( #23518, #19182 ),
 ( #26326, #27953 ) ),
 .UNSPECIFIED., .F., .F., .F. ) 
 B_SPLINE_SURFACE_WITH_KNOTS ( ( 4, 4 ),
 ( 2, 2 ),
 ( 0.000000000000000000, 1.000000000000000000 ),
 ( 0.000000000000000000, 1.000000000000000000 ),
 .UNSPECIFIED. ) 
 GEOMETRIC_REPRESENTATION_ITEM ( )  RATIONAL_B_SPLINE_SURFACE ( (
 ( 1.000000000000000000, 1.000000000000000000),
 ( 0.9956975270656955868, 0.8568959468854907557),
 ( 0.9956975270656955868, 0.8568959468854907557),
 ( 1.000000000000000000, 1.000000000000000000) ) ) 
 REPRESENTATION_ITEM ( '' )  SURFACE ( )  );
#21630=CARTESIAN_POINT ( 'NONE',  ( 25.70243777736191149, -83.44449745408483921, -76.12033502296601739 ) ) ;
#21638=AXIS2_PLACEMENT_3D ( 'NONE', #19150, #5784, #16982 ) ;
#21639=CARTESIAN_POINT ( 'NONE',  ( 2.433796855181205476, 109.1007109081238724, -96.28145139437575040 ) ) ;
#21640=EDGE_CURVE ( 'NONE', #26700, #24455, #11232, .T. ) ;
#21643=VECTOR ( 'NONE', #15624, 1000.000000000000000 ) ;
#21644=VERTEX_POINT ( 'NONE', #9909 ) ;
#21645=EDGE_LOOP ( 'NONE', ( #11999, #15374, #15396, #11005 ) ) ;
#21646=CARTESIAN_POINT ( 'NONE',  ( 24.22246935314087324, -90.00000000000005684, 39.99999999999997158 ) ) ;
#21647=CARTESIAN_POINT ( 'NONE',  ( 16.75465622695638146, 39.51671382433948310, 136.6258322711653364 ) ) ;
#21648=CARTESIAN_POINT ( 'NONE',  ( 25.64681081121879203, -103.3177883989776547, -45.54494737132326776 ) ) ;
#21649=DIRECTION ( 'NONE',  ( -1.000000000000000000, -0.000000000000000000, -0.000000000000000000 ) ) ;
#21650=CARTESIAN_POINT ( 'NONE',  ( 0.000000000000000000, 0.000000000000000000, 0.000000000000000000 ) ) ;
#21651=ORIENTED_EDGE ( 'NONE', *, *, #10859, .F. ) ;
#21652=DIRECTION ( 'NONE',  ( 0.000000000000000000, 0.000000000000000000, 1.000000000000000000 ) ) ;
#21655=ORIENTED_EDGE ( 'NONE', *, *, #22168, .T. ) ;
#21656=ORIENTED_EDGE ( 'NONE', *, *, #12967, .T. ) ;
#21660=AXIS2_PLACEMENT_3D ( 'NONE', #6772, #15517, #4317 ) ;
#21662=CARTESIAN_POINT ( 'NONE',  ( 16.05277956358201052, 113.1291064380275344, -87.96830019103548182 ) ) ;
#21663=AXIS2_PLACEMENT_3D ( 'NONE', #27499, #21019, #18142 ) ;
#21664=ADVANCED_FACE ( 'NONE', ( #21104 ), #17684, .F. ) ;
#21665=VERTEX_POINT ( 'NONE', #10200 ) ;
#21673=CARTESIAN_POINT ( 'NONE',  ( 109.1778270068192853, 0.005755170886745419705, 0.007323887274081471339 ) ) ;
#21674=CARTESIAN_POINT ( 'NONE',  ( 32.73300124599740002, -8.473903470905288060, -117.3295799645430151 ) ) ;
#21675=ORIENTED_EDGE ( 'NONE', *, *, #1767, .T. ) ;
#21676=B_SPLINE_CURVE_WITH_KNOTS ( 'NONE', 3,
 ( #13592, #2509, #20073, #355 ),
 .UNSPECIFIED., .F., .F.,
 ( 4, 4 ),
 ( 0.000000000000000000, 0.01077107196513851436 ),
 .UNSPECIFIED. ) ;
#21677=ADVANCED_FACE ( 'NONE', ( #16666 ), #9808, .F. ) ;
#21678=CARTESIAN_POINT ( 'NONE',  ( 1.833838848569430802, 125.7577269771232551, 72.40075357737693196 ) ) ;
#21679=CARTESIAN_POINT ( 'NONE',  ( 109.1589550718174877, 0.007132058561965951352, 0.002553077953671635102 ) ) ;
#21680=CARTESIAN_POINT ( 'NONE',  ( 26.04756280548352265, -10.72497307632870189, 112.6689254848258628 ) ) ;
#21683=ORIENTED_EDGE ( 'NONE', *, *, #426, .T. ) ;
#21684=CARTESIAN_POINT ( 'NONE',  ( 8.186469777910733825, 19.05650978729195444, 148.1306754055309511 ) ) ;
#21685=CARTESIAN_POINT ( 'NONE',  ( 1.833691583653525470, -72.86287859464681560, 125.4903330494897062 ) ) ;
#21686=CARTESIAN_POINT ( 'NONE',  ( 1.831572820252009626, 144.2101521542832643, -16.14965423926062016 ) ) ;
#21688=CARTESIAN_POINT ( 'NONE',  ( 25.98552792386800192, -90.89136171349133519, 67.36997957637636603 ) ) ;
#21691=VERTEX_POINT ( 'NONE', #20834 ) ;
#21692=CARTESIAN_POINT ( 'NONE',  ( 1.833691583653491941, -45.17974255430909380, 137.8971124741067058 ) ) ;
#21693=CARTESIAN_POINT ( 'NONE',  ( 109.1587776205901861, 0.0006832286435016865327, -0.007297420966932449682 ) ) ;
#21696=VERTEX_POINT ( 'NONE', #12471 ) ;
#21697=CARTESIAN_POINT ( 'NONE',  ( 1.834118845439484335, -138.0627591860432801, 44.67218053242348930 ) ) ;
#21698=CARTESIAN_POINT ( 'NONE',  ( 109.1778270068192853, -0.005755170886745368530, -0.007323887274081511238 ) ) ;
#21700=ORIENTED_EDGE ( 'NONE', *, *, #12923, .T. ) ;
#21705=CARTESIAN_POINT ( 'NONE',  ( 1.831572820252009626, -97.82994539998308881, -107.1759352627516222 ) ) ;
#21706=ADVANCED_FACE ( 'NONE', ( #27446 ), #21735, .F. ) ;
#21708=CIRCLE ( 'NONE', #21255, 80.00000000000000000 ) ;
#21711=VECTOR ( 'NONE', #8129, 1000.000000000000227 ) ;
#21712=EDGE_CURVE ( 'NONE', #9601, #19089, #16393, .T. ) ;
#21713=DIRECTION ( 'NONE',  ( -1.000000000000000000, -0.000000000000000000, -0.000000000000000000 ) ) ;
#21717=CARTESIAN_POINT ( 'NONE',  ( 94.22246935314088034, 70.00000000000001421, -12.50000000000000888 ) ) ;
#21718=EDGE_CURVE ( 'NONE', #26175, #18662, #5759, .T. ) ;
#21719=CARTESIAN_POINT ( 'NONE',  ( 30.58324630866351157, 83.81536267638941240, 87.19147450740381089 ) ) ;
#21720=CARTESIAN_POINT ( 'NONE',  ( 5.340103556456538669, -71.72120378849517408, -128.8311297043953232 ) ) ;
#21721=CARTESIAN_POINT ( 'NONE',  ( 32.73300124599732897, 117.3295799645430151, 8.473903470906510194 ) ) ;
#21723=ORIENTED_EDGE ( 'NONE', *, *, #14733, .F. ) ;
#21726=CARTESIAN_POINT ( 'NONE',  ( 32.73300124599735739, -105.8473486001054482, 51.32617430724869223 ) ) ;
#21727=CARTESIAN_POINT ( 'NONE',  ( 10.93730112725971004, 10.89264110825002163, 150.7858122213661147 ) ) ;
#21728=CARTESIAN_POINT ( 'NONE',  ( 1.833485406944043827, -141.8265699653865113, -30.69200235379080510 ) ) ;
#21729=CARTESIAN_POINT ( 'NONE',  ( 25.64681081121879203, -91.59071981940525120, -66.03065707439029097 ) ) ;
#21730=DIRECTION ( 'NONE',  ( -1.000000000000000000, 0.000000000000000000, 0.000000000000000000 ) ) ;
#21731=CARTESIAN_POINT ( 'NONE',  ( 16.05277956358202829, -53.98852998724671437, 132.7473359121864291 ) ) ;
#21733=CARTESIAN_POINT ( 'NONE',  ( 10.93730112725932635, 0.000000000000000000, 0.000000000000000000 ) ) ;
#21734=CARTESIAN_POINT ( 'NONE',  ( 28.37603512858357035, -114.2774673387025217, -10.20681926544481044 ) ) ;
#21735=( BOUNDED_SURFACE ( )  B_SPLINE_SURFACE ( 3, 1, ( 
 ( #25303, #12748 ),
 ( #17214, #21532 ),
 ( #8874, #23585 ),
 ( #11029, #1949 ) ),
 .UNSPECIFIED., .F., .F., .F. ) 
 B_SPLINE_SURFACE_WITH_KNOTS ( ( 4, 4 ),
 ( 2, 2 ),
 ( 0.000000000000000000, 1.000000000000000000 ),
 ( 0.000000000000000000, 1.000000000000000000 ),
 .UNSPECIFIED. ) 
 GEOMETRIC_REPRESENTATION_ITEM ( )  RATIONAL_B_SPLINE_SURFACE ( (
 ( 1.000000000000000000, 1.000000000000000000),
 ( 0.9956975270656955868, 0.8568959468854907557),
 ( 0.9956975270656955868, 0.8568959468854907557),
 ( 1.000000000000000000, 1.000000000000000000) ) ) 
 REPRESENTATION_ITEM ( '' )  SURFACE ( )  );
#21736=FACE_OUTER_BOUND ( 'NONE', #13646, .T. ) ;
#21740=CARTESIAN_POINT ( 'NONE',  ( 6.224689322667630975, -76.23997225729357297, 126.9212313063842430 ) ) ;
#21741=CIRCLE ( 'NONE', #8872, 117.6351876552689504 ) ;
#21743=ORIENTED_EDGE ( 'NONE', *, *, #23530, .T. ) ;
#21744=CARTESIAN_POINT ( 'NONE',  ( 1.833206308920084293, 44.13245285122266637, 138.2356393957897751 ) ) ;
#21745=CARTESIAN_POINT ( 'NONE',  ( 25.64700659047697684, -11.57609179463883464, -112.3162501909140474 ) ) ;
#21746=ORIENTED_EDGE ( 'NONE', *, *, #12887, .F. ) ;
#21747=ORIENTED_EDGE ( 'NONE', *, *, #10988, .T. ) ;
#21754=B_SPLINE_CURVE_WITH_KNOTS ( 'NONE', 3,
 ( #27162, #7471, #5295, #7764, #3141, #9916, #1256, #14352, #11919, #10056 ),
 .UNSPECIFIED., .F., .F.,
 ( 4, 3, 3, 4 ),
 ( 1.962615573354718958E-17, 0.0002669559177086156237, 0.0005339118354150979712, 0.001067817517169166418 ),
 .UNSPECIFIED. ) ;
#21757=CARTESIAN_POINT ( 'NONE',  ( 21.16825799904901473, 87.29264348877980240, -103.5479404090027629 ) ) ;
#21758=ORIENTED_EDGE ( 'NONE', *, *, #13997, .T. ) ;
#21759=ORIENTED_EDGE ( 'NONE', *, *, #10839, .T. ) ;
#21761=CARTESIAN_POINT ( 'NONE',  ( 1.833809397773872307, -44.67209459544969974, -138.0624841332892174 ) ) ;
#21762=DIRECTION ( 'NONE',  ( -0.5914120900931443270, -0.6942916636548165377, 0.4101107478122046346 ) ) ;
#21768=DIRECTION ( 'NONE',  ( -1.000000000000000000, -0.000000000000000000, -0.000000000000000000 ) ) ;
#21769=ORIENTED_EDGE ( 'NONE', *, *, #23496, .T. ) ;
#21770=VECTOR ( 'NONE', #3469, 1000.000000000000000 ) ;
#21772=CARTESIAN_POINT ( 'NONE',  ( 109.1586900883932856, 0.006561743627143329545, -0.002810909342011622906 ) ) ;
#21773=CARTESIAN_POINT ( 'NONE',  ( 32.73300124599738581, 32.68291970228383292, -113.0038235389598782 ) ) ;
#21775=PRODUCT_DEFINITION_FORMATION_WITH_SPECIFIED_SOURCE ( 'ANY', '', #32, .NOT_KNOWN. ) ;
#21777=VERTEX_POINT ( 'NONE', #8448 ) ;
#21779=CARTESIAN_POINT ( 'NONE',  ( 1.832998868059890096, -84.86110816369526333, -117.7096351258396254 ) ) ;
#21780=EDGE_CURVE ( 'NONE', #14585, #771, #12092, .T. ) ;
#21781=CARTESIAN_POINT ( 'NONE',  ( 109.1589550718174877, 0.005477029346537774616, 0.005233222325298243251 ) ) ;
#21782=EDGE_CURVE ( 'NONE', #21644, #24473, #2612, .T. ) ;
#21783=CARTESIAN_POINT ( 'NONE',  ( 1.833485406944043827, -144.2578170162064168, 15.69895494453337648 ) ) ;
#21784=CARTESIAN_POINT ( 'NONE',  ( 109.1586900883932856, -0.003481399864218472865, 0.006231977675084978893 ) ) ;
#21787=CONICAL_SURFACE ( 'NONE', #12592, 117.6351876552689504, 0.9945805576725580410 ) ;
#21790=DIRECTION ( 'NONE',  ( 0.000000000000000000, 0.000000000000000000, 1.000000000000000000 ) ) ;
#21791=FACE_OUTER_BOUND ( 'NONE', #26581, .T. ) ;
#21792=CARTESIAN_POINT ( 'NONE',  ( 109.1778270068192853, -0.003210287141653740423, -0.008743876326162627541 ) ) ;
#21793=CARTESIAN_POINT ( 'NONE',  ( 25.64660436782563835, 112.9095526718339784, -0.5800540083555767445 ) ) ;
#21794=ORIENTED_EDGE ( 'NONE', *, *, #1624, .F. ) ;
#21795=ORIENTED_EDGE ( 'NONE', *, *, #6864, .F. ) ;
#21796=CARTESIAN_POINT ( 'NONE',  ( 28.37599760073042887, 114.2774414139536390, -10.20682761621814727 ) ) ;
#21797=CARTESIAN_POINT ( 'NONE',  ( 13.84597867724968623, 40.76072889493758566, 140.9259526407711292 ) ) ;
#21800=DIRECTION ( 'NONE',  ( -1.000000000000000000, -0.000000000000000000, -0.000000000000000000 ) ) ;
#21802=DIRECTION ( 'NONE',  ( -1.000000000000000000, -0.000000000000000000, -0.000000000000000000 ) ) ;
#21803=CARTESIAN_POINT ( 'NONE',  ( 32.73300124599739291, 81.52272205837319063, -84.80615050150287004 ) ) ;
#21805=ORIENTED_EDGE ( 'NONE', *, *, #15572, .F. ) ;
#21809=ORIENTED_EDGE ( 'NONE', *, *, #5325, .T. ) ;
#21810=CARTESIAN_POINT ( 'NONE',  ( 25.65782528836480836, 107.2118488517900943, 35.44279022896523657 ) ) ;
#21816=FACE_OUTER_BOUND ( 'NONE', #8861, .T. ) ;
#21818=CARTESIAN_POINT ( 'NONE',  ( 32.73300124599732186, 0.000000000000000000, 0.000000000000000000 ) ) ;
#21819=LINE ( 'NONE', #2077, #7890 ) ;
#21820=CARTESIAN_POINT ( 'NONE',  ( 10.93730112725932813, 151.0983828010088246, -4.928439153520510985 ) ) ;
#21821=CARTESIAN_POINT ( 'NONE',  ( 25.70243777736188306, -112.2504268534933374, -12.53519966262598473 ) ) ;
#21822=DIRECTION ( 'NONE',  ( 0.000000000000000000, 0.000000000000000000, 1.000000000000000000 ) ) ;
#21823=CARTESIAN_POINT ( 'NONE',  ( 2.063896406836605024, -13.84738934186092862, -144.6078654718903067 ) ) ;
#21824=CARTESIAN_POINT ( 'NONE',  ( 25.64660436782541808, -11.22538561721967376, 112.3516544824821182 ) ) ;
#21825=CARTESIAN_POINT ( 'NONE',  ( 25.64704443564078318, -56.57116289738674908, 97.71717520928662282 ) ) ;
#21829=CARTESIAN_POINT ( 'NONE',  ( 1.894214914920958392, -31.11059045489028563, -141.7768822502890202 ) ) ;
#21830=CARTESIAN_POINT ( 'NONE',  ( 1.833485406944057594, 44.33323125130110043, -138.1714136985304151 ) ) ;
#21831=CARTESIAN_POINT ( 'NONE',  ( 109.1624594426973260, 0.01102230012606003617, -0.01154818537150963803 ) ) ;
#21833=ORIENTED_EDGE ( 'NONE', *, *, #27521, .T. ) ;
#21834=CARTESIAN_POINT ( 'NONE',  ( 25.64708228042119131, -34.85404436489419311, -107.3971738194635321 ) ) ;
#21836=ADVANCED_FACE ( 'NONE', ( #10888 ), #24695, .F. ) ;
#21839=CARTESIAN_POINT ( 'NONE',  ( 1.833750490713712322, 117.2391074582372568, 85.50916867388838227 ) ) ;
#21840=ORIENTED_EDGE ( 'NONE', *, *, #2831, .T. ) ;
#21841=CARTESIAN_POINT ( 'NONE',  ( 109.1587776205901861, -0.003736572840496174032, -0.006305329297950490811 ) ) ;
#21842=ADVANCED_FACE ( 'NONE', ( #2811 ), #2395, .T. ) ;
#21843=EDGE_CURVE ( 'NONE', #1309, #20568, #15646, .T. ) ;
#21844=FACE_OUTER_BOUND ( 'NONE', #19026, .T. ) ;
#21845=CARTESIAN_POINT ( 'NONE',  ( 1.833485406944057594, -59.50871042846138437, -132.3460930279897241 ) ) ;
#21847=CARTESIAN_POINT ( 'NONE',  ( 109.1592201516379674, -0.007302213399787572945, -0.002913740842103159506 ) ) ;
#21848=B_SPLINE_CURVE_WITH_KNOTS ( 'NONE', 3,
 ( #21648, #17455, #8149, #19488, #14887, #16916, #23550, #17318, #3813, #6134 ),
 .UNSPECIFIED., .F., .F.,
 ( 4, 3, 3, 4 ),
 ( 1.387778780781445676E-17, 0.0002669560319015670509, 0.0005492286108966479589, 0.0008315040496093511861 ),
 .UNSPECIFIED. ) ;
#21850=DIRECTION ( 'NONE',  ( 0.000000000000000000, 0.000000000000000000, 1.000000000000000000 ) ) ;
#21853=CARTESIAN_POINT ( 'NONE',  ( 5.340103579038220971, -143.7310399932979408, 32.90561047415553020 ) ) ;
#21856=CARTESIAN_POINT ( 'NONE',  ( 1.833838848569429247, -138.0625820091621563, -44.67212175381978057 ) ) ;
#21859=CARTESIAN_POINT ( 'NONE',  ( 2.430230287190592531, -98.44218333480698391, -107.1617224697474313 ) ) ;
#21860=CARTESIAN_POINT ( 'NONE',  ( 21.16825799904930605, 93.85612807858977646, 97.63815233965053153 ) ) ;
#21862=CARTESIAN_POINT ( 'NONE',  ( 28.37603512858359522, 114.2774673387025359, 10.20681926544401996 ) ) ;
#21863=ORIENTED_EDGE ( 'NONE', *, *, #3223, .T. ) ;
#21864=VERTEX_POINT ( 'NONE', #13884 ) ;
#21865=CARTESIAN_POINT ( 'NONE',  ( 25.64681081121879203, 102.9795863647028682, 46.30456157731362765 ) ) ;
#21869=CARTESIAN_POINT ( 'NONE',  ( 9.884929003653626367, -144.4113244745768725, -42.50195158091179337 ) ) ;
#21870=CARTESIAN_POINT ( 'NONE',  ( 1.833485406944043827, 73.01664920993141550, -125.4007332306537563 ) ) ;
#21875=CARTESIAN_POINT ( 'NONE',  ( 9.884929003653608603, 57.36421526887158961, 139.1775604444705721 ) ) ;
#21876=CARTESIAN_POINT ( 'NONE',  ( 6.224689322667630975, -43.30635742325279125, -141.5842213414017863 ) ) ;
#21879=EDGE_CURVE ( 'NONE', #13376, #6084, #3994, .T. ) ;
#21881=CARTESIAN_POINT ( 'NONE',  ( 1.833750490713699888, -108.0159692407137015, 96.89879583303815025 ) ) ;
#21883=FACE_OUTER_BOUND ( 'NONE', #13552, .T. ) ;
#21884=EDGE_LOOP ( 'NONE', ( #21205, #5738, #14256, #21284 ) ) ;
#21886=EDGE_CURVE ( 'NONE', #22931, #24940, #27703, .T. ) ;
#21887=ORIENTED_EDGE ( 'NONE', *, *, #24357, .F. ) ;
#21888=ORIENTED_EDGE ( 'NONE', *, *, #17788, .F. ) ;
#21891=ORIENTED_EDGE ( 'NONE', *, *, #26089, .T. ) ;
#21892=CARTESIAN_POINT ( 'NONE',  ( 55.49584447822657296, -66.16986612640796750, 29.75369869230931386 ) ) ;
#21893=CARTESIAN_POINT ( 'NONE',  ( 8.186469829614267724, -113.2805153378644576, 97.33125097511842228 ) ) ;
#21896=ORIENTED_EDGE ( 'NONE', *, *, #20701, .F. ) ;
#21898=CARTESIAN_POINT ( 'NONE',  ( 1.833603222531973387, -44.41798579679444003, -138.1443021179085804 ) ) ;
#21901=CARTESIAN_POINT ( 'NONE',  ( 1.833721034905633429, 96.83259691102649924, -108.0754384393924852 ) ) ;
#21902=CARTESIAN_POINT ( 'NONE',  ( 5.340103556456499589, -57.86178752079229071, -135.6222865117687775 ) ) ;
#21904=EDGE_CURVE ( 'NONE', #2974, #3159, #16017, .T. ) ;
#21907=LINE ( 'NONE', #6241, #19447 ) ;
#21908=VERTEX_POINT ( 'NONE', #9146 ) ;
#21909=ORIENTED_EDGE ( 'NONE', *, *, #3196, .T. ) ;
#21910=CARTESIAN_POINT ( 'NONE',  ( 2.433796855181233454, -109.1007109081219539, -96.28145139437795308 ) ) ;
#21912=CARTESIAN_POINT ( 'NONE',  ( 26.28373643307406837, 35.44121223575024970, -122.5382646256986305 ) ) ;
#21914=B_SPLINE_CURVE_WITH_KNOTS ( 'NONE', 3,
 ( #7925, #14078, #12217, #14209 ),
 .UNSPECIFIED., .F., .F.,
 ( 4, 4 ),
 ( 6.938893903907228378E-18, 0.008383560773332719013 ),
 .UNSPECIFIED. ) ;
#21915=ORIENTED_EDGE ( 'NONE', *, *, #9464, .F. ) ;
#21917=CARTESIAN_POINT ( 'NONE',  ( 32.73300124599735028, 84.80615050150375112, 81.52272205837232377 ) ) ;
#21918=CARTESIAN_POINT ( 'NONE',  ( 25.98107933586725338, 10.73978443746734079, 112.6229961579375782 ) ) ;
#21921=DIRECTION ( 'NONE',  ( -1.000000000000000000, -0.000000000000000000, -0.000000000000000000 ) ) ;
#21922=CARTESIAN_POINT ( 'NONE',  ( 32.73300124599735739, -20.69176323058707823, 115.8010721414082980 ) ) ;
#21924=B_SPLINE_CURVE_WITH_KNOTS ( 'NONE', 3,
 ( #127, #17810, #407, #2710, #9188, #17951, #15811, #26595 ),
 .UNSPECIFIED., .F., .F.,
 ( 4, 2, 2, 4 ),
 ( 6.938893903907228378E-18, 0.0002429588503611219996, 0.0004859177007222370602, 0.0009718354014444671816 ),
 .UNSPECIFIED. ) ;
#21927=CARTESIAN_POINT ( 'NONE',  ( 55.49584447822657296, -7.317474139115140552, -72.18163437663947946 ) ) ;
#21931=CARTESIAN_POINT ( 'NONE',  ( 9.884929003653626367, -150.0922431698404012, -11.54837932063185413 ) ) ;
#21932=EDGE_CURVE ( 'NONE', #11599, #24182, #5251, .T. ) ;
#21939=CARTESIAN_POINT ( 'NONE',  ( 13.84597867724965248, 101.6650905919627803, -105.7628030201710487 ) ) ;
#21940=EDGE_CURVE ( 'NONE', #1343, #15699, #20793, .T. ) ;
#21943=VERTEX_POINT ( 'NONE', #5539 ) ;
#21944=ADVANCED_FACE ( 'NONE', ( #7577 ), #12715, .F. ) ;
#21945=PLANE ( 'NONE',  #9860 ) ;
#21947=CARTESIAN_POINT ( 'NONE',  ( 26.11404676487257603, 107.3263591096430218, 36.06104232266487486 ) ) ;
#21949=CARTESIAN_POINT ( 'NONE',  ( 26.11404676487257603, 1.130420376097130086, 113.2169081140374090 ) ) ;
#21951=EDGE_CURVE ( 'NONE', #5719, #3608, #14278, .T. ) ;
#21954=CARTESIAN_POINT ( 'NONE',  ( 25.64681081121880624, 103.3177883989785499, -45.54494737132120008 ) ) ;
#21955=CARTESIAN_POINT ( 'NONE',  ( 109.1592201516379674, 0.007845213074654433863, -0.0005146241775983094154 ) ) ;
#21956=CARTESIAN_POINT ( 'NONE',  ( 16.75465622695656265, -4.637075857202498597, 142.1502242093126256 ) ) ;
#21957=ADVANCED_FACE ( 'NONE', ( #12165 ), #15653, .F. ) ;
#21960=DIRECTION ( 'NONE',  ( 0.000000000000000000, 0.000000000000000000, 1.000000000000000000 ) ) ;
#21961=ORIENTED_EDGE ( 'NONE', *, *, #5176, .F. ) ;
#21962=CARTESIAN_POINT ( 'NONE',  ( 28.37603512858462196, -68.88140609180129559, -91.75440368549998027 ) ) ;
#21965=CARTESIAN_POINT ( 'NONE',  ( 25.64660436782531505, -75.98230157781813432, -83.52001792470981911 ) ) ;
#21966=CARTESIAN_POINT ( 'NONE',  ( 16.75465622695667278, 140.0080030360329602, -25.01894884133717056 ) ) ;
#21968=EDGE_CURVE ( 'NONE', #3668, #546, #28344, .T. ) ;
#21969=EDGE_LOOP ( 'NONE', ( #27388, #24251, #20405, #13521 ) ) ;
#21970=CARTESIAN_POINT ( 'NONE',  ( 1.833485406944057594, -44.33323125130021225, 138.1714136985306993 ) ) ;
#21972=CARTESIAN_POINT ( 'NONE',  ( 109.1586900883932856, -0.006231977675085013588, -0.003481399864218412150 ) ) ;
#21974=B_SPLINE_CURVE_WITH_KNOTS ( 'NONE', 3,
 ( #7557, #23249, #22818, #25252, #16609, #3083 ),
 .UNSPECIFIED., .F., .F.,
 ( 4, 2, 4 ),
 ( 1.041737195591640451E-17, 0.0006311571484586031870, 0.001262314296917195749 ),
 .UNSPECIFIED. ) ;
#21975=CARTESIAN_POINT ( 'NONE',  ( 25.64700659047696618, 75.72132282458984776, -83.75695331063654692 ) ) ;
#21976=VERTEX_POINT ( 'NONE', #10687 ) ;
#21978=CARTESIAN_POINT ( 'NONE',  ( 13.36082413113061307, -97.52406103376675617, -117.7941133658648596 ) ) ;
#21979=VERTEX_POINT ( 'NONE', #17286 ) ;
#21980=CARTESIAN_POINT ( 'NONE',  ( 25.64704443564076897, -112.9111375659905718, -0.1334765861215692628 ) ) ;
#21982=ORIENTED_EDGE ( 'NONE', *, *, #7535, .T. ) ;
#21983=CARTESIAN_POINT ( 'NONE',  ( 25.64704443564079028, 103.2037466592380781, -45.80316013050731527 ) ) ;
#21986=DIRECTION ( 'NONE',  ( 0.5946245182733607137, 0.5401723099040918186, -0.5955128528260758003 ) ) ;
#21987=CARTESIAN_POINT ( 'NONE',  ( 10.93730112725990367, -108.9902118373734652, -104.7670965581022671 ) ) ;
#21989=CARTESIAN_POINT ( 'NONE',  ( 109.1778270068192853, -0.009293669915253103403, 0.0006237116683805770051 ) ) ;
#21991=ADVANCED_FACE ( 'NONE', ( #24499 ), #27258, .F. ) ;
#21992=CARTESIAN_POINT ( 'NONE',  ( 26.11404676487257603, 67.46175819463486789, -90.92995828888132337 ) ) ;
#21993=LINE ( 'NONE', #24307, #27225 ) ;
#21994=DIRECTION ( 'NONE',  ( 0.5946245182733606027, -0.08110646981859072346, -0.7999021332774026716 ) ) ;
#21995=ORIENTED_EDGE ( 'NONE', *, *, #20987, .F. ) ;
#21996=EDGE_CURVE ( 'NONE', #27786, #709, #22183, .T. ) ;
#21997=ORIENTED_EDGE ( 'NONE', *, *, #9044, .F. ) ;
#22002=CARTESIAN_POINT ( 'NONE',  ( 1.833206310202333045, -97.64934828277021950, -107.3376456496891223 ) ) ;
#22003=CARTESIAN_POINT ( 'NONE',  ( 1.833838850855475489, 72.63194208529650098, -125.6242502389378899 ) ) ;
#22004=CARTESIAN_POINT ( 'NONE',  ( 2.433796855181205476, -43.58222566461547132, -138.8296532063092457 ) ) ;
#22006=DIRECTION ( 'NONE',  ( 0.000000000000000000, 0.000000000000000000, 1.000000000000000000 ) ) ;
#22007=CARTESIAN_POINT ( 'NONE',  ( 32.73300124599734318, 92.86301839380026024, 72.21147546950587071 ) ) ;
#22008=CARTESIAN_POINT ( 'NONE',  ( 9.884929003653608603, -42.50195158090934200, -144.4113244745776115 ) ) ;
#22009=CARTESIAN_POINT ( 'NONE',  ( 109.1592201516379674, -0.001331853079201447297, 0.007748443302134876837 ) ) ;
#22010=CARTESIAN_POINT ( 'NONE',  ( 16.75465622695655199, 136.6258322711655637, -39.51671382433799096 ) ) ;
#22011=CARTESIAN_POINT ( 'NONE',  ( 6.224689322667647851, 145.3353551538641000, 28.26953958630669916 ) ) ;
#22012=CARTESIAN_POINT ( 'NONE',  ( 1.833838848569445013, -107.7184832843401949, 97.22964245509723469 ) ) ;
#22014=ORIENTED_EDGE ( 'NONE', *, *, #513, .T. ) ;
#22015=CONICAL_SURFACE ( 'NONE', #22567, 117.6351876552689504, 0.9945805576725580410 ) ;
#22018=B_SPLINE_CURVE_WITH_KNOTS ( 'NONE', 3,
 ( #13788, #3012, #27891, #19387 ),
 .UNSPECIFIED., .F., .F.,
 ( 4, 4 ),
 ( 9.813077866773594792E-18, 0.008383560773332722482 ),
 .UNSPECIFIED. ) ;
#22020=CARTESIAN_POINT ( 'NONE',  ( 21.16825799904908223, -37.62905626541790127, 130.1008673867301866 ) ) ;
#22021=CARTESIAN_POINT ( 'NONE',  ( 109.1592201516379674, -0.007856029051018016685, -0.0003082430541935813001 ) ) ;
#22022=CARTESIAN_POINT ( 'NONE',  ( 109.1592201516379674, -0.007620268632971095163, 0.001934867487021801630 ) ) ;
#22023=EDGE_CURVE ( 'NONE', #18831, #14195, #26752, .T. ) ;
#22024=VERTEX_POINT ( 'NONE', #13243 ) ;
#22028=EDGE_CURVE ( 'NONE', #21575, #546, #19872, .T. ) ;
#22029=CARTESIAN_POINT ( 'NONE',  ( 55.79472521941428198, 8.328398066091761365, 72.27573336313956531 ) ) ;
#22031=CARTESIAN_POINT ( 'NONE',  ( 32.73300124599732186, 0.000000000000000000, 0.000000000000000000 ) ) ;
#22033=CARTESIAN_POINT ( 'NONE',  ( 1.832998868059858122, -45.34898734665954123, -137.8420662456174739 ) ) ;
#22034=EDGE_CURVE ( 'NONE', #18167, #9317, #4348, .T. ) ;
#22037=CARTESIAN_POINT ( 'NONE',  ( 30.59138290137918759, 113.0806461017758267, -26.79783179610908661 ) ) ;
#22038=CARTESIAN_POINT ( 'NONE',  ( 24.22246935314087324, 0.000000000000000000, 0.000000000000000000 ) ) ;
#22040=CARTESIAN_POINT ( 'NONE',  ( 2.263178607246671969, 141.9207363487298323, -31.59906277834084065 ) ) ;
#22041=EDGE_LOOP ( 'NONE', ( #3660, #25490, #23651, #4349 ) ) ;
#22042=ORIENTED_EDGE ( 'NONE', *, *, #19599, .T. ) ;
#22043=CARTESIAN_POINT ( 'NONE',  ( 26.11404676487259024, -55.62948129436313849, 98.61392875273344316 ) ) ;
#22044=B_SPLINE_CURVE_WITH_KNOTS ( 'NONE', 3,
 ( #24163, #10637, #23759, #8611, #4560, #6743, #23892, #28177 ),
 .UNSPECIFIED., .F., .F.,
 ( 4, 2, 2, 4 ),
 ( 6.938893903907228378E-18, 0.0002429592666046868975, 0.0004859185332093668560, 0.0009718370664186821040 ),
 .UNSPECIFIED. ) ;
#22046=ORIENTED_EDGE ( 'NONE', *, *, #1113, .T. ) ;
#22047=ORIENTED_EDGE ( 'NONE', *, *, #8425, .T. ) ;
#22048=ADVANCED_FACE ( 'NONE', ( #19726 ), #9626, .F. ) ;
#22051=CARTESIAN_POINT ( 'NONE',  ( 28.37603512858455801, -100.2461737936626633, -55.80522682147376656 ) ) ;
#22052=CARTESIAN_POINT ( 'NONE',  ( 25.65782528836480836, -107.2118488517898669, -35.44279022896596842 ) ) ;
#22054=VECTOR ( 'NONE', #4186, 1000.000000000000114 ) ;
#22058=DIRECTION ( 'NONE',  ( 0.5914120900931444380, 0.6045864222316746917, -0.5335794202785202334 ) ) ;
#22060=CARTESIAN_POINT ( 'NONE',  ( 109.1624594426973118, 0.01154818537151455250, -0.01102230012606814254 ) ) ;
#22062=CARTESIAN_POINT ( 'NONE',  ( 2.433796855181233454, -107.1581411821792216, 98.43889364293823974 ) ) ;
#22065=EDGE_LOOP ( 'NONE', ( #18986, #25465, #24888, #24258, #13924, #27680 ) ) ;
#22066=CARTESIAN_POINT ( 'NONE',  ( 109.1589550718175161, -0.002874971999837467197, 0.007008495014555471414 ) ) ;
#22069=CARTESIAN_POINT ( 'NONE',  ( 1.833485406944057594, -144.3694338680884073, -14.63699153649508311 ) ) ;
#22071=CARTESIAN_POINT ( 'NONE',  ( 6.224689322667630975, 33.28770499679534112, -144.2687111683192143 ) ) ;
#22072=CARTESIAN_POINT ( 'NONE',  ( 16.05277956358202829, -134.7758735858406851, 48.70400867629053465 ) ) ;
#22073=ORIENTED_EDGE ( 'NONE', *, *, #28034, .T. ) ;
#22076=CARTESIAN_POINT ( 'NONE',  ( 2.108985857320914370, -84.36123201973892094, 118.2933707022555865 ) ) ;
#22077=CARTESIAN_POINT ( 'NONE',  ( 21.16825799904897920, -93.85612807858952067, -97.63815233965159734 ) ) ;
#22078=ORIENTED_EDGE ( 'NONE', *, *, #2237, .T. ) ;
#22080=B_SPLINE_CURVE_WITH_KNOTS ( 'NONE', 3,
 ( #3284, #10055, #9771, #12205, #25168, #23438, #5741 ),
 .UNSPECIFIED., .F., .F.,
 ( 4, 3, 4 ),
 ( 0.000000000000000000, 0.02398743853561303638, 0.04000277880656216700 ),
 .UNSPECIFIED. ) ;
#22081=CARTESIAN_POINT ( 'NONE',  ( 1.834118845439484335, -0.1779704863080166510, 145.1099497418795750 ) ) ;
#22082=ORIENTED_EDGE ( 'NONE', *, *, #18893, .F. ) ;
#22083=FACE_OUTER_BOUND ( 'NONE', #17020, .T. ) ;
#22084=ORIENTED_EDGE ( 'NONE', *, *, #24067, .T. ) ;
#22088=CIRCLE ( 'NONE', #15166, 117.6351876552689504 ) ;
#22089=CARTESIAN_POINT ( 'NONE',  ( 109.1721716018069515, -0.01157047143378747006, 0.01254847260354031470 ) ) ;
#22090=EDGE_CURVE ( 'NONE', #9341, #1180, #8953, .T. ) ;
#22092=CARTESIAN_POINT ( 'NONE',  ( 28.37603512858450472, 78.09501335733588689, 84.05169593519752880 ) ) ;
#22094=CARTESIAN_POINT ( 'NONE',  ( 109.1624594426973118, -0.01318243916935001731, -0.009004164758064509000 ) ) ;
#22095=EDGE_CURVE ( 'NONE', #14412, #22982, #18423, .T. ) ;
#22096=DIRECTION ( 'NONE',  ( 1.000000000000000000, 0.000000000000000000, 0.000000000000000000 ) ) ;
#22097=CARTESIAN_POINT ( 'NONE',  ( 10.93730112725945602, 84.82621002473440797, 125.1380233598478640 ) ) ;
#22098=EDGE_CURVE ( 'NONE', #4882, #15045, #8496, .T. ) ;
#22099=B_SPLINE_CURVE_WITH_KNOTS ( 'NONE', 3,
 ( #12028, #7285, #7727, #13889, #7429, #16483, #25274, #18498, #23130, #11880 ),
 .UNSPECIFIED., .F., .F.,
 ( 4, 3, 3, 4 ),
 ( 3.925231146709437917E-17, 0.0002669559177086244599, 0.0005339118354150962364, 0.001067817517169172706 ),
 .UNSPECIFIED. ) ;
#22100=( BOUNDED_SURFACE ( )  B_SPLINE_SURFACE ( 3, 1, ( 
 ( #19283, #126 ),
 ( #19560, #13211 ),
 ( #28330, #17678 ),
 ( #26457, #4160 ) ),
 .UNSPECIFIED., .F., .F., .F. ) 
 B_SPLINE_SURFACE_WITH_KNOTS ( ( 4, 4 ),
 ( 2, 2 ),
 ( 0.000000000000000000, 1.000000000000000000 ),
 ( 0.000000000000000000, 1.000000000000000000 ),
 .UNSPECIFIED. ) 
 GEOMETRIC_REPRESENTATION_ITEM ( )  RATIONAL_B_SPLINE_SURFACE ( (
 ( 1.000000000000000000, 1.000000000000000000),
 ( 0.9956975270656954757, 0.8568959468854893125),
 ( 0.9956975270656954757, 0.8568959468854893125),
 ( 1.000000000000000000, 1.000000000000000000) ) ) 
 REPRESENTATION_ITEM ( '' )  SURFACE ( )  );
#22101=DIRECTION ( 'NONE',  ( 0.000000000000000000, 0.000000000000000000, 1.000000000000000000 ) ) ;
#22102=CARTESIAN_POINT ( 'NONE',  ( 9.884929003653626367, -27.17402761732445526, 148.0628878137279685 ) ) ;
#22103=DIRECTION ( 'NONE',  ( 0.000000000000000000, 0.000000000000000000, 1.000000000000000000 ) ) ;
#22105=CARTESIAN_POINT ( 'NONE',  ( 25.64660436782543940, 83.52001792470993280, -75.98230157781777905 ) ) ;
#22107=CARTESIAN_POINT ( 'NONE',  ( 10.93730112726006176, 146.7718404940648611, -36.23586118136403655 ) ) ;
#22108=B_SPLINE_CURVE_WITH_KNOTS ( 'NONE', 3,
 ( #6128, #5540, #20932, #3946 ),
 .UNSPECIFIED., .F., .F.,
 ( 4, 4 ),
 ( 0.000000000000000000, 0.01077107196513860457 ),
 .UNSPECIFIED. ) ;
#22110=CARTESIAN_POINT ( 'NONE',  ( 1.833485406944043827, 84.86072343962567288, 117.7091014914953320 ) ) ;
#22111=CARTESIAN_POINT ( 'NONE',  ( 55.49584447822657296, 22.67407039687241621, 68.91748907713598271 ) ) ;
#22112=VERTEX_POINT ( 'NONE', #15647 ) ;
#22115=B_SPLINE_CURVE_WITH_KNOTS ( 'NONE', 3,
 ( #25652, #28065, #10666, #5931 ),
 .UNSPECIFIED., .F., .F.,
 ( 4, 4 ),
 ( 3.469446951953614189E-18, 0.008383560773332696461 ),
 .UNSPECIFIED. ) ;
#22116=CARTESIAN_POINT ( 'NONE',  ( 26.11404676487259024, 113.2169081140373947, -1.130420376097525326 ) ) ;
#22117=DIRECTION ( 'NONE',  ( 0.000000000000000000, 0.000000000000000000, 1.000000000000000000 ) ) ;
#22118=CIRCLE ( 'NONE', #8789, 151.1787379149930359 ) ;
#22119=ORIENTED_EDGE ( 'NONE', *, *, #14695, .F. ) ;
#22122=DIRECTION ( 'NONE',  ( 0.000000000000000000, -1.000000000000000000, -3.122502256758243698E-15 ) ) ;
#22124=VERTEX_POINT ( 'NONE', #11787 ) ;
#22127=DIRECTION ( 'NONE',  ( -1.000000000000000000, -0.000000000000000000, -0.000000000000000000 ) ) ;
#22128=EDGE_CURVE ( 'NONE', #6453, #15531, #3798, .T. ) ;
#22129=ORIENTED_EDGE ( 'NONE', *, *, #1971, .T. ) ;
#22133=CARTESIAN_POINT ( 'NONE',  ( 109.1721716018069515, 0.008708654716135744156, -0.01467989464938425186 ) ) ;
#22134=CARTESIAN_POINT ( 'NONE',  ( 13.84597867724970577, -105.7628030201713045, -101.6650905919622829 ) ) ;
#22135=CARTESIAN_POINT ( 'NONE',  ( 25.64703792032470631, 110.4746717456749252, 23.32999623362163177 ) ) ;
#22136=VECTOR ( 'NONE', #12913, 1000.000000000000114 ) ;
#22137=ORIENTED_EDGE ( 'NONE', *, *, #1565, .F. ) ;
#22138=DIRECTION ( 'NONE',  ( 0.5946245182733607137, -0.7992853357633872280, -0.08697490616139179342 ) ) ;
#22139=CARTESIAN_POINT ( 'NONE',  ( 109.1721716018069515, 0.003746085893651815869, -0.01665253177025272785 ) ) ;
#22143=( BOUNDED_SURFACE ( )  B_SPLINE_SURFACE ( 3, 1, ( 
 ( #3563, #12758 ),
 ( #16950, #6030 ),
 ( #14786, #17085 ),
 ( #14922, #23741 ) ),
 .UNSPECIFIED., .F., .F., .F. ) 
 B_SPLINE_SURFACE_WITH_KNOTS ( ( 4, 4 ),
 ( 2, 2 ),
 ( 0.000000000000000000, 1.000000000000000000 ),
 ( 0.000000000000000000, 1.000000000000000000 ),
 .UNSPECIFIED. ) 
 GEOMETRIC_REPRESENTATION_ITEM ( )  RATIONAL_B_SPLINE_SURFACE ( (
 ( 1.000000000000000000, 1.000000000000000000),
 ( 0.9960225298536222738, 0.9999952330161893110),
 ( 0.9960225298536222738, 0.9999952330161893110),
 ( 1.000000000000000000, 1.000000000000000000) ) ) 
 REPRESENTATION_ITEM ( '' )  SURFACE ( )  );
#22145=ORIENTED_EDGE ( 'NONE', *, *, #11313, .T. ) ;
#22146=ORIENTED_EDGE ( 'NONE', *, *, #21027, .F. ) ;
#22147=CARTESIAN_POINT ( 'NONE',  ( 2.108393763691155609, -43.67806918959044538, -138.5721856399489695 ) ) ;
#22149=DIRECTION ( 'NONE',  ( -0.5946245182733608248, 0.3297108033645218539, 0.7332888028688936410 ) ) ;
#22150=FACE_OUTER_BOUND ( 'NONE', #21170, .T. ) ;
#22151=CARTESIAN_POINT ( 'NONE',  ( 25.64703792032471341, -91.43447020678384263, -66.24710921678151010 ) ) ;
#22152=ORIENTED_EDGE ( 'NONE', *, *, #6808, .F. ) ;
#22153=CARTESIAN_POINT ( 'NONE',  ( 25.98107933586708995, -33.92073193606511694, -107.9289867379275307 ) ) ;
#22154=FACE_OUTER_BOUND ( 'NONE', #3729, .T. ) ;
#22155=LINE ( 'NONE', #7331, #16597 ) ;
#22157=CARTESIAN_POINT ( 'NONE',  ( 2.433796855181233454, 142.6247129145648387, 28.83182736670586266 ) ) ;
#22159=CARTESIAN_POINT ( 'NONE',  ( 26.11404676487257603, 83.38016054979783576, 76.59696442953219275 ) ) ;
#22160=B_SPLINE_CURVE_WITH_KNOTS ( 'NONE', 3,
 ( #7325, #16088, #8183, #5440 ),
 .UNSPECIFIED., .F., .F.,
 ( 4, 4 ),
 ( 2.226941760980096400E-16, 0.008383748772659700005 ),
 .UNSPECIFIED. ) ;
#22161=CARTESIAN_POINT ( 'NONE',  ( 1.833838848569417923, -117.5008734796305845, -85.14939661881690824 ) ) ;
#22165=ORIENTED_EDGE ( 'NONE', *, *, #15965, .T. ) ;
#22168=EDGE_CURVE ( 'NONE', #26221, #14104, #15947, .T. ) ;
#22169=CARTESIAN_POINT ( 'NONE',  ( 55.79472521941428198, -8.328398066091271090, -72.27573336313960795 ) ) ;
#22173=VERTEX_POINT ( 'NONE', #17950 ) ;
#22178=ORIENTED_EDGE ( 'NONE', *, *, #16544, .F. ) ;
#22180=CARTESIAN_POINT ( 'NONE',  ( 10.93730112725971715, 4.928439153520177030, 151.0983828010091372 ) ) ;
#22181=CARTESIAN_POINT ( 'NONE',  ( 1.833485406944057594, -29.64752363041639782, 142.0485807715645024 ) ) ;
#22183=LINE ( 'NONE', #24212, #22188 ) ;
#22185=VECTOR ( 'NONE', #2925, 1000.000000000000000 ) ;
#22187=DIRECTION ( 'NONE',  ( 0.000000000000000000, 0.000000000000000000, 1.000000000000000000 ) ) ;
#22188=VECTOR ( 'NONE', #2158, 1000.000000000000114 ) ;
#22189=DIRECTION ( 'NONE',  ( 1.000000000000000000, -0.000000000000000000, -0.000000000000000000 ) ) ;
#22190=CARTESIAN_POINT ( 'NONE',  ( 1.894214914920973269, -43.94587946447497728, 138.3376769255506815 ) ) ;
#22191=( BOUNDED_SURFACE ( )  B_SPLINE_SURFACE ( 3, 1, ( 
 ( #21037, #23235 ),
 ( #16884, #14853 ),
 ( #3624, #25384 ),
 ( #21333, #7983 ) ),
 .UNSPECIFIED., .F., .F., .F. ) 
 B_SPLINE_SURFACE_WITH_KNOTS ( ( 4, 4 ),
 ( 2, 2 ),
 ( 0.000000000000000000, 1.000000000000000000 ),
 ( 0.000000000000000000, 1.000000000000000000 ),
 .UNSPECIFIED. ) 
 GEOMETRIC_REPRESENTATION_ITEM ( )  RATIONAL_B_SPLINE_SURFACE ( (
 ( 1.000000000000000000, 1.000000000000000000),
 ( 0.6386103224230302855, 0.9954351624131538845),
 ( 0.6386103224230302855, 0.9954351624131538845),
 ( 1.000000000000000000, 1.000000000000000000) ) ) 
 REPRESENTATION_ITEM ( '' )  SURFACE ( )  );
#22193=ADVANCED_FACE ( 'NONE', ( #24755 ), #11459, .F. ) ;
#22194=ORIENTED_EDGE ( 'NONE', *, *, #21027, .T. ) ;
#22196=CARTESIAN_POINT ( 'NONE',  ( 26.11404676487259024, -92.25884714080363835, -65.63269960453335727 ) ) ;
#22197=ORIENTED_EDGE ( 'NONE', *, *, #3578, .F. ) ;
#22199=VERTEX_POINT ( 'NONE', #7768 ) ;
#22202=CARTESIAN_POINT ( 'NONE',  ( 26.11404676487259024, 83.38016054979885894, -76.59696442953111273 ) ) ;
#22204=EDGE_CURVE ( 'NONE', #437, #21420, #9795, .T. ) ;
#22205=CIRCLE ( 'NONE', #8893, 151.1787379149930359 ) ;
#22206=B_SPLINE_CURVE_WITH_KNOTS ( 'NONE', 3,
 ( #22405, #2667, #20803, #16787 ),
 .UNSPECIFIED., .F., .F.,
 ( 4, 4 ),
 ( 2.400696848537691317E-16, 0.008383748772659717352 ),
 .UNSPECIFIED. ) ;
#22208=EDGE_LOOP ( 'NONE', ( #20225, #19440, #7166, #13177 ) ) ;
#22209=CARTESIAN_POINT ( 'NONE',  ( 2.433796855181219243, -13.76554153471791864, 144.8571464219888583 ) ) ;
#22211=CARTESIAN_POINT ( 'NONE',  ( 32.73300124599735739, 28.19767303745605602, 114.2056417606549132 ) ) ;
#22213=B_SPLINE_CURVE_WITH_KNOTS ( 'NONE', 3,
 ( #14541, #7805, #23346, #12659 ),
 .UNSPECIFIED., .F., .F.,
 ( 4, 4 ),
 ( 0.000000000000000000, 0.008383560773332698196 ),
 .UNSPECIFIED. ) ;
#22214=B_SPLINE_CURVE_WITH_KNOTS ( 'NONE', 3,
 ( #25525, #3339, #27810, #23653, #25794, #18599, #12537, #3476 ),
 .UNSPECIFIED., .F., .F.,
 ( 4, 2, 2, 4 ),
 ( 0.000000000000000000, 0.0002429588503611251709, 0.0004859177007222503417, 0.0009718354014444904919 ),
 .UNSPECIFIED. ) ;
#22216=CARTESIAN_POINT ( 'NONE',  ( 25.70243777736189728, 24.19989514742873737, -110.3252221127464026 ) ) ;
#22218=CARTESIAN_POINT ( 'NONE',  ( 2.433796855181205476, -133.5135467655521779, 57.85512797797844087 ) ) ;
#22219=CARTESIAN_POINT ( 'NONE',  ( 109.1721716018069657, 0.006757465437538790615, -0.01567407524362082055 ) ) ;
#22221=ORIENTED_EDGE ( 'NONE', *, *, #1905, .F. ) ;
#22222=CARTESIAN_POINT ( 'NONE',  ( 25.64699802086724389, 91.48665801621663718, 66.17503410043930501 ) ) ;
#22223=CARTESIAN_POINT ( 'NONE',  ( 109.1721716018069515, -0.003746085893651930360, 0.01665253177025270356 ) ) ;
#22225=CARTESIAN_POINT ( 'NONE',  ( 25.64692232868534560, 46.22343382108737586, 103.0161468101948827 ) ) ;
#22226=CARTESIAN_POINT ( 'NONE',  ( 2.433796855181205476, 57.85512797797890272, 133.5135467655520074 ) ) ;
#22227=CARTESIAN_POINT ( 'NONE',  ( 2.433796855181205476, 144.8571464219891141, -13.76554153471544417 ) ) ;
#22228=ORIENTED_EDGE ( 'NONE', *, *, #27147, .F. ) ;
#22229=CARTESIAN_POINT ( 'NONE',  ( 25.64703792032469920, 97.70949518026583291, -56.58441811305505098 ) ) ;
#22230=VECTOR ( 'NONE', #19562, 1000.000000000000114 ) ;
#22231=EDGE_CURVE ( 'NONE', #17054, #20235, #22885, .T. ) ;
#22232=ORIENTED_EDGE ( 'NONE', *, *, #20571, .T. ) ;
#22233=CARTESIAN_POINT ( 'NONE',  ( 1.832998868059858122, 84.86110816369603072, 117.7096351258390854 ) ) ;
#22235=CARTESIAN_POINT ( 'NONE',  ( 1.833485406944043827, 0.5339064996905048543, -145.1085452359073145 ) ) ;
#22236=VERTEX_POINT ( 'NONE', #14202 ) ;
#22237=VERTEX_POINT ( 'NONE', #10059 ) ;
#22240=VERTEX_POINT ( 'NONE', #25605 ) ;
#22241=CARTESIAN_POINT ( 'NONE',  ( 1.831572820252008738, -96.36280042115856759, -108.4969585352564678 ) ) ;
#22243=EDGE_CURVE ( 'NONE', #26223, #27903, #20846, .T. ) ;
#22245=EDGE_CURVE ( 'NONE', #13623, #3154, #23442, .T. ) ;
#22246=CIRCLE ( 'NONE', #9842, 151.1787379149930359 ) ;
#22249=FACE_OUTER_BOUND ( 'NONE', #22697, .T. ) ;
#22250=CARTESIAN_POINT ( 'NONE',  ( 1.834118845439484335, 137.9527673765111899, -45.01070051384449044 ) ) ;
#22252=CARTESIAN_POINT ( 'NONE',  ( 109.1586059443104944, -0.004935564877224718136, -0.005067816690886739472 ) ) ;
#22254=CARTESIAN_POINT ( 'NONE',  ( 26.11404676487257603, -110.5078194225159223, -24.64483677384961879 ) ) ;
#22255=CARTESIAN_POINT ( 'NONE',  ( 32.73300124599740002, -81.52272205837138586, -84.80615050150450429 ) ) ;
#22257=ORIENTED_EDGE ( 'NONE', *, *, #23686, .F. ) ;
#22261=CARTESIAN_POINT ( 'NONE',  ( 16.05277956358201052, -137.6634701901228652, -39.81690014528805222 ) ) ;
#22262=CARTESIAN_POINT ( 'NONE',  ( 109.1586900883932856, 0.003481399864218433400, -0.006231977675085001445 ) ) ;
#22264=CARTESIAN_POINT ( 'NONE',  ( 25.64692872815575342, -34.58541472378575321, -107.4838747185724515 ) ) ;
#22265=CARTESIAN_POINT ( 'NONE',  ( 32.73300124599732186, 0.000000000000000000, 0.000000000000000000 ) ) ;
#22266=CARTESIAN_POINT ( 'NONE',  ( 25.64692872815578184, 110.5102270591925588, -23.16082795281147355 ) ) ;
#22269=CARTESIAN_POINT ( 'NONE',  ( 109.1586900883932856, 0.006231977675082105324, -0.003481399864227396716 ) ) ;
#22272=CARTESIAN_POINT ( 'NONE',  ( 2.430230287190592531, -71.49654683843598946, 126.7388733285342823 ) ) ;
#22273=CARTESIAN_POINT ( 'NONE',  ( 1.833485406944043827, -96.69979900902241354, 108.1939177044922786 ) ) ;
#22276=CARTESIAN_POINT ( 'NONE',  ( 25.98552792386798771, 112.3992180166320480, -12.89843290883410987 ) ) ;
#22277=ORIENTED_EDGE ( 'NONE', *, *, #23489, .F. ) ;
#22278=CARTESIAN_POINT ( 'NONE',  ( 109.1721716018069657, 0.008358834333183932583, -0.01488186354166049288 ) ) ;
#22279=ORIENTED_EDGE ( 'NONE', *, *, #10768, .T. ) ;
#22280=SHAPE_REPRESENTATION_RELATIONSHIP ( 'NONE' , 'NONE' ,  #7571, #26090 ) ;
#22281=( BOUNDED_SURFACE ( )  B_SPLINE_SURFACE ( 3, 1, ( 
 ( #28193, #6760 ),
 ( #15504, #24319 ),
 ( #4580, #8495 ),
 ( #11786, #2559 ) ),
 .UNSPECIFIED., .F., .F., .F. ) 
 B_SPLINE_SURFACE_WITH_KNOTS ( ( 4, 4 ),
 ( 2, 2 ),
 ( 0.000000000000000000, 1.000000000000000000 ),
 ( 0.000000000000000000, 1.000000000000000000 ),
 .UNSPECIFIED. ) 
 GEOMETRIC_REPRESENTATION_ITEM ( )  RATIONAL_B_SPLINE_SURFACE ( (
 ( 1.000000000000000000, 1.000000000000000000),
 ( 0.9956975270656954757, 0.8568959468854893125),
 ( 0.9956975270656954757, 0.8568959468854893125),
 ( 1.000000000000000000, 1.000000000000000000) ) ) 
 REPRESENTATION_ITEM ( '' )  SURFACE ( )  );
#22283=CARTESIAN_POINT ( 'NONE',  ( 55.49584447822657296, 70.91003759562335063, -15.34602024131217846 ) ) ;
#22285=B_SPLINE_CURVE_WITH_KNOTS ( 'NONE', 3,
 ( #17822, #17965, #17545, #19851, #28474, #15822, #26747 ),
 .UNSPECIFIED., .F., .F.,
 ( 4, 3, 4 ),
 ( 5.958491062770612542E-16, 0.02816610861753249956, 0.04000277880656279150 ),
 .UNSPECIFIED. ) ;
#22286=CARTESIAN_POINT ( 'NONE',  ( 1.834118845439484335, -59.18411796427140814, 132.4921483272726164 ) ) ;
#22287=ORIENTED_EDGE ( 'NONE', *, *, #8815, .T. ) ;
#22288=CARTESIAN_POINT ( 'NONE',  ( 5.340103556456464950, -133.7487107983440637, -62.06990747183822066 ) ) ;
#22289=CARTESIAN_POINT ( 'NONE',  ( 26.11404676487257603, 33.91085499298520034, -108.0249973236464314 ) ) ;
#22290=CARTESIAN_POINT ( 'NONE',  ( 25.87036335909428075, -98.40409479825397909, -55.67065048714113118 ) ) ;
#22292=ORIENTED_EDGE ( 'NONE', *, *, #7824, .T. ) ;
#22295=LINE ( 'NONE', #7048, #3647 ) ;
#22296=B_SPLINE_CURVE_WITH_KNOTS ( 'NONE', 3,
 ( #4871, #24047, #6900, #2265 ),
 .UNSPECIFIED., .F., .F.,
 ( 4, 4 ),
 ( 0.000000000000000000, 0.01077107196513949622 ),
 .UNSPECIFIED. ) ;
#22298=CARTESIAN_POINT ( 'NONE',  ( 55.49584447822657296, -42.42793568432917795, -58.85239198729230026 ) ) ;
#22300=CARTESIAN_POINT ( 'NONE',  ( 25.64704443564078318, -91.26857357624521683, -66.47548630737952635 ) ) ;
#22302=CARTESIAN_POINT ( 'NONE',  ( 2.433796855181205476, 132.3327394885231456, 60.50726454507948660 ) ) ;
#22303=CARTESIAN_POINT ( 'NONE',  ( 109.1592201516379674, -0.007780772729118872952, -0.001127733110579658832 ) ) ;
#22304=DIRECTION ( 'NONE',  ( 1.000000000000000000, -0.000000000000000000, -0.000000000000000000 ) ) ;
#22306=CARTESIAN_POINT ( 'NONE',  ( 109.1778270068192853, 0.009307953841270274684, -0.0003511581237512639711 ) ) ;
#22307=EDGE_CURVE ( 'NONE', #7524, #19216, #2236, .T. ) ;
#22308=ORIENTED_EDGE ( 'NONE', *, *, #6493, .T. ) ;
#22309=CARTESIAN_POINT ( 'NONE',  ( 109.1592201516379674, -0.005631912476305732905, -0.005485778713193728215 ) ) ;
#22310=ORIENTED_EDGE ( 'NONE', *, *, #15120, .F. ) ;
#22312=ADVANCED_FACE ( 'NONE', ( #4543 ), #15478, .F. ) ;
#22313=CARTESIAN_POINT ( 'NONE',  ( 25.64708010899966695, -56.50300922386526992, -97.75667227735142717 ) ) ;
#22315=EDGE_CURVE ( 'NONE', #26223, #25791, #4294, .T. ) ;
#22316=VERTEX_POINT ( 'NONE', #8883 ) ;
#22317=ORIENTED_EDGE ( 'NONE', *, *, #10544, .T. ) ;
#22320=CARTESIAN_POINT ( 'NONE',  ( 9.884929003653626367, 144.4113244745771851, 42.50195158091081993 ) ) ;
#22322=CARTESIAN_POINT ( 'NONE',  ( 10.93730112725990367, -84.82621002473354110, -125.1380233598488019 ) ) ;
#22324=CARTESIAN_POINT ( 'NONE',  ( 10.93730112726003156, 84.82621002473607064, -125.1380233598471960 ) ) ;
#22325=EDGE_CURVE ( 'NONE', #4812, #20099, #5687, .T. ) ;
#22326=FACE_OUTER_BOUND ( 'NONE', #6113, .T. ) ;
#22327=ORIENTED_EDGE ( 'NONE', *, *, #4246, .F. ) ;
#22328=CARTESIAN_POINT ( 'NONE',  ( 1.833485406944043827, 85.72460230293849293, -117.0814567582535659 ) ) ;
#22329=VERTEX_POINT ( 'NONE', #6436 ) ;
#22331=B_SPLINE_CURVE_WITH_KNOTS ( 'NONE', 3,
 ( #22869, #11472, #11334, #19970, #27001, #20245, #9333, #9175 ),
 .UNSPECIFIED., .F., .F.,
 ( 4, 2, 2, 4 ),
 ( 8.673617379884035472E-19, 0.0002429592666046771939, 0.0004859185332093535203, 0.0009718370664186919703 ),
 .UNSPECIFIED. ) ;
#22334=CARTESIAN_POINT ( 'NONE',  ( 19.66333377628711432, 24.23123354948839747, 135.6014041990442252 ) ) ;
#22336=EDGE_CURVE ( 'NONE', #13485, #14349, #21114, .T. ) ;
#22337=CARTESIAN_POINT ( 'NONE',  ( 10.93730112725992853, -56.95489579269655422, -140.0398180619117738 ) ) ;
#22338=DIRECTION ( 'NONE',  ( -1.000000000000000000, -0.000000000000000000, -0.000000000000000000 ) ) ;
#22339=EDGE_CURVE ( 'NONE', #7653, #21943, #4647, .T. ) ;
#22340=CARTESIAN_POINT ( 'NONE',  ( 26.11404676487259024, 97.48350837663691948, -57.58742681967348176 ) ) ;
#22342=CARTESIAN_POINT ( 'NONE',  ( 1.833485406944057594, 141.8265699653871366, -30.69200235378795227 ) ) ;
#22344=AXIS2_PLACEMENT_3D ( 'NONE', #8693, #21649, #2058 ) ;
#22345=ORIENTED_EDGE ( 'NONE', *, *, #5675, .F. ) ;
#22347=CARTESIAN_POINT ( 'NONE',  ( 25.87036335909424878, 24.47383578007130112, 110.3794299719620682 ) ) ;
#22348=CARTESIAN_POINT ( 'NONE',  ( 109.1586900883932856, 0.004851151255037359014, 0.005236795036860563031 ) ) ;
#22350=ORIENTED_EDGE ( 'NONE', *, *, #5260, .F. ) ;
#22351=ORIENTED_EDGE ( 'NONE', *, *, #20304, .F. ) ;
#22354=B_SPLINE_CURVE_WITH_KNOTS ( 'NONE', 3,
 ( #25723, #19638, #10594, #21525 ),
 .UNSPECIFIED., .F., .F.,
 ( 4, 4 ),
 ( 0.000000000000000000, 0.01077107196513848661 ),
 .UNSPECIFIED. ) ;
#22359=CARTESIAN_POINT ( 'NONE',  ( 26.11404676487259024, -103.8885755249566643, -45.01677474591514283 ) ) ;
#22362=CARTESIAN_POINT ( 'NONE',  ( 10.93730112725936721, 145.2260730187397542, 42.00474393596321931 ) ) ;
#22363=CARTESIAN_POINT ( 'NONE',  ( 109.1592201516379674, -0.004867031887019586216, -0.006174480289199391417 ) ) ;
#22368=FACE_BOUND ( 'NONE', #14181, .T. ) ;
#22370=ORIENTED_EDGE ( 'NONE', *, *, #20442, .F. ) ;
#22372=CARTESIAN_POINT ( 'NONE',  ( 25.64703792032471696, -66.48786612795814221, -91.25955007190280810 ) ) ;
#22373=CARTESIAN_POINT ( 'NONE',  ( 25.73574536432413495, -22.69874377039358038, -110.6664861019686583 ) ) ;
#22374=CARTESIAN_POINT ( 'NONE',  ( 25.64708010899961721, 45.97512510001905639, 103.1273237223351344 ) ) ;
#22378=CARTESIAN_POINT ( 'NONE',  ( 32.73300124599735739, -3.836798148479648507, 117.5726003567929610 ) ) ;
#22380=CARTESIAN_POINT ( 'NONE',  ( 2.263178607246706164, -84.32376080825635256, 118.4461883615812070 ) ) ;
#22381=VERTEX_POINT ( 'NONE', #17640 ) ;
#22383=ORIENTED_EDGE ( 'NONE', *, *, #24817, .F. ) ;
#22384=CARTESIAN_POINT ( 'NONE',  ( 1.832998868059858122, -96.70023740551049229, -108.1944082009167403 ) ) ;
#22385=VERTEX_POINT ( 'NONE', #24009 ) ;
#22388=DIRECTION ( 'NONE',  ( 0.000000000000000000, 0.000000000000000000, 1.000000000000000000 ) ) ;
#22389=CARTESIAN_POINT ( 'NONE',  ( 2.433796855181205476, 137.9325382748285165, 46.34326152018790168 ) ) ;
#22390=CARTESIAN_POINT ( 'NONE',  ( 1.833603222531957622, 29.73464781350257624, 142.0304769734129877 ) ) ;
#22391=EDGE_CURVE ( 'NONE', #7760, #5960, #9455, .T. ) ;
#22392=CARTESIAN_POINT ( 'NONE',  ( 109.1586059443104944, -0.006570129623060891148, 0.002622205828288661032 ) ) ;
#22394=CARTESIAN_POINT ( 'NONE',  ( 2.433796855181233454, 71.49415740225254012, -126.7346379669248222 ) ) ;
#22395=EDGE_CURVE ( 'NONE', #2245, #6115, #13199, .T. ) ;
#22396=CARTESIAN_POINT ( 'NONE',  ( 25.64670758986457955, -110.3390515846396909, -23.96231489925003899 ) ) ;
#22397=CARTESIAN_POINT ( 'NONE',  ( 32.73300124599740002, -89.94078864464006529, -75.82012867748569818 ) ) ;
#22398=DIRECTION ( 'NONE',  ( -1.000000000000000000, -0.000000000000000000, -0.000000000000000000 ) ) ;
#22399=( BOUNDED_SURFACE ( )  B_SPLINE_SURFACE ( 3, 1, ( 
 ( #21337, #3781 ),
 ( #8394, #23515 ),
 ( #6103, #10416 ),
 ( #3491, #23804 ) ),
 .UNSPECIFIED., .F., .F., .F. ) 
 B_SPLINE_SURFACE_WITH_KNOTS ( ( 4, 4 ),
 ( 2, 2 ),
 ( 0.000000000000000000, 1.000000000000000000 ),
 ( 0.000000000000000000, 1.000000000000000000 ),
 .UNSPECIFIED. ) 
 GEOMETRIC_REPRESENTATION_ITEM ( )  RATIONAL_B_SPLINE_SURFACE ( (
 ( 1.000000000000000000, 1.000000000000000000),
 ( 0.6386103224230316178, 0.9954351624131538845),
 ( 0.6386103224230316178, 0.9954351624131538845),
 ( 1.000000000000000000, 1.000000000000000000) ) ) 
 REPRESENTATION_ITEM ( '' )  SURFACE ( )  );
#22400=ADVANCED_FACE ( 'NONE', ( #2372 ), #23094, .F. ) ;
#22403=CARTESIAN_POINT ( 'NONE',  ( 8.186469777911003831, 145.3272523831809053, -34.43598809570011099 ) ) ;
#22405=CARTESIAN_POINT ( 'NONE',  ( 32.73300124599735739, -110.6325518752276622, 39.98094346392273479 ) ) ;
#22406=CARTESIAN_POINT ( 'NONE',  ( 13.84597867724967379, 135.8932891738225806, -55.26821062125426920 ) ) ;
#22408=EDGE_CURVE ( 'NONE', #21273, #7383, #2927, .T. ) ;
#22409=EDGE_LOOP ( 'NONE', ( #26293, #2836, #8463, #21400 ) ) ;
#22410=CARTESIAN_POINT ( 'NONE',  ( 25.73574536432417048, 98.23578516675037520, -55.78561308781378614 ) ) ;
#22412=VERTEX_POINT ( 'NONE', #10136 ) ;
#22413=CARTESIAN_POINT ( 'NONE',  ( 5.340103579038252057, -88.52145169228889188, -117.9209211655066696 ) ) ;
#22414=ORIENTED_EDGE ( 'NONE', *, *, #28325, .F. ) ;
#22415=DIRECTION ( 'NONE',  ( -1.000000000000000000, -0.000000000000000000, -0.000000000000000000 ) ) ;
#22416=B_SPLINE_CURVE_WITH_KNOTS ( 'NONE', 3,
 ( #19267, #21853, #26032, #28039 ),
 .UNSPECIFIED., .F., .F.,
 ( 4, 4 ),
 ( 3.048060820747882759E-16, 0.01077107486149818383 ),
 .UNSPECIFIED. ) ;
#22419=CARTESIAN_POINT ( 'NONE',  ( 25.64681081121879203, 112.2483031020015147, -12.21581276189692211 ) ) ;
#22420=ORIENTED_EDGE ( 'NONE', *, *, #3879, .T. ) ;
#22421=CARTESIAN_POINT ( 'NONE',  ( 13.84597867724975551, -132.0026437215596786, -64.00674338125978124 ) ) ;
#22422=ORIENTED_EDGE ( 'NONE', *, *, #6733, .F. ) ;
#22424=CARTESIAN_POINT ( 'NONE',  ( 24.01988960052052491, -115.5642432877696848, 61.78678588189985277 ) ) ;
#22425=EDGE_CURVE ( 'NONE', #3673, #19518, #16707, .T. ) ;
#22426=B_SPLINE_CURVE_WITH_KNOTS ( 'NONE', 3,
 ( #26401, #2203, #1789, #10735 ),
 .UNSPECIFIED., .F., .F.,
 ( 4, 4 ),
 ( 3.628665131031684266E-16, 0.01077107486149826536 ),
 .UNSPECIFIED. ) ;
#22427=CARTESIAN_POINT ( 'NONE',  ( 25.64708228042120908, 107.3971738194636458, -34.85404436489383784 ) ) ;
#22428=CARTESIAN_POINT ( 'NONE',  ( 10.93730112725990011, -151.0983828010091656, -4.928439153521871674 ) ) ;
#22429=LINE ( 'NONE', #17936, #71 ) ;
#22430=ADVANCED_FACE ( 'NONE', ( #27676 ), #17012, .T. ) ;
#22431=ORIENTED_EDGE ( 'NONE', *, *, #7030, .T. ) ;
#22432=CARTESIAN_POINT ( 'NONE',  ( 9.884929003653626367, 150.0922431698404864, 11.54837932063081674 ) ) ;
#22434=CARTESIAN_POINT ( 'NONE',  ( 10.93730112725997294, 36.23586118136742584, -146.7718404940639516 ) ) ;
#22436=EDGE_CURVE ( 'NONE', #2536, #7054, #13119, .T. ) ;
#22437=ORIENTED_EDGE ( 'NONE', *, *, #22967, .F. ) ;
#22438=CARTESIAN_POINT ( 'NONE',  ( 55.49584447822657296, 66.16986612640775434, 29.75369869230976860 ) ) ;
#22440=CARTESIAN_POINT ( 'NONE',  ( 25.86096068574582318, -24.48003142199159043, 110.3716997142157510 ) ) ;
#22443=CARTESIAN_POINT ( 'NONE',  ( 26.04756280548354042, 47.04636360340825263, 102.9366382251194807 ) ) ;
#22444=ORIENTED_EDGE ( 'NONE', *, *, #12634, .T. ) ;
#22445=CARTESIAN_POINT ( 'NONE',  ( 2.433796855181233454, 145.5024947199069913, -1.451562450950139249 ) ) ;
#22447=CIRCLE ( 'NONE', #24290, 151.1787379149930359 ) ;
#22448=CARTESIAN_POINT ( 'NONE',  ( 1.833603222531971610, -145.1089511853978422, -0.4449221977534632000 ) ) ;
#22450=( BOUNDED_SURFACE ( )  B_SPLINE_SURFACE ( 3, 1, ( 
 ( #24169, #10506 ),
 ( #6199, #12651 ),
 ( #19274, #15216 ),
 ( #28047, #23897 ) ),
 .UNSPECIFIED., .F., .F., .F. ) 
 B_SPLINE_SURFACE_WITH_KNOTS ( ( 4, 4 ),
 ( 2, 2 ),
 ( 0.000000000000000000, 1.000000000000000000 ),
 ( 0.000000000000000000, 1.000000000000000000 ),
 .UNSPECIFIED. ) 
 GEOMETRIC_REPRESENTATION_ITEM ( )  RATIONAL_B_SPLINE_SURFACE ( (
 ( 1.000000000000000000, 1.000000000000000000),
 ( 0.9956975270656955868, 0.8568959468854907557),
 ( 0.9956975270656955868, 0.8568959468854907557),
 ( 1.000000000000000000, 1.000000000000000000) ) ) 
 REPRESENTATION_ITEM ( '' )  SURFACE ( )  );
#22451=CARTESIAN_POINT ( 'NONE',  ( 109.1624594426973118, 0.01102230012606810090, 0.01154818537151459067 ) ) ;
#22453=CARTESIAN_POINT ( 'NONE',  ( 109.1586059443104944, -0.002447596125905633375, 0.006637156007973973003 ) ) ;
#22455=CARTESIAN_POINT ( 'NONE',  ( 1.893872463202025624, 142.1730500379302384, -29.24569695044102602 ) ) ;
#22456=CARTESIAN_POINT ( 'NONE',  ( 2.263178607246643992, -142.5035407554793494, -28.85718361841066582 ) ) ;
#22457=ORIENTED_EDGE ( 'NONE', *, *, #18337, .T. ) ;
#22458=B_SPLINE_CURVE_WITH_KNOTS ( 'NONE', 3,
 ( #18136, #26624, #11377, #11521, #20297, #3042 ),
 .UNSPECIFIED., .F., .F.,
 ( 4, 2, 4 ),
 ( 9.745765416140531346E-18, 0.0006311636237756831393, 0.001262327247551356521 ),
 .UNSPECIFIED. ) ;
#22459=( BOUNDED_SURFACE ( )  B_SPLINE_SURFACE ( 3, 1, ( 
 ( #26203, #15395 ),
 ( #24646, #16553 ),
 ( #12100, #16413 ),
 ( #11950, #27343 ) ),
 .UNSPECIFIED., .F., .F., .F. ) 
 B_SPLINE_SURFACE_WITH_KNOTS ( ( 4, 4 ),
 ( 2, 2 ),
 ( 0.000000000000000000, 1.000000000000000000 ),
 ( 0.000000000000000000, 1.000000000000000000 ),
 .UNSPECIFIED. ) 
 GEOMETRIC_REPRESENTATION_ITEM ( )  RATIONAL_B_SPLINE_SURFACE ( (
 ( 1.000000000000000000, 1.000000000000000000),
 ( 0.9956975270656954757, 0.8568959468854893125),
 ( 0.9956975270656954757, 0.8568959468854893125),
 ( 1.000000000000000000, 1.000000000000000000) ) ) 
 REPRESENTATION_ITEM ( '' )  SURFACE ( )  );
#22460=EDGE_LOOP ( 'NONE', ( #5168, #20598, #15915, #9502 ) ) ;
#22463=AXIS2_PLACEMENT_3D ( 'NONE', #22510, #11275, #24383 ) ;
#22466=VECTOR ( 'NONE', #11421, 1000.000000000000000 ) ;
#22467=CARTESIAN_POINT ( 'NONE',  ( 28.37644542392843405, -69.76573497039019855, -102.9230687709016081 ) ) ;
#22469=ORIENTED_EDGE ( 'NONE', *, *, #15901, .T. ) ;
#22471=ADVANCED_FACE ( 'NONE', ( #28092 ), #5414, .F. ) ;
#22472=CARTESIAN_POINT ( 'NONE',  ( 25.64708010899964918, -103.1273237223352766, 45.97512510001868691 ) ) ;
#22474=ORIENTED_EDGE ( 'NONE', *, *, #2933, .F. ) ;
#22475=ADVANCED_FACE ( 'NONE', ( #5450, #8809 ), #301, .F. ) ;
#22478=CARTESIAN_POINT ( 'NONE',  ( 26.28373643307399377, 123.8418562193902659, -30.57614217577341620 ) ) ;
#22479=CARTESIAN_POINT ( 'NONE',  ( 2.433796855181205476, -145.5024947199069629, -1.451562450951161987 ) ) ;
#22482=CARTESIAN_POINT ( 'NONE',  ( 109.1624594426973260, -0.006066618937909569638, -0.01476644236456057385 ) ) ;
#22488=CARTESIAN_POINT ( 'NONE',  ( 55.79472521941426777, -48.13855120843846436, -54.55111121764132776 ) ) ;
#22490=EDGE_LOOP ( 'NONE', ( #17170, #10837, #19353, #14249 ) ) ;
#22491=CARTESIAN_POINT ( 'NONE',  ( 1.833206308920067196, -96.54250175814047452, -108.3342547309375306 ) ) ;
#22492=B_SPLINE_CURVE_WITH_KNOTS ( 'NONE', 3,
 ( #10936, #6340, #19699, #6764, #19987, #13506 ),
 .UNSPECIFIED., .F., .F.,
 ( 4, 2, 4 ),
 ( 1.042864983293993125E-17, 0.0006311571484585992839, 0.001262314296917197484 ),
 .UNSPECIFIED. ) ;
#22493=CARTESIAN_POINT ( 'NONE',  ( 1.834118845439484335, -117.2918069668795056, -85.43746956709969709 ) ) ;
#22494=ORIENTED_EDGE ( 'NONE', *, *, #9403, .F. ) ;
#22495=VERTEX_POINT ( 'NONE', #2603 ) ;
#22496=ORIENTED_EDGE ( 'NONE', *, *, #4084, .T. ) ;
#22501=EDGE_CURVE ( 'NONE', #21108, #5582, #8428, .T. ) ;
#22504=CARTESIAN_POINT ( 'NONE',  ( 26.11404676487257603, -112.4785329405481065, -12.95861723607569438 ) ) ;
#22505=CARTESIAN_POINT ( 'NONE',  ( 2.433796855181205476, 16.65276281464756636, -144.5536872373190533 ) ) ;
#22506=CARTESIAN_POINT ( 'NONE',  ( 25.98107933586700469, 33.92073193606590564, 107.9289867379274312 ) ) ;
#22507=CARTESIAN_POINT ( 'NONE',  ( 55.79472521941428198, 48.13855120843958701, -54.55111121764033300 ) ) ;
#22510=CARTESIAN_POINT ( 'NONE',  ( -40.00000000000000000, 0.000000000000000000, 0.000000000000000000 ) ) ;
#22511=ORIENTED_EDGE ( 'NONE', *, *, #6968, .T. ) ;
#22512=LINE ( 'NONE', #22808, #24975 ) ;
#22514=CARTESIAN_POINT ( 'NONE',  ( 13.36082413113063083, -135.4964217943302458, -70.90215303572267658 ) ) ;
#22515=CARTESIAN_POINT ( 'NONE',  ( 32.73300124599740002, 72.21147546950675178, -92.86301839379947864 ) ) ;
#22519=CARTESIAN_POINT ( 'NONE',  ( 109.1592201516379674, -0.006649399203953420406, -0.004194960840980667231 ) ) ;
#22520=ORIENTED_EDGE ( 'NONE', *, *, #11019, .T. ) ;
#22521=CARTESIAN_POINT ( 'NONE',  ( 26.11404676487259024, 103.8885755249575453, -45.01677474591305383 ) ) ;
#22523=ORIENTED_EDGE ( 'NONE', *, *, #9432, .F. ) ;
#22525=DIRECTION ( 'NONE',  ( -1.000000000000000000, -0.000000000000000000, -0.000000000000000000 ) ) ;
#22527=ORIENTED_EDGE ( 'NONE', *, *, #19717, .F. ) ;
#22529=ORIENTED_EDGE ( 'NONE', *, *, #8024, .T. ) ;
#22530=DIRECTION ( 'NONE',  ( -1.000000000000000000, -0.000000000000000000, -0.000000000000000000 ) ) ;
#22532=EDGE_CURVE ( 'NONE', #25711, #17719, #10835, .T. ) ;
#22533=B_SPLINE_CURVE_WITH_KNOTS ( 'NONE', 3,
 ( #12929, #19686, #686, #9340, #12060, #14060, #11626 ),
 .UNSPECIFIED., .F., .F.,
 ( 4, 3, 4 ),
 ( 0.000000000000000000, 0.02398743853561428538, 0.04000277880656220864 ),
 .UNSPECIFIED. ) ;
#22536=( BOUNDED_SURFACE ( )  B_SPLINE_SURFACE ( 3, 1, ( 
 ( #10535, #13231 ),
 ( #28346, #2282 ),
 ( #4325, #11091 ),
 ( #22021, #148 ) ),
 .UNSPECIFIED., .F., .F., .F. ) 
 B_SPLINE_SURFACE_WITH_KNOTS ( ( 4, 4 ),
 ( 2, 2 ),
 ( 0.000000000000000000, 1.000000000000000000 ),
 ( 0.000000000000000000, 1.000000000000000000 ),
 .UNSPECIFIED. ) 
 GEOMETRIC_REPRESENTATION_ITEM ( )  RATIONAL_B_SPLINE_SURFACE ( (
 ( 1.000000000000000000, 1.000000000000000000),
 ( 0.6386103224230316178, 0.9954351624131538845),
 ( 0.6386103224230316178, 0.9954351624131538845),
 ( 1.000000000000000000, 1.000000000000000000) ) ) 
 REPRESENTATION_ITEM ( '' )  SURFACE ( )  );
#22539=B_SPLINE_CURVE_WITH_KNOTS ( 'NONE', 3,
 ( #27081, #7693, #23093, #24821, #25099, #5364, #16595 ),
 .UNSPECIFIED., .F., .F.,
 ( 4, 3, 4 ),
 ( 5.601303642928431203E-16, 0.02816610861753243017, 0.04000277880656278456 ),
 .UNSPECIFIED. ) ;
#22540=CARTESIAN_POINT ( 'NONE',  ( 109.1586900883932856, 0.005715190711481724431, -0.004277182003227242291 ) ) ;
#22541=CARTESIAN_POINT ( 'NONE',  ( 32.73300124599732186, 0.000000000000000000, 0.000000000000000000 ) ) ;
#22544=CARTESIAN_POINT ( 'NONE',  ( 25.64670758986456889, -0.4979020485385241557, 112.9099239813695448 ) ) ;
#22546=EDGE_LOOP ( 'NONE', ( #22745, #22474, #26739, #14983 ) ) ;
#22549=CARTESIAN_POINT ( 'NONE',  ( 25.64670758986457244, 45.46974729533283721, 103.3508631837546119 ) ) ;
#22551=DIRECTION ( 'NONE',  ( 0.000000000000000000, 0.000000000000000000, 1.000000000000000000 ) ) ;
#22554=CARTESIAN_POINT ( 'NONE',  ( 25.70243777736191149, 98.18050844655147102, -55.83795591307026029 ) ) ;
#22556=CARTESIAN_POINT ( 'NONE',  ( 26.28373643307408614, -91.96212244992437945, 88.40064398364035014 ) ) ;
#22557=ORIENTED_EDGE ( 'NONE', *, *, #24817, .T. ) ;
#22558=CARTESIAN_POINT ( 'NONE',  ( 1.834118845439484335, 96.96525081350146991, -107.9567937753783298 ) ) ;
#22559=ORIENTED_EDGE ( 'NONE', *, *, #1469, .F. ) ;
#22561=ADVANCED_FACE ( 'NONE', ( #13389 ), #19730, .T. ) ;
#22562=VECTOR ( 'NONE', #15227, 999.9999999999998863 ) ;
#22564=AXIS2_PLACEMENT_3D ( 'NONE', #18484, #11579, #12012 ) ;
#22565=EDGE_LOOP ( 'NONE', ( #20404, #17093, #889, #13121 ) ) ;
#22567=AXIS2_PLACEMENT_3D ( 'NONE', #21099, #8042, #25588 ) ;
#22569=VERTEX_POINT ( 'NONE', #22340 ) ;
#22570=FACE_OUTER_BOUND ( 'NONE', #14046, .T. ) ;
#22572=( LENGTH_UNIT ( ) NAMED_UNIT ( * ) SI_UNIT ( .MILLI., .METRE. ) );
#22575=CARTESIAN_POINT ( 'NONE',  ( 2.433796855181219243, 28.83182736670734059, -142.6247129145645829 ) ) ;
#22576=CARTESIAN_POINT ( 'NONE',  ( 25.64700659047696263, 110.3963107228936309, 23.69811251893771242 ) ) ;
#22578=CARTESIAN_POINT ( 'NONE',  ( 9.884929003653608603, 50.49804566712312237, -141.8132360130352936 ) ) ;
#22579=CARTESIAN_POINT ( 'NONE',  ( 1.894214914920949289, -96.41356089048353795, 108.5033568857721491 ) ) ;
#22580=CARTESIAN_POINT ( 'NONE',  ( 109.1586900883932856, -0.006561743627143346892, 0.002810909342011579538 ) ) ;
#22581=ORIENTED_EDGE ( 'NONE', *, *, #19812, .F. ) ;
#22582=AXIS2_PLACEMENT_3D ( 'NONE', #8734, #10900, #28297 ) ;
#22585=CARTESIAN_POINT ( 'NONE',  ( 109.1587776205901861, 0.005390665547495581203, -0.004965871434398060232 ) ) ;
#22586=CARTESIAN_POINT ( 'NONE',  ( 26.11404676487259024, 10.71016160607567080, 112.7148551500680753 ) ) ;
#22588=CONICAL_SURFACE ( 'NONE', #2327, 117.6351876552689504, 0.9945805576725580410 ) ;
#22589=B_SPLINE_CURVE_WITH_KNOTS ( 'NONE', 3,
 ( #3291, #10063, #20692, #9486 ),
 .UNSPECIFIED., .F., .F.,
 ( 4, 4 ),
 ( 0.000000000000000000, 0.01077107196513853692 ),
 .UNSPECIFIED. ) ;
#22594=ORIENTED_EDGE ( 'NONE', *, *, #18829, .F. ) ;
#22595=FACE_OUTER_BOUND ( 'NONE', #16766, .T. ) ;
#22596=CARTESIAN_POINT ( 'NONE',  ( 109.1589550718175161, -0.005233222325307201363, -0.005477029346534909721 ) ) ;
#22598=CARTESIAN_POINT ( 'NONE',  ( 25.64699802086725455, 12.03888878460473855, 112.2675771984164754 ) ) ;
#22601=VERTEX_POINT ( 'NONE', #11385 ) ;
#22602=DIRECTION ( 'NONE',  ( -1.000000000000000000, -0.000000000000000000, -0.000000000000000000 ) ) ;
#22603=EDGE_CURVE ( 'NONE', #20657, #17799, #5006, .T. ) ;
#22606=ORIENTED_EDGE ( 'NONE', *, *, #24190, .F. ) ;
#22609=EDGE_LOOP ( 'NONE', ( #2757, #19396, #4514, #19464 ) ) ;
#22610=EDGE_CURVE ( 'NONE', #15531, #6453, #18994, .T. ) ;
#22615=CARTESIAN_POINT ( 'NONE',  ( 1.833485406944043827, -132.3460930279887293, -59.50871042846357994 ) ) ;
#22616=AXIS2_PLACEMENT_3D ( 'NONE', #20451, #13969, #22634 ) ;
#22617=CARTESIAN_POINT ( 'NONE',  ( 1.831572820252009626, -108.4969585352548478, -96.36280042116040079 ) ) ;
#22618=DIRECTION ( 'NONE',  ( 0.000000000000000000, 0.000000000000000000, 1.000000000000000000 ) ) ;
#22619=ORIENTED_EDGE ( 'NONE', *, *, #12440, .F. ) ;
#22621=CARTESIAN_POINT ( 'NONE',  ( 25.64700659047694131, 34.67498789830447947, 107.4550658295752470 ) ) ;
#22622=DIRECTION ( 'NONE',  ( 0.000000000000000000, 0.000000000000000000, 1.000000000000000000 ) ) ;
#22627=CARTESIAN_POINT ( 'NONE',  ( 1.834118845439484335, -144.3336252355296097, -14.99112450600394553 ) ) ;
#22628=CARTESIAN_POINT ( 'NONE',  ( 13.36082413113063083, 151.2941478187910604, -22.28175172543404869 ) ) ;
#22629=B_SPLINE_CURVE_WITH_KNOTS ( 'NONE', 3,
 ( #20111, #24883, #22579, #13633, #22731, #11475 ),
 .UNSPECIFIED., .F., .F.,
 ( 4, 2, 4 ),
 ( 0.000000000000000000, 0.0006311571484585993923, 0.001262314296917198785 ),
 .UNSPECIFIED. ) ;
#22630=CARTESIAN_POINT ( 'NONE',  ( 2.430230287190581429, -107.1617224697457544, -98.44218333480878869 ) ) ;
#22631=CARTESIAN_POINT ( 'NONE',  ( 32.73300124599735739, -16.10546300444903167, 116.5274707358854869 ) ) ;
#22634=DIRECTION ( 'NONE',  ( 0.000000000000000000, 0.000000000000000000, 1.000000000000000000 ) ) ;
#22636=( BOUNDED_SURFACE ( )  B_SPLINE_SURFACE ( 3, 1, ( 
 ( #9060, #4735 ),
 ( #7197, #17815 ),
 ( #18244, #24761 ),
 ( #13508, #26889 ) ),
 .UNSPECIFIED., .F., .F., .F. ) 
 B_SPLINE_SURFACE_WITH_KNOTS ( ( 4, 4 ),
 ( 2, 2 ),
 ( 0.000000000000000000, 1.000000000000000000 ),
 ( 0.000000000000000000, 1.000000000000000000 ),
 .UNSPECIFIED. ) 
 GEOMETRIC_REPRESENTATION_ITEM ( )  RATIONAL_B_SPLINE_SURFACE ( (
 ( 1.000000000000000000, 1.000000000000000000),
 ( 0.9956975270656954757, 0.8568959468854893125),
 ( 0.9956975270656954757, 0.8568959468854893125),
 ( 1.000000000000000000, 1.000000000000000000) ) ) 
 REPRESENTATION_ITEM ( '' )  SURFACE ( )  );
#22637=CARTESIAN_POINT ( 'NONE',  ( 109.1624594426973260, -0.01358749486988124894, -0.008380433676406191107 ) ) ;
#22638=CIRCLE ( 'NONE', #12501, 12.50000000000000178 ) ;
#22640=DIRECTION ( 'NONE',  ( 0.7071067811865465735, 2.453269466693394677E-16, -0.7071067811865485719 ) ) ;
#22641=ORIENTED_EDGE ( 'NONE', *, *, #3936, .T. ) ;
#22643=ORIENTED_EDGE ( 'NONE', *, *, #12391, .T. ) ;
#22645=CARTESIAN_POINT ( 'NONE',  ( 25.64681081121880624, -102.9795863647025556, -46.30456157731431688 ) ) ;
#22646=CARTESIAN_POINT ( 'NONE',  ( 2.430230287190572103, -31.67257033707601011, 142.0258656395020864 ) ) ;
#22648=B_SPLINE_CURVE_WITH_KNOTS ( 'NONE', 3,
 ( #17099, #26712, #20093, #4418 ),
 .UNSPECIFIED., .F., .F.,
 ( 4, 4 ),
 ( 0.000000000000000000, 0.01077107196513880406 ),
 .UNSPECIFIED. ) ;
#22650=CARTESIAN_POINT ( 'NONE',  ( 26.28373643307406482, 48.05579805965698625, -118.1623717393430582 ) ) ;
#22651=CIRCLE ( 'NONE', #104, 151.1787379149930359 ) ;
#22654=CARTESIAN_POINT ( 'NONE',  ( 32.73300124599738581, -62.10906484417165530, -99.90245962373897726 ) ) ;
#22658=CARTESIAN_POINT ( 'NONE',  ( 32.73300124599738581, 84.80615050150476009, -81.52272205837115848 ) ) ;
#22661=CARTESIAN_POINT ( 'NONE',  ( 1.833485406944057594, -85.72460230293616235, -117.0814567582553281 ) ) ;
#22662=CARTESIAN_POINT ( 'NONE',  ( 10.93730112725990011, -119.3442956573265974, -92.80059208661810999 ) ) ;
#22665=CARTESIAN_POINT ( 'NONE',  ( 25.98552792386801968, -22.46612985365048232, 110.8838436908325917 ) ) ;
#22667=CARTESIAN_POINT ( 'NONE',  ( 109.1778270068192853, -0.006489198140359578836, -0.006682187084648886881 ) ) ;
#22668=CARTESIAN_POINT ( 'NONE',  ( 25.64692872815575342, 84.12425003484143815, -75.31297890941186779 ) ) ;
#22670=( BOUNDED_SURFACE ( )  B_SPLINE_SURFACE ( 3, 1, ( 
 ( #5046, #11961 ),
 ( #3049, #3468 ),
 ( #22783, #20887 ),
 ( #27355, #9819 ) ),
 .UNSPECIFIED., .F., .F., .F. ) 
 B_SPLINE_SURFACE_WITH_KNOTS ( ( 4, 4 ),
 ( 2, 2 ),
 ( 0.000000000000000000, 1.000000000000000000 ),
 ( 0.000000000000000000, 1.000000000000000000 ),
 .UNSPECIFIED. ) 
 GEOMETRIC_REPRESENTATION_ITEM ( )  RATIONAL_B_SPLINE_SURFACE ( (
 ( 1.000000000000000000, 1.000000000000000000),
 ( 0.9956975270656955868, 0.8568959468854907557),
 ( 0.9956975270656955868, 0.8568959468854907557),
 ( 1.000000000000000000, 1.000000000000000000) ) ) 
 REPRESENTATION_ITEM ( '' )  SURFACE ( )  );
#22673=CARTESIAN_POINT ( 'NONE',  ( 26.11404676487259024, 12.95861723607453619, 112.4785329405482628 ) ) ;
#22675=ADVANCED_FACE ( 'NONE', ( #25745 ), #19197, .F. ) ;
#22677=ORIENTED_EDGE ( 'NONE', *, *, #8029, .F. ) ;
#22678=AXIS2_PLACEMENT_3D ( 'NONE', #13112, #10960, #2025 ) ;
#22679=EDGE_LOOP ( 'NONE', ( #26473, #2785 ) ) ;
#22680=EDGE_CURVE ( 'NONE', #21489, #20545, #9930, .T. ) ;
#22681=EDGE_CURVE ( 'NONE', #2573, #3393, #17695, .T. ) ;
#22682=CARTESIAN_POINT ( 'NONE',  ( 1.832998868059858122, 59.50898020732689986, -132.3466930259787944 ) ) ;
#22683=EDGE_CURVE ( 'NONE', #14104, #10838, #10183, .T. ) ;
#22687=CARTESIAN_POINT ( 'NONE',  ( 25.64692872815577473, -66.62748454953222677, 91.15762468787718831 ) ) ;
#22688=CARTESIAN_POINT ( 'NONE',  ( 2.433796855181219243, 107.1581411821798895, -98.43889364293755762 ) ) ;
#22689=CARTESIAN_POINT ( 'NONE',  ( 32.73300124599740002, 97.37344512919945316, -66.00340565729239017 ) ) ;
#22691=DIRECTION ( 'NONE',  ( 0.000000000000000000, 0.000000000000000000, 1.000000000000000000 ) ) ;
#22692=CARTESIAN_POINT ( 'NONE',  ( 8.186469777910573953, 137.8131828745823952, 57.56191611950351472 ) ) ;
#22694=CARTESIAN_POINT ( 'NONE',  ( 25.73574536432415627, 83.41179791497867768, 76.18908113044783192 ) ) ;
#22695=VECTOR ( 'NONE', #15970, 1000.000000000000000 ) ;
#22696=ORIENTED_EDGE ( 'NONE', *, *, #27190, .T. ) ;
#22697=EDGE_LOOP ( 'NONE', ( #20430, #9769, #633, #5633 ) ) ;
#22698=CARTESIAN_POINT ( 'NONE',  ( 28.37603512858359522, 13.77584568114293617, 113.9023475466375288 ) ) ;
#22699=CARTESIAN_POINT ( 'NONE',  ( 1.833485406944043827, -15.69895494453482598, 144.2578170162062463 ) ) ;
#22701=CARTESIAN_POINT ( 'NONE',  ( 25.70243777736186885, -84.42566495012501093, 75.03063812272023370 ) ) ;
#22702=DIRECTION ( 'NONE',  ( 0.000000000000000000, 0.000000000000000000, 1.000000000000000000 ) ) ;
#22704=EDGE_CURVE ( 'NONE', #19926, #11082, #887, .T. ) ;
#22705=EDGE_LOOP ( 'NONE', ( #25893, #15266, #5652, #488 ) ) ;
#22706=CARTESIAN_POINT ( 'NONE',  ( 28.43349137099853863, 124.1860347533531979, -4.052139611198855462 ) ) ;
#22708=CARTESIAN_POINT ( 'NONE',  ( 30.58324630866349025, 74.24222250960228564, 95.47492154584176660 ) ) ;
#22711=EDGE_CURVE ( 'NONE', #22316, #23136, #25633, .T. ) ;
#22712=ORIENTED_EDGE ( 'NONE', *, *, #2518, .F. ) ;
#22713=CARTESIAN_POINT ( 'NONE',  ( 1.832998868059858122, -125.4013017422225857, -73.01698022778488451 ) ) ;
#22715=CARTESIAN_POINT ( 'NONE',  ( 30.59141879584292667, -66.10404588653725000, -95.58042137919522929 ) ) ;
#22716=( BOUNDED_SURFACE ( )  B_SPLINE_SURFACE ( 3, 1, ( 
 ( #16295, #7685 ),
 ( #27219, #25090 ),
 ( #9678, #13845 ),
 ( #11981, #20468 ) ),
 .UNSPECIFIED., .F., .F., .F. ) 
 B_SPLINE_SURFACE_WITH_KNOTS ( ( 4, 4 ),
 ( 2, 2 ),
 ( 0.000000000000000000, 1.000000000000000000 ),
 ( 0.000000000000000000, 1.000000000000000000 ),
 .UNSPECIFIED. ) 
 GEOMETRIC_REPRESENTATION_ITEM ( )  RATIONAL_B_SPLINE_SURFACE ( (
 ( 1.000000000000000000, 1.000000000000000000),
 ( 0.6386103224230316178, 0.9954351624131538845),
 ( 0.6386103224230316178, 0.9954351624131538845),
 ( 1.000000000000000000, 1.000000000000000000) ) ) 
 REPRESENTATION_ITEM ( '' )  SURFACE ( )  );
#22717=ORIENTED_EDGE ( 'NONE', *, *, #13903, .T. ) ;
#22721=ORIENTED_EDGE ( 'NONE', *, *, #20276, .F. ) ;
#22723=B_SPLINE_CURVE_WITH_KNOTS ( 'NONE', 3,
 ( #22389, #15753, #18190, #4825, #20206, #4678 ),
 .UNSPECIFIED., .F., .F.,
 ( 4, 2, 4 ),
 ( 1.474514954580286030E-17, 0.0006311636237757010286, 0.001262327247551387095 ),
 .UNSPECIFIED. ) ;
#22724=B_SPLINE_CURVE_WITH_KNOTS ( 'NONE', 3,
 ( #8736, #4271, #23604, #2674, #15341, #20087, #4843, #21975, #18210, #9453 ),
 .UNSPECIFIED., .F., .F.,
 ( 4, 3, 3, 4 ),
 ( 1.962615573354718958E-17, 0.0002669560319015498121, 0.0005492286108966249738, 0.0008315040496093325378 ),
 .UNSPECIFIED. ) ;
#22725=CARTESIAN_POINT ( 'NONE',  ( 21.16825799904893657, -103.5479404090030897, -87.29264348877946134 ) ) ;
#22726=FACE_OUTER_BOUND ( 'NONE', #12046, .T. ) ;
#22728=CARTESIAN_POINT ( 'NONE',  ( 1.833691583653537460, -125.8462703805704166, 72.24637705290446377 ) ) ;
#22730=CARTESIAN_POINT ( 'NONE',  ( 10.93730112725972248, -36.23586118136624634, 146.7718404940640653 ) ) ;
#22731=CARTESIAN_POINT ( 'NONE',  ( 2.263178607246683516, -96.24282447295516363, 108.9830946142710530 ) ) ;
#22732=CARTESIAN_POINT ( 'NONE',  ( 32.73300124599735739, -16.10546300444903167, 116.5274707358854869 ) ) ;
#22735=ORIENTED_EDGE ( 'NONE', *, *, #20012, .F. ) ;
#22738=FACE_OUTER_BOUND ( 'NONE', #15044, .T. ) ;
#22739=CARTESIAN_POINT ( 'NONE',  ( 10.93730112726007775, 51.37919228020501805, -142.1801301103781725 ) ) ;
#22741=CARTESIAN_POINT ( 'NONE',  ( 1.833809397773869865, 144.2961330457379177, 15.34508223002496941 ) ) ;
#22742=CARTESIAN_POINT ( 'NONE',  ( 1.833485406944057594, 72.09189602597886903, -125.9346397303427665 ) ) ;
#22745=ORIENTED_EDGE ( 'NONE', *, *, #10538, .T. ) ;
#22747=CARTESIAN_POINT ( 'NONE',  ( 32.73300124599735028, -8.473903470906931190, 117.3295799645429156 ) ) ;
#22748=CARTESIAN_POINT ( 'NONE',  ( 25.64681081121880624, 11.38886654529674303, 112.3352186517031157 ) ) ;
#22749=CARTESIAN_POINT ( 'NONE',  ( 109.1586900883932856, -0.005236795036860577776, 0.004851151255037344269 ) ) ;
#22750=EDGE_CURVE ( 'NONE', #12091, #24050, #25260, .T. ) ;
#22751=CARTESIAN_POINT ( 'NONE',  ( 32.73300124599741423, -97.37344512919810313, -66.00340565729437969 ) ) ;
#22752=B_SPLINE_CURVE_WITH_KNOTS ( 'NONE', 3,
 ( #7856, #14154, #26868, #5388, #5688, #23259, #22428 ),
 .UNSPECIFIED., .F., .F.,
 ( 4, 3, 4 ),
 ( 0.000000000000000000, 0.02398743853561347353, 0.04000277880656219476 ),
 .UNSPECIFIED. ) ;
#22753=CARTESIAN_POINT ( 'NONE',  ( 109.1592201516379674, 0.004368284148529012062, 0.006536841731953418715 ) ) ;
#22754=ORIENTED_EDGE ( 'NONE', *, *, #18333, .F. ) ;
#22755=CARTESIAN_POINT ( 'NONE',  ( 109.1778270068192853, -0.008360410075186638576, -0.004106684808172209912 ) ) ;
#22759=ORIENTED_EDGE ( 'NONE', *, *, #26538, .F. ) ;
#22763=CARTESIAN_POINT ( 'NONE',  ( 6.224689322667630975, 108.2965163446074399, 100.9623537450655419 ) ) ;
#22766=CARTESIAN_POINT ( 'NONE',  ( 2.433796855181205476, 107.1581411821785821, 98.43889364293895028 ) ) ;
#22767=ORIENTED_EDGE ( 'NONE', *, *, #23837, .T. ) ;
#22769=CARTESIAN_POINT ( 'NONE',  ( 109.1589550718174877, -0.002553077953671659388, 0.007132058561965940943 ) ) ;
#22770=CARTESIAN_POINT ( 'NONE',  ( 25.98552792386802679, -45.02923844025552569, 103.7897946223263830 ) ) ;
#22771=ORIENTED_EDGE ( 'NONE', *, *, #25670, .T. ) ;
#22772=EDGE_CURVE ( 'NONE', #1034, #18134, #1893, .T. ) ;
#22773=ORIENTED_EDGE ( 'NONE', *, *, #15120, .T. ) ;
#22775=ADVANCED_FACE ( 'NONE', ( #1965 ), #18044, .T. ) ;
#22778=CARTESIAN_POINT ( 'NONE',  ( 32.73300124599732186, 0.000000000000000000, 0.000000000000000000 ) ) ;
#22779=CARTESIAN_POINT ( 'NONE',  ( 2.063896406836605024, -107.0521644432410682, -98.19887492195967127 ) ) ;
#22781=ORIENTED_EDGE ( 'NONE', *, *, #3039, .T. ) ;
#22783=CARTESIAN_POINT ( 'NONE',  ( 109.1589550718175161, 0.007507020724820355310, -0.001014448720249569230 ) ) ;
#22784=EDGE_CURVE ( 'NONE', #1034, #15045, #11038, .T. ) ;
#22787=CARTESIAN_POINT ( 'NONE',  ( 25.64708228042119131, -107.3971738194634185, 34.85404436489458391 ) ) ;
#22788=EDGE_CURVE ( 'NONE', #11885, #8709, #18671, .T. ) ;
#22789=ORIENTED_EDGE ( 'NONE', *, *, #3029, .T. ) ;
#22793=VECTOR ( 'NONE', #21986, 1000.000000000000227 ) ;
#22794=ORIENTED_EDGE ( 'NONE', *, *, #21782, .F. ) ;
#22796=CARTESIAN_POINT ( 'NONE',  ( 2.063896406836609909, 125.1295119249449499, -73.79559738457622586 ) ) ;
#22800=CARTESIAN_POINT ( 'NONE',  ( 25.64660436782552821, -75.12017330820535221, 84.29628170537232279 ) ) ;
#22801=CARTESIAN_POINT ( 'NONE',  ( 25.73574536432416338, 107.6875787074511521, -34.14219540448021206 ) ) ;
#22802=EDGE_CURVE ( 'NONE', #8105, #6339, #8876, .T. ) ;
#22803=FACE_OUTER_BOUND ( 'NONE', #4260, .T. ) ;
#22804=CARTESIAN_POINT ( 'NONE',  ( 5.340103556456505807, -139.5040934094288332, -47.74933482044516353 ) ) ;
#22806=LINE ( 'NONE', #3074, #23875 ) ;
#22807=EDGE_CURVE ( 'NONE', #11372, #18716, #13460, .T. ) ;
#22808=CARTESIAN_POINT ( 'NONE',  ( 99.22246935314075245, -70.00000000000000000, 40.00000000000003553 ) ) ;
#22809=CARTESIAN_POINT ( 'NONE',  ( 28.43349137099837876, -21.85613782299062180, 122.3147591366315510 ) ) ;
#22811=FACE_OUTER_BOUND ( 'NONE', #7272, .T. ) ;
#22813=CARTESIAN_POINT ( 'NONE',  ( 32.73300124599735028, 66.00340565729339914, 97.37344512919882789 ) ) ;
#22814=CARTESIAN_POINT ( 'NONE',  ( 10.93730112725983439, -146.7718404940644916, 36.23586118136483236 ) ) ;
#22816=CARTESIAN_POINT ( 'NONE',  ( 21.16825799904907868, 32.46271504707934241, 131.4851843440076209 ) ) ;
#22817=ORIENTED_EDGE ( 'NONE', *, *, #26959, .T. ) ;
#22818=CARTESIAN_POINT ( 'NONE',  ( 1.894214914920929749, -16.12044375672191165, -144.2521558665609973 ) ) ;
#22819=CARTESIAN_POINT ( 'NONE',  ( 25.81918753295380142, 12.74259626488151476, 112.3053965977761663 ) ) ;
#22822=EDGE_LOOP ( 'NONE', ( #10745, #9454, #5118, #2890 ) ) ;
#22823=B_SPLINE_CURVE_WITH_KNOTS ( 'NONE', 3,
 ( #22586, #20408, #832, #7913 ),
 .UNSPECIFIED., .F., .F.,
 ( 4, 4 ),
 ( 1.055191096010040543E-17, 0.008383560773332703400 ),
 .UNSPECIFIED. ) ;
#22826=CARTESIAN_POINT ( 'NONE',  ( 55.49584447822657296, 72.18163437663950788, -7.317474139114888310 ) ) ;
#22827=CARTESIAN_POINT ( 'NONE',  ( 109.1587776205901861, 0.005978137617721842115, 0.004240403845331894121 ) ) ;
#22828=CARTESIAN_POINT ( 'NONE',  ( 1.833838850093452821, 144.3148362521194485, -15.16810397409632927 ) ) ;
#22829=CARTESIAN_POINT ( 'NONE',  ( 1.833838850093440165, 30.17001957361989994, 141.9387658801232703 ) ) ;
#22830=CARTESIAN_POINT ( 'NONE',  ( 26.11404676487259024, -97.48350837663652158, 57.58742681967414256 ) ) ;
#22831=CARTESIAN_POINT ( 'NONE',  ( 109.1592201516379674, -0.0005146241775907877628, 0.007845213074660000591 ) ) ;
#22832=CARTESIAN_POINT ( 'NONE',  ( 2.433796855181233454, 13.76554153471886366, -144.8571464219887730 ) ) ;
#22833=EDGE_CURVE ( 'NONE', #3159, #182, #11180, .T. ) ;
#22834=CARTESIAN_POINT ( 'NONE',  ( 1.834118845439484335, 59.18411796427052707, 132.4921483272730143 ) ) ;
#22836=CARTESIAN_POINT ( 'NONE',  ( 13.36082413113061307, -137.0038452127796234, -67.94366799842953242 ) ) ;
#22837=DIRECTION ( 'NONE',  ( 0.000000000000000000, 0.000000000000000000, 1.000000000000000000 ) ) ;
#22839=ORIENTED_EDGE ( 'NONE', *, *, #26274, .F. ) ;
#22840=ORIENTED_EDGE ( 'NONE', *, *, #1774, .T. ) ;
#22841=CARTESIAN_POINT ( 'NONE',  ( 109.1592201516379674, -0.006174480289199440856, 0.004867031887019522031 ) ) ;
#22842=LINE ( 'NONE', #656, #1032 ) ;
#22844=EDGE_CURVE ( 'NONE', #2065, #7617, #4953, .T. ) ;
#22845=CARTESIAN_POINT ( 'NONE',  ( 10.93730112725978287, -97.44200844886353252, 115.5857507957700250 ) ) ;
#22846=DIRECTION ( 'NONE',  ( 0.000000000000000000, 0.000000000000000000, 1.000000000000000000 ) ) ;
#22848=EDGE_LOOP ( 'NONE', ( #5876, #23055, #14645, #8028 ) ) ;
#22849=CARTESIAN_POINT ( 'NONE',  ( 55.79472521941428198, -6.880567342320201618, 72.42790650415570042 ) ) ;
#22854=CARTESIAN_POINT ( 'NONE',  ( 2.433796855181205476, -132.3327394885227477, -60.50726454508036056 ) ) ;
#22857=CARTESIAN_POINT ( 'NONE',  ( 32.73300124599739291, -66.00340565729273123, -97.37344512919924000 ) ) ;
#22859=DIRECTION ( 'NONE',  ( 0.5914120900931444380, -0.7693434820005567998, 0.2415416038592884396 ) ) ;
#22860=ORIENTED_EDGE ( 'NONE', *, *, #26478, .F. ) ;
#22861=CARTESIAN_POINT ( 'NONE',  ( 25.64670758986456534, -45.46974729533215509, -103.3508631837548677 ) ) ;
#22862=CARTESIAN_POINT ( 'NONE',  ( 28.37599760073042177, 1.794331790581030983, -114.7183216384031113 ) ) ;
#22863=ORIENTED_EDGE ( 'NONE', *, *, #7736, .T. ) ;
#22866=CARTESIAN_POINT ( 'NONE',  ( 26.11404676487257603, 98.61392875273364211, 55.62948129436280453 ) ) ;
#22867=CARTESIAN_POINT ( 'NONE',  ( 109.1586900883932856, -0.006479576224398268976, 0.002995460350188374095 ) ) ;
#22869=CARTESIAN_POINT ( 'NONE',  ( 26.11404676487257603, -113.2169081140374232, 1.130420376096734847 ) ) ;
#22872=EDGE_CURVE ( 'NONE', #19971, #20059, #9155, .T. ) ;
#22875=CARTESIAN_POINT ( 'NONE',  ( 109.1721716018069657, 0.01706748904932341507, -0.0002019688922673717113 ) ) ;
#22877=ORIENTED_EDGE ( 'NONE', *, *, #3384, .T. ) ;
#22878=ORIENTED_EDGE ( 'NONE', *, *, #19595, .T. ) ;
#22879=ORIENTED_EDGE ( 'NONE', *, *, #20035, .F. ) ;
#22884=CARTESIAN_POINT ( 'NONE',  ( 28.37644542392841629, 46.84227702240779223, 115.1790646972551144 ) ) ;
#22885=B_SPLINE_CURVE_WITH_KNOTS ( 'NONE', 3,
 ( #16378, #20974, #16824, #12071, #14355, #23022, #25173, #1402, #12209, #1260 ),
 .UNSPECIFIED., .F., .F.,
 ( 4, 3, 3, 4 ),
 ( 5.003707553108401214E-17, 0.0002669559177086214242, 0.0005339118354151109816, 0.001067817517169154708 ),
 .UNSPECIFIED. ) ;
#22888=CARTESIAN_POINT ( 'NONE',  ( 25.64681081121879203, 46.30456157731467925, -102.9795863647023850 ) ) ;
#22890=CARTESIAN_POINT ( 'NONE',  ( 8.186469829614440030, 122.8338389144559244, -84.95702201190418634 ) ) ;
#22893=CARTESIAN_POINT ( 'NONE',  ( 5.340103556456469391, -135.6222865117685217, 57.86178752079269572 ) ) ;
#22894=CARTESIAN_POINT ( 'NONE',  ( 28.37603512858451182, 111.8384105897145133, -25.60641750873795175 ) ) ;
#22895=CARTESIAN_POINT ( 'NONE',  ( 28.37599760073041821, -104.0705811520810897, -48.29934869928272434 ) ) ;
#22897=( BOUNDED_SURFACE ( )  B_SPLINE_SURFACE ( 3, 1, ( 
 ( #9461, #3119 ),
 ( #3265, #11899 ),
 ( #2835, #27432 ),
 ( #14177, #5416 ) ),
 .UNSPECIFIED., .F., .F., .F. ) 
 B_SPLINE_SURFACE_WITH_KNOTS ( ( 4, 4 ),
 ( 2, 2 ),
 ( 0.000000000000000000, 1.000000000000000000 ),
 ( 0.000000000000000000, 1.000000000000000000 ),
 .UNSPECIFIED. ) 
 GEOMETRIC_REPRESENTATION_ITEM ( )  RATIONAL_B_SPLINE_SURFACE ( (
 ( 1.000000000000000000, 1.000000000000000000),
 ( 0.9960225298536222738, 0.9999952330161893110),
 ( 0.9960225298536222738, 0.9999952330161893110),
 ( 1.000000000000000000, 1.000000000000000000) ) ) 
 REPRESENTATION_ITEM ( '' )  SURFACE ( )  );
#22900=ORIENTED_EDGE ( 'NONE', *, *, #23257, .T. ) ;
#22901=B_SPLINE_CURVE_WITH_KNOTS ( 'NONE', 3,
 ( #19546, #111, #26305, #11053 ),
 .UNSPECIFIED., .F., .F.,
 ( 4, 4 ),
 ( 0.000000000000000000, 0.008383560773332715543 ),
 .UNSPECIFIED. ) ;
#22902=B_SPLINE_CURVE_WITH_KNOTS ( 'NONE', 3,
 ( #1642, #12854, #27981, #21505, #21647, #21797, #1918 ),
 .UNSPECIFIED., .F., .F.,
 ( 4, 3, 4 ),
 ( 0.000000000000000000, 0.02398743853561384476, 0.04000277880656215312 ),
 .UNSPECIFIED. ) ;
#22903=CARTESIAN_POINT ( 'NONE',  ( 1.833485406944043827, 30.69200235379130959, -141.8265699653863976 ) ) ;
#22904=CARTESIAN_POINT ( 'NONE',  ( 9.884929003653626367, -65.04493172071387619, -135.7578851563892215 ) ) ;
#22905=EDGE_CURVE ( 'NONE', #21696, #14673, #26983, .T. ) ;
#22906=CARTESIAN_POINT ( 'NONE',  ( -90.83090735639699176, 0.000000000000000000, 0.000000000000000000 ) ) ;
#22907=EDGE_CURVE ( 'NONE', #27330, #13865, #9759, .T. ) ;
#22908=CARTESIAN_POINT ( 'NONE',  ( 32.73300124599739291, -66.00340565729273123, -97.37344512919924000 ) ) ;
#22909=CARTESIAN_POINT ( 'NONE',  ( 13.84597867724971287, 20.08297016719580697, -145.3211459389822835 ) ) ;
#22911=CARTESIAN_POINT ( 'NONE',  ( 2.433796855181233454, 84.34988187691088513, -118.5671979538048504 ) ) ;
#22912=ADVANCED_FACE ( 'NONE', ( #24858 ), #25100, .F. ) ;
#22913=CARTESIAN_POINT ( 'NONE',  ( 109.1589550718174877, 0.004900004919104999912, 0.005777059646704606720 ) ) ;
#22914=ORIENTED_EDGE ( 'NONE', *, *, #1726, .F. ) ;
#22916=ORIENTED_EDGE ( 'NONE', *, *, #19891, .F. ) ;
#22919=CARTESIAN_POINT ( 'NONE',  ( 10.93730112725996229, -20.69552240458240888, -149.7554878793151545 ) ) ;
#22920=DIRECTION ( 'NONE',  ( -1.000000000000000000, -0.000000000000000000, -0.000000000000000000 ) ) ;
#22922=CARTESIAN_POINT ( 'NONE',  ( 1.833691583653556334, -138.1170938425794930, 44.50270951807501518 ) ) ;
#22926=B_SPLINE_CURVE_WITH_KNOTS ( 'NONE', 3,
 ( #10911, #1979, #17657, #6317, #15066, #26436 ),
 .UNSPECIFIED., .F., .F.,
 ( 4, 2, 4 ),
 ( 0.000000000000000000, 0.0006311571484586089333, 0.001262314296917217650 ),
 .UNSPECIFIED. ) ;
#22931=VERTEX_POINT ( 'NONE', #13749 ) ;
#22935=ORIENTED_EDGE ( 'NONE', *, *, #5361, .T. ) ;
#22936=EDGE_CURVE ( 'NONE', #309, #10869, #16219, .T. ) ;
#22938=FACE_OUTER_BOUND ( 'NONE', #12167, .T. ) ;
#22939=EDGE_CURVE ( 'NONE', #3393, #4316, #24196, .T. ) ;
#22944=CARTESIAN_POINT ( 'NONE',  ( 32.73300124599732897, 117.3295799645430151, 8.473903470906510194 ) ) ;
#22945=ORIENTED_EDGE ( 'NONE', *, *, #14621, .T. ) ;
#22946=CARTESIAN_POINT ( 'NONE',  ( 8.186469829614388516, 3.468244397269210300, -149.3111477833938352 ) ) ;
#22947=VECTOR ( 'NONE', #25243, 1000.000000000000000 ) ;
#22948=CARTESIAN_POINT ( 'NONE',  ( 10.93730112725990367, -108.9902118373734652, -104.7670965581022671 ) ) ;
#22949=CARTESIAN_POINT ( 'NONE',  ( 1.833485406944043827, -85.72460230293772554, 117.0814567582541201 ) ) ;
#22950=DIRECTION ( 'NONE',  ( 0.000000000000000000, 0.000000000000000000, 1.000000000000000000 ) ) ;
#22951=AXIS2_PLACEMENT_3D ( 'NONE', #17687, #2717, #9197 ) ;
#22953=B_SPLINE_CURVE_WITH_KNOTS ( 'NONE', 3,
 ( #7170, #26996, #11764, #9168 ),
 .UNSPECIFIED., .F., .F.,
 ( 4, 4 ),
 ( 3.628665131031684266E-16, 0.01077107486149801903 ),
 .UNSPECIFIED. ) ;
#22955=DIRECTION ( 'NONE',  ( 0.5914120900931444380, -0.4101107478122166805, 0.6942916636548092102 ) ) ;
#22957=CARTESIAN_POINT ( 'NONE',  ( 1.832998868059858122, 84.86110816369759391, -117.7096351258379485 ) ) ;
#22958=CARTESIAN_POINT ( 'NONE',  ( 1.833206310202334377, -107.3376456496887812, 97.64934828277057477 ) ) ;
#22960=CARTESIAN_POINT ( 'NONE',  ( 109.1778270068192853, 0.008360410075186669801, 0.004106684808172150064 ) ) ;
#22961=VERTEX_POINT ( 'NONE', #7017 ) ;
#22962=CARTESIAN_POINT ( 'NONE',  ( 28.37603512858360233, -22.09615328858523498, 112.5845402829047970 ) ) ;
#22963=CARTESIAN_POINT ( 'NONE',  ( 26.11404676487259024, 103.8885755249569485, 45.01677474591446781 ) ) ;
#22967=EDGE_CURVE ( 'NONE', #16711, #19505, #949, .T. ) ;
#22969=EDGE_CURVE ( 'NONE', #6918, #14537, #24431, .T. ) ;
#22972=ADVANCED_FACE ( 'NONE', ( #369 ), #16263, .F. ) ;
#22974=B_SPLINE_CURVE_WITH_KNOTS ( 'NONE', 3,
 ( #21870, #2126, #24180, #13212, #26458, #22003, #11069, #268, #17679, #22742 ),
 .UNSPECIFIED., .F., .F.,
 ( 4, 3, 3, 4 ),
 ( 5.003707553108401214E-17, 0.0002669559177086480413, 0.0005339118354151201973, 0.001067817517169143433 ),
 .UNSPECIFIED. ) ;
#22975=EDGE_CURVE ( 'NONE', #21026, #9703, #8391, .T. ) ;
#22977=CARTESIAN_POINT ( 'NONE',  ( 10.93730112725932635, 0.000000000000000000, 0.000000000000000000 ) ) ;
#22980=CARTESIAN_POINT ( 'NONE',  ( 1.834118845439484335, 58.85894970554917194, 132.6369225636075839 ) ) ;
#22982=VERTEX_POINT ( 'NONE', #3671 ) ;
#22984=DIRECTION ( 'NONE',  ( -0.5946245182733607137, 0.4701913299128860912, -0.6521823330502943827 ) ) ;
#22985=CARTESIAN_POINT ( 'NONE',  ( 8.186469829614434701, 63.89871393833212920, -134.9918587494107953 ) ) ;
#22986=CARTESIAN_POINT ( 'NONE',  ( 25.65782528836479770, 56.95887699624874756, -97.50004228081002111 ) ) ;
#22988=CARTESIAN_POINT ( 'NONE',  ( 1.893872463202057821, 138.3372034345896679, -43.94661640105876899 ) ) ;
#22990=ORIENTED_EDGE ( 'NONE', *, *, #19472, .T. ) ;
#22991=CARTESIAN_POINT ( 'NONE',  ( 8.186469829614230420, -49.43817854882404106, 140.9315935955037276 ) ) ;
#22992=CARTESIAN_POINT ( 'NONE',  ( 25.69398547355837792, -35.60637981494781457, -107.1830796521258264 ) ) ;
#22993=CARTESIAN_POINT ( 'NONE',  ( 1.833721034905616776, -14.81406766076032078, 144.3516387774751877 ) ) ;
#22995=CARTESIAN_POINT ( 'NONE',  ( 25.64699802086724034, -97.66487797954053462, 56.66140964017699844 ) ) ;
#22996=EDGE_CURVE ( 'NONE', #24138, #7370, #26557, .T. ) ;
#22997=VERTEX_POINT ( 'NONE', #21237 ) ;
#22998=CARTESIAN_POINT ( 'NONE',  ( 10.93730112725932635, 0.000000000000000000, 0.000000000000000000 ) ) ;
#22999=EDGE_CURVE ( 'NONE', #21238, #1868, #20396, .T. ) ;
#23001=CARTESIAN_POINT ( 'NONE',  ( 26.28373643307398311, -60.14387450369918042, 112.4918671811459490 ) ) ;
#23002=ORIENTED_EDGE ( 'NONE', *, *, #1572, .T. ) ;
#23005=B_SPLINE_CURVE_WITH_KNOTS ( 'NONE', 3,
 ( #26309, #6886, #10788, #116 ),
 .UNSPECIFIED., .F., .F.,
 ( 4, 4 ),
 ( 2.416688344895611942E-16, 0.008383748772659726026 ),
 .UNSPECIFIED. ) ;
#23006=CARTESIAN_POINT ( 'NONE',  ( 26.11404676487257603, 110.9778746459749641, -22.43340081644658213 ) ) ;
#23007=CARTESIAN_POINT ( 'NONE',  ( 2.433796855181219243, 132.3327394885239698, -60.50726454507772445 ) ) ;
#23009=ORIENTED_EDGE ( 'NONE', *, *, #21295, .F. ) ;
#23014=ORIENTED_EDGE ( 'NONE', *, *, #23450, .F. ) ;
#23015=VERTEX_POINT ( 'NONE', #5850 ) ;
#23018=CARTESIAN_POINT ( 'NONE',  ( 55.79472521941426777, -72.42790650415579989, 6.880567342319468871 ) ) ;
#23019=CARTESIAN_POINT ( 'NONE',  ( 24.01988960052050359, 103.4492499592085437, 80.44223964539884264 ) ) ;
#23020=CARTESIAN_POINT ( 'NONE',  ( 25.64700659047692355, 12.02873506870318998, -112.2686754657454316 ) ) ;
#23022=CARTESIAN_POINT ( 'NONE',  ( 1.833838850855499913, -132.5281727421681524, -59.10274688031982748 ) ) ;
#23023=CARTESIAN_POINT ( 'NONE',  ( 25.64681081121879203, -83.63051021305953725, 75.86069728268962820 ) ) ;
#23024=CARTESIAN_POINT ( 'NONE',  ( 32.73300124599737160, -117.5726003567929610, 3.836798148478423265 ) ) ;
#23026=CARTESIAN_POINT ( 'NONE',  ( 28.37644542392846247, -116.9383271603242491, -42.25924161794007006 ) ) ;
#23028=CARTESIAN_POINT ( 'NONE',  ( 25.64681081121879203, -66.70335573067929147, 91.10197563707923507 ) ) ;
#23029=DIRECTION ( 'NONE',  ( 0.000000000000000000, 0.000000000000000000, 1.000000000000000000 ) ) ;
#23033=CARTESIAN_POINT ( 'NONE',  ( 26.11404676487257603, -102.9690087468798509, -47.08215554553621729 ) ) ;
#23034=AXIS2_PLACEMENT_3D ( 'NONE', #22541, #26689, #13593 ) ;
#23035=ORIENTED_EDGE ( 'NONE', *, *, #14098, .F. ) ;
#23037=CARTESIAN_POINT ( 'NONE',  ( 26.04756280548353686, -12.93458011762399984, -112.4366864265128783 ) ) ;
#23041=EDGE_CURVE ( 'NONE', #26014, #27008, #20758, .T. ) ;
#23044=EDGE_CURVE ( 'NONE', #24848, #16392, #17993, .T. ) ;
#23047=CARTESIAN_POINT ( 'NONE',  ( 2.108393763691205347, 73.75286979200633652, -125.1820217068188015 ) ) ;
#23048=CIRCLE ( 'NONE', #10617, 117.6351876552689504 ) ;
#23049=CARTESIAN_POINT ( 'NONE',  ( 32.73300124599735739, -51.32617430724984331, 105.8473486001049224 ) ) ;
#23050=CARTESIAN_POINT ( 'NONE',  ( 25.64660436782553177, 97.49251393956843970, -56.95711784271874478 ) ) ;
#23051=CARTESIAN_POINT ( 'NONE',  ( 1.833206308920056538, -144.3905119031281004, 14.42724735286800986 ) ) ;
#23052=VECTOR ( 'NONE', #3129, 1000.000000000000114 ) ;
#23055=ORIENTED_EDGE ( 'NONE', *, *, #16857, .T. ) ;
#23056=VECTOR ( 'NONE', #2665, 1000.000000000000000 ) ;
#23057=ORIENTED_EDGE ( 'NONE', *, *, #28105, .T. ) ;
#23059=CARTESIAN_POINT ( 'NONE',  ( 109.1721716018069657, -0.01281875973824533367, -0.01127028715940098409 ) ) ;
#23062=CARTESIAN_POINT ( 'NONE',  ( 1.831572820252008738, -107.1759352627499595, -97.82994539998490779 ) ) ;
#23064=CARTESIAN_POINT ( 'NONE',  ( 1.833721034905618774, -137.8972080590635017, 45.17977675814267968 ) ) ;
#23065=DIRECTION ( 'NONE',  ( -1.000000000000000000, -0.000000000000000000, -0.000000000000000000 ) ) ;
#23067=CARTESIAN_POINT ( 'NONE',  ( 25.98107933586728535, 84.80123094405293216, -74.88680433646143797 ) ) ;
#23068=CARTESIAN_POINT ( 'NONE',  ( 1.833485406944043827, 15.69895494453577101, -144.2578170162061326 ) ) ;
#23069=DIRECTION ( 'NONE',  ( -1.000000000000000000, -0.000000000000000000, -0.000000000000000000 ) ) ;
#23070=CARTESIAN_POINT ( 'NONE',  ( 109.1586900883932856, 0.004113747440992326053, -0.005833932871491330496 ) ) ;
#23071=EDGE_CURVE ( 'NONE', #17905, #8156, #12156, .T. ) ;
#23072=ORIENTED_EDGE ( 'NONE', *, *, #1076, .F. ) ;
#23074=CARTESIAN_POINT ( 'NONE',  ( 25.70243777736192214, 22.76560620137062330, 110.6300896395617741 ) ) ;
#23075=AXIS2_PLACEMENT_3D ( 'NONE', #27662, #27514, #8239 ) ;
#23078=VECTOR ( 'NONE', #27267, 1000.000000000000000 ) ;
#23083=CONICAL_SURFACE ( 'NONE', #25827, 117.6351876552689504, 0.9945805576725580410 ) ;
#23084=CARTESIAN_POINT ( 'NONE',  ( 25.64700659047696263, -110.3963107228934746, -23.69811251893846560 ) ) ;
#23085=CARTESIAN_POINT ( 'NONE',  ( 28.37644542392840563, -119.4444529625692724, 34.54617949428059376 ) ) ;
#23087=CARTESIAN_POINT ( 'NONE',  ( 2.108985857320863744, -13.91228467251917067, 144.6256801373126564 ) ) ;
#23092=CARTESIAN_POINT ( 'NONE',  ( 25.69398547355839213, -110.3177996916215733, 24.20764173643367556 ) ) ;
#23093=CARTESIAN_POINT ( 'NONE',  ( 21.16825799904904315, -119.4343305756974587, -63.85626241912861900 ) ) ;
#23094=( BOUNDED_SURFACE ( )  B_SPLINE_SURFACE ( 3, 1, ( 
 ( #22262, #2523 ),
 ( #9307, #4971 ),
 ( #16051, #20082 ),
 ( #2971, #11746 ) ),
 .UNSPECIFIED., .F., .F., .F. ) 
 B_SPLINE_SURFACE_WITH_KNOTS ( ( 4, 4 ),
 ( 2, 2 ),
 ( 0.000000000000000000, 1.000000000000000000 ),
 ( 0.000000000000000000, 1.000000000000000000 ),
 .UNSPECIFIED. ) 
 GEOMETRIC_REPRESENTATION_ITEM ( )  RATIONAL_B_SPLINE_SURFACE ( (
 ( 1.000000000000000000, 1.000000000000000000),
 ( 0.9960225298536222738, 0.9999952330161893110),
 ( 0.9960225298536222738, 0.9999952330161893110),
 ( 1.000000000000000000, 1.000000000000000000) ) ) 
 REPRESENTATION_ITEM ( '' )  SURFACE ( )  );
#23095=VECTOR ( 'NONE', #19003, 1000.000000000000227 ) ;
#23096=EDGE_CURVE ( 'NONE', #9151, #22124, #10868, .T. ) ;
#23097=CARTESIAN_POINT ( 'NONE',  ( 6.224689322667630975, 145.3353551538644979, -28.26953958630477004 ) ) ;
#23098=CARTESIAN_POINT ( 'NONE',  ( 8.186469829614354765, -148.1306754360700211, -19.05650981809974098 ) ) ;
#23099=CARTESIAN_POINT ( 'NONE',  ( 13.84597867724974307, 35.16314962060035754, -142.4258194868989449 ) ) ;
#23101=DIRECTION ( 'NONE',  ( -1.000000000000000000, -0.000000000000000000, -0.000000000000000000 ) ) ;
#23102=EDGE_CURVE ( 'NONE', #17407, #22931, #25213, .T. ) ;
#23107=CARTESIAN_POINT ( 'NONE',  ( 2.430230287190589422, 142.0258656395025980, -31.67257033707363689 ) ) ;
#23110=ORIENTED_EDGE ( 'NONE', *, *, #10305, .T. ) ;
#23111=ORIENTED_EDGE ( 'NONE', *, *, #7450, .T. ) ;
#23113=CARTESIAN_POINT ( 'NONE',  ( 1.832998868059890096, -125.9352106559988869, 72.09222286251041112 ) ) ;
#23114=AXIS2_PLACEMENT_3D ( 'NONE', #1669, #6292, #28007 ) ;
#23115=CARTESIAN_POINT ( 'NONE',  ( 109.1589550718175161, 0.006669585340474266412, 0.003591809816099548244 ) ) ;
#23116=CARTESIAN_POINT ( 'NONE',  ( 25.87036335909426299, 107.8283083010004617, 33.99475147239049022 ) ) ;
#23119=CARTESIAN_POINT ( 'NONE',  ( 1.833750490713698111, -58.77746103890191165, -132.6726660571949594 ) ) ;
#23120=CARTESIAN_POINT ( 'NONE',  ( 8.186469829614223315, 27.65107825763956839, 146.7694295239425060 ) ) ;
#23121=CARTESIAN_POINT ( 'NONE',  ( 1.833485406944043827, 59.50871042846404180, -132.3460930279885019 ) ) ;
#23122=CARTESIAN_POINT ( 'NONE',  ( 2.433796855181205476, 57.85512797797890272, 133.5135467655520074 ) ) ;
#23127=AXIS2_PLACEMENT_3D ( 'NONE', #14690, #21458, #15100 ) ;
#23130=CARTESIAN_POINT ( 'NONE',  ( 1.833721034905659630, 85.58110185770094347, 117.1867194831481669 ) ) ;
#23133=CARTESIAN_POINT ( 'NONE',  ( 26.11404676487256893, -92.25884714080449100, 65.63269960453210672 ) ) ;
#23134=ORIENTED_EDGE ( 'NONE', *, *, #27698, .F. ) ;
#23135=VECTOR ( 'NONE', #19240, 1000.000000000000000 ) ;
#23136=VERTEX_POINT ( 'NONE', #26115 ) ;
#23138=AXIS2_PLACEMENT_3D ( 'NONE', #19801, #9023, #22117 ) ;
#23143=CARTESIAN_POINT ( 'NONE',  ( 6.224689322667630975, -145.3353551538643273, 28.26953958630572217 ) ) ;
#23149=ORIENTED_EDGE ( 'NONE', *, *, #25101, .T. ) ;
#23151=CARTESIAN_POINT ( 'NONE',  ( 55.49584447822657296, 71.02133150427273733, -14.82242356767866021 ) ) ;
#23153=AXIS2_PLACEMENT_3D ( 'NONE', #2662, #19943, #22101 ) ;
#23154=CARTESIAN_POINT ( 'NONE',  ( 2.430230287190589422, 57.85706160874325832, -133.5180086894985436 ) ) ;
#23156=LINE ( 'NONE', #16807, #10260 ) ;
#23159=B_SPLINE_CURVE_WITH_KNOTS ( 'NONE', 3,
 ( #15510, #2715, #11488, #272, #26742, #9193 ),
 .UNSPECIFIED., .F., .F.,
 ( 4, 2, 4 ),
 ( 7.372574772901430151E-18, 0.0006311636237756744656, 0.001262327247551341559 ),
 .UNSPECIFIED. ) ;
#23162=CARTESIAN_POINT ( 'NONE',  ( 26.28373643307437391, 97.52903534490830850, 82.21796085350655403 ) ) ;
#23163=CARTESIAN_POINT ( 'NONE',  ( 109.1624594426973118, 0.01476644236456989799, 0.006066618937910955682 ) ) ;
#23164=CARTESIAN_POINT ( 'NONE',  ( 25.64681081121879203, 97.99105938547923245, 56.09509703373377931 ) ) ;
#23165=VERTEX_POINT ( 'NONE', #8800 ) ;
#23167=ORIENTED_EDGE ( 'NONE', *, *, #23720, .F. ) ;
#23168=ORIENTED_EDGE ( 'NONE', *, *, #27400, .T. ) ;
#23171=EDGE_CURVE ( 'NONE', #19971, #7054, #14895, .T. ) ;
#23173=CARTESIAN_POINT ( 'NONE',  ( 5.340103579038339099, 139.5040934216406754, -47.74933483136739198 ) ) ;
#23175=CARTESIAN_POINT ( 'NONE',  ( 2.430230287190589422, -126.7388733285340123, -71.49654683843642999 ) ) ;
#23176=ORIENTED_EDGE ( 'NONE', *, *, #22844, .T. ) ;
#23178=CARTESIAN_POINT ( 'NONE',  ( 16.05277956358202474, -143.2298391883442719, 4.672229451527324606 ) ) ;
#23179=ORIENTED_EDGE ( 'NONE', *, *, #10235, .T. ) ;
#23180=CARTESIAN_POINT ( 'NONE',  ( 32.73300124599740002, -110.6325518752271080, -39.98094346392423404 ) ) ;
#23181=CARTESIAN_POINT ( 'NONE',  ( 32.73300124599739291, -20.69176323058542621, -115.8010721414085538 ) ) ;
#23182=CARTESIAN_POINT ( 'NONE',  ( 109.1592201516379674, -0.007620268632968129653, -0.001934867487012907703 ) ) ;
#23183=EDGE_CURVE ( 'NONE', #26534, #8900, #15744, .T. ) ;
#23184=CARTESIAN_POINT ( 'NONE',  ( 10.93730112725977932, -108.9902118373748863, 104.7670965581006755 ) ) ;
#23185=CARTESIAN_POINT ( 'NONE',  ( 2.433796855181205476, -118.5671979538062146, 84.34988187690890982 ) ) ;
#23188=CARTESIAN_POINT ( 'NONE',  ( 13.84597867724976439, -112.1633818588832554, 94.55652763153787532 ) ) ;
#23189=CARTESIAN_POINT ( 'NONE',  ( 9.884929003653626367, -57.36421526887254885, 139.1775604444702026 ) ) ;
#23190=ORIENTED_EDGE ( 'NONE', *, *, #18564, .T. ) ;
#23193=CARTESIAN_POINT ( 'NONE',  ( 109.1721716018069657, -0.006757465437538680460, 0.01567407524362086566 ) ) ;
#23194=CARTESIAN_POINT ( 'NONE',  ( 25.69398547355838502, -102.8740393624597402, 46.61500694509608422 ) ) ;
#23196=CARTESIAN_POINT ( 'NONE',  ( 1.833750490713699666, 138.0897889879345257, -44.58740205676186008 ) ) ;
#23197=ORIENTED_EDGE ( 'NONE', *, *, #24763, .F. ) ;
#23198=CARTESIAN_POINT ( 'NONE',  ( 1.833721034905634317, 142.0123736691687384, 29.82176961966964512 ) ) ;
#23200=CARTESIAN_POINT ( 'NONE',  ( 25.64681081121880624, -45.54494737132293380, 103.3177883989777825 ) ) ;
#23202=ORIENTED_EDGE ( 'NONE', *, *, #21088, .T. ) ;
#23203=CARTESIAN_POINT ( 'NONE',  ( 1.833485406944043827, -30.69200235379031838, 141.8265699653866250 ) ) ;
#23206=CARTESIAN_POINT ( 'NONE',  ( 30.58324630866347604, -74.24222250960175984, -95.47492154584236346 ) ) ;
#23207=CARTESIAN_POINT ( 'NONE',  ( 2.433796855181233454, 1.451562450949631211, 145.5024947199069913 ) ) ;
#23208=CARTESIAN_POINT ( 'NONE',  ( 109.1592201516379674, 0.007748443302134881173, 0.001331853079201419324 ) ) ;
#23210=LINE ( 'NONE', #7957, #27653 ) ;
#23212=CARTESIAN_POINT ( 'NONE',  ( 24.01988960052069189, 100.1926921796494412, -84.46375358746813333 ) ) ;
#23215=EDGE_CURVE ( 'NONE', #9129, #3533, #6791, .T. ) ;
#23216=EDGE_CURVE ( 'NONE', #12888, #19804, #5995, .T. ) ;
#23217=CARTESIAN_POINT ( 'NONE',  ( 55.79472521941426777, 21.78881894124704388, 69.41463258328519714 ) ) ;
#23218=CARTESIAN_POINT ( 'NONE',  ( 32.73300124599736449, -115.8010721414085253, 20.69176323058589162 ) ) ;
#23219=VERTEX_POINT ( 'NONE', #7084 ) ;
#23224=ORIENTED_EDGE ( 'NONE', *, *, #19743, .T. ) ;
#23226=EDGE_CURVE ( 'NONE', #10266, #9920, #27581, .T. ) ;
#23227=CARTESIAN_POINT ( 'NONE',  ( 55.79472521941426777, 72.75035398477136539, 0.7279028900796241652 ) ) ;
#23228=CARTESIAN_POINT ( 'NONE',  ( 109.1586900883932856, 0.004113747441000917271, 0.005833932871487527982 ) ) ;
#23231=EDGE_CURVE ( 'NONE', #6108, #27587, #5638, .T. ) ;
#23233=ORIENTED_EDGE ( 'NONE', *, *, #17573, .F. ) ;
#23234=CARTESIAN_POINT ( 'NONE',  ( 1.833838850093465700, 132.5643663243757260, 59.02145475724694279 ) ) ;
#23235=CARTESIAN_POINT ( 'NONE',  ( 2.430230287190572103, -107.1617224697457402, -98.44218333480880290 ) ) ;
#23237=CARTESIAN_POINT ( 'NONE',  ( 8.186469829614361871, -140.9315935955035854, -49.43817854882455975 ) ) ;
#23238=CARTESIAN_POINT ( 'NONE',  ( 55.79472521941428198, 66.75682020267529992, 28.92526238350497536 ) ) ;
#23239=CARTESIAN_POINT ( 'NONE',  ( 2.433796855181219243, 142.0211193075555798, 31.67151202413018396 ) ) ;
#23245=VECTOR ( 'NONE', #6745, 1000.000000000000227 ) ;
#23246=ORIENTED_EDGE ( 'NONE', *, *, #6203, .F. ) ;
#23247=CARTESIAN_POINT ( 'NONE',  ( 94.22246935314088034, 90.00000000000005684, -6.938893903907228378E-15 ) ) ;
#23248=ORIENTED_EDGE ( 'NONE', *, *, #10105, .T. ) ;
#23249=CARTESIAN_POINT ( 'NONE',  ( 1.833206310202322387, -15.90849712171641883, -144.2348262833783394 ) ) ;
#23250=CARTESIAN_POINT ( 'NONE',  ( 30.59138290137870797, 107.2355347544032469, 44.78723476287341043 ) ) ;
#23252=VERTEX_POINT ( 'NONE', #16123 ) ;
#23253=ORIENTED_EDGE ( 'NONE', *, *, #12197, .T. ) ;
#23254=B_SPLINE_CURVE_WITH_KNOTS ( 'NONE', 3,
 ( #7417, #22390, #2955, #14018, #926, #2656, #22829, #18191, #18487, #11299 ),
 .UNSPECIFIED., .F., .F.,
 ( 4, 3, 3, 4 ),
 ( 3.816391647148975608E-17, 0.0002669559177086169789, 0.0005339118354150987301, 0.001067817517169160346 ),
 .UNSPECIFIED. ) ;
#23256=B_SPLINE_CURVE_WITH_KNOTS ( 'NONE', 3,
 ( #13999, #20483, #6979, #13859 ),
 .UNSPECIFIED., .F., .F.,
 ( 4, 4 ),
 ( 1.040834085586084257E-17, 0.008383560773332703400 ),
 .UNSPECIFIED. ) ;
#23257=EDGE_CURVE ( 'NONE', #21489, #25711, #22458, .T. ) ;
#23259=CARTESIAN_POINT ( 'NONE',  ( 13.84597867724968445, -146.6243035057531756, -4.782757490007365497 ) ) ;
#23260=EDGE_CURVE ( 'NONE', #28132, #7273, #11125, .T. ) ;
#23261=CARTESIAN_POINT ( 'NONE',  ( 109.1721716018069657, 0.007126480965770705736, 0.01550977894512768802 ) ) ;
#23265=CARTESIAN_POINT ( 'NONE',  ( 1.833691583653597634, 132.7086741139089838, -58.69608658929788447 ) ) ;
#23267=VERTEX_POINT ( 'NONE', #13380 ) ;
#23268=CARTESIAN_POINT ( 'NONE',  ( 1.831572820252008738, 0.9871191512934829326, -145.1082523917586968 ) ) ;
#23272=CARTESIAN_POINT ( 'NONE',  ( 109.1592201516379674, -0.004194960840980736620, 0.006649399203953376171 ) ) ;
#23275=CARTESIAN_POINT ( 'NONE',  ( 1.833485406944057594, -58.53321471326971448, 132.7804117027886548 ) ) ;
#23276=CARTESIAN_POINT ( 'NONE',  ( 1.833603222531955179, -15.61050054119129094, 144.2675221341993677 ) ) ;
#23278=DIRECTION ( 'NONE',  ( -0.5914120900931443270, 0.2567974902965093342, 0.7643865440136115019 ) ) ;
#23280=ORIENTED_EDGE ( 'NONE', *, *, #25438, .F. ) ;
#23284=FACE_OUTER_BOUND ( 'NONE', #24063, .T. ) ;
#23286=B_SPLINE_CURVE_WITH_KNOTS ( 'NONE', 3,
 ( #12982, #21622, #14866, #21912, #3793, #2169, #21773 ),
 .UNSPECIFIED., .F., .F.,
 ( 4, 3, 4 ),
 ( 5.818982450679147801E-16, 0.02816610861753245446, 0.04000277880656277762 ),
 .UNSPECIFIED. ) ;
#23290=CARTESIAN_POINT ( 'NONE',  ( 32.73300124599735739, 55.46353551262010484, 103.7392577722178260 ) ) ;
#23291=CARTESIAN_POINT ( 'NONE',  ( 1.833838850093517214, 1.355257560975019971E-17, -145.1097630783160923 ) ) ;
#23293=EDGE_LOOP ( 'NONE', ( #6071, #26520, #6776, #6954 ) ) ;
#23294=ADVANCED_FACE ( 'NONE', ( #3176 ), #20287, .F. ) ;
#23296=CARTESIAN_POINT ( 'NONE',  ( 10.93730112725990011, -150.7858122213662000, -10.89264110825150489 ) ) ;
#23298=CARTESIAN_POINT ( 'NONE',  ( 25.98107933586724272, -102.9042679418245854, -47.01057192495372306 ) ) ;
#23299=VERTEX_POINT ( 'NONE', #21302 ) ;
#23304=CARTESIAN_POINT ( 'NONE',  ( 2.430230287190589422, 144.5585181921888420, -16.65331920325590431 ) ) ;
#23305=CARTESIAN_POINT ( 'NONE',  ( 109.1589550718175161, 0.007359857714025723127, -0.001793588804100419752 ) ) ;
#23306=CARTESIAN_POINT ( 'NONE',  ( 2.433796855181233454, -60.50726454507816499, -132.3327394885237425 ) ) ;
#23307=CARTESIAN_POINT ( 'NONE',  ( 109.1587776205901577, 0.004842060007774048359, 0.005502145856754178839 ) ) ;
#23308=DIRECTION ( 'NONE',  ( 0.5914120900931444380, 0.3352908775637205574, -0.7333565075147343570 ) ) ;
#23311=EDGE_LOOP ( 'NONE', ( #24419, #9745, #23110, #6809 ) ) ;
#23312=CARTESIAN_POINT ( 'NONE',  ( 6.224689322667630975, 136.2818611715198642, -57.86870174583292226 ) ) ;
#23313=CARTESIAN_POINT ( 'NONE',  ( 19.66333377628710366, -24.23123354948742048, -135.6014041990444809 ) ) ;
#23317=CARTESIAN_POINT ( 'NONE',  ( 5.340103579038194326, -108.0219267094752809, 100.3626145943030963 ) ) ;
#23319=CARTESIAN_POINT ( 'NONE',  ( 32.73300124599739291, -105.8473486001047235, -51.32617430725011332 ) ) ;
#23321=B_SPLINE_CURVE_WITH_KNOTS ( 'NONE', 3,
 ( #25614, #1269, #22893, #12079 ),
 .UNSPECIFIED., .F., .F.,
 ( 4, 4 ),
 ( 0.000000000000000000, 0.01077107196513859763 ),
 .UNSPECIFIED. ) ;
#23322=CARTESIAN_POINT ( 'NONE',  ( 24.01988960052061728, -31.41104197353406491, 127.2243989116373086 ) ) ;
#23323=CARTESIAN_POINT ( 'NONE',  ( 2.433796855181233454, 118.5671979538056888, 84.34988187690970562 ) ) ;
#23324=CARTESIAN_POINT ( 'NONE',  ( 6.224689322667647851, 118.2566963816783101, -89.08920297664090526 ) ) ;
#23325=ORIENTED_EDGE ( 'NONE', *, *, #21129, .T. ) ;
#23329=EDGE_CURVE ( 'NONE', #7408, #8318, #15536, .T. ) ;
#23330=CARTESIAN_POINT ( 'NONE',  ( 6.224689322667630975, 126.9212313063844562, 76.23997225729313243 ) ) ;
#23334=VECTOR ( 'NONE', #21994, 1000.000000000000227 ) ;
#23336=CARTESIAN_POINT ( 'NONE',  ( 1.833485406944057594, 142.0485807715645876, 29.64752363041592531 ) ) ;
#23338=CARTESIAN_POINT ( 'NONE',  ( 1.833485406944043827, -59.50871042846314651, 132.3460930279889567 ) ) ;
#23340=CARTESIAN_POINT ( 'NONE',  ( 10.93730112725982195, -145.2260730187404079, 42.00474393596209666 ) ) ;
#23343=CARTESIAN_POINT ( 'NONE',  ( 1.832998868059890096, -14.63705790013914054, -144.3700883710218648 ) ) ;
#23345=DIRECTION ( 'NONE',  ( 0.5946245182733607137, -0.5401723099040960374, 0.5955128528260720255 ) ) ;
#23346=CARTESIAN_POINT ( 'NONE',  ( 30.59141879584314694, 26.79785525806573432, -113.0806649571965323 ) ) ;
#23347=CARTESIAN_POINT ( 'NONE',  ( 26.04756280548352620, -92.21166514879054432, -65.62256188141817859 ) ) ;
#23349=LINE ( 'NONE', #3599, #4196 ) ;
#23350=ORIENTED_EDGE ( 'NONE', *, *, #11966, .T. ) ;
#23351=CARTESIAN_POINT ( 'NONE',  ( 109.1586900883932856, -0.006130969560687385411, 0.003656351050331833278 ) ) ;
#23352=CARTESIAN_POINT ( 'NONE',  ( 109.1592201516379674, -0.007376275279030860763, -0.002720803050361382969 ) ) ;
#23353=( BOUNDED_SURFACE ( )  B_SPLINE_SURFACE ( 3, 1, ( 
 ( #13210, #8764 ),
 ( #26047, #6336 ),
 ( #28329, #17119 ),
 ( #17392, #4159 ) ),
 .UNSPECIFIED., .F., .F., .F. ) 
 B_SPLINE_SURFACE_WITH_KNOTS ( ( 4, 4 ),
 ( 2, 2 ),
 ( 0.000000000000000000, 1.000000000000000000 ),
 ( 0.000000000000000000, 1.000000000000000000 ),
 .UNSPECIFIED. ) 
 GEOMETRIC_REPRESENTATION_ITEM ( )  RATIONAL_B_SPLINE_SURFACE ( (
 ( 1.000000000000000000, 1.000000000000000000),
 ( 0.9960225298536222738, 0.9999952330161893110),
 ( 0.9960225298536222738, 0.9999952330161893110),
 ( 1.000000000000000000, 1.000000000000000000) ) ) 
 REPRESENTATION_ITEM ( '' )  SURFACE ( )  );
#23354=CARTESIAN_POINT ( 'NONE',  ( 26.11404676487257603, -74.91683232331033082, 84.89295829319468112 ) ) ;
#23356=DIRECTION ( 'NONE',  ( 0.000000000000000000, -1.000000000000000000, 0.000000000000000000 ) ) ;
#23357=CARTESIAN_POINT ( 'NONE',  ( 109.1586900883932856, 0.001385221016527459588, -0.007002774699553642249 ) ) ;
#23358=ORIENTED_EDGE ( 'NONE', *, *, #24311, .F. ) ;
#23359=CARTESIAN_POINT ( 'NONE',  ( 26.11404676487257603, -57.58742681967381571, -97.48350837663670632 ) ) ;
#23360=CARTESIAN_POINT ( 'NONE',  ( 55.49584447822657296, -72.55110015779771970, -0.2676470673964289615 ) ) ;
#23362=EDGE_LOOP ( 'NONE', ( #27634, #1370, #17397, #6844 ) ) ;
#23363=VERTEX_POINT ( 'NONE', #14100 ) ;
#23365=CARTESIAN_POINT ( 'NONE',  ( 25.64704443564078318, -110.4160069635932331, -23.60610532597069877 ) ) ;
#23367=EDGE_CURVE ( 'NONE', #1868, #17200, #8675, .T. ) ;
#23368=CARTESIAN_POINT ( 'NONE',  ( 1.831572820252008738, -58.11906524360392012, -132.9644823688601321 ) ) ;
#23369=EDGE_CURVE ( 'NONE', #9124, #21691, #3522, .T. ) ;
#23370=B_SPLINE_CURVE_WITH_KNOTS ( 'NONE', 3,
 ( #3350, #23237, #22804, #9988 ),
 .UNSPECIFIED., .F., .F.,
 ( 4, 4 ),
 ( 0.000000000000000000, 0.01077107196513872600 ),
 .UNSPECIFIED. ) ;
#23371=CARTESIAN_POINT ( 'NONE',  ( 6.224689322667647851, -2.565137105442716781, -148.0369967195763081 ) ) ;
#23375=CARTESIAN_POINT ( 'NONE',  ( 32.73300124599735739, 39.98094346392311138, 110.6325518752275485 ) ) ;
#23376=CARTESIAN_POINT ( 'NONE',  ( 10.93730112725972425, -79.81734490845995822, 128.3908183996588264 ) ) ;
#23378=CARTESIAN_POINT ( 'NONE',  ( 2.433796855181219243, -145.5024947199069913, 1.451562450949123395 ) ) ;
#23379=DIRECTION ( 'NONE',  ( -1.000000000000000000, -0.000000000000000000, -0.000000000000000000 ) ) ;
#23380=CARTESIAN_POINT ( 'NONE',  ( 6.224689322667630975, -146.9579047224768260, -18.02516478984294324 ) ) ;
#23381=FACE_OUTER_BOUND ( 'NONE', #18968, .T. ) ;
#23382=CARTESIAN_POINT ( 'NONE',  ( 24.01988960052057465, 130.7041393974935772, -9.440825210282081770 ) ) ;
#23385=ORIENTED_EDGE ( 'NONE', *, *, #1369, .F. ) ;
#23386=CARTESIAN_POINT ( 'NONE',  ( 30.59138290137879324, -21.51300488027205660, 114.2039707400270885 ) ) ;
#23390=PRODUCT_DEFINITION ( 'UNKNOWN', '', #21775, #11698 ) ;
#23392=ORIENTED_EDGE ( 'NONE', *, *, #3759, .T. ) ;
#23398=CARTESIAN_POINT ( 'NONE',  ( 8.186469829614464899, 146.7694295239429607, -27.65107825763805849 ) ) ;
#23399=CARTESIAN_POINT ( 'NONE',  ( 109.1586900883932856, -0.001582822706032874097, -0.006960773163852184385 ) ) ;
#23401=CARTESIAN_POINT ( 'NONE',  ( 1.833838850855474600, 132.6005571022087395, -58.94016894581336885 ) ) ;
#23402=EDGE_LOOP ( 'NONE', ( #18839, #17787, #15189, #11045 ) ) ;
#23404=DIRECTION ( 'NONE',  ( 0.000000000000000000, 0.000000000000000000, 1.000000000000000000 ) ) ;
#23406=CARTESIAN_POINT ( 'NONE',  ( 9.884929003653626367, -128.2151425008046886, 78.87917189084865299 ) ) ;
#23407=CARTESIAN_POINT ( 'NONE',  ( 10.93730112725932635, 0.000000000000000000, 0.000000000000000000 ) ) ;
#23408=CARTESIAN_POINT ( 'NONE',  ( 1.833485406944043827, -72.09189602597619739, -125.9346397303442728 ) ) ;
#23409=EDGE_LOOP ( 'NONE', ( #8304, #12521, #23816, #7604 ) ) ;
#23411=FACE_OUTER_BOUND ( 'NONE', #12653, .T. ) ;
#23412=CARTESIAN_POINT ( 'NONE',  ( 28.43349137099854929, 122.3147591366313947, 21.85613782299017416 ) ) ;
#23413=ORIENTED_EDGE ( 'NONE', *, *, #27558, .T. ) ;
#23415=CARTESIAN_POINT ( 'NONE',  ( 2.063896406836605024, -125.1295119249434009, -73.79559738457884066 ) ) ;
#23417=ORIENTED_EDGE ( 'NONE', *, *, #12117, .F. ) ;
#23421=CARTESIAN_POINT ( 'NONE',  ( 1.833750490713699444, 96.89879583303846289, 108.0159692407134031 ) ) ;
#23422=( BOUNDED_SURFACE ( )  B_SPLINE_SURFACE ( 3, 1, ( 
 ( #22960, #5674 ),
 ( #27681, #3498 ),
 ( #1338, #12282 ),
 ( #21048, #10141 ) ),
 .UNSPECIFIED., .F., .F., .F. ) 
 B_SPLINE_SURFACE_WITH_KNOTS ( ( 4, 4 ),
 ( 2, 2 ),
 ( 0.000000000000000000, 1.000000000000000000 ),
 ( 0.000000000000000000, 1.000000000000000000 ),
 .UNSPECIFIED. ) 
 GEOMETRIC_REPRESENTATION_ITEM ( )  RATIONAL_B_SPLINE_SURFACE ( (
 ( 1.000000000000000000, 1.000000000000000000),
 ( 0.6386103224230316178, 0.9954351624131538845),
 ( 0.6386103224230316178, 0.9954351624131538845),
 ( 1.000000000000000000, 1.000000000000000000) ) ) 
 REPRESENTATION_ITEM ( '' )  SURFACE ( )  );
#23423=ORIENTED_EDGE ( 'NONE', *, *, #25410, .F. ) ;
#23424=FACE_OUTER_BOUND ( 'NONE', #26419, .T. ) ;
#23426=DIRECTION ( 'NONE',  ( -0.5914120900931443270, 0.4674599267565434091, -0.6570486713847197846 ) ) ;
#23428=CARTESIAN_POINT ( 'NONE',  ( 109.1624594426973118, -0.009754804742280876254, -0.01263706729759555072 ) ) ;
#23429=CARTESIAN_POINT ( 'NONE',  ( 13.84597867724978570, 137.9700459519987703, 49.85807424839799040 ) ) ;
#23431=CARTESIAN_POINT ( 'NONE',  ( 25.64699802086724745, -97.90265915239990591, -56.24956056770124491 ) ) ;
#23432=CARTESIAN_POINT ( 'NONE',  ( 6.224689322667647851, -139.9988794244335679, 48.18553814189983342 ) ) ;
#23436=EDGE_LOOP ( 'NONE', ( #12988, #10217, #12765, #22914 ) ) ;
#23438=CARTESIAN_POINT ( 'NONE',  ( 13.84597867724998999, 82.31427113894766023, 121.4327876424614772 ) ) ;
#23439=CARTESIAN_POINT ( 'NONE',  ( 55.49584447822657296, -62.69727227546427173, 36.50733923851176144 ) ) ;
#23440=CARTESIAN_POINT ( 'NONE',  ( 25.70243777736189017, -98.18050844655108733, 55.83795591307098505 ) ) ;
#23442=LINE ( 'NONE', #9919, #5643 ) ;
#23443=VERTEX_POINT ( 'NONE', #6065 ) ;
#23447=CARTESIAN_POINT ( 'NONE',  ( 1.894214914920993698, -0.9536781033349790437, -145.1469726764543964 ) ) ;
#23448=CARTESIAN_POINT ( 'NONE',  ( 25.64704443564080094, -112.3065506427462168, 11.66968230815876950 ) ) ;
#23449=CARTESIAN_POINT ( 'NONE',  ( 109.1778270068192853, 0.003210287141656879405, -0.008743876326153473405 ) ) ;
#23450=EDGE_CURVE ( 'NONE', #7920, #20945, #23904, .T. ) ;
#23451=CARTESIAN_POINT ( 'NONE',  ( 13.36082413113063083, 97.52406103376918622, -117.7941133658628559 ) ) ;
#23453=CARTESIAN_POINT ( 'NONE',  ( 25.65782528836479770, -110.5695798068304896, 22.91156770660766284 ) ) ;
#23456=ORIENTED_EDGE ( 'NONE', *, *, #2831, .F. ) ;
#23457=CARTESIAN_POINT ( 'NONE',  ( 6.224689322667647851, 12.92299475787155316, -147.4941644018826992 ) ) ;
#23458=EDGE_CURVE ( 'NONE', #1490, #22412, #28054, .T. ) ;
#23460=FACE_OUTER_BOUND ( 'NONE', #5965, .T. ) ;
#23461=B_SPLINE_CURVE_WITH_KNOTS ( 'NONE', 3,
 ( #2132, #28337, #15095, #8774, #6074, #11075, #28202, #8503, #4168, #26325 ),
 .UNSPECIFIED., .F., .F.,
 ( 4, 3, 3, 4 ),
 ( 6.938893903907228378E-18, 0.0002669560319015663462, 0.0005492286108966397190, 0.0008315040496093490177 ),
 .UNSPECIFIED. ) ;
#23462=EDGE_LOOP ( 'NONE', ( #22221, #21651, #22197, #23417 ) ) ;
#23463=CARTESIAN_POINT ( 'NONE',  ( 1.833485406944043827, 117.0814567582544612, 85.72460230293732764 ) ) ;
#23464=ORIENTED_EDGE ( 'NONE', *, *, #19363, .T. ) ;
#23467=CARTESIAN_POINT ( 'NONE',  ( 1.832998868059858122, -73.01698022778271024, -125.4013017422238363 ) ) ;
#23470=CARTESIAN_POINT ( 'NONE',  ( 32.73300124599739291, 55.46353551262154014, -103.7392577722169875 ) ) ;
#23471=CARTESIAN_POINT ( 'NONE',  ( 30.59138290137882521, -55.75105126023986912, 101.9665464510085400 ) ) ;
#23474=CARTESIAN_POINT ( 'NONE',  ( 25.69398547355838858, -75.02007992711763507, 84.42756928260550353 ) ) ;
#23475=CARTESIAN_POINT ( 'NONE',  ( 25.64692872815576052, 35.19724814978057026, -107.2850779876530822 ) ) ;
#23476=ORIENTED_EDGE ( 'NONE', *, *, #9535, .F. ) ;
#23477=VERTEX_POINT ( 'NONE', #17533 ) ;
#23478=CARTESIAN_POINT ( 'NONE',  ( 13.36082413113063083, 56.35051087435157058, -142.1654513177082606 ) ) ;
#23480=CARTESIAN_POINT ( 'NONE',  ( 1.834118845439484335, 132.6369225636082376, -58.85894970554785743 ) ) ;
#23481=CONICAL_SURFACE ( 'NONE', #23034, 117.6351876552689504, 0.9945805576725580410 ) ;
#23482=CARTESIAN_POINT ( 'NONE',  ( 1.893872463202030731, 144.2520230501565948, 16.11957794552817802 ) ) ;
#23484=LINE ( 'NONE', #10800, #22230 ) ;
#23486=ORIENTED_EDGE ( 'NONE', *, *, #23914, .F. ) ;
#23487=CARTESIAN_POINT ( 'NONE',  ( 1.832998868059858122, 107.4798986104872967, -97.49378069860692619 ) ) ;
#23489=EDGE_CURVE ( 'NONE', #21261, #7427, #19281, .T. ) ;
#23490=B_SPLINE_CURVE_WITH_KNOTS ( 'NONE', 3,
 ( #27074, #14671, #26939, #27784, #7384, #23474, #22800, #10381 ),
 .UNSPECIFIED., .F., .F.,
 ( 4, 2, 2, 4 ),
 ( 0.000000000000000000, 0.0002429592666046789557, 0.0004859185332093579114, 0.0009718370664186629137 ),
 .UNSPECIFIED. ) ;
#23491=EDGE_CURVE ( 'NONE', #5899, #17261, #13822, .T. ) ;
#23492=CARTESIAN_POINT ( 'NONE',  ( 25.69398547355840634, 0.7422864227365167933, 112.9401428107247511 ) ) ;
#23493=CARTESIAN_POINT ( 'NONE',  ( 25.64707127832795663, 0.04449220797125042620, -112.9112343549835487 ) ) ;
#23495=CARTESIAN_POINT ( 'NONE',  ( 25.64700659047694131, -46.13293552475862214, 103.0567718204600709 ) ) ;
#23496=EDGE_CURVE ( 'NONE', #18704, #25954, #6335, .T. ) ;
#23498=VERTEX_POINT ( 'NONE', #10513 ) ;
#23500=ORIENTED_EDGE ( 'NONE', *, *, #7445, .F. ) ;
#23501=ORIENTED_EDGE ( 'NONE', *, *, #14422, .F. ) ;
#23503=AXIS2_PLACEMENT_3D ( 'NONE', #349, #19544, #12776 ) ;
#23504=CARTESIAN_POINT ( 'NONE',  ( 2.108393763691202238, 28.95405853987516664, 142.3786741588520499 ) ) ;
#23506=AXIS2_PLACEMENT_3D ( 'NONE', #27372, #16999, #25224 ) ;
#23507=B_SPLINE_CURVE_WITH_KNOTS ( 'NONE', 3,
 ( #15349, #19813, #10910, #1831 ),
 .UNSPECIFIED., .F., .F.,
 ( 4, 4 ),
 ( 4.443059973708341306E-17, 0.008383748772659519594 ),
 .UNSPECIFIED. ) ;
#23508=DIRECTION ( 'NONE',  ( -1.000000000000000000, -0.000000000000000000, -0.000000000000000000 ) ) ;
#23509=( BOUNDED_SURFACE ( )  B_SPLINE_SURFACE ( 3, 1, ( 
 ( #7061, #25184 ),
 ( #7486, #9788 ),
 ( #22453, #24768 ),
 ( #13794, #7337 ) ),
 .UNSPECIFIED., .F., .F., .F. ) 
 B_SPLINE_SURFACE_WITH_KNOTS ( ( 4, 4 ),
 ( 2, 2 ),
 ( 0.000000000000000000, 1.000000000000000000 ),
 ( 0.000000000000000000, 1.000000000000000000 ),
 .UNSPECIFIED. ) 
 GEOMETRIC_REPRESENTATION_ITEM ( )  RATIONAL_B_SPLINE_SURFACE ( (
 ( 1.000000000000000000, 1.000000000000000000),
 ( 0.9960225298536222738, 0.9999952330161893110),
 ( 0.9960225298536222738, 0.9999952330161893110),
 ( 1.000000000000000000, 1.000000000000000000) ) ) 
 REPRESENTATION_ITEM ( '' )  SURFACE ( )  );
#23510=VERTEX_POINT ( 'NONE', #17118 ) ;
#23511=CARTESIAN_POINT ( 'NONE',  ( 109.1721716018069515, 0.01695288006056418911, 0.001984900887706716240 ) ) ;
#23512=CARTESIAN_POINT ( 'NONE',  ( 26.11404676487257603, -24.64483677384923865, 110.5078194225160360 ) ) ;
#23514=CARTESIAN_POINT ( 'NONE',  ( 109.1586059443104944, -0.006971743774739767863, -0.001198897580738971869 ) ) ;
#23515=CARTESIAN_POINT ( 'NONE',  ( 9.884929003653626367, 50.49804566712126075, 141.8132360130359757 ) ) ;
#23517=B_SPLINE_CURVE_WITH_KNOTS ( 'NONE', 3,
 ( #17955, #7055, #15814, #12486 ),
 .UNSPECIFIED., .F., .F.,
 ( 4, 4 ),
 ( 3.428463280104494194E-16, 0.01077107486149824628 ),
 .UNSPECIFIED. ) ;
#23518=CARTESIAN_POINT ( 'NONE',  ( 109.1589550718175161, -0.0005685167901217975548, 0.007553890059316982486 ) ) ;
#23522=CARTESIAN_POINT ( 'NONE',  ( 8.186469777910977186, 127.5731248346298514, -77.65916160569786086 ) ) ;
#23524=CARTESIAN_POINT ( 'NONE',  ( 1.832998868059858122, 73.01698022778357711, 125.4013017422233247 ) ) ;
#23525=CARTESIAN_POINT ( 'NONE',  ( 10.93730112725990189, -148.8212007290660495, -26.59437931460901439 ) ) ;
#23528=ORIENTED_EDGE ( 'NONE', *, *, #25442, .T. ) ;
#23529=CARTESIAN_POINT ( 'NONE',  ( 10.93730112725969938, 79.81734490845904872, 128.3908183996593948 ) ) ;
#23530=EDGE_CURVE ( 'NONE', #26730, #20281, #2498, .T. ) ;
#23531=CARTESIAN_POINT ( 'NONE',  ( 32.73300124599732186, 0.000000000000000000, 0.000000000000000000 ) ) ;
#23532=ORIENTED_EDGE ( 'NONE', *, *, #14319, .T. ) ;
#23533=ORIENTED_EDGE ( 'NONE', *, *, #1473, .T. ) ;
#23536=AXIS2_PLACEMENT_3D ( 'NONE', #10780, #4283, #13484 ) ;
#23540=CARTESIAN_POINT ( 'NONE',  ( 55.79472521941428198, -63.36760613016198818, -35.74479459808913617 ) ) ;
#23541=DIRECTION ( 'NONE',  ( 0.7071067811865485719, 0.000000000000000000, 0.7071067811865465735 ) ) ;
#23542=CARTESIAN_POINT ( 'NONE',  ( 1.833485406944057594, -117.7091014914944225, -84.86072343962690923 ) ) ;
#23543=ORIENTED_EDGE ( 'NONE', *, *, #9975, .F. ) ;
#23545=VERTEX_POINT ( 'NONE', #8917 ) ;
#23547=CARTESIAN_POINT ( 'NONE',  ( 1.832998868059890096, -30.69214149073911457, -141.8272129421612249 ) ) ;
#23550=CARTESIAN_POINT ( 'NONE',  ( 25.64704443564079384, -103.0951670221011511, -46.04703398841390793 ) ) ;
#23551=CARTESIAN_POINT ( 'NONE',  ( 55.49584447822657296, -7.849835876628820763, 72.12568090333340365 ) ) ;
#23552=CARTESIAN_POINT ( 'NONE',  ( 25.65782528836480125, 91.69136324939191240, -65.90345832277380111 ) ) ;
#23554=CARTESIAN_POINT ( 'NONE',  ( 2.263178607246734142, 137.8402782326817260, -46.26071628252303469 ) ) ;
#23555=CARTESIAN_POINT ( 'NONE',  ( 2.263178113027036975, -144.4462808674009295, -16.59120315151724867 ) ) ;
#23557=CARTESIAN_POINT ( 'NONE',  ( 1.833750490713699444, -15.43355859895757298, 144.2866297127913242 ) ) ;
#23558=ORIENTED_EDGE ( 'NONE', *, *, #22711, .T. ) ;
#23559=B_SPLINE_CURVE_WITH_KNOTS ( 'NONE', 3,
 ( #20537, #17935, #9605, #25028, #20828, #27738, #7899 ),
 .UNSPECIFIED., .F., .F.,
 ( 4, 3, 4 ),
 ( 0.000000000000000000, 0.02398743853561352210, 0.04000277880656211149 ),
 .UNSPECIFIED. ) ;
#23560=ORIENTED_EDGE ( 'NONE', *, *, #2222, .T. ) ;
#23563=AXIS2_PLACEMENT_3D ( 'NONE', #20479, #24684, #2330 ) ;
#23564=( BOUNDED_SURFACE ( )  B_SPLINE_SURFACE ( 3, 1, ( 
 ( #18735, #27507 ),
 ( #3472, #1312 ),
 ( #10112, #18877 ),
 ( #27651, #16732 ) ),
 .UNSPECIFIED., .F., .F., .F. ) 
 B_SPLINE_SURFACE_WITH_KNOTS ( ( 4, 4 ),
 ( 2, 2 ),
 ( 0.000000000000000000, 1.000000000000000000 ),
 ( 0.000000000000000000, 1.000000000000000000 ),
 .UNSPECIFIED. ) 
 GEOMETRIC_REPRESENTATION_ITEM ( )  RATIONAL_B_SPLINE_SURFACE ( (
 ( 1.000000000000000000, 1.000000000000000000),
 ( 0.9956975270656954757, 0.8568959468854893125),
 ( 0.9956975270656954757, 0.8568959468854893125),
 ( 1.000000000000000000, 1.000000000000000000) ) ) 
 REPRESENTATION_ITEM ( '' )  SURFACE ( )  );
#23565=ORIENTED_EDGE ( 'NONE', *, *, #13369, .T. ) ;
#23566=AXIS2_PLACEMENT_3D ( 'NONE', #25530, #27666, #12685 ) ;
#23568=ADVANCED_FACE ( 'NONE', ( #19980 ), #12560, .F. ) ;
#23569=EDGE_CURVE ( 'NONE', #9601, #8709, #16085, .T. ) ;
#23570=CARTESIAN_POINT ( 'NONE',  ( 26.28373643307403640, 100.6987277884695260, -78.30371666786294327 ) ) ;
#23571=VERTEX_POINT ( 'NONE', #15641 ) ;
#23572=CARTESIAN_POINT ( 'NONE',  ( 28.43349137099828994, -58.58376153369790984, 109.5743306972606064 ) ) ;
#23573=CARTESIAN_POINT ( 'NONE',  ( 1.894214914920948845, -73.39939580274850073, -125.2241265685477885 ) ) ;
#23574=EDGE_CURVE ( 'NONE', #1087, #16492, #403, .T. ) ;
#23575=CARTESIAN_POINT ( 'NONE',  ( 109.1592201516379674, -0.003476928926134757649, -0.007051465909552751508 ) ) ;
#23577=CARTESIAN_POINT ( 'NONE',  ( 26.28373643307435614, 112.4918671811455511, 60.14387450369848409 ) ) ;
#23578=DIRECTION ( 'NONE',  ( 0.5946245182733608248, -0.4045541647807529007, 0.6948076064830616128 ) ) ;
#23579=CARTESIAN_POINT ( 'NONE',  ( 1.833691583653525026, -107.5990239011820364, -97.36155720551585091 ) ) ;
#23581=CONICAL_SURFACE ( 'NONE', #23563, 117.6351876552689504, 0.9945805576725580410 ) ;
#23582=EDGE_CURVE ( 'NONE', #1068, #19971, #27221, .T. ) ;
#23584=CARTESIAN_POINT ( 'NONE',  ( 25.64704443564077252, -97.71717520928642386, -56.57116289738710435 ) ) ;
#23585=CARTESIAN_POINT ( 'NONE',  ( 2.063896406836605024, -31.51663808384653720, 141.8093313989359956 ) ) ;
#23586=CARTESIAN_POINT ( 'NONE',  ( 32.73300124599740002, 62.10906484417377271, -99.90245962373766986 ) ) ;
#23587=CIRCLE ( 'NONE', #8860, 117.6351876552689504 ) ;
#23588=VERTEX_POINT ( 'NONE', #13499 ) ;
#23591=CARTESIAN_POINT ( 'NONE',  ( 55.49584447822657296, -7.849835876627842879, -72.12568090333350312 ) ) ;
#23592=LINE ( 'NONE', #6298, #23135 ) ;
#23594=CARTESIAN_POINT ( 'NONE',  ( 2.433796855181233454, 125.2830755159764777, -74.00833731765430912 ) ) ;
#23599=EDGE_LOOP ( 'NONE', ( #24707, #26597, #8925, #7657 ) ) ;
#23600=CARTESIAN_POINT ( 'NONE',  ( 109.1586900883932856, -0.006561743627145281976, -0.002810909342002382467 ) ) ;
#23601=FACE_OUTER_BOUND ( 'NONE', #18965, .T. ) ;
#23602=CARTESIAN_POINT ( 'NONE',  ( 25.98107933586721430, 74.88680433646234746, 84.80123094405227846 ) ) ;
#23603=CARTESIAN_POINT ( 'NONE',  ( 2.063896406836605024, -126.4736179849652871, 71.46753739785971504 ) ) ;
#23604=CARTESIAN_POINT ( 'NONE',  ( 25.64699802086726166, 75.37548011155837457, -84.06830990999249309 ) ) ;
#23606=CARTESIAN_POINT ( 'NONE',  ( 24.01988960052063504, 57.17607523395366798, -117.9135177031530759 ) ) ;
#23607=( BOUNDED_SURFACE ( )  B_SPLINE_SURFACE ( 3, 1, ( 
 ( #19429, #16722 ),
 ( #25514, #21164 ),
 ( #8224, #14547 ),
 ( #23352, #19017 ) ),
 .UNSPECIFIED., .F., .F., .F. ) 
 B_SPLINE_SURFACE_WITH_KNOTS ( ( 4, 4 ),
 ( 2, 2 ),
 ( 0.000000000000000000, 1.000000000000000000 ),
 ( 0.000000000000000000, 1.000000000000000000 ),
 .UNSPECIFIED. ) 
 GEOMETRIC_REPRESENTATION_ITEM ( )  RATIONAL_B_SPLINE_SURFACE ( (
 ( 1.000000000000000000, 1.000000000000000000),
 ( 0.6386103224230316178, 0.9954351624131538845),
 ( 0.6386103224230316178, 0.9954351624131538845),
 ( 1.000000000000000000, 1.000000000000000000) ) ) 
 REPRESENTATION_ITEM ( '' )  SURFACE ( )  );
#23609=CIRCLE ( 'NONE', #12089, 117.6351876552689504 ) ;
#23611=CARTESIAN_POINT ( 'NONE',  ( 109.1778270068192853, -0.008360410075196044247, 0.004106684808170100488 ) ) ;
#23612=B_SPLINE_CURVE_WITH_KNOTS ( 'NONE', 3,
 ( #17081, #88, #8315, #8882, #6026, #23594 ),
 .UNSPECIFIED., .F., .F.,
 ( 4, 2, 4 ),
 ( 2.778605206969998010E-17, 0.0006311571484586209679, 0.001262314296917214397 ),
 .UNSPECIFIED. ) ;
#23621=CARTESIAN_POINT ( 'NONE',  ( 1.831572820252008738, 145.1082523917587253, 0.9871191512919631483 ) ) ;
#23624=ADVANCED_FACE ( 'NONE', ( #26880 ), #10404, .F. ) ;
#23626=CARTESIAN_POINT ( 'NONE',  ( 8.186469829614329896, -148.8557359502362942, 12.15801983495572003 ) ) ;
#23628=ADVANCED_FACE ( 'NONE', ( #831 ), #4258, .T. ) ;
#23629=ORIENTED_EDGE ( 'NONE', *, *, #14621, .F. ) ;
#23630=CARTESIAN_POINT ( 'NONE',  ( 25.70243777736188306, -97.44734253939043356, -57.10783651465066413 ) ) ;
#23632=FACE_OUTER_BOUND ( 'NONE', #178, .T. ) ;
#23634=CARTESIAN_POINT ( 'NONE',  ( 28.43349137099837876, 123.0821667346709489, -17.01091693849615183 ) ) ;
#23635=CIRCLE ( 'NONE', #2440, 117.6351876552689504 ) ;
#23636=CARTESIAN_POINT ( 'NONE',  ( 2.430230287190581429, 133.5180086894999363, -57.85706160874013904 ) ) ;
#23639=CARTESIAN_POINT ( 'NONE',  ( 1.833485406944043827, -144.2578170162064168, 15.69895494453337648 ) ) ;
#23641=CIRCLE ( 'NONE', #6156, 37.50000000000002132 ) ;
#23642=CARTESIAN_POINT ( 'NONE',  ( 1.833838848569428359, 117.2916552720330543, -85.43736077718747879 ) ) ;
#23643=VECTOR ( 'NONE', #11371, 1000.000000000000000 ) ;
#23644=CARTESIAN_POINT ( 'NONE',  ( 1.832998868059890096, 14.63705790014011932, 144.3700883710217795 ) ) ;
#23646=ORIENTED_EDGE ( 'NONE', *, *, #26351, .T. ) ;
#23648=CARTESIAN_POINT ( 'NONE',  ( 25.87036335909426654, -97.41424496619563911, 57.38512068812975286 ) ) ;
#23649=ORIENTED_EDGE ( 'NONE', *, *, #21221, .F. ) ;
#23651=ORIENTED_EDGE ( 'NONE', *, *, #16880, .F. ) ;
#23653=CARTESIAN_POINT ( 'NONE',  ( 25.70243777736189372, -107.6443926015132604, 34.20488708978063386 ) ) ;
#23654=CARTESIAN_POINT ( 'NONE',  ( 1.831572820252009626, -132.1614873090352944, 59.92262167723391286 ) ) ;
#23655=EDGE_CURVE ( 'NONE', #6108, #28186, #14351, .T. ) ;
#23656=EDGE_CURVE ( 'NONE', #28480, #24250, #27749, .T. ) ;
#23657=CARTESIAN_POINT ( 'NONE',  ( 2.263178113027036531, -133.3897502891098839, 57.85473702513823469 ) ) ;
#23658=B_SPLINE_CURVE_WITH_KNOTS ( 'NONE', 3,
 ( #17884, #2495, #17755, #4665, #20056, #337 ),
 .UNSPECIFIED., .F., .F.,
 ( 4, 2, 4 ),
 ( 1.215080616515954935E-17, 0.0006311636237756828140, 0.001262327247551361942 ),
 .UNSPECIFIED. ) ;
#23659=CARTESIAN_POINT ( 'NONE',  ( 13.36082413113061307, 119.8836995922726629, 94.94363694444093937 ) ) ;
#23660=ORIENTED_EDGE ( 'NONE', *, *, #23955, .T. ) ;
#23661=PLANE ( 'NONE',  #11044 ) ;
#23662=EDGE_CURVE ( 'NONE', #26589, #8900, #22080, .T. ) ;
#23664=CARTESIAN_POINT ( 'NONE',  ( 1.834118845439484335, 132.6369225636073850, 58.85894970554959826 ) ) ;
#23667=AXIS2_PLACEMENT_3D ( 'NONE', #4846, #9743, #18353 ) ;
#23669=CARTESIAN_POINT ( 'NONE',  ( 109.1778270068192853, -0.002542344697958529715, -0.008960903982061008133 ) ) ;
#23672=CARTESIAN_POINT ( 'NONE',  ( 6.224689322667647851, 71.79702446228485258, -129.4863684118279821 ) ) ;
#23673=CARTESIAN_POINT ( 'NONE',  ( 1.833809397011862519, -0.1779683723488788560, 145.1096615925545734 ) ) ;
#23675=ORIENTED_EDGE ( 'NONE', *, *, #15865, .T. ) ;
#23676=CARTESIAN_POINT ( 'NONE',  ( 1.833485406944057594, -108.1939177044919376, -96.69979900902278303 ) ) ;
#23677=CARTESIAN_POINT ( 'NONE',  ( 19.66333377628721735, -38.27269871460961070, -132.3257119126252519 ) ) ;
#23678=VERTEX_POINT ( 'NONE', #979 ) ;
#23681=ORIENTED_EDGE ( 'NONE', *, *, #26475, .T. ) ;
#23683=CARTESIAN_POINT ( 'NONE',  ( 1.833485406944043827, -96.69979900902241354, 108.1939177044922786 ) ) ;
#23684=CARTESIAN_POINT ( 'NONE',  ( 25.86096068574582674, -83.34468010038236230, -76.38617895399430324 ) ) ;
#23686=EDGE_CURVE ( 'NONE', #16228, #27632, #15276, .T. ) ;
#23687=CARTESIAN_POINT ( 'NONE',  ( 1.833838850855463054, -141.9572669680997592, 30.08297881069633561 ) ) ;
#23691=LINE ( 'NONE', #28382, #10674 ) ;
#23693=CARTESIAN_POINT ( 'NONE',  ( 109.1592201516379674, 0.007620268632971107306, -0.001934867487021749589 ) ) ;
#23694=CARTESIAN_POINT ( 'NONE',  ( 109.1721716018069515, 0.005082060336465269064, 0.01629455849719225330 ) ) ;
#23697=VERTEX_POINT ( 'NONE', #8052 ) ;
#23698=CARTESIAN_POINT ( 'NONE',  ( 25.64692232868534560, 112.9106972861223426, -0.3267662677155435680 ) ) ;
#23699=CARTESIAN_POINT ( 'NONE',  ( 109.1624594426973260, 0.01154818537150960160, 0.01102230012606007781 ) ) ;
#23700=CARTESIAN_POINT ( 'NONE',  ( 8.186469777910970080, 97.33125097303862105, -113.2805152945346805 ) ) ;
#23701=CARTESIAN_POINT ( 'NONE',  ( 8.186469777910879486, -113.2805152945350073, -97.33125097303823736 ) ) ;
#23702=CARTESIAN_POINT ( 'NONE',  ( 25.98107933586724627, 92.16448350435805992, -65.61242423298341464 ) ) ;
#23703=ORIENTED_EDGE ( 'NONE', *, *, #24882, .F. ) ;
#23704=CARTESIAN_POINT ( 'NONE',  ( 1.833485406944043827, -73.01664920993054864, 125.4007332306543105 ) ) ;
#23705=CARTESIAN_POINT ( 'NONE',  ( 55.49584447822657296, 71.02133150427255259, 14.82242356767960345 ) ) ;
#23708=VERTEX_POINT ( 'NONE', #14199 ) ;
#23711=ORIENTED_EDGE ( 'NONE', *, *, #6651, .T. ) ;
#23713=CARTESIAN_POINT ( 'NONE',  ( 109.1778270068192853, -0.007885345421907767605, -0.004958088776550184651 ) ) ;
#23718=LINE ( 'NONE', #25722, #24305 ) ;
#23719=CARTESIAN_POINT ( 'NONE',  ( 8.186469777910783563, -127.5731248346292688, 77.65916160569861404 ) ) ;
#23720=EDGE_CURVE ( 'NONE', #9703, #12630, #13915, .T. ) ;
#23721=CARTESIAN_POINT ( 'NONE',  ( 9.884929003653608603, 71.59798461011331483, 132.4189379373572990 ) ) ;
#23723=CARTESIAN_POINT ( 'NONE',  ( 32.73300124599733607, 103.7392577722176270, 55.46353551262048853 ) ) ;
#23725=CARTESIAN_POINT ( 'NONE',  ( 55.79472521941426777, 35.74479459808846826, 63.36760613016235766 ) ) ;
#23726=EDGE_CURVE ( 'NONE', #13256, #9946, #18820, .T. ) ;
#23727=ORIENTED_EDGE ( 'NONE', *, *, #15856, .F. ) ;
#23728=B_SPLINE_CURVE_WITH_KNOTS ( 'NONE', 3,
 ( #3818, #18791, #20943, #12585, #1647, #19212, #27423, #27987, #17047, #25844 ),
 .UNSPECIFIED., .F., .F.,
 ( 4, 3, 3, 4 ),
 ( 1.962615573354718958E-17, 0.0002669560319015795735, 0.0005492286108966419958, 0.0008315040496093461988 ),
 .UNSPECIFIED. ) ;
#23730=CARTESIAN_POINT ( 'NONE',  ( 2.430230287190589422, -144.5585181921887283, 16.65331920325691684 ) ) ;
#23733=ORIENTED_EDGE ( 'NONE', *, *, #14563, .T. ) ;
#23734=ORIENTED_EDGE ( 'NONE', *, *, #10156, .F. ) ;
#23737=DIRECTION ( 'NONE',  ( -0.5946245182733607137, -0.6948076064830687182, 0.4045541647807407992 ) ) ;
#23739=CARTESIAN_POINT ( 'NONE',  ( 10.93730112725945602, 104.7670965581007607, 108.9902118373744742 ) ) ;
#23741=CARTESIAN_POINT ( 'NONE',  ( 1.832998868059890096, 125.4013017422231115, 73.01698022778396080 ) ) ;
#23744=CARTESIAN_POINT ( 'NONE',  ( 30.59138290137869021, 116.1811451928592334, -2.701446546448577735 ) ) ;
#23745=CARTESIAN_POINT ( 'NONE',  ( 25.98107933586716101, -92.16448350435771886, 65.61242423298415360 ) ) ;
#23746=B_SPLINE_CURVE_WITH_KNOTS ( 'NONE', 3,
 ( #8400, #27961, #28368, #23529 ),
 .UNSPECIFIED., .F., .F.,
 ( 4, 4 ),
 ( 3.386856006650903455E-16, 0.01077107486149799648 ),
 .UNSPECIFIED. ) ;
#23747=CARTESIAN_POINT ( 'NONE',  ( 25.98552792386800192, -55.63155129533001997, 98.51438617140721021 ) ) ;
#23748=ORIENTED_EDGE ( 'NONE', *, *, #21057, .F. ) ;
#23750=CARTESIAN_POINT ( 'NONE',  ( 2.430230287190589422, -13.76600171652741800, 144.8619874886005903 ) ) ;
#23751=VERTEX_POINT ( 'NONE', #16521 ) ;
#23752=EDGE_CURVE ( 'NONE', #19603, #26070, #18290, .T. ) ;
#23754=B_SPLINE_CURVE_WITH_KNOTS ( 'NONE', 3,
 ( #16339, #20652, #25136, #6267, #3815, #23408 ),
 .UNSPECIFIED., .F., .F.,
 ( 4, 2, 4 ),
 ( 4.770489558936219510E-18, 0.0006311636237756704541, 0.001262327247551336138 ),
 .UNSPECIFIED. ) ;
#23755=CARTESIAN_POINT ( 'NONE',  ( 2.433796855181219243, -132.3327394885235435, 60.50726454507858421 ) ) ;
#23756=ADVANCED_FACE ( 'NONE', ( #10892 ), #6517, .F. ) ;
#23757=CARTESIAN_POINT ( 'NONE',  ( 25.64703792032473828, 103.0889146124071374, -46.06101937225500365 ) ) ;
#23759=CARTESIAN_POINT ( 'NONE',  ( 25.98552792386799482, 55.63155129533072341, -98.51438617140682652 ) ) ;
#23761=CARTESIAN_POINT ( 'NONE',  ( 109.1586900883932856, -0.002810909342011644156, -0.006561743627143320871 ) ) ;
#23762=FACE_BOUND ( 'NONE', #3705, .T. ) ;
#23763=CARTESIAN_POINT ( 'NONE',  ( 25.64708010899964918, 110.4552579818685274, 23.42206246795045033 ) ) ;
#23764=CARTESIAN_POINT ( 'NONE',  ( 1.833485406944043827, -44.33323125129830089, -138.1714136985312962 ) ) ;
#23765=CARTESIAN_POINT ( 'NONE',  ( 109.1778270068192853, -0.001591747944966589697, 0.009177562596833062358 ) ) ;
#23766=CARTESIAN_POINT ( 'NONE',  ( 119.2224693531408803, -90.00000000000005684, -40.00000000000002842 ) ) ;
#23767=CARTESIAN_POINT ( 'NONE',  ( 1.833485406944057594, -58.53321471326971448, 132.7804117027886548 ) ) ;
#23769=ORIENTED_EDGE ( 'NONE', *, *, #26257, .F. ) ;
#23770=EDGE_LOOP ( 'NONE', ( #28100, #8490, #9555, #26335 ) ) ;
#23771=CARTESIAN_POINT ( 'NONE',  ( 30.59141879584289470, -114.2039975081482481, 21.51299111590015301 ) ) ;
#23774=CARTESIAN_POINT ( 'NONE',  ( 2.430230287190589422, 144.8619874886006471, 13.76600171652692062 ) ) ;
#23775=CARTESIAN_POINT ( 'NONE',  ( 1.833206308920068750, -141.7818018507500426, -30.89799439741769760 ) ) ;
#23777=CARTESIAN_POINT ( 'NONE',  ( 25.64681081121879203, 35.28660243342691416, -107.2555980796237804 ) ) ;
#23778=CARTESIAN_POINT ( 'NONE',  ( 109.1587776205901577, -0.002343968083389405717, 0.006944419901758085156 ) ) ;
#23779=ORIENTED_EDGE ( 'NONE', *, *, #1109, .T. ) ;
#23780=DIRECTION ( 'NONE',  ( 0.000000000000000000, 0.000000000000000000, 1.000000000000000000 ) ) ;
#23782=( BOUNDED_SURFACE ( )  B_SPLINE_SURFACE ( 3, 1, ( 
 ( #25130, #13461 ),
 ( #15764, #11308 ),
 ( #11590, #2966 ),
 ( #9148, #17906 ) ),
 .UNSPECIFIED., .F., .F., .F. ) 
 B_SPLINE_SURFACE_WITH_KNOTS ( ( 4, 4 ),
 ( 2, 2 ),
 ( 0.000000000000000000, 1.000000000000000000 ),
 ( 0.000000000000000000, 1.000000000000000000 ),
 .UNSPECIFIED. ) 
 GEOMETRIC_REPRESENTATION_ITEM ( )  RATIONAL_B_SPLINE_SURFACE ( (
 ( 1.000000000000000000, 1.000000000000000000),
 ( 0.9960225298536222738, 0.9999952330161893110),
 ( 0.9960225298536222738, 0.9999952330161893110),
 ( 1.000000000000000000, 1.000000000000000000) ) ) 
 REPRESENTATION_ITEM ( '' )  SURFACE ( )  );
#23783=CARTESIAN_POINT ( 'NONE',  ( 1.833838850855475044, 117.4485666028830053, -85.22139087168962135 ) ) ;
#23786=CARTESIAN_POINT ( 'NONE',  ( 25.64704443564076541, -46.04703398841358819, 103.0951670221013217 ) ) ;
#23789=ORIENTED_EDGE ( 'NONE', *, *, #22307, .F. ) ;
#23790=EDGE_CURVE ( 'NONE', #25020, #16841, #10760, .T. ) ;
#23791=B_SPLINE_CURVE_WITH_KNOTS ( 'NONE', 3,
 ( #12760, #8464, #1407, #17228 ),
 .UNSPECIFIED., .F., .F.,
 ( 4, 4 ),
 ( 0.000000000000000000, 0.008383560773332694727 ),
 .UNSPECIFIED. ) ;
#23792=ORIENTED_EDGE ( 'NONE', *, *, #24088, .T. ) ;
#23793=EDGE_CURVE ( 'NONE', #24227, #12813, #26206, .T. ) ;
#23796=FACE_OUTER_BOUND ( 'NONE', #11150, .T. ) ;
#23797=CARTESIAN_POINT ( 'NONE',  ( 2.433796855181233454, -125.2830755159759519, 74.00833731765517598 ) ) ;
#23798=CARTESIAN_POINT ( 'NONE',  ( 9.884929003653608603, 119.2676479132373828, 91.84919534721981904 ) ) ;
#23799=ORIENTED_EDGE ( 'NONE', *, *, #22325, .T. ) ;
#23800=CARTESIAN_POINT ( 'NONE',  ( 109.1592201516379674, 0.004194960840980690650, -0.006649399203953405661 ) ) ;
#23801=CARTESIAN_POINT ( 'NONE',  ( 8.186469829614358318, -97.33125097511801016, -113.2805153378648839 ) ) ;
#23804=CARTESIAN_POINT ( 'NONE',  ( 2.430230287190592531, 46.34481016236826179, 137.9371479820464117 ) ) ;
#23806=CARTESIAN_POINT ( 'NONE',  ( 9.884929003653626367, -114.6392083957111083, -97.56484214660738985 ) ) ;
#23807=CARTESIAN_POINT ( 'NONE',  ( 19.66333377628702905, 137.3914191246406062, -9.924285918885045632 ) ) ;
#23808=ORIENTED_EDGE ( 'NONE', *, *, #26929, .T. ) ;
#23809=ADVANCED_FACE ( 'NONE', ( #8455 ), #3741, .F. ) ;
#23812=DIRECTION ( 'NONE',  ( -0.000000000000000000, 1.000000000000000000, -0.000000000000000000 ) ) ;
#23813=ORIENTED_EDGE ( 'NONE', *, *, #14620, .F. ) ;
#23814=( BOUNDED_SURFACE ( )  B_SPLINE_SURFACE ( 3, 1, ( 
 ( #14148, #18047 ),
 ( #18630, #20781 ),
 ( #12010, #20494 ),
 ( #7140, #1073 ) ),
 .UNSPECIFIED., .F., .F., .F. ) 
 B_SPLINE_SURFACE_WITH_KNOTS ( ( 4, 4 ),
 ( 2, 2 ),
 ( 0.000000000000000000, 1.000000000000000000 ),
 ( 0.000000000000000000, 1.000000000000000000 ),
 .UNSPECIFIED. ) 
 GEOMETRIC_REPRESENTATION_ITEM ( )  RATIONAL_B_SPLINE_SURFACE ( (
 ( 1.000000000000000000, 1.000000000000000000),
 ( 0.6386103224230316178, 0.9954351624131538845),
 ( 0.6386103224230316178, 0.9954351624131538845),
 ( 1.000000000000000000, 1.000000000000000000) ) ) 
 REPRESENTATION_ITEM ( '' )  SURFACE ( )  );
#23816=ORIENTED_EDGE ( 'NONE', *, *, #11182, .T. ) ;
#23818=EDGE_CURVE ( 'NONE', #9740, #17967, #6024, .T. ) ;
#23819=CARTESIAN_POINT ( 'NONE',  ( 13.84597867724993314, 94.55652763153807427, 112.1633818588827438 ) ) ;
#23820=CARTESIAN_POINT ( 'NONE',  ( 1.834118845439484335, -59.18411796426966731, -132.4921483272733838 ) ) ;
#23822=CARTESIAN_POINT ( 'NONE',  ( 26.11404676487257603, -83.38016054979729574, -76.59696442953277540 ) ) ;
#23823=CARTESIAN_POINT ( 'NONE',  ( 26.11404676487259024, 83.38016054979885894, -76.59696442953111273 ) ) ;
#23824=CARTESIAN_POINT ( 'NONE',  ( 25.98107933586736706, 24.58827779736931163, -110.4296102877911494 ) ) ;
#23826=CARTESIAN_POINT ( 'NONE',  ( 1.831572820252009626, -59.92262167723350785, -132.1614873090354934 ) ) ;
#23828=ORIENTED_EDGE ( 'NONE', *, *, #22936, .F. ) ;
#23830=CARTESIAN_POINT ( 'NONE',  ( 25.64681081121879203, 112.9102952884414464, 0.4157506337731812773 ) ) ;
#23832=CARTESIAN_POINT ( 'NONE',  ( 25.81918753295379432, 22.58534689649824756, -110.7464580477335687 ) ) ;
#23833=CARTESIAN_POINT ( 'NONE',  ( 25.86096068574580897, 110.3716997142158220, 24.48003142199124582 ) ) ;
#23835=ORIENTED_EDGE ( 'NONE', *, *, #7103, .F. ) ;
#23837=EDGE_CURVE ( 'NONE', #21665, #17077, #8312, .T. ) ;
#23839=B_SPLINE_CURVE_WITH_KNOTS ( 'NONE', 3,
 ( #19200, #4642, #24237, #13269, #24679, #18014, #26375, #24532, #6529, #6965 ),
 .UNSPECIFIED., .F., .F.,
 ( 4, 3, 3, 4 ),
 ( 0.000000000000000000, 0.0002669560319015763209, 0.0005492286108966422126, 0.0008315040496093427293 ),
 .UNSPECIFIED. ) ;
#23840=CARTESIAN_POINT ( 'NONE',  ( 26.11404676487257603, 112.4785329405483765, -12.95861723607337979 ) ) ;
#23841=ORIENTED_EDGE ( 'NONE', *, *, #4084, .F. ) ;
#23842=ORIENTED_EDGE ( 'NONE', *, *, #14009, .F. ) ;
#23844=CARTESIAN_POINT ( 'NONE',  ( 32.73300124599735739, 3.836798148478847370, 117.5726003567930178 ) ) ;
#23847=( BOUNDED_SURFACE ( )  B_SPLINE_SURFACE ( 3, 1, ( 
 ( #9551, #5228 ),
 ( #16019, #3213 ),
 ( #14281, #18172 ),
 ( #18309, #20768 ) ),
 .UNSPECIFIED., .F., .F., .F. ) 
 B_SPLINE_SURFACE_WITH_KNOTS ( ( 4, 4 ),
 ( 2, 2 ),
 ( 0.000000000000000000, 1.000000000000000000 ),
 ( 0.000000000000000000, 1.000000000000000000 ),
 .UNSPECIFIED. ) 
 GEOMETRIC_REPRESENTATION_ITEM ( )  RATIONAL_B_SPLINE_SURFACE ( (
 ( 1.000000000000000000, 1.000000000000000000),
 ( 0.6386103224230316178, 0.9954351624131538845),
 ( 0.6386103224230316178, 0.9954351624131538845),
 ( 1.000000000000000000, 1.000000000000000000) ) ) 
 REPRESENTATION_ITEM ( '' )  SURFACE ( )  );
#23849=EDGE_CURVE ( 'NONE', #12008, #1309, #4235, .T. ) ;
#23851=DIRECTION ( 'NONE',  ( 0.5946245182733608248, 0.4749651461092296856, -0.6487139525627699799 ) ) ;
#23853=ORIENTED_EDGE ( 'NONE', *, *, #3071, .T. ) ;
#23854=CARTESIAN_POINT ( 'NONE',  ( 109.1592201516379674, -0.001331853079208366458, -0.007748443302128551168 ) ) ;
#23859=FACE_OUTER_BOUND ( 'NONE', #25035, .T. ) ;
#23861=DIRECTION ( 'NONE',  ( 0.5914120900931444380, -0.3962188444547240507, -0.7023121577978139740 ) ) ;
#23863=CARTESIAN_POINT ( 'NONE',  ( 1.833485406944057594, 0.5339064996884692604, 145.1085452359073429 ) ) ;
#23865=CARTESIAN_POINT ( 'NONE',  ( 10.93730112726003156, 97.44200844886434254, -115.5857507957695276 ) ) ;
#23867=ORIENTED_EDGE ( 'NONE', *, *, #5562, .F. ) ;
#23868=DIRECTION ( 'NONE',  ( -1.000000000000000000, -0.000000000000000000, -0.000000000000000000 ) ) ;
#23869=DIRECTION ( 'NONE',  ( 0.5946245182733607137, 0.7356888587241657840, -0.3243201896541563212 ) ) ;
#23871=CARTESIAN_POINT ( 'NONE',  ( 25.64681081121879203, -97.99105938547964456, 56.09509703373309719 ) ) ;
#23872=CARTESIAN_POINT ( 'NONE',  ( 1.833485406944043827, -144.2578170162064168, 15.69895494453337648 ) ) ;
#23873=CARTESIAN_POINT ( 'NONE',  ( 2.263178113027037419, 84.32376073259221982, 118.4461880110606131 ) ) ;
#23875=VECTOR ( 'NONE', #7256, 1000.000000000000114 ) ;
#23876=ORIENTED_EDGE ( 'NONE', *, *, #22939, .F. ) ;
#23879=CARTESIAN_POINT ( 'NONE',  ( 2.108393763691186695, -46.11438684123258724, 137.7805780486504545 ) ) ;
#23881=ORIENTED_EDGE ( 'NONE', *, *, #28105, .F. ) ;
#23882=FACE_OUTER_BOUND ( 'NONE', #8357, .T. ) ;
#23884=CARTESIAN_POINT ( 'NONE',  ( 1.832998868059858122, -14.63705790014105546, 144.3700883710216658 ) ) ;
#23885=EDGE_CURVE ( 'NONE', #17556, #13659, #6256, .T. ) ;
#23886=ORIENTED_EDGE ( 'NONE', *, *, #28380, .F. ) ;
#23887=CARTESIAN_POINT ( 'NONE',  ( 2.108393763691158274, 116.7869873529609919, 86.43392821214625599 ) ) ;
#23888=FACE_OUTER_BOUND ( 'NONE', #10757, .T. ) ;
#23889=CARTESIAN_POINT ( 'NONE',  ( 0.000000000000000000, 0.000000000000000000, 0.000000000000000000 ) ) ;
#23890=CARTESIAN_POINT ( 'NONE',  ( 25.64708010899963497, 97.81137751680995507, 56.40825696968293812 ) ) ;
#23892=CARTESIAN_POINT ( 'NONE',  ( 25.64660436782556729, 55.95243482911524069, -98.07256794792259313 ) ) ;
#23895=CARTESIAN_POINT ( 'NONE',  ( 16.75465622695655910, -102.5353941815396439, -98.56308464785165313 ) ) ;
#23896=CARTESIAN_POINT ( 'NONE',  ( 32.73300124599732186, 0.000000000000000000, 0.000000000000000000 ) ) ;
#23897=CARTESIAN_POINT ( 'NONE',  ( 2.430230287190581429, 132.3371620660951180, 60.50928654924798167 ) ) ;
#23898=CARTESIAN_POINT ( 'NONE',  ( 6.224689322667630975, -2.565137105444788901, 148.0369967195762797 ) ) ;
#23900=EDGE_LOOP ( 'NONE', ( #14662, #19777, #25445, #19029 ) ) ;
#23901=VERTEX_POINT ( 'NONE', #15008 ) ;
#23902=ORIENTED_EDGE ( 'NONE', *, *, #9204, .T. ) ;
#23903=CARTESIAN_POINT ( 'NONE',  ( 25.64704443564077607, 103.0951670221014496, 46.04703398841322581 ) ) ;
#23904=LINE ( 'NONE', #6207, #3345 ) ;
#23908=CARTESIAN_POINT ( 'NONE',  ( 10.93730112726002979, 79.81734490846109509, -128.3908183996583432 ) ) ;
#23911=CARTESIAN_POINT ( 'NONE',  ( 26.11404676487259024, 36.06104232266452669, 107.3263591096431639 ) ) ;
#23913=CARTESIAN_POINT ( 'NONE',  ( 109.1587776205901861, -0.002343968083398788402, -0.006944419901758122453 ) ) ;
#23914=EDGE_CURVE ( 'NONE', #5234, #14104, #25152, .T. ) ;
#23915=CARTESIAN_POINT ( 'NONE',  ( 1.833485406944043827, -73.01664920992880070, -125.4007332306553195 ) ) ;
#23917=CARTESIAN_POINT ( 'NONE',  ( 25.64681081121879203, -112.2483031020012589, -12.21581276189922427 ) ) ;
#23918=EDGE_CURVE ( 'NONE', #4343, #10772, #6821, .T. ) ;
#23919=DIRECTION ( 'NONE',  ( -1.000000000000000000, -0.000000000000000000, -0.000000000000000000 ) ) ;
#23921=EDGE_CURVE ( 'NONE', #22316, #14882, #15566, .T. ) ;
#23922=ORIENTED_EDGE ( 'NONE', *, *, #24154, .F. ) ;
#23923=ORIENTED_EDGE ( 'NONE', *, *, #17543, .F. ) ;
#23924=CARTESIAN_POINT ( 'NONE',  ( 109.1592201516379674, -0.007566779963318568183, 0.002134489919774338555 ) ) ;
#23926=LINE ( 'NONE', #4460, #14296 ) ;
#23928=CARTESIAN_POINT ( 'NONE',  ( 24.01988960052031530, 111.2910478358005122, 69.18817751538362870 ) ) ;
#23929=ORIENTED_EDGE ( 'NONE', *, *, #19741, .T. ) ;
#23930=CARTESIAN_POINT ( 'NONE',  ( 1.833603222531983379, 59.42758433816144503, -132.3826570575577364 ) ) ;
#23931=B_SPLINE_CURVE_WITH_KNOTS ( 'NONE', 3,
 ( #20221, #17784, #17912, #26703, #7293, #26849, #24430 ),
 .UNSPECIFIED., .F., .F.,
 ( 4, 3, 4 ),
 ( 5.319721237705389368E-16, 0.02816610861753246486, 0.04000277880656274293 ),
 .UNSPECIFIED. ) ;
#23933=CARTESIAN_POINT ( 'NONE',  ( 109.1587776205901577, 0.006661366261224497057, 0.003057017121591230555 ) ) ;
#23934=EDGE_CURVE ( 'NONE', #1461, #2416, #8334, .T. ) ;
#23936=CARTESIAN_POINT ( 'NONE',  ( 99.22246935314079508, 70.00000000000004263, 39.99999999999999289 ) ) ;
#23937=ADVANCED_FACE ( 'NONE', ( #21791 ), #26016, .F. ) ;
#23938=CARTESIAN_POINT ( 'NONE',  ( 109.1586059443104944, -0.004524147648833204242, -0.005438258427225600017 ) ) ;
#23939=DIRECTION ( 'NONE',  ( -0.5914120900931443270, -0.1598001217819418063, 0.7903769105750340085 ) ) ;
#23941=CARTESIAN_POINT ( 'NONE',  ( 6.224689322667630975, 121.2721959030549499, -84.93872395422852151 ) ) ;
#23944=CARTESIAN_POINT ( 'NONE',  ( 109.1586059443104944, 0.006808232911144239917, -0.001921075557427576489 ) ) ;
#23947=ORIENTED_EDGE ( 'NONE', *, *, #22339, .T. ) ;
#23948=ORIENTED_EDGE ( 'NONE', *, *, #21482, .F. ) ;
#23951=FACE_OUTER_BOUND ( 'NONE', #18120, .T. ) ;
#23953=CARTESIAN_POINT ( 'NONE',  ( 1.834118845439484335, 44.67218053242574882, -138.0627591860425412 ) ) ;
#23955=EDGE_CURVE ( 'NONE', #8031, #18704, #9218, .T. ) ;
#23956=CARTESIAN_POINT ( 'NONE',  ( 30.59138290137916627, 75.73279410806848944, -88.14703743378181855 ) ) ;
#23958=B_SPLINE_CURVE_WITH_KNOTS ( 'NONE', 3,
 ( #4241, #15748, #2070, #4822, #11015, #17621 ),
 .UNSPECIFIED., .F., .F.,
 ( 4, 2, 4 ),
 ( 6.938893903907228378E-18, 0.0006311636237756803203, 0.001262327247551353702 ),
 .UNSPECIFIED. ) ;
#23960=CIRCLE ( 'NONE', #24893, 151.1787379149930359 ) ;
#23962=B_SPLINE_CURVE_WITH_KNOTS ( 'NONE', 3,
 ( #20556, #23178, #16237, #5299, #18687, #27459, #23024 ),
 .UNSPECIFIED., .F., .F.,
 ( 4, 3, 4 ),
 ( 5.669813051359019560E-16, 0.02816610861753245793, 0.04000277880656276375 ),
 .UNSPECIFIED. ) ;
#23963=ADVANCED_FACE ( 'NONE', ( #22803 ), #15133, .F. ) ;
#23964=CARTESIAN_POINT ( 'NONE',  ( 109.1586900883932856, 0.004701023939953857290, 0.005371970278523981006 ) ) ;
#23967=ADVANCED_FACE ( 'NONE', ( #897 ), #24339, .F. ) ;
#23968=ORIENTED_EDGE ( 'NONE', *, *, #6868, .F. ) ;
#23969=ORIENTED_EDGE ( 'NONE', *, *, #626, .F. ) ;
#23971=CARTESIAN_POINT ( 'NONE',  ( 25.98552792386802324, 22.46612985365126036, -110.8838436908324212 ) ) ;
#23973=DIRECTION ( 'NONE',  ( 0.000000000000000000, 0.000000000000000000, 1.000000000000000000 ) ) ;
#23974=CARTESIAN_POINT ( 'NONE',  ( 2.063896406836609909, -71.46753739786105086, 126.4736179849645481 ) ) ;
#23975=( BOUNDED_SURFACE ( )  B_SPLINE_SURFACE ( 3, 1, ( 
 ( #18424, #18721 ),
 ( #27049, #23062 ),
 ( #3464, #22779 ),
 ( #23208, #22630 ) ),
 .UNSPECIFIED., .F., .F., .F. ) 
 B_SPLINE_SURFACE_WITH_KNOTS ( ( 4, 4 ),
 ( 2, 2 ),
 ( 0.000000000000000000, 1.000000000000000000 ),
 ( 0.000000000000000000, 1.000000000000000000 ),
 .UNSPECIFIED. ) 
 GEOMETRIC_REPRESENTATION_ITEM ( )  RATIONAL_B_SPLINE_SURFACE ( (
 ( 1.000000000000000000, 1.000000000000000000),
 ( 0.9956975270656955868, 0.8568959468854907557),
 ( 0.9956975270656955868, 0.8568959468854907557),
 ( 1.000000000000000000, 1.000000000000000000) ) ) 
 REPRESENTATION_ITEM ( '' )  SURFACE ( )  );
#23978=CARTESIAN_POINT ( 'NONE',  ( 2.108393763691197353, 118.2927144690670787, -84.36147263237450034 ) ) ;
#23980=ORIENTED_EDGE ( 'NONE', *, *, #27151, .F. ) ;
#23981=ORIENTED_EDGE ( 'NONE', *, *, #21482, .T. ) ;
#23985=VERTEX_POINT ( 'NONE', #20180 ) ;
#23988=CARTESIAN_POINT ( 'NONE',  ( 2.063896406836605024, -138.5688025270881383, 43.61045647697645933 ) ) ;
#23990=ORIENTED_EDGE ( 'NONE', *, *, #1051, .F. ) ;
#23991=CARTESIAN_POINT ( 'NONE',  ( 2.263178113027032978, 126.6115605262348112, -71.48082833564930638 ) ) ;
#23992=EDGE_CURVE ( 'NONE', #1180, #24611, #8515, .T. ) ;
#23993=CARTESIAN_POINT ( 'NONE',  ( 1.832998868059858122, -117.0819875546701070, 85.72499093308064744 ) ) ;
#23994=CARTESIAN_POINT ( 'NONE',  ( 25.98107933586730667, -112.3948402207511208, -12.91054317625230397 ) ) ;
#23995=ADVANCED_FACE ( 'NONE', ( #20613 ), #4652, .F. ) ;
#23997=CARTESIAN_POINT ( 'NONE',  ( 25.81918753295378721, -103.6306245682012701, -45.11728622333246363 ) ) ;
#23998=CARTESIAN_POINT ( 'NONE',  ( 1.833721036429677875, 0.3559391723980712685, 145.1093571290645627 ) ) ;
#23999=CARTESIAN_POINT ( 'NONE',  ( 25.98552792386796995, -10.75254026142880548, 112.6247604222998433 ) ) ;
#24001=EDGE_CURVE ( 'NONE', #11755, #27686, #16410, .T. ) ;
#24004=CARTESIAN_POINT ( 'NONE',  ( 8.186469777910868828, -140.9315935720373147, 49.43817851234016558 ) ) ;
#24007=CARTESIAN_POINT ( 'NONE',  ( 25.65782528836481191, -98.07785559018917354, 55.95807498711450023 ) ) ;
#24009=CARTESIAN_POINT ( 'NONE',  ( 10.93730112725932813, 150.7858122213658305, 10.89264110825069132 ) ) ;
#24010=CARTESIAN_POINT ( 'NONE',  ( 25.64681081121879203, 91.10197563708035773, -66.70335573067774249 ) ) ;
#24011=EDGE_CURVE ( 'NONE', #21239, #26564, #11259, .T. ) ;
#24013=CARTESIAN_POINT ( 'NONE',  ( 25.64707127832796019, 6.059145946834079367E-17, -112.9112343549835487 ) ) ;
#24014=VECTOR ( 'NONE', #22138, 1000.000000000000341 ) ;
#24015=CARTESIAN_POINT ( 'NONE',  ( 2.063896406836609909, 138.5688025270878541, 43.61045647697738303 ) ) ;
#24016=CARTESIAN_POINT ( 'NONE',  ( 25.64670758986457599, -91.63870681572869614, 65.96397693491134362 ) ) ;
#24019=DIRECTION ( 'NONE',  ( -0.5946245182733607137, -0.1642747008466245162, 0.7870422510449649467 ) ) ;
#24020=CARTESIAN_POINT ( 'NONE',  ( 9.884929003653626367, -71.59798461011423854, 132.4189379373568443 ) ) ;
#24022=VERTEX_POINT ( 'NONE', #1022 ) ;
#24023=DIRECTION ( 'NONE',  ( -1.000000000000000000, -0.000000000000000000, -0.000000000000000000 ) ) ;
#24025=CARTESIAN_POINT ( 'NONE',  ( 5.340103579038038895, 146.8647350263016165, 13.12023871299778932 ) ) ;
#24026=CARTESIAN_POINT ( 'NONE',  ( 1.833206310202337486, -71.90885922990241852, 126.0392056382539892 ) ) ;
#24027=VECTOR ( 'NONE', #6827, 1000.000000000000341 ) ;
#24028=DIRECTION ( 'NONE',  ( 0.000000000000000000, 0.000000000000000000, 1.000000000000000000 ) ) ;
#24030=VECTOR ( 'NONE', #12005, 1000.000000000000000 ) ;
#24031=CARTESIAN_POINT ( 'NONE',  ( 2.433796855181219243, 132.3327394885239698, -60.50726454507772445 ) ) ;
#24032=CARTESIAN_POINT ( 'NONE',  ( 55.49584447822657296, -58.53775398922284978, 42.86099773636522059 ) ) ;
#24033=CARTESIAN_POINT ( 'NONE',  ( 30.59141879584282719, 21.51299111590054380, 114.2039975081481344 ) ) ;
#24036=DIRECTION ( 'NONE',  ( 0.000000000000000000, 0.000000000000000000, 1.000000000000000000 ) ) ;
#24038=CARTESIAN_POINT ( 'NONE',  ( 25.64681081121879203, 45.54494737132223747, 103.3177883989780952 ) ) ;
#24039=ORIENTED_EDGE ( 'NONE', *, *, #13405, .T. ) ;
#24040=ADVANCED_FACE ( 'NONE', ( #20884 ), #11822, .F. ) ;
#24046=DIRECTION ( 'NONE',  ( 0.000000000000000000, -0.000000000000000000, -1.000000000000000000 ) ) ;
#24047=CARTESIAN_POINT ( 'NONE',  ( 8.186469829614525295, 131.0413692472670277, -71.65198613712843212 ) ) ;
#24048=CARTESIAN_POINT ( 'NONE',  ( 30.59138290137909877, -14.83088430729485552, -115.2623146671593020 ) ) ;
#24050=VERTEX_POINT ( 'NONE', #20590 ) ;
#24051=CARTESIAN_POINT ( 'NONE',  ( 26.11404676487257603, 112.4785329405482059, 12.95861723607491456 ) ) ;
#24054=CARTESIAN_POINT ( 'NONE',  ( 109.1587776205901861, -0.001442274044995847443, 0.007186028091168150840 ) ) ;
#24056=CARTESIAN_POINT ( 'NONE',  ( 109.1592201516379674, -0.0003082430542016361633, -0.007856029051022768092 ) ) ;
#24059=CARTESIAN_POINT ( 'NONE',  ( 1.833603222531957844, -108.1346772638452904, 96.76619886578292551 ) ) ;
#24060=CARTESIAN_POINT ( 'NONE',  ( 25.64692232868533139, -56.73833653200176030, -97.62014907493936278 ) ) ;
#24062=VERTEX_POINT ( 'NONE', #12248 ) ;
#24063=EDGE_LOOP ( 'NONE', ( #1221, #14913, #13895, #15386 ) ) ;
#24065=FACE_OUTER_BOUND ( 'NONE', #10298, .T. ) ;
#24066=CARTESIAN_POINT ( 'NONE',  ( 9.884929003653608603, 141.8132360130357768, 50.49804566712172260 ) ) ;
#24067=EDGE_CURVE ( 'NONE', #26154, #21665, #9962, .T. ) ;
#24071=VECTOR ( 'NONE', #26183, 1000.000000000000114 ) ;
#24072=CARTESIAN_POINT ( 'NONE',  ( 2.108393763691171596, -142.3786741588522773, 28.95405853987470479 ) ) ;
#24079=CARTESIAN_POINT ( 'NONE',  ( 2.433796855181205476, 125.2830755159753977, 74.00833731765604284 ) ) ;
#24084=ORIENTED_EDGE ( 'NONE', *, *, #7894, .F. ) ;
#24085=CARTESIAN_POINT ( 'NONE',  ( 2.108985857320913482, -108.8271972979193833, -96.26411661813142473 ) ) ;
#24086=CARTESIAN_POINT ( 'NONE',  ( 10.93730112725932635, 0.000000000000000000, 0.000000000000000000 ) ) ;
#24088=EDGE_CURVE ( 'NONE', #10927, #2573, #3749, .T. ) ;
#24090=VERTEX_POINT ( 'NONE', #12940 ) ;
#24091=ADVANCED_FACE ( 'NONE', ( #26049 ), #25262, .F. ) ;
#24092=CARTESIAN_POINT ( 'NONE',  ( 1.833206310202337264, -144.2348262833783110, 15.90849712171692509 ) ) ;
#24093=CARTESIAN_POINT ( 'NONE',  ( 5.340103579038279591, -146.8647350263016449, -13.12023871299875566 ) ) ;
#24094=EDGE_CURVE ( 'NONE', #7451, #25971, #5772, .T. ) ;
#24095=CARTESIAN_POINT ( 'NONE',  ( 25.86096068574580187, -107.2082119295150022, -35.88291140784026112 ) ) ;
#24096=ADVANCED_FACE ( 'NONE', ( #28059 ), #6685, .F. ) ;
#24099=CARTESIAN_POINT ( 'NONE',  ( 109.1589550718175161, -0.003591809816099570795, 0.006669585340474254269 ) ) ;
#24100=CARTESIAN_POINT ( 'NONE',  ( 25.64681081121879203, 46.30456157731467925, -102.9795863647023850 ) ) ;
#24103=CARTESIAN_POINT ( 'NONE',  ( 25.87036335909428075, 113.0557711752706354, -0.9898498320591554434 ) ) ;
#24104=LINE ( 'NONE', #21927, #20161 ) ;
#24106=EDGE_LOOP ( 'NONE', ( #10739, #1261, #15707, #12299 ) ) ;
#24109=B_SPLINE_CURVE_WITH_KNOTS ( 'NONE', 3,
 ( #16265, #24918, #5179, #22766 ),
 .UNSPECIFIED., .F., .F.,
 ( 4, 4 ),
 ( 0.000000000000000000, 0.01077107196513814660 ),
 .UNSPECIFIED. ) ;
#24111=CARTESIAN_POINT ( 'NONE',  ( 2.433796855181233454, -133.5135467655514390, -57.85512797798025275 ) ) ;
#24117=ORIENTED_EDGE ( 'NONE', *, *, #14293, .T. ) ;
#24118=ORIENTED_EDGE ( 'NONE', *, *, #5169, .T. ) ;
#24119=CARTESIAN_POINT ( 'NONE',  ( 109.1586900883932856, 0.001385221016527459588, -0.007002774699553642249 ) ) ;
#24120=ORIENTED_EDGE ( 'NONE', *, *, #15419, .F. ) ;
#24121=CARTESIAN_POINT ( 'NONE',  ( 109.1586900883932856, -0.004851151255037395443, -0.005236795036860529204 ) ) ;
#24122=ORIENTED_EDGE ( 'NONE', *, *, #19204, .T. ) ;
#24124=EDGE_CURVE ( 'NONE', #25504, #8387, #6211, .T. ) ;
#24126=VERTEX_POINT ( 'NONE', #25777 ) ;
#24127=CARTESIAN_POINT ( 'NONE',  ( 13.84597867724986919, 142.4258194868990017, 35.16314962059880855 ) ) ;
#24128=CARTESIAN_POINT ( 'NONE',  ( 24.01988960052056754, -80.44223964539912686, 103.4492499592081600 ) ) ;
#24129=B_SPLINE_CURVE_WITH_KNOTS ( 'NONE', 3,
 ( #18812, #16366, #12469, #14343 ),
 .UNSPECIFIED., .F., .F.,
 ( 4, 4 ),
 ( 0.000000000000000000, 0.01077107196513875723 ),
 .UNSPECIFIED. ) ;
#24130=CARTESIAN_POINT ( 'NONE',  ( 6.224689322667630975, 71.79702446228303359, 129.4863684118289768 ) ) ;
#24131=FACE_OUTER_BOUND ( 'NONE', #1967, .T. ) ;
#24132=FACE_OUTER_BOUND ( 'NONE', #3147, .T. ) ;
#24134=CARTESIAN_POINT ( 'NONE',  ( 25.98552792386798771, 103.7897946223266246, 45.02923844025520594 ) ) ;
#24137=CARTESIAN_POINT ( 'NONE',  ( 25.64703792032469565, -56.32669596053506211, 97.85829113439940841 ) ) ;
#24138=VERTEX_POINT ( 'NONE', #25645 ) ;
#24139=CARTESIAN_POINT ( 'NONE',  ( 25.64681081121879203, 107.5125461021407318, -34.49579773461672971 ) ) ;
#24140=CARTESIAN_POINT ( 'NONE',  ( 1.833603222531973609, -72.93978951866073146, 125.4455769441940021 ) ) ;
#24141=CARTESIAN_POINT ( 'NONE',  ( 2.263178607246701723, -31.59906277834119592, -141.9207363487297187 ) ) ;
#24143=CARTESIAN_POINT ( 'NONE',  ( 25.65782528836480481, 97.50004228081050428, 56.95887699624769596 ) ) ;
#24144=CARTESIAN_POINT ( 'NONE',  ( 1.833485406944057594, -0.5339064996874559599, -145.1085452359073429 ) ) ;
#24145=CARTESIAN_POINT ( 'NONE',  ( 1.833603222531957844, -45.26427810762999826, 137.8693250773476393 ) ) ;
#24148=CARTESIAN_POINT ( 'NONE',  ( 25.64708010899964208, 110.4325102642037848, -23.52908206539794023 ) ) ;
#24149=ORIENTED_EDGE ( 'NONE', *, *, #9468, .F. ) ;
#24151=EDGE_CURVE ( 'NONE', #21420, #437, #23641, .T. ) ;
#24152=CARTESIAN_POINT ( 'NONE',  ( 109.1721716018069657, 0.01127028715940102920, -0.01281875973824529898 ) ) ;
#24153=CARTESIAN_POINT ( 'NONE',  ( 2.433796855181233454, -60.50726454507816499, -132.3327394885237425 ) ) ;
#24154=EDGE_CURVE ( 'NONE', #6991, #16951, #23484, .T. ) ;
#24155=EDGE_LOOP ( 'NONE', ( #10295, #16957, #13530, #5292 ) ) ;
#24156=CARTESIAN_POINT ( 'NONE',  ( 25.64681081121879203, -112.9102952884414606, 0.4157506337723927414 ) ) ;
#24157=EDGE_CURVE ( 'NONE', #4316, #10927, #25347, .T. ) ;
#24159=CARTESIAN_POINT ( 'NONE',  ( 109.1592201516379674, 0.001331853079208314200, 0.007748443302128560708 ) ) ;
#24160=VERTEX_POINT ( 'NONE', #1588 ) ;
#24162=EDGE_CURVE ( 'NONE', #14748, #3038, #12631, .T. ) ;
#24163=CARTESIAN_POINT ( 'NONE',  ( 26.11404676487259024, 55.62948129436384193, -98.61392875273304526 ) ) ;
#24165=CARTESIAN_POINT ( 'NONE',  ( 2.430230287190592531, 133.5180086894991405, 57.85706160874190829 ) ) ;
#24166=CARTESIAN_POINT ( 'NONE',  ( 2.433796855181233454, -46.34326152018648060, -137.9325382748289996 ) ) ;
#24167=CARTESIAN_POINT ( 'NONE',  ( 1.833691583653553003, -132.7086741139086712, 58.69608658929877976 ) ) ;
#24168=CARTESIAN_POINT ( 'NONE',  ( 55.49584447822657296, 72.12568090333341786, 7.849835876628574738 ) ) ;
#24169=CARTESIAN_POINT ( 'NONE',  ( 109.1586900883932856, -0.006960773163856040675, -0.001582822706024231271 ) ) ;
#24170=LINE ( 'NONE', #10790, #7015 ) ;
#24171=CARTESIAN_POINT ( 'NONE',  ( 13.36082413113061307, 67.94366799843001559, -137.0038452127793676 ) ) ;
#24174=ORIENTED_EDGE ( 'NONE', *, *, #20796, .T. ) ;
#24175=ORIENTED_EDGE ( 'NONE', *, *, #13601, .F. ) ;
#24178=CARTESIAN_POINT ( 'NONE',  ( 109.1589550718175161, 0.002553077953680937557, 0.007132058561966991318 ) ) ;
#24179=CARTESIAN_POINT ( 'NONE',  ( 2.108393763691168932, -141.8460676169243015, -31.45977531353440071 ) ) ;
#24180=CARTESIAN_POINT ( 'NONE',  ( 1.833691583653482615, 72.86287859464769667, -125.4903330494892515 ) ) ;
#24182=VERTEX_POINT ( 'NONE', #23777 ) ;
#24183=CARTESIAN_POINT ( 'NONE',  ( 25.64670758986458310, -34.41755235608670205, -107.5375791514046568 ) ) ;
#24184=CARTESIAN_POINT ( 'NONE',  ( 109.1721716018069657, -0.01467989464939304170, 0.008708654716139565752 ) ) ;
#24185=CARTESIAN_POINT ( 'NONE',  ( 1.833750490713712322, 117.5529286802298401, -85.07723081767763063 ) ) ;
#24186=CARTESIAN_POINT ( 'NONE',  ( 2.430230287190572103, 98.44218333480918659, -107.1617224697454134 ) ) ;
#24187=CARTESIAN_POINT ( 'NONE',  ( 1.833838850093517436, -0.08898415480133092803, 145.1097630783160923 ) ) ;
#24188=CARTESIAN_POINT ( 'NONE',  ( 1.833485406944043827, 85.72460230293849293, -117.0814567582535659 ) ) ;
#24189=PRODUCT_DEFINITION_SHAPE ( 'NONE', 'NONE',  #23390 ) ;
#24190=EDGE_CURVE ( 'NONE', #675, #22412, #11609, .T. ) ;
#24192=CARTESIAN_POINT ( 'NONE',  ( 1.833838850855486369, -107.8971100408355994, 97.03125735562200305 ) ) ;
#24193=CARTESIAN_POINT ( 'NONE',  ( 25.64703792032472407, -56.58441811305539915, -97.70949518026556291 ) ) ;
#24194=ORIENTED_EDGE ( 'NONE', *, *, #5315, .F. ) ;
#24195=EDGE_CURVE ( 'NONE', #1130, #12174, #24757, .T. ) ;
#24196=B_SPLINE_CURVE_WITH_KNOTS ( 'NONE', 3,
 ( #11316, #9451, #7440, #22556, #9588, #18208, #18348 ),
 .UNSPECIFIED., .F., .F.,
 ( 4, 3, 4 ),
 ( 5.253892930763821798E-16, 0.02816610861753246833, 0.04000277880656270824 ),
 .UNSPECIFIED. ) ;
#24198=EDGE_LOOP ( 'NONE', ( #14580, #28, #22754, #3927 ) ) ;
#24200=CARTESIAN_POINT ( 'NONE',  ( 13.36082413113061307, 117.7941133658651438, -97.52406103376640090 ) ) ;
#24201=CARTESIAN_POINT ( 'NONE',  ( 2.430230287190589422, 96.28466919684248637, -109.1043569252004488 ) ) ;
#24202=CARTESIAN_POINT ( 'NONE',  ( 2.433796855181219243, 86.69855925933974561, 116.8607839509059829 ) ) ;
#24203=EDGE_LOOP ( 'NONE', ( #4119, #18736, #7221, #26258 ) ) ;
#24206=ORIENTED_EDGE ( 'NONE', *, *, #25718, .F. ) ;
#24208=EDGE_LOOP ( 'NONE', ( #28400, #26239, #19634, #20486 ) ) ;
#24209=DIRECTION ( 'NONE',  ( 0.000000000000000000, 0.000000000000000000, 1.000000000000000000 ) ) ;
#24210=CARTESIAN_POINT ( 'NONE',  ( 1.833838850093465922, -44.84138612520995082, -138.0075846865485403 ) ) ;
#24212=CARTESIAN_POINT ( 'NONE',  ( 55.79472521941426777, -58.42842213658298078, -43.35047097963510510 ) ) ;
#24216=DIRECTION ( 'NONE',  ( -0.000000000000000000, 1.000000000000000000, 0.000000000000000000 ) ) ;
#24218=( BOUNDED_SURFACE ( )  B_SPLINE_SURFACE ( 3, 1, ( 
 ( #1044, #25091 ),
 ( #16002, #18291 ),
 ( #9834, #27375 ),
 ( #9984, #12268 ) ),
 .UNSPECIFIED., .F., .F., .F. ) 
 B_SPLINE_SURFACE_WITH_KNOTS ( ( 4, 4 ),
 ( 2, 2 ),
 ( 0.000000000000000000, 1.000000000000000000 ),
 ( 0.000000000000000000, 1.000000000000000000 ),
 .UNSPECIFIED. ) 
 GEOMETRIC_REPRESENTATION_ITEM ( )  RATIONAL_B_SPLINE_SURFACE ( (
 ( 1.000000000000000000, 1.000000000000000000),
 ( 0.9960225298536222738, 0.9999952330161893110),
 ( 0.9960225298536222738, 0.9999952330161893110),
 ( 1.000000000000000000, 1.000000000000000000) ) ) 
 REPRESENTATION_ITEM ( '' )  SURFACE ( )  );
#24220=EDGE_LOOP ( 'NONE', ( #20170, #3137, #9527, #15265 ) ) ;
#24222=B_SPLINE_CURVE_WITH_KNOTS ( 'NONE', 3,
 ( #14683, #12522, #18870, #16987 ),
 .UNSPECIFIED., .F., .F.,
 ( 4, 4 ),
 ( 0.000000000000000000, 0.01077107196513812405 ),
 .UNSPECIFIED. ) ;
#24224=ORIENTED_EDGE ( 'NONE', *, *, #16012, .T. ) ;
#24225=ADVANCED_FACE ( 'NONE', ( #269 ), #15312, .F. ) ;
#24227=VERTEX_POINT ( 'NONE', #2562 ) ;
#24228=CARTESIAN_POINT ( 'NONE',  ( 109.1586900883932856, -0.002995460350188440014, -0.006479576224398238618 ) ) ;
#24230=EDGE_CURVE ( 'NONE', #19162, #12813, #28463, .T. ) ;
#24231=CARTESIAN_POINT ( 'NONE',  ( 109.1592201516379674, 0.005027640251767214602, 0.006044422199822552418 ) ) ;
#24232=CARTESIAN_POINT ( 'NONE',  ( 25.98107933586729601, -83.34070894055808765, -76.50887835172612483 ) ) ;
#24234=CARTESIAN_POINT ( 'NONE',  ( 25.86096068574581963, 10.82483750674603407, 112.5344699600049410 ) ) ;
#24237=CARTESIAN_POINT ( 'NONE',  ( 25.64699802086721903, 66.55977212001160126, 91.20712948285684263 ) ) ;
#24238=CARTESIAN_POINT ( 'NONE',  ( 28.37644542392834168, -42.25924161793970768, 116.9383271603245191 ) ) ;
#24239=CARTESIAN_POINT ( 'NONE',  ( 25.64708010899966339, -110.4325102642036001, 23.52908206539865787 ) ) ;
#24242=CARTESIAN_POINT ( 'NONE',  ( 32.73300124599739291, -103.7392577722171865, -55.46353551262117776 ) ) ;
#24243=EDGE_LOOP ( 'NONE', ( #7399, #25544, #26892, #23649 ) ) ;
#24246=CARTESIAN_POINT ( 'NONE',  ( 8.186469829613987059, 140.9315935955037844, 49.43817854882337315 ) ) ;
#24249=CARTESIAN_POINT ( 'NONE',  ( 30.58324630866340854, -113.7441547345750195, 41.10517620771165070 ) ) ;
#24250=VERTEX_POINT ( 'NONE', #6902 ) ;
#24251=ORIENTED_EDGE ( 'NONE', *, *, #70, .F. ) ;
#24252=CARTESIAN_POINT ( 'NONE',  ( 25.64681081121880624, 103.3177883989785499, -45.54494737132120008 ) ) ;
#24258=ORIENTED_EDGE ( 'NONE', *, *, #8210, .T. ) ;
#24260=EDGE_LOOP ( 'NONE', ( #22414, #4524, #8732, #9894, #26138, #18061, #21759, #22900, #18810, #17390, #14611, #24489, #3056, #6538, #21351, #25835, #12196, #1110, #14465, #28342, #25372, #571, #26906, #8840, #22781, #14099, #2122, #22073, #2540, #5433, #12639, #16224, #1163, #16614, #23253, #21577, #24854, #4595, #13223, #8282, #26197, #2826, #10728, #6522, #7882, #26721, #23947, #25701, #8274, #15576, #2839, #5855, #9452, #18045, #25360, #21241, #26812, #27250, #3901, #634, #2755, #12835, #28268, #4164, #14494, #27132, #719, #24746, #11467, #26961, #10424, #12697, #6022, #15444, #17692, #18519, #17704, #13793, #14197, #15499, #2553, #20054, #11097, #16278, #13578, #16690, #12729, #7060, #18943, #10698, #12333, #7929, #12989, #7186, #22817, #10145, #3611, #4454, #11916, #26930, #24969, #11121, #400, #6186, #24174, #18562, #16026, #5823, #2621, #24671, #16255, #18724, #17954, #6370, #18767, #27806, #13401, #7644, #14234, #25610, #5681, #27169, #9695, #9826, #6147, #14960, #10582, #26204, #5824, #26081, #3473, #7271, #7328, #23660, #23681, #6399, #22529, #16853, #17550, #22287, #16286, #10053, #22520, #15639, #7958, #19056, #19145, #10302, #23565, #11145, #2722, #2187, #6755, #12953, #11595, #21747, #26364, #15522, #7554, #7981, #23002, #22863, #12789, #22641, #18319, #23711, #17559, #6904, #24117, #11218, #13428, #26112, #20193, #9996, #14051, #27291, #7677, #5474, #682, #12733, #22232, #4499, #1714, #19153 ) ) ;
#24261=B_SPLINE_CURVE_WITH_KNOTS ( 'NONE', 3,
 ( #8217, #14821, #10250, #10387, #21443, #12246, #19011, #14240, #16859, #21011 ),
 .UNSPECIFIED., .F., .F.,
 ( 4, 3, 3, 4 ),
 ( 1.387778780781445676E-17, 0.0002669560319015811456, 0.0005492286108966765818, 0.0008315040496093515114 ),
 .UNSPECIFIED. ) ;
#24262=B_SPLINE_CURVE_WITH_KNOTS ( 'NONE', 3,
 ( #9118, #13710, #51, #19758 ),
 .UNSPECIFIED., .F., .F.,
 ( 4, 4 ),
 ( 0.000000000000000000, 0.01077107196513807721 ),
 .UNSPECIFIED. ) ;
#24263=CARTESIAN_POINT ( 'NONE',  ( 25.69398547355840634, 66.98507266663752091, 90.93418986874829102 ) ) ;
#24267=CARTESIAN_POINT ( 'NONE',  ( 1.833485406944057594, -141.8265699653869376, 30.69200235378888308 ) ) ;
#24268=CARTESIAN_POINT ( 'NONE',  ( 2.063896406836609909, 13.84738934186382586, -144.6078654718900225 ) ) ;
#24269=CARTESIAN_POINT ( 'NONE',  ( 5.340103579038256498, -100.3626145943027268, -108.0219267094756503 ) ) ;
#24272=CARTESIAN_POINT ( 'NONE',  ( 10.93730112725932635, 0.000000000000000000, 0.000000000000000000 ) ) ;
#24274=CARTESIAN_POINT ( 'NONE',  ( 10.93730112725978287, -97.44200844886353252, 115.5857507957700250 ) ) ;
#24275=CARTESIAN_POINT ( 'NONE',  ( 2.433796855181219243, 142.0211193075560061, -31.67151202412830813 ) ) ;
#24276=CARTESIAN_POINT ( 'NONE',  ( 32.73300124599739291, -113.0038235389599635, -32.68291970228351317 ) ) ;
#24277=CARTESIAN_POINT ( 'NONE',  ( 13.36082413113063083, 81.89226687792086068, 129.1512766091124149 ) ) ;
#24279=CARTESIAN_POINT ( 'NONE',  ( 1.833838850093516104, -0.1779693352084075475, -145.1097630783160923 ) ) ;
#24280=EDGE_CURVE ( 'NONE', #8439, #2946, #6125, .T. ) ;
#24281=ORIENTED_EDGE ( 'NONE', *, *, #11494, .F. ) ;
#24282=CARTESIAN_POINT ( 'NONE',  ( 109.1587776205901861, -0.004965871434398078446, -0.005390665547495563856 ) ) ;
#24283=EDGE_CURVE ( 'NONE', #10817, #1068, #14368, .T. ) ;
#24285=CARTESIAN_POINT ( 'NONE',  ( 30.59138290137912009, 55.75105126024056545, -101.9665464510083979 ) ) ;
#24286=CARTESIAN_POINT ( 'NONE',  ( 109.1587776205901861, 0.004240403845331873305, -0.005978137617721855993 ) ) ;
#24287=EDGE_LOOP ( 'NONE', ( #5089, #26451, #24910, #10607 ) ) ;
#24290=AXIS2_PLACEMENT_3D ( 'NONE', #21733, #13216, #22006 ) ;
#24291=( BOUNDED_SURFACE ( )  B_SPLINE_SURFACE ( 3, 1, ( 
 ( #10012, #25414 ),
 ( #24991, #5689 ),
 ( #23261, #12294 ),
 ( #21064, #27974 ) ),
 .UNSPECIFIED., .F., .F., .F. ) 
 B_SPLINE_SURFACE_WITH_KNOTS ( ( 4, 4 ),
 ( 2, 2 ),
 ( 0.000000000000000000, 1.000000000000000000 ),
 ( 0.000000000000000000, 1.000000000000000000 ),
 .UNSPECIFIED. ) 
 GEOMETRIC_REPRESENTATION_ITEM ( )  RATIONAL_B_SPLINE_SURFACE ( (
 ( 1.000000000000000000, 1.000000000000000000),
 ( 0.6386103224230302855, 0.9954351624131538845),
 ( 0.6386103224230302855, 0.9954351624131538845),
 ( 1.000000000000000000, 1.000000000000000000) ) ) 
 REPRESENTATION_ITEM ( '' )  SURFACE ( )  );
#24293=ORIENTED_EDGE ( 'NONE', *, *, #25927, .F. ) ;
#24294=CARTESIAN_POINT ( 'NONE',  ( 109.1778270068192853, -0.002542344697966384976, 0.008960903982066587004 ) ) ;
#24295=CARTESIAN_POINT ( 'NONE',  ( 1.834118845439484335, -125.7578880615050281, 72.40084790867285847 ) ) ;
#24296=FACE_OUTER_BOUND ( 'NONE', #16144, .T. ) ;
#24297=EDGE_LOOP ( 'NONE', ( #910, #19835, #23902, #49 ) ) ;
#24298=( BOUNDED_SURFACE ( )  B_SPLINE_SURFACE ( 3, 1, ( 
 ( #7980, #9540 ),
 ( #3202, #9835 ),
 ( #7687, #20753 ),
 ( #11983, #16445 ) ),
 .UNSPECIFIED., .F., .F., .F. ) 
 B_SPLINE_SURFACE_WITH_KNOTS ( ( 4, 4 ),
 ( 2, 2 ),
 ( 0.000000000000000000, 1.000000000000000000 ),
 ( 0.000000000000000000, 1.000000000000000000 ),
 .UNSPECIFIED. ) 
 GEOMETRIC_REPRESENTATION_ITEM ( )  RATIONAL_B_SPLINE_SURFACE ( (
 ( 1.000000000000000000, 1.000000000000000000),
 ( 0.9956975270656955868, 0.8568959468854907557),
 ( 0.9956975270656955868, 0.8568959468854907557),
 ( 1.000000000000000000, 1.000000000000000000) ) ) 
 REPRESENTATION_ITEM ( '' )  SURFACE ( )  );
#24300=LINE ( 'NONE', #28448, #13894 ) ;
#24301=CARTESIAN_POINT ( 'NONE',  ( 25.64692872815577473, 23.16082795281256068, 110.5102270591923457 ) ) ;
#24302=CARTESIAN_POINT ( 'NONE',  ( 25.64692232868535626, 110.5112661748245131, 23.15582834340323259 ) ) ;
#24303=ORIENTED_EDGE ( 'NONE', *, *, #17280, .T. ) ;
#24304=CARTESIAN_POINT ( 'NONE',  ( 1.833485406944057594, -125.9346397303430223, -72.09189602597842850 ) ) ;
#24305=VECTOR ( 'NONE', #23426, 1000.000000000000114 ) ;
#24307=CARTESIAN_POINT ( 'NONE',  ( 55.49584447822657296, 14.82242356768033886, -71.02133150427242470 ) ) ;
#24308=VECTOR ( 'NONE', #23278, 1000.000000000000114 ) ;
#24310=ORIENTED_EDGE ( 'NONE', *, *, #20276, .T. ) ;
#24311=EDGE_CURVE ( 'NONE', #10429, #21463, #10271, .T. ) ;
#24313=B_SPLINE_CURVE_WITH_KNOTS ( 'NONE', 3,
 ( #1794, #28139, #26126, #216, #17204, #24127, #9004 ),
 .UNSPECIFIED., .F., .F.,
 ( 4, 3, 4 ),
 ( 0.000000000000000000, 0.02398743853561356720, 0.04000277880656211843 ),
 .UNSPECIFIED. ) ;
#24314=VERTEX_POINT ( 'NONE', #18547 ) ;
#24315=LINE ( 'NONE', #402, #8793 ) ;
#24316=B_SPLINE_CURVE_WITH_KNOTS ( 'NONE', 3,
 ( #19776, #24404, #2505, #4674 ),
 .UNSPECIFIED., .F., .F.,
 ( 4, 4 ),
 ( 1.092738104725961435E-16, 0.008383748772659562962 ),
 .UNSPECIFIED. ) ;
#24319=CARTESIAN_POINT ( 'NONE',  ( 2.063896406836609909, -84.29612368209232898, 118.3103904147678804 ) ) ;
#24320=CARTESIAN_POINT ( 'NONE',  ( 32.73300124599732186, 0.000000000000000000, 0.000000000000000000 ) ) ;
#24323=ORIENTED_EDGE ( 'NONE', *, *, #23044, .T. ) ;
#24325=CARTESIAN_POINT ( 'NONE',  ( 25.64692232868535982, 12.12735788170810913, 112.2580042965357592 ) ) ;
#24326=CARTESIAN_POINT ( 'NONE',  ( 109.1592201516379674, -0.0003082430542016361633, -0.007856029051022768092 ) ) ;
#24327=EDGE_CURVE ( 'NONE', #6378, #24693, #14073, .T. ) ;
#24328=CARTESIAN_POINT ( 'NONE',  ( 25.98107933586707574, -74.88680433646190693, -84.80123094405294637 ) ) ;
#24329=CARTESIAN_POINT ( 'NONE',  ( 1.833485406944043827, 45.34878176254417070, -137.8414413349080974 ) ) ;
#24330=FACE_OUTER_BOUND ( 'NONE', #9352, .T. ) ;
#24332=ORIENTED_EDGE ( 'NONE', *, *, #1885, .T. ) ;
#24333=ORIENTED_EDGE ( 'NONE', *, *, #15416, .T. ) ;
#24337=CARTESIAN_POINT ( 'NONE',  ( 109.1589550718174877, -0.007008495014548490887, 0.002874971999843633271 ) ) ;
#24339=( BOUNDED_SURFACE ( )  B_SPLINE_SURFACE ( 3, 1, ( 
 ( #22363, #9544 ),
 ( #9260, #3204 ),
 ( #2771, #2626 ),
 ( #15873, #27076 ) ),
 .UNSPECIFIED., .F., .F., .F. ) 
 B_SPLINE_SURFACE_WITH_KNOTS ( ( 4, 4 ),
 ( 2, 2 ),
 ( 0.000000000000000000, 1.000000000000000000 ),
 ( 0.000000000000000000, 1.000000000000000000 ),
 .UNSPECIFIED. ) 
 GEOMETRIC_REPRESENTATION_ITEM ( )  RATIONAL_B_SPLINE_SURFACE ( (
 ( 1.000000000000000000, 1.000000000000000000),
 ( 0.6386103224230302855, 0.9954351624131538845),
 ( 0.6386103224230302855, 0.9954351624131538845),
 ( 1.000000000000000000, 1.000000000000000000) ) ) 
 REPRESENTATION_ITEM ( '' )  SURFACE ( )  );
#24341=DIRECTION ( 'NONE',  ( -1.000000000000000000, -0.000000000000000000, -0.000000000000000000 ) ) ;
#24344=EDGE_CURVE ( 'NONE', #2563, #4669, #24998, .T. ) ;
#24345=CARTESIAN_POINT ( 'NONE',  ( 25.64660436782554243, 91.68669413043151906, 65.89729635302943223 ) ) ;
#24347=CARTESIAN_POINT ( 'NONE',  ( 1.833485406944057594, 125.9346397303435197, 72.09189602597754742 ) ) ;
#24348=EDGE_CURVE ( 'NONE', #7024, #1356, #4280, .T. ) ;
#24352=B_SPLINE_CURVE_WITH_KNOTS ( 'NONE', 3,
 ( #23203, #3459, #18861, #16713, #25505, #16024, #7267, #7131, #15737, #8994 ),
 .UNSPECIFIED., .F., .F.,
 ( 4, 3, 3, 4 ),
 ( 4.163336342344337027E-17, 0.0002669559177086231047, 0.0005339118354151080542, 0.001067817517169163816 ),
 .UNSPECIFIED. ) ;
#24353=CARTESIAN_POINT ( 'NONE',  ( 2.263178607246658203, 73.90841395012587611, 125.2099936970370635 ) ) ;
#24357=EDGE_CURVE ( 'NONE', #15804, #26995, #23962, .T. ) ;
#24358=CARTESIAN_POINT ( 'NONE',  ( 1.833838850855475933, 15.07960613928627325, 144.3241377520099604 ) ) ;
#24361=CARTESIAN_POINT ( 'NONE',  ( 25.87036335909428431, -0.9898498320579764975, -113.0557711752706354 ) ) ;
#24362=EDGE_CURVE ( 'NONE', #11536, #22381, #22589, .T. ) ;
#24364=ORIENTED_EDGE ( 'NONE', *, *, #20397, .F. ) ;
#24365=DIRECTION ( 'NONE',  ( 0.000000000000000000, -1.000000000000000000, -3.469446951953603342E-16 ) ) ;
#24368=EDGE_LOOP ( 'NONE', ( #340, #25732, #22712, #11898 ) ) ;
#24369=ORIENTED_EDGE ( 'NONE', *, *, #9890, .F. ) ;
#24370=B_SPLINE_CURVE_WITH_KNOTS ( 'NONE', 3,
 ( #6303, #28295, #8595, #26426, #6725, #20084 ),
 .UNSPECIFIED., .F., .F.,
 ( 4, 2, 4 ),
 ( 2.168404344971008868E-18, 0.0006311636237756755499, 0.001262327247551348931 ),
 .UNSPECIFIED. ) ;
#24371=CARTESIAN_POINT ( 'NONE',  ( 32.73300124599741423, 117.3295799645430435, -8.473903470904879498 ) ) ;
#24374=DIRECTION ( 'NONE',  ( 0.000000000000000000, 0.000000000000000000, 1.000000000000000000 ) ) ;
#24378=EDGE_CURVE ( 'NONE', #15269, #14457, #613, .T. ) ;
#24381=CARTESIAN_POINT ( 'NONE',  ( 26.11404676487257603, -65.63269960453305885, 92.25884714080386573 ) ) ;
#24382=FACE_OUTER_BOUND ( 'NONE', #15081, .T. ) ;
#24383=DIRECTION ( 'NONE',  ( 0.000000000000000000, 0.000000000000000000, 1.000000000000000000 ) ) ;
#24384=EDGE_CURVE ( 'NONE', #15583, #20437, #5454, .T. ) ;
#24385=VERTEX_POINT ( 'NONE', #27314 ) ;
#24387=CARTESIAN_POINT ( 'NONE',  ( 6.224689322667647851, -147.4941644018827560, -12.92299475787110019 ) ) ;
#24388=CIRCLE ( 'NONE', #27112, 151.1787379149930359 ) ;
#24389=CARTESIAN_POINT ( 'NONE',  ( 1.833809397773872307, -144.2961330457378608, -15.34508223002595884 ) ) ;
#24391=B_SPLINE_CURVE_WITH_KNOTS ( 'NONE', 3,
 ( #19519, #15466, #17218, #24274 ),
 .UNSPECIFIED., .F., .F.,
 ( 4, 4 ),
 ( 3.450729209734431367E-16, 0.01077107486149810056 ),
 .UNSPECIFIED. ) ;
#24392=CARTESIAN_POINT ( 'NONE',  ( 13.36082413113061307, 37.97423473099499347, -148.1362653800998999 ) ) ;
#24393=DIRECTION ( 'NONE',  ( 0.000000000000000000, 0.000000000000000000, 1.000000000000000000 ) ) ;
#24396=FACE_OUTER_BOUND ( 'NONE', #6079, .T. ) ;
#24399=ORIENTED_EDGE ( 'NONE', *, *, #23662, .T. ) ;
#24401=ORIENTED_EDGE ( 'NONE', *, *, #22336, .F. ) ;
#24402=CARTESIAN_POINT ( 'NONE',  ( 32.73300124599739291, -99.90245962373785460, -62.10906484417343165 ) ) ;
#24403=ORIENTED_EDGE ( 'NONE', *, *, #21879, .F. ) ;
#24404=CARTESIAN_POINT ( 'NONE',  ( 30.59138290137876837, 70.47507990428549363, 92.40465044710759912 ) ) ;
#24405=AXIS2_PLACEMENT_3D ( 'NONE', #6978, #18169, #13711 ) ;
#24406=AXIS2_PLACEMENT_3D ( 'NONE', #21312, #23069, #19019 ) ;
#24409=DIRECTION ( 'NONE',  ( 0.000000000000000000, 0.000000000000000000, -1.000000000000000000 ) ) ;
#24411=LINE ( 'NONE', #20209, #15617 ) ;
#24413=CARTESIAN_POINT ( 'NONE',  ( 2.433796855181233454, 133.5135467655518369, 57.85512797797937168 ) ) ;
#24415=CARTESIAN_POINT ( 'NONE',  ( 25.69398547355841700, -34.19446713634657442, 107.6418378907642932 ) ) ;
#24417=( BOUNDED_SURFACE ( )  B_SPLINE_SURFACE ( 3, 1, ( 
 ( #19668, #26296 ),
 ( #6592, #15344 ),
 ( #24152, #4415 ),
 ( #13186, #21978 ) ),
 .UNSPECIFIED., .F., .F., .F. ) 
 B_SPLINE_SURFACE_WITH_KNOTS ( ( 4, 4 ),
 ( 2, 2 ),
 ( 0.000000000000000000, 1.000000000000000000 ),
 ( 0.000000000000000000, 1.000000000000000000 ),
 .UNSPECIFIED. ) 
 GEOMETRIC_REPRESENTATION_ITEM ( )  RATIONAL_B_SPLINE_SURFACE ( (
 ( 1.000000000000000000, 1.000000000000000000),
 ( 0.6386103224230302855, 0.9954351624131538845),
 ( 0.6386103224230302855, 0.9954351624131538845),
 ( 1.000000000000000000, 1.000000000000000000) ) ) 
 REPRESENTATION_ITEM ( '' )  SURFACE ( )  );
#24419=ORIENTED_EDGE ( 'NONE', *, *, #935, .T. ) ;
#24420=CARTESIAN_POINT ( 'NONE',  ( 10.93730112725971715, 20.69552240458328995, 149.7554878793148703 ) ) ;
#24427=VERTEX_POINT ( 'NONE', #11000 ) ;
#24428=CARTESIAN_POINT ( 'NONE',  ( 1.833809397773814576, -45.01060836636616358, 137.9524943416724625 ) ) ;
#24429=AXIS2_PLACEMENT_3D ( 'NONE', #18594, #14409, #16139 ) ;
#24430=CARTESIAN_POINT ( 'NONE',  ( 32.73300124599739291, -108.9684813982485707, -44.31599526638064646 ) ) ;
#24431=LINE ( 'NONE', #4841, #19896 ) ;
#24432=CARTESIAN_POINT ( 'NONE',  ( 2.433796855181205476, 46.34326152018925171, -137.9325382748280333 ) ) ;
#24433=VECTOR ( 'NONE', #3657, 1000.000000000000114 ) ;
#24435=CARTESIAN_POINT ( 'NONE',  ( 1.832998868059890096, -137.8420662456173034, 45.34898734666001019 ) ) ;
#24437=EDGE_LOOP ( 'NONE', ( #20201, #5651, #828, #8426 ) ) ;
#24438=CARTESIAN_POINT ( 'NONE',  ( 30.59138290137911653, 33.33271994911483915, -111.3296280985502165 ) ) ;
#24439=EDGE_CURVE ( 'NONE', #27978, #11607, #3986, .T. ) ;
#24441=CARTESIAN_POINT ( 'NONE',  ( 109.1587776205901577, 0.002904816147418920556, 0.006729130500857913137 ) ) ;
#24442=VERTEX_POINT ( 'NONE', #1681 ) ;
#24446=CARTESIAN_POINT ( 'NONE',  ( 32.73300124599732186, 0.000000000000000000, 0.000000000000000000 ) ) ;
#24448=CARTESIAN_POINT ( 'NONE',  ( 109.1586900883932856, 0.004113747440992326053, -0.005833932871491330496 ) ) ;
#24455=VERTEX_POINT ( 'NONE', #8987 ) ;
#24456=CIRCLE ( 'NONE', #14808, 151.1787379149930359 ) ;
#24459=B_SPLINE_CURVE_WITH_KNOTS ( 'NONE', 3,
 ( #3620, #18741, #1737, #5495, #6092, #18886, #20897 ),
 .UNSPECIFIED., .F., .F.,
 ( 4, 3, 4 ),
 ( 0.000000000000000000, 0.02398743853561404946, 0.04000277880656225027 ),
 .UNSPECIFIED. ) ;
#24461=DIRECTION ( 'NONE',  ( -0.5914120900931443270, 0.6476200150380249099, -0.4804373588864701006 ) ) ;
#24464=CARTESIAN_POINT ( 'NONE',  ( 1.833838848569457225, 144.3334397096297721, 14.99110384899575621 ) ) ;
#24466=CARTESIAN_POINT ( 'NONE',  ( 13.84597867724985321, -121.4327876424619461, 82.31427113894737602 ) ) ;
#24468=CARTESIAN_POINT ( 'NONE',  ( 30.59138290137878613, 2.701446546448210029, 116.1811451928593044 ) ) ;
#24469=FACE_OUTER_BOUND ( 'NONE', #26789, .T. ) ;
#24470=CARTESIAN_POINT ( 'NONE',  ( 109.1721716018069657, 0.01392660302850754449, 0.009868622090676223979 ) ) ;
#24472=CARTESIAN_POINT ( 'NONE',  ( 6.224689322667630975, 89.08920297664369059, -118.2566963816762211 ) ) ;
#24473=VERTEX_POINT ( 'NONE', #13283 ) ;
#24474=CARTESIAN_POINT ( 'NONE',  ( 1.834118845439484335, 72.40084790867331321, 125.7578880615047439 ) ) ;
#24477=VERTEX_POINT ( 'NONE', #25608 ) ;
#24479=( BOUNDED_SURFACE ( )  B_SPLINE_SURFACE ( 3, 1, ( 
 ( #24119, #6841 ),
 ( #4382, #65 ),
 ( #19771, #22081 ),
 ( #13156, #11152 ) ),
 .UNSPECIFIED., .F., .F., .F. ) 
 B_SPLINE_SURFACE_WITH_KNOTS ( ( 4, 4 ),
 ( 2, 2 ),
 ( 0.000000000000000000, 1.000000000000000000 ),
 ( 0.000000000000000000, 1.000000000000000000 ),
 .UNSPECIFIED. ) 
 GEOMETRIC_REPRESENTATION_ITEM ( )  RATIONAL_B_SPLINE_SURFACE ( (
 ( 1.000000000000000000, 1.000000000000000000),
 ( 0.9960225298536222738, 0.9999952330161893110),
 ( 0.9960225298536222738, 0.9999952330161893110),
 ( 1.000000000000000000, 1.000000000000000000) ) ) 
 REPRESENTATION_ITEM ( '' )  SURFACE ( )  );
#24480=ORIENTED_EDGE ( 'NONE', *, *, #10128, .T. ) ;
#24481=ORIENTED_EDGE ( 'NONE', *, *, #5525, .T. ) ;
#24482=VECTOR ( 'NONE', #16849, 1000.000000000000000 ) ;
#24483=CARTESIAN_POINT ( 'NONE',  ( 109.1721716018069657, 0.01281875973824526428, 0.01127028715940106736 ) ) ;
#24484=DIRECTION ( 'NONE',  ( 0.000000000000000000, 0.000000000000000000, 1.000000000000000000 ) ) ;
#24486=FACE_OUTER_BOUND ( 'NONE', #2682, .T. ) ;
#24488=CARTESIAN_POINT ( 'NONE',  ( 2.433796855181205476, 28.83182736670536528, 142.6247129145649239 ) ) ;
#24489=ORIENTED_EDGE ( 'NONE', *, *, #10163, .T. ) ;
#24493=CARTESIAN_POINT ( 'NONE',  ( 25.81918753295377300, 91.98563552013041544, 65.67738364544763385 ) ) ;
#24495=CARTESIAN_POINT ( 'NONE',  ( 1.833838850855486147, 141.9572669680999013, -30.08297881069537993 ) ) ;
#24496=CARTESIAN_POINT ( 'NONE',  ( 25.64692232868535626, -46.22343382108668663, -103.0161468101951954 ) ) ;
#24499=FACE_OUTER_BOUND ( 'NONE', #8863, .T. ) ;
#24500=CARTESIAN_POINT ( 'NONE',  ( 55.49584447822657296, 68.91748907713619587, -22.67407039687169501 ) ) ;
#24501=CARTESIAN_POINT ( 'NONE',  ( 1.833485406944043827, 58.53321471326877656, 132.7804117027889674 ) ) ;
#24503=VECTOR ( 'NONE', #7848, 999.9999999999998863 ) ;
#24508=ORIENTED_EDGE ( 'NONE', *, *, #23183, .F. ) ;
#24511=CARTESIAN_POINT ( 'NONE',  ( 25.69398547355841700, 107.1830796521259259, -35.60637981494741666 ) ) ;
#24512=VERTEX_POINT ( 'NONE', #12621 ) ;
#24514=AXIS2_PLACEMENT_3D ( 'NONE', #8059, #4227, #21121 ) ;
#24515=ORIENTED_EDGE ( 'NONE', *, *, #74, .T. ) ;
#24516=( BOUNDED_SURFACE ( )  B_SPLINE_SURFACE ( 3, 1, ( 
 ( #4295, #28452 ),
 ( #6749, #8617 ),
 ( #2116, #1841 ),
 ( #4567, #13339 ) ),
 .UNSPECIFIED., .F., .F., .F. ) 
 B_SPLINE_SURFACE_WITH_KNOTS ( ( 4, 4 ),
 ( 2, 2 ),
 ( 0.000000000000000000, 1.000000000000000000 ),
 ( 0.000000000000000000, 1.000000000000000000 ),
 .UNSPECIFIED. ) 
 GEOMETRIC_REPRESENTATION_ITEM ( )  RATIONAL_B_SPLINE_SURFACE ( (
 ( 1.000000000000000000, 1.000000000000000000),
 ( 0.9956975270656954757, 0.8568959468854893125),
 ( 0.9956975270656954757, 0.8568959468854893125),
 ( 1.000000000000000000, 1.000000000000000000) ) ) 
 REPRESENTATION_ITEM ( '' )  SURFACE ( )  );
#24518=CARTESIAN_POINT ( 'NONE',  ( 6.224689322667630975, -33.28770499679432504, 144.2687111683194416 ) ) ;
#24520=ADVANCED_FACE ( 'NONE', ( #28019 ), #22143, .F. ) ;
#24521=B_SPLINE_CURVE_WITH_KNOTS ( 'NONE', 3,
 ( #11278, #21796, #20046, #1917 ),
 .UNSPECIFIED., .F., .F.,
 ( 4, 4 ),
 ( 0.000000000000000000, 0.008383560773332731156 ),
 .UNSPECIFIED. ) ;
#24524=CARTESIAN_POINT ( 'NONE',  ( 1.833721034905622549, 138.1171912769431174, 44.50273803001984874 ) ) ;
#24527=EDGE_CURVE ( 'NONE', #9673, #25484, #23256, .T. ) ;
#24529=CARTESIAN_POINT ( 'NONE',  ( 109.1587776205901577, 0.006944419901758093830, 0.002343968083389380997 ) ) ;
#24532=CARTESIAN_POINT ( 'NONE',  ( 25.64700659047694131, 66.18331466615558156, 91.48068002582046176 ) ) ;
#24533=CARTESIAN_POINT ( 'NONE',  ( 24.01988960052067767, 4.273195451970473790, -130.9749633972836023 ) ) ;
#24534=CARTESIAN_POINT ( 'NONE',  ( 109.1589550718174877, 0.003591809816104994842, 0.006669585340466659650 ) ) ;
#24536=CARTESIAN_POINT ( 'NONE',  ( 2.063896406836605024, -98.19887492195931600, 107.0521644432414092 ) ) ;
#24537=CIRCLE ( 'NONE', #3375, 117.6351876552689504 ) ;
#24540=CARTESIAN_POINT ( 'NONE',  ( 25.64703792032470275, 91.43447020678432580, 66.24710921678085640 ) ) ;
#24541=CARTESIAN_POINT ( 'NONE',  ( 25.64692232868534560, -66.63160215461202540, -91.15460455808893414 ) ) ;
#24542=CARTESIAN_POINT ( 'NONE',  ( 109.1721716018069515, -0.01019541462303045869, 0.01368917435590585353 ) ) ;
#24546=ORIENTED_EDGE ( 'NONE', *, *, #11221, .T. ) ;
#24547=CARTESIAN_POINT ( 'NONE',  ( 26.11404676487257603, -47.08215554553588333, 102.9690087468800073 ) ) ;
#24548=AXIS2_PLACEMENT_3D ( 'NONE', #5025, #9214, #574 ) ;
#24550=CARTESIAN_POINT ( 'NONE',  ( 10.93730112725972781, -56.95489579269845137, 140.0398180619108359 ) ) ;
#24552=EDGE_LOOP ( 'NONE', ( #17216, #16270, #814, #14929 ) ) ;
#24557=CARTESIAN_POINT ( 'NONE',  ( 1.833838850855450398, -97.03125735562164778, -107.8971100408360684 ) ) ;
#24563=EDGE_CURVE ( 'NONE', #24705, #22495, #11921, .T. ) ;
#24565=( BOUNDED_SURFACE ( )  B_SPLINE_SURFACE ( 3, 1, ( 
 ( #2941, #22233 ),
 ( #772, #13719 ),
 ( #27093, #19923 ),
 ( #15442, #4510 ) ),
 .UNSPECIFIED., .F., .F., .F. ) 
 B_SPLINE_SURFACE_WITH_KNOTS ( ( 4, 4 ),
 ( 2, 2 ),
 ( 0.000000000000000000, 1.000000000000000000 ),
 ( 0.000000000000000000, 1.000000000000000000 ),
 .UNSPECIFIED. ) 
 GEOMETRIC_REPRESENTATION_ITEM ( )  RATIONAL_B_SPLINE_SURFACE ( (
 ( 1.000000000000000000, 1.000000000000000000),
 ( 0.9956975270656955868, 0.8568959468854907557),
 ( 0.9956975270656955868, 0.8568959468854907557),
 ( 1.000000000000000000, 1.000000000000000000) ) ) 
 REPRESENTATION_ITEM ( '' )  SURFACE ( )  );
#24568=CARTESIAN_POINT ( 'NONE',  ( 1.833750490713712766, -72.32354185792470957, -125.8019536335927597 ) ) ;
#24572=CARTESIAN_POINT ( 'NONE',  ( 25.70243777736189728, -0.7331659071603116029, 112.9457924277214005 ) ) ;
#24573=CARTESIAN_POINT ( 'NONE',  ( 32.73300124599769134, -51.32617430724849328, -105.8473486001054198 ) ) ;
#24575=ORIENTED_EDGE ( 'NONE', *, *, #653, .T. ) ;
#24579=CARTESIAN_POINT ( 'NONE',  ( 1.833721036429677875, -0.3559391723973897581, -145.1093571290645627 ) ) ;
#24580=CARTESIAN_POINT ( 'NONE',  ( 1.833838848569415036, 45.01064392477934462, 137.9525894882059447 ) ) ;
#24583=ORIENTED_EDGE ( 'NONE', *, *, #13795, .T. ) ;
#24584=CARTESIAN_POINT ( 'NONE',  ( 2.063896406836605024, -118.3103904147687331, 84.29612368209116369 ) ) ;
#24585=ORIENTED_EDGE ( 'NONE', *, *, #18448, .F. ) ;
#24586=CARTESIAN_POINT ( 'NONE',  ( 25.86096068574581253, -112.5344699600049978, 10.82483750674566814 ) ) ;
#24587=B_SPLINE_CURVE_WITH_KNOTS ( 'NONE', 3,
 ( #13140, #6684, #17872, #20184, #46, #4935, #2482 ),
 .UNSPECIFIED., .F., .F.,
 ( 4, 3, 4 ),
 ( 6.445168920560267517E-16, 0.02816610861753245099, 0.04000277880656284701 ),
 .UNSPECIFIED. ) ;
#24591=ORIENTED_EDGE ( 'NONE', *, *, #24384, .F. ) ;
#24592=CARTESIAN_POINT ( 'NONE',  ( 25.87036335909425944, 112.3329723497412118, -12.80197335559845584 ) ) ;
#24594=EDGE_CURVE ( 'NONE', #2946, #7265, #24637, .T. ) ;
#24595=CARTESIAN_POINT ( 'NONE',  ( 109.1592201516379674, 0.007845213074660002325, 0.0005146241775907644525 ) ) ;
#24597=EDGE_CURVE ( 'NONE', #675, #7808, #9417, .T. ) ;
#24598=DIRECTION ( 'NONE',  ( 0.000000000000000000, 0.000000000000000000, 1.000000000000000000 ) ) ;
#24600=( BOUNDED_SURFACE ( )  B_SPLINE_SURFACE ( 3, 1, ( 
 ( #5160, #273 ),
 ( #17959, #18390 ),
 ( #13509, #20418 ),
 ( #13357, #9061 ) ),
 .UNSPECIFIED., .F., .F., .F. ) 
 B_SPLINE_SURFACE_WITH_KNOTS ( ( 4, 4 ),
 ( 2, 2 ),
 ( 0.000000000000000000, 1.000000000000000000 ),
 ( 0.000000000000000000, 1.000000000000000000 ),
 .UNSPECIFIED. ) 
 GEOMETRIC_REPRESENTATION_ITEM ( )  RATIONAL_B_SPLINE_SURFACE ( (
 ( 1.000000000000000000, 1.000000000000000000),
 ( 0.6386103224230302855, 0.9954351624131538845),
 ( 0.6386103224230302855, 0.9954351624131538845),
 ( 1.000000000000000000, 1.000000000000000000) ) ) 
 REPRESENTATION_ITEM ( '' )  SURFACE ( )  );
#24601=CARTESIAN_POINT ( 'NONE',  ( 109.1586900883932856, -0.004851151255031890298, 0.005236795036868143773 ) ) ;
#24604=CARTESIAN_POINT ( 'NONE',  ( 1.833485406944043827, -125.9346397303440455, 72.09189602597663793 ) ) ;
#24605=EDGE_LOOP ( 'NONE', ( #15735, #7460, #11362, #4725 ) ) ;
#24606=CARTESIAN_POINT ( 'NONE',  ( 6.224689322667647851, 147.4941644018828129, 12.92299475787008234 ) ) ;
#24608=DIRECTION ( 'NONE',  ( 0.000000000000000000, 0.000000000000000000, 1.000000000000000000 ) ) ;
#24609=ORIENTED_EDGE ( 'NONE', *, *, #12313, .F. ) ;
#24611=VERTEX_POINT ( 'NONE', #7260 ) ;
#24614=CARTESIAN_POINT ( 'NONE',  ( 25.70243777736190438, -24.19989514742795933, 110.3252221127464736 ) ) ;
#24617=CARTESIAN_POINT ( 'NONE',  ( 32.73300124599732186, 0.000000000000000000, 0.000000000000000000 ) ) ;
#24618=ADVANCED_FACE ( 'NONE', ( #16016 ), #17174, .F. ) ;
#24620=ORIENTED_EDGE ( 'NONE', *, *, #219, .T. ) ;
#24621=CARTESIAN_POINT ( 'NONE',  ( 2.063896406836609909, -142.3682421260905642, -28.88716984836465684 ) ) ;
#24623=CARTESIAN_POINT ( 'NONE',  ( 1.833838850093440387, -145.1097630783161492, 3.453305159929904334E-06 ) ) ;
#24625=CARTESIAN_POINT ( 'NONE',  ( 9.884929003653608603, 78.87917189085089831, -128.2151425008033243 ) ) ;
#24626=VERTEX_POINT ( 'NONE', #9693 ) ;
#24628=EDGE_CURVE ( 'NONE', #4100, #23015, #7124, .T. ) ;
#24629=B_SPLINE_CURVE_WITH_KNOTS ( 'NONE', 3,
 ( #4542, #22261, #13604, #11449, #18066, #5114, #24276 ),
 .UNSPECIFIED., .F., .F.,
 ( 4, 3, 4 ),
 ( 5.872724359755720846E-16, 0.02816610861753247527, 0.04000277880656283314 ),
 .UNSPECIFIED. ) ;
#24631=CARTESIAN_POINT ( 'NONE',  ( 2.433796855181205476, 142.6247129145651797, -28.83182736670396196 ) ) ;
#24633=VERTEX_POINT ( 'NONE', #18469 ) ;
#24634=EDGE_CURVE ( 'NONE', #14882, #2900, #26989, .T. ) ;
#24636=ORIENTED_EDGE ( 'NONE', *, *, #27190, .F. ) ;
#24637=B_SPLINE_CURVE_WITH_KNOTS ( 'NONE', 3,
 ( #13425, #22225, #13712, #330, #22374, #2637, #5226, #11418, #3077, #11851 ),
 .UNSPECIFIED., .F., .F.,
 ( 4, 3, 3, 4 ),
 ( 1.387778780781445676E-17, 0.0002669560319015815792, 0.0005492286108966455737, 0.0008315040496093443556 ),
 .UNSPECIFIED. ) ;
#24638=CARTESIAN_POINT ( 'NONE',  ( 10.93730112725972425, -42.00474393596362432, 145.2260730187398678 ) ) ;
#24639=CARTESIAN_POINT ( 'NONE',  ( 109.1624594426973118, -0.01358749486988776456, 0.008380433676413060612 ) ) ;
#24641=CARTESIAN_POINT ( 'NONE',  ( 2.063896406836609909, -108.8509294491458661, -96.20114399516505443 ) ) ;
#24642=CARTESIAN_POINT ( 'NONE',  ( 119.2224693531408803, 70.00000000000002842, 19.99999999999997513 ) ) ;
#24643=EDGE_LOOP ( 'NONE', ( #5312, #19304, #26254, #8130 ) ) ;
#24645=CARTESIAN_POINT ( 'NONE',  ( 25.64660436782558151, 45.39454672041254923, -103.3839381879726886 ) ) ;
#24646=CARTESIAN_POINT ( 'NONE',  ( 109.1589550718174877, -0.006257602293694239197, 0.004269295012386535582 ) ) ;
#24647=ORIENTED_EDGE ( 'NONE', *, *, #27619, .T. ) ;
#24649=EDGE_LOOP ( 'NONE', ( #7971, #17076, #2752, #17506 ) ) ;
#24655=CARTESIAN_POINT ( 'NONE',  ( 1.833691583653523693, 58.69608658929927714, 132.7086741139084722 ) ) ;
#24657=B_SPLINE_CURVE_WITH_KNOTS ( 'NONE', 3,
 ( #12662, #21731, #28060, #1589, #26050, #4163, #6477 ),
 .UNSPECIFIED., .F., .F.,
 ( 4, 3, 4 ),
 ( 6.397367602755259510E-16, 0.02816610861753244405, 0.04000277880656278456 ),
 .UNSPECIFIED. ) ;
#24659=CARTESIAN_POINT ( 'NONE',  ( 109.1586900883932856, -0.006130969560693689396, -0.003656351050324864460 ) ) ;
#24661=( BOUNDED_SURFACE ( )  B_SPLINE_SURFACE ( 3, 1, ( 
 ( #23449, #10068 ),
 ( #12216, #25478 ),
 ( #5600, #21123 ),
 ( #23182, #27760 ) ),
 .UNSPECIFIED., .F., .F., .F. ) 
 B_SPLINE_SURFACE_WITH_KNOTS ( ( 4, 4 ),
 ( 2, 2 ),
 ( 0.000000000000000000, 1.000000000000000000 ),
 ( 0.000000000000000000, 1.000000000000000000 ),
 .UNSPECIFIED. ) 
 GEOMETRIC_REPRESENTATION_ITEM ( )  RATIONAL_B_SPLINE_SURFACE ( (
 ( 1.000000000000000000, 1.000000000000000000),
 ( 0.6386103224230316178, 0.9954351624131538845),
 ( 0.6386103224230316178, 0.9954351624131538845),
 ( 1.000000000000000000, 1.000000000000000000) ) ) 
 REPRESENTATION_ITEM ( '' )  SURFACE ( )  );
#24662=FACE_OUTER_BOUND ( 'NONE', #13421, .T. ) ;
#24663=EDGE_CURVE ( 'NONE', #17576, #19356, #19805, .T. ) ;
#24664=EDGE_CURVE ( 'NONE', #24250, #19237, #1258, .T. ) ;
#24667=CARTESIAN_POINT ( 'NONE',  ( 26.11404676487259024, 107.3263591096435476, -36.06104232266339693 ) ) ;
#24668=EDGE_LOOP ( 'NONE', ( #19909, #4994, #18827, #28389 ) ) ;
#24671=ORIENTED_EDGE ( 'NONE', *, *, #8647, .T. ) ;
#24672=CARTESIAN_POINT ( 'NONE',  ( 26.11404676487257603, -98.61392875273402581, 55.62948129436210110 ) ) ;
#24674=CARTESIAN_POINT ( 'NONE',  ( 2.430230287190589422, 125.2872625092172569, -74.01081053030968349 ) ) ;
#24675=CARTESIAN_POINT ( 'NONE',  ( 25.64681081121879203, -103.3177883989782657, 45.54494737132187510 ) ) ;
#24677=CARTESIAN_POINT ( 'NONE',  ( 109.1592201516379674, 0.006649399203953390916, 0.004194960840980714069 ) ) ;
#24678=CARTESIAN_POINT ( 'NONE',  ( 109.1589550718175161, 0.005994046294305907172, -0.004632048724982925844 ) ) ;
#24679=CARTESIAN_POINT ( 'NONE',  ( 25.64708010899961721, 66.41183455464135932, 91.31497827399759615 ) ) ;
#24680=CARTESIAN_POINT ( 'NONE',  ( 8.186469777910854617, -134.9918587298867863, 63.89871389959409242 ) ) ;
#24681=CARTESIAN_POINT ( 'NONE',  ( 109.1592201516379674, 0.002913740842108636896, 0.007302213399779935825 ) ) ;
#24684=DIRECTION ( 'NONE',  ( -1.000000000000000000, -0.000000000000000000, -0.000000000000000000 ) ) ;
#24686=ADVANCED_FACE ( 'NONE', ( #7840 ), #13300, .F. ) ;
#24687=ORIENTED_EDGE ( 'NONE', *, *, #19717, .T. ) ;
#24689=CARTESIAN_POINT ( 'NONE',  ( 1.833603222531972277, -144.2675221341993108, -15.61050054119179187 ) ) ;
#24690=DIRECTION ( 'NONE',  ( -0.5946245182733608248, -0.4749651461092209148, -0.6487139525627763081 ) ) ;
#24691=CARTESIAN_POINT ( 'NONE',  ( 6.224689322667647851, -97.14981701196397523, 111.7293398381261653 ) ) ;
#24693=VERTEX_POINT ( 'NONE', #12408 ) ;
#24694=CARTESIAN_POINT ( 'NONE',  ( 16.05277956358212066, 34.34928806929423217, 139.1285124304119165 ) ) ;
#24695=( BOUNDED_SURFACE ( )  B_SPLINE_SURFACE ( 3, 1, ( 
 ( #2663, #11736 ),
 ( #26692, #22102 ),
 ( #11169, #4535 ),
 ( #15760, #7004 ) ),
 .UNSPECIFIED., .F., .F., .F. ) 
 B_SPLINE_SURFACE_WITH_KNOTS ( ( 4, 4 ),
 ( 2, 2 ),
 ( 0.000000000000000000, 1.000000000000000000 ),
 ( 0.000000000000000000, 1.000000000000000000 ),
 .UNSPECIFIED. ) 
 GEOMETRIC_REPRESENTATION_ITEM ( )  RATIONAL_B_SPLINE_SURFACE ( (
 ( 1.000000000000000000, 1.000000000000000000),
 ( 0.6386103224230316178, 0.9954351624131538845),
 ( 0.6386103224230316178, 0.9954351624131538845),
 ( 1.000000000000000000, 1.000000000000000000) ) ) 
 REPRESENTATION_ITEM ( '' )  SURFACE ( )  );
#24696=EDGE_CURVE ( 'NONE', #18134, #22961, #27366, .T. ) ;
#24697=ORIENTED_EDGE ( 'NONE', *, *, #14566, .F. ) ;
#24699=CARTESIAN_POINT ( 'NONE',  ( 55.79472521941428198, -30.25520714117862653, -66.16469064668328315 ) ) ;
#24700=ORIENTED_EDGE ( 'NONE', *, *, #27657, .F. ) ;
#24702=EDGE_CURVE ( 'NONE', #3658, #23165, #18076, .T. ) ;
#24704=CARTESIAN_POINT ( 'NONE',  ( 1.833691583653538348, -96.83253123394135287, -108.0753610255262913 ) ) ;
#24705=VERTEX_POINT ( 'NONE', #7651 ) ;
#24707=ORIENTED_EDGE ( 'NONE', *, *, #8363, .T. ) ;
#24709=FACE_OUTER_BOUND ( 'NONE', #13078, .T. ) ;
#24712=CARTESIAN_POINT ( 'NONE',  ( 32.73300124599735739, 62.10906484417237294, 99.90245962373859356 ) ) ;
#24715=CARTESIAN_POINT ( 'NONE',  ( 25.65782528836480481, 83.52701600504883572, 75.98558751977803638 ) ) ;
#24718=ADVANCED_FACE ( 'NONE', ( #16264 ), #8442, .T. ) ;
#24719=DIRECTION ( 'NONE',  ( 0.8320502949607718746, 0.000000000000000000, -0.5547001952908368061 ) ) ;
#24722=CARTESIAN_POINT ( 'NONE',  ( 24.22246935314087324, -69.99999999999998579, 40.00000000000003553 ) ) ;
#24723=ORIENTED_EDGE ( 'NONE', *, *, #6351, .T. ) ;
#24725=EDGE_CURVE ( 'NONE', #13256, #1421, #717, .T. ) ;
#24727=CARTESIAN_POINT ( 'NONE',  ( 10.93730112725953596, 92.80059208661681680, 119.3442956573276206 ) ) ;
#24728=ORIENTED_EDGE ( 'NONE', *, *, #23257, .F. ) ;
#24729=FACE_OUTER_BOUND ( 'NONE', #9133, .T. ) ;
#24731=CARTESIAN_POINT ( 'NONE',  ( 1.833485406944043827, 117.0814567582556407, -85.72460230293573602 ) ) ;
#24733=( BOUNDED_SURFACE ( )  B_SPLINE_SURFACE ( 3, 1, ( 
 ( #7945, #18853 ),
 ( #14811, #23621 ),
 ( #3881, #21431 ),
 ( #10502, #3314 ) ),
 .UNSPECIFIED., .F., .F., .F. ) 
 B_SPLINE_SURFACE_WITH_KNOTS ( ( 4, 4 ),
 ( 2, 2 ),
 ( 0.000000000000000000, 1.000000000000000000 ),
 ( 0.000000000000000000, 1.000000000000000000 ),
 .UNSPECIFIED. ) 
 GEOMETRIC_REPRESENTATION_ITEM ( )  RATIONAL_B_SPLINE_SURFACE ( (
 ( 1.000000000000000000, 1.000000000000000000),
 ( 0.9956975270656955868, 0.8568959468854907557),
 ( 0.9956975270656955868, 0.8568959468854907557),
 ( 1.000000000000000000, 1.000000000000000000) ) ) 
 REPRESENTATION_ITEM ( '' )  SURFACE ( )  );
#24734=VERTEX_POINT ( 'NONE', #24488 ) ;
#24736=VERTEX_POINT ( 'NONE', #7074 ) ;
#24737=CARTESIAN_POINT ( 'NONE',  ( 28.37644542392843405, -111.8804331835011681, -54.25112470585834501 ) ) ;
#24738=B_SPLINE_CURVE_WITH_KNOTS ( 'NONE', 3,
 ( #9217, #2735, #577, #861, #26907, #1010 ),
 .UNSPECIFIED., .F., .F.,
 ( 4, 2, 4 ),
 ( 1.041737195591640451E-17, 0.0006311571484586107764, 0.001262314296917211144 ),
 .UNSPECIFIED. ) ;
#24740=B_SPLINE_CURVE_WITH_KNOTS ( 'NONE', 3,
 ( #16311, #11285, #9125, #26953, #9273, #9421, #20053, #15734, #4810, #13576 ),
 .UNSPECIFIED., .F., .F.,
 ( 4, 3, 3, 4 ),
 ( 3.816391647148975608E-17, 0.0002669559177086187137, 0.0005339118354150955859, 0.001067817517169158828 ),
 .UNSPECIFIED. ) ;
#24741=LINE ( 'NONE', #9328, #4634 ) ;
#24742=CARTESIAN_POINT ( 'NONE',  ( 10.93730112725997294, 26.59437931460951177, -148.8212007290660210 ) ) ;
#24745=CARTESIAN_POINT ( 'NONE',  ( 119.2224693531408803, -90.00000000000005684, -40.00000000000002842 ) ) ;
#24746=ORIENTED_EDGE ( 'NONE', *, *, #3216, .T. ) ;
#24747=CARTESIAN_POINT ( 'NONE',  ( 10.93730112725972425, -65.95960219663204782, 136.0306644680981094 ) ) ;
#24748=CARTESIAN_POINT ( 'NONE',  ( 109.1586059443104944, -0.006808232911144252927, 0.001921075557427531387 ) ) ;
#24750=VERTEX_POINT ( 'NONE', #5178 ) ;
#24751=CARTESIAN_POINT ( 'NONE',  ( 25.65782528836481546, -91.01210296572892844, -66.83837989650162115 ) ) ;
#24753=EDGE_CURVE ( 'NONE', #26116, #7560, #24917, .T. ) ;
#24755=FACE_OUTER_BOUND ( 'NONE', #13018, .T. ) ;
#24756=CARTESIAN_POINT ( 'NONE',  ( 1.833721034905647418, 108.0754384393934799, 96.83259691102536237 ) ) ;
#24757=LINE ( 'NONE', #8769, #8896 ) ;
#24759=CARTESIAN_POINT ( 'NONE',  ( 109.1589550718174877, 0.005994046294307805826, 0.004632048724973738749 ) ) ;
#24760=CARTESIAN_POINT ( 'NONE',  ( 26.11404676487256893, -55.62948129436175293, -98.61392875273419634 ) ) ;
#24761=CARTESIAN_POINT ( 'NONE',  ( 1.831572820252009626, 145.1082523917587253, -0.9871191512919683664 ) ) ;
#24762=CARTESIAN_POINT ( 'NONE',  ( 32.73300124599739291, 55.46353551262154014, -103.7392577722169875 ) ) ;
#24763=EDGE_CURVE ( 'NONE', #20443, #8696, #19460, .T. ) ;
#24765=CARTESIAN_POINT ( 'NONE',  ( 10.93730112725994275, -26.59437931460641025, -148.8212007290665042 ) ) ;
#24767=B_SPLINE_CURVE_WITH_KNOTS ( 'NONE', 3,
 ( #10463, #15316, #14901, #78 ),
 .UNSPECIFIED., .F., .F.,
 ( 4, 4 ),
 ( 6.938893903907228378E-18, 0.008383560773332717278 ),
 .UNSPECIFIED. ) ;
#24768=CARTESIAN_POINT ( 'NONE',  ( 1.834118845439484335, 59.18411796427230342, -132.4921483272722185 ) ) ;
#24769=VERTEX_POINT ( 'NONE', #1007 ) ;
#24772=ORIENTED_EDGE ( 'NONE', *, *, #13331, .T. ) ;
#24773=ORIENTED_EDGE ( 'NONE', *, *, #9241, .T. ) ;
#24775=CARTESIAN_POINT ( 'NONE',  ( 25.87036335909429496, 84.67915015758852348, 74.91347493818284420 ) ) ;
#24776=CARTESIAN_POINT ( 'NONE',  ( 109.1592201516379674, -0.007566779963325582538, -0.002134489919768117836 ) ) ;
#24779=CARTESIAN_POINT ( 'NONE',  ( 1.833838848569427249, 125.5797553397079724, -72.70900949568641636 ) ) ;
#24780=CARTESIAN_POINT ( 'NONE',  ( 30.58324630866343696, 102.7123253644124219, -63.85566901681510643 ) ) ;
#24781=CARTESIAN_POINT ( 'NONE',  ( 1.833838848569456559, 44.67212175382018557, -138.0625820091619573 ) ) ;
#24782=DIRECTION ( 'NONE',  ( -1.000000000000000000, -0.000000000000000000, -0.000000000000000000 ) ) ;
#24783=ORIENTED_EDGE ( 'NONE', *, *, #18488, .T. ) ;
#24784=ORIENTED_EDGE ( 'NONE', *, *, #13448, .F. ) ;
#24785=CARTESIAN_POINT ( 'NONE',  ( 26.11404676487257603, 47.08215554553657256, -102.9690087468796662 ) ) ;
#24787=EDGE_CURVE ( 'NONE', #21943, #16608, #10730, .T. ) ;
#24790=FACE_OUTER_BOUND ( 'NONE', #8436, .T. ) ;
#24791=VERTEX_POINT ( 'NONE', #2586 ) ;
#24794=ADVANCED_FACE ( 'NONE', ( #20288 ), #26176, .F. ) ;
#24796=CARTESIAN_POINT ( 'NONE',  ( 10.93730112725945602, 84.82621002473440797, 125.1380233598478640 ) ) ;
#24797=CARTESIAN_POINT ( 'NONE',  ( 25.86096068574582674, -76.38617895399404745, 83.34468010038263230 ) ) ;
#24798=CARTESIAN_POINT ( 'NONE',  ( 109.1721716018069515, -0.009868622090669465496, -0.01392660302850068019 ) ) ;
#24799=B_SPLINE_CURVE_WITH_KNOTS ( 'NONE', 3,
 ( #20853, #15952, #16094, #26888 ),
 .UNSPECIFIED., .F., .F.,
 ( 4, 4 ),
 ( 0.000000000000000000, 0.01077107196513859590 ),
 .UNSPECIFIED. ) ;
#24800=ORIENTED_EDGE ( 'NONE', *, *, #5793, .T. ) ;
#24801=CARTESIAN_POINT ( 'NONE',  ( 2.108393763691201350, -96.26428731761910740, -108.8265195087758599 ) ) ;
#24802=ORIENTED_EDGE ( 'NONE', *, *, #11574, .T. ) ;
#24804=EDGE_LOOP ( 'NONE', ( #12723, #23813, #25669, #10052 ) ) ;
#24806=CARTESIAN_POINT ( 'NONE',  ( 55.79472521941426777, 8.328398066092729479, -72.27573336313943742 ) ) ;
#24807=CARTESIAN_POINT ( 'NONE',  ( 109.1589550718175161, 0.002874971999837422094, -0.007008495014555490496 ) ) ;
#24811=CARTESIAN_POINT ( 'NONE',  ( 32.73300124599738581, -92.86301839380070078, 72.21147546950520280 ) ) ;
#24812=ADVANCED_FACE ( 'NONE', ( #10378 ), #2461, .F. ) ;
#24814=CARTESIAN_POINT ( 'NONE',  ( 10.93730112726003156, 71.28103789255123957, -133.3192575531793693 ) ) ;
#24815=CARTESIAN_POINT ( 'NONE',  ( 25.64681081121879203, -34.49579773461859133, 107.5125461021401492 ) ) ;
#24816=CARTESIAN_POINT ( 'NONE',  ( 25.64681081121879203, 34.49579773461785948, 107.5125461021403765 ) ) ;
#24817=EDGE_CURVE ( 'NONE', #10890, #2646, #19113, .T. ) ;
#24818=CARTESIAN_POINT ( 'NONE',  ( 1.893872463202063816, -31.10971550360678606, 141.7768406633803409 ) ) ;
#24819=CARTESIAN_POINT ( 'NONE',  ( 2.433796855181233454, 60.50726454507903895, 132.3327394885233446 ) ) ;
#24820=CARTESIAN_POINT ( 'NONE',  ( 9.884929003653608603, -128.2151425008035517, -78.87917189085047198 ) ) ;
#24821=CARTESIAN_POINT ( 'NONE',  ( 26.28373643307408969, -112.4918671811455511, -60.14387450369948596 ) ) ;
#24822=B_SPLINE_CURVE_WITH_KNOTS ( 'NONE', 3,
 ( #819, #11469, #22424, #13488, #677, #248, #16070 ),
 .UNSPECIFIED., .F., .F.,
 ( 4, 3, 4 ),
 ( 0.000000000000000000, 0.02398743853561366088, 0.04000277880656216006 ),
 .UNSPECIFIED. ) ;
#24825=CARTESIAN_POINT ( 'NONE',  ( 1.832998868059890096, -125.9352106559978921, -72.09222286251215905 ) ) ;
#24826=CARTESIAN_POINT ( 'NONE',  ( 109.1592201516379674, 0.007566779963318552571, -0.002134489919774391464 ) ) ;
#24827=CARTESIAN_POINT ( 'NONE',  ( 25.64708228042118421, 83.93578330383188302, -75.52311986517946707 ) ) ;
#24828=VERTEX_POINT ( 'NONE', #1704 ) ;
#24829=ORIENTED_EDGE ( 'NONE', *, *, #12262, .T. ) ;
#24830=CARTESIAN_POINT ( 'NONE',  ( 25.64670758986457955, 103.3508631837550809, -45.46974729533181403 ) ) ;
#24832=ORIENTED_EDGE ( 'NONE', *, *, #10275, .T. ) ;
#24835=CARTESIAN_POINT ( 'NONE',  ( 32.73300124599738581, -16.10546300444743650, -116.5274707358856858 ) ) ;
#24836=FACE_OUTER_BOUND ( 'NONE', #10403, .T. ) ;
#24839=CARTESIAN_POINT ( 'NONE',  ( 25.64692232868534205, -66.10288322707258146, 91.53874134430776621 ) ) ;
#24840=ADVANCED_FACE ( 'NONE', ( #3733 ), #16439, .F. ) ;
#24842=CARTESIAN_POINT ( 'NONE',  ( 1.833485406944057594, -84.86072343962649711, 117.7091014914947209 ) ) ;
#24843=VECTOR ( 'NONE', #7713, 1000.000000000000114 ) ;
#24844=CARTESIAN_POINT ( 'NONE',  ( 25.70243777736188662, -110.3252221127464452, -24.19989514742834658 ) ) ;
#24846=CARTESIAN_POINT ( 'NONE',  ( 32.73300124599735739, -81.52272205837257957, 84.80615050150346690 ) ) ;
#24848=VERTEX_POINT ( 'NONE', #14227 ) ;
#24850=CARTESIAN_POINT ( 'NONE',  ( 55.79472521941428198, 6.880567342320674129, -72.42790650415567200 ) ) ;
#24851=CARTESIAN_POINT ( 'NONE',  ( 25.86096068574583029, 57.38862431273717846, -97.40497849554822096 ) ) ;
#24852=CARTESIAN_POINT ( 'NONE',  ( 1.832998868059858122, -44.33343224355328971, 138.1720401012265427 ) ) ;
#24854=ORIENTED_EDGE ( 'NONE', *, *, #13944, .T. ) ;
#24856=CARTESIAN_POINT ( 'NONE',  ( 1.833485406944057594, -30.69200235378832176, -141.8265699653870513 ) ) ;
#24858=FACE_OUTER_BOUND ( 'NONE', #16433, .T. ) ;
#24861=VERTEX_POINT ( 'NONE', #23049 ) ;
#24862=FACE_OUTER_BOUND ( 'NONE', #4986, .T. ) ;
#24864=CARTESIAN_POINT ( 'NONE',  ( 10.93730112725971004, 10.89264110825002163, 150.7858122213661147 ) ) ;
#24865=CARTESIAN_POINT ( 'NONE',  ( 1.894214914920947068, -132.2104617488241445, 59.90782071839149836 ) ) ;
#24866=LINE ( 'NONE', #20528, #17899 ) ;
#24868=EDGE_CURVE ( 'NONE', #28115, #17891, #24987, .T. ) ;
#24870=CARTESIAN_POINT ( 'NONE',  ( 19.66333377628710366, -123.9466021833767684, -60.10102584214492794 ) ) ;
#24877=CARTESIAN_POINT ( 'NONE',  ( 1.834118845439484335, 117.2918069668812393, -85.43746956709730966 ) ) ;
#24881=ORIENTED_EDGE ( 'NONE', *, *, #426, .F. ) ;
#24882=EDGE_CURVE ( 'NONE', #8623, #5605, #17060, .T. ) ;
#24883=CARTESIAN_POINT ( 'NONE',  ( 1.833206310202330158, -96.54250248081064001, 108.3342540861875705 ) ) ;
#24884=CARTESIAN_POINT ( 'NONE',  ( 26.04756280548353686, 98.56594554799121966, 55.62433096787456321 ) ) ;
#24885=ORIENTED_EDGE ( 'NONE', *, *, #11341, .F. ) ;
#24886=CIRCLE ( 'NONE', #14759, 151.1787379149930359 ) ;
#24887=ORIENTED_EDGE ( 'NONE', *, *, #25197, .F. ) ;
#24888=ORIENTED_EDGE ( 'NONE', *, *, #18532, .T. ) ;
#24889=DIRECTION ( 'NONE',  ( -0.000000000000000000, 1.000000000000000000, -0.000000000000000000 ) ) ;
#24893=AXIS2_PLACEMENT_3D ( 'NONE', #14025, #18494, #22837 ) ;
#24894=DIRECTION ( 'NONE',  ( 0.000000000000000000, 1.110223024625156343E-15, 1.000000000000000000 ) ) ;
#24898=FACE_OUTER_BOUND ( 'NONE', #12225, .T. ) ;
#24902=CARTESIAN_POINT ( 'NONE',  ( 109.1586900883932856, 0.002301750759599774983, -0.006757191295060855155 ) ) ;
#24904=ORIENTED_EDGE ( 'NONE', *, *, #16114, .F. ) ;
#24906=( BOUNDED_SURFACE ( )  B_SPLINE_SURFACE ( 3, 1, ( 
 ( #19508, #15458 ),
 ( #4245, #1942 ),
 ( #8866, #11021 ),
 ( #13031, #10748 ) ),
 .UNSPECIFIED., .F., .F., .F. ) 
 B_SPLINE_SURFACE_WITH_KNOTS ( ( 4, 4 ),
 ( 2, 2 ),
 ( 0.000000000000000000, 1.000000000000000000 ),
 ( 0.000000000000000000, 1.000000000000000000 ),
 .UNSPECIFIED. ) 
 GEOMETRIC_REPRESENTATION_ITEM ( )  RATIONAL_B_SPLINE_SURFACE ( (
 ( 1.000000000000000000, 1.000000000000000000),
 ( 0.6386103224230302855, 0.9954351624131538845),
 ( 0.6386103224230302855, 0.9954351624131538845),
 ( 1.000000000000000000, 1.000000000000000000) ) ) 
 REPRESENTATION_ITEM ( '' )  SURFACE ( )  );
#24907=CYLINDRICAL_SURFACE ( 'NONE', #11550, 37.50000000000001421 ) ;
#24910=ORIENTED_EDGE ( 'NONE', *, *, #6928, .F. ) ;
#24911=ORIENTED_EDGE ( 'NONE', *, *, #25719, .T. ) ;
#24913=EDGE_CURVE ( 'NONE', #11774, #15699, #4010, .T. ) ;
#24914=DIRECTION ( 'NONE',  ( -1.000000000000000000, -0.000000000000000000, -0.000000000000000000 ) ) ;
#24915=CIRCLE ( 'NONE', #22616, 117.6351876552689504 ) ;
#24917=LINE ( 'NONE', #14090, #12130 ) ;
#24918=CARTESIAN_POINT ( 'NONE',  ( 8.186469829614045679, 108.6390983847750107, 102.4860667297597416 ) ) ;
#24919=CARTESIAN_POINT ( 'NONE',  ( 10.93730112726005999, 128.3908183996603327, -79.81734490845792607 ) ) ;
#24920=CARTESIAN_POINT ( 'NONE',  ( 1.833809397773857874, 45.01060836636703044, -137.9524943416720930 ) ) ;
#24921=CARTESIAN_POINT ( 'NONE',  ( 109.1586900883932856, 0.005833932871491316619, 0.004113747440992344268 ) ) ;
#24922=ORIENTED_EDGE ( 'NONE', *, *, #13846, .F. ) ;
#24925=CARTESIAN_POINT ( 'NONE',  ( 28.43349137099828994, 120.6297847406441122, -29.78331910005377026 ) ) ;
#24927=DIRECTION ( 'NONE',  ( -1.000000000000000000, -0.000000000000000000, -0.000000000000000000 ) ) ;
#24928=CARTESIAN_POINT ( 'NONE',  ( 1.832998868059890096, -108.1944082009163566, 96.70023740551089020 ) ) ;
#24929=CARTESIAN_POINT ( 'NONE',  ( 1.833838850855475489, -138.0350826608190573, 44.75675607098882836 ) ) ;
#24932=DIRECTION ( 'NONE',  ( 0.000000000000000000, 0.000000000000000000, 1.000000000000000000 ) ) ;
#24935=CARTESIAN_POINT ( 'NONE',  ( 30.59138290137880745, -44.78723476287375860, 107.2355347544031616 ) ) ;
#24936=CARTESIAN_POINT ( 'NONE',  ( 25.64681081121879203, -107.5125461021405044, 34.49579773461748999 ) ) ;
#24939=( BOUNDED_SURFACE ( )  B_SPLINE_SURFACE ( 3, 1, ( 
 ( #6728, #11318 ),
 ( #24286, #7160 ),
 ( #15920, #24584 ),
 ( #13319, #2379 ) ),
 .UNSPECIFIED., .F., .F., .F. ) 
 B_SPLINE_SURFACE_WITH_KNOTS ( ( 4, 4 ),
 ( 2, 2 ),
 ( 0.000000000000000000, 1.000000000000000000 ),
 ( 0.000000000000000000, 1.000000000000000000 ),
 .UNSPECIFIED. ) 
 GEOMETRIC_REPRESENTATION_ITEM ( )  RATIONAL_B_SPLINE_SURFACE ( (
 ( 1.000000000000000000, 1.000000000000000000),
 ( 0.9956975270656955868, 0.8568959468854907557),
 ( 0.9956975270656955868, 0.8568959468854907557),
 ( 1.000000000000000000, 1.000000000000000000) ) ) 
 REPRESENTATION_ITEM ( '' )  SURFACE ( )  );
#24940=VERTEX_POINT ( 'NONE', #4290 ) ;
#24941=CARTESIAN_POINT ( 'NONE',  ( 10.93730112725990367, -125.1380233598473950, -84.82621002473567273 ) ) ;
#24942=ORIENTED_EDGE ( 'NONE', *, *, #13443, .F. ) ;
#24944=ORIENTED_EDGE ( 'NONE', *, *, #22936, .T. ) ;
#24946=CARTESIAN_POINT ( 'NONE',  ( 2.430230287190589422, 86.70145658344658557, 116.8646894862415166 ) ) ;
#24951=CARTESIAN_POINT ( 'NONE',  ( 2.430230287190581429, -144.8619874886007892, 13.76600171652596849 ) ) ;
#24952=EDGE_CURVE ( 'NONE', #14748, #391, #7063, .T. ) ;
#24953=CARTESIAN_POINT ( 'NONE',  ( 2.263178113027024096, -98.32595894905907130, 107.1074314657341091 ) ) ;
#24954=AXIS2_PLACEMENT_3D ( 'NONE', #4529, #22096, #24409 ) ;
#24956=CARTESIAN_POINT ( 'NONE',  ( 2.433796855181233454, -144.8571464219888298, -13.76554153471842312 ) ) ;
#24957=CARTESIAN_POINT ( 'NONE',  ( 1.833485406944057594, 107.4794113447422603, -97.49333871408586560 ) ) ;
#24958=CARTESIAN_POINT ( 'NONE',  ( 109.1592201516379674, 0.007856029051022768092, -0.0003082430542016078114 ) ) ;
#24959=DIRECTION ( 'NONE',  ( 0.5946245182733607137, 0.08110646981858531113, 0.7999021332774032267 ) ) ;
#24961=CARTESIAN_POINT ( 'NONE',  ( 25.98552792386799126, -83.35136888841289249, 76.50165414343540249 ) ) ;
#24962=CARTESIAN_POINT ( 'NONE',  ( 26.04756280548352976, 76.55292122840037905, 83.36043467252048345 ) ) ;
#24963=CARTESIAN_POINT ( 'NONE',  ( 28.37644542392847313, 76.32685750075128794, -98.15613422114005004 ) ) ;
#24965=FACE_OUTER_BOUND ( 'NONE', #25720, .T. ) ;
#24966=CARTESIAN_POINT ( 'NONE',  ( 109.1624594426973118, -0.008380433676413013774, -0.01358749486988779405 ) ) ;
#24967=CARTESIAN_POINT ( 'NONE',  ( 28.43349137099834678, -120.6297847406439558, 29.78331910005459093 ) ) ;
#24968=EDGE_CURVE ( 'NONE', #7628, #3847, #4006, .T. ) ;
#24969=ORIENTED_EDGE ( 'NONE', *, *, #19645, .T. ) ;
#24970=CARTESIAN_POINT ( 'NONE',  ( 55.49584447822657296, 66.16986612640816645, -29.75369869230888753 ) ) ;
#24971=VERTEX_POINT ( 'NONE', #10784 ) ;
#24973=CARTESIAN_POINT ( 'NONE',  ( 25.64670758986457599, -12.29747533046042740, 112.2393466678477694 ) ) ;
#24974=VERTEX_POINT ( 'NONE', #2112 ) ;
#24975=VECTOR ( 'NONE', #5930, 1000.000000000000000 ) ;
#24976=EDGE_CURVE ( 'NONE', #26958, #16481, #22901, .T. ) ;
#24977=ORIENTED_EDGE ( 'NONE', *, *, #6406, .F. ) ;
#24978=B_SPLINE_CURVE_WITH_KNOTS ( 'NONE', 3,
 ( #25427, #5547, #14032, #10024 ),
 .UNSPECIFIED., .F., .F.,
 ( 4, 4 ),
 ( 0.000000000000000000, 0.01077107196513844151 ),
 .UNSPECIFIED. ) ;
#24979=VECTOR ( 'NONE', #20086, 1000.000000000000227 ) ;
#24981=EDGE_CURVE ( 'NONE', #20437, #20945, #16348, .T. ) ;
#24982=ADVANCED_FACE ( 'NONE', ( #6459, #8346 ), #6744, .F. ) ;
#24983=CARTESIAN_POINT ( 'NONE',  ( 109.1586900883932856, -0.001582822706024301744, 0.006960773163856025063 ) ) ;
#24984=FACE_OUTER_BOUND ( 'NONE', #26851, .T. ) ;
#24985=B_SPLINE_CURVE_WITH_KNOTS ( 'NONE', 3,
 ( #13066, #24025, #8898, #105 ),
 .UNSPECIFIED., .F., .F.,
 ( 4, 4 ),
 ( 3.141122122899962401E-16, 0.01077107486149752116 ),
 .UNSPECIFIED. ) ;
#24986=CARTESIAN_POINT ( 'NONE',  ( 1.831572820252008738, -84.49389457294057593, -117.9752562883675466 ) ) ;
#24987=B_SPLINE_CURVE_WITH_KNOTS ( 'NONE', 3,
 ( #16546, #10085, #21429, #14526 ),
 .UNSPECIFIED., .F., .F.,
 ( 4, 4 ),
 ( 6.721062925282177188E-16, 0.008383748772660126747 ),
 .UNSPECIFIED. ) ;
#24989=CARTESIAN_POINT ( 'NONE',  ( 1.833838850855475266, 144.3241377520101025, -15.07960613928478644 ) ) ;
#24991=CARTESIAN_POINT ( 'NONE',  ( 109.1624594426973118, 0.0004639210235602615490, 0.01595733256932007488 ) ) ;
#24992=CARTESIAN_POINT ( 'NONE',  ( 0.000000000000000000, 0.000000000000000000, 0.000000000000000000 ) ) ;
#24994=FACE_OUTER_BOUND ( 'NONE', #3959, .T. ) ;
#24996=CARTESIAN_POINT ( 'NONE',  ( 109.1778270068192853, -0.002278716897417678439, -0.009031542838326005879 ) ) ;
#24998=CIRCLE ( 'NONE', #13942, 117.6351876552689504 ) ;
#24999=ORIENTED_EDGE ( 'NONE', *, *, #20997, .T. ) ;
#25000=ORIENTED_EDGE ( 'NONE', *, *, #4039, .F. ) ;
#25003=CARTESIAN_POINT ( 'NONE',  ( 25.64681081121879203, 66.03065707439057519, -91.59071981940505225 ) ) ;
#25004=CARTESIAN_POINT ( 'NONE',  ( 10.93730112726002623, 56.95489579269933955, -140.0398180619107507 ) ) ;
#25006=CARTESIAN_POINT ( 'NONE',  ( 2.433796855181205476, 138.8296532063094162, -43.58222566461498815 ) ) ;
#25009=CARTESIAN_POINT ( 'NONE',  ( 2.433796855181205476, -46.34326152018838485, 137.9325382748283744 ) ) ;
#25012=EDGE_LOOP ( 'NONE', ( #13801, #15578, #21769, #7097 ) ) ;
#25013=LINE ( 'NONE', #20658, #10533 ) ;
#25014=FACE_OUTER_BOUND ( 'NONE', #688, .T. ) ;
#25015=EDGE_CURVE ( 'NONE', #26642, #10842, #24300, .T. ) ;
#25016=EDGE_CURVE ( 'NONE', #24473, #19926, #8753, .T. ) ;
#25017=CARTESIAN_POINT ( 'NONE',  ( 26.11404676487257603, -65.63269960453179408, -92.25884714080473259 ) ) ;
#25018=EDGE_CURVE ( 'NONE', #3333, #8623, #13333, .T. ) ;
#25019=B_SPLINE_CURVE_WITH_KNOTS ( 'NONE', 3,
 ( #2609, #4779, #7238, #22347, #11390, #17854, #13396, #452 ),
 .UNSPECIFIED., .F., .F.,
 ( 4, 2, 2, 4 ),
 ( 2.860979249076398407E-17, 0.0002429592666046945682, 0.0004859185332093605134, 0.0009718370664186819956 ),
 .UNSPECIFIED. ) ;
#25020=VERTEX_POINT ( 'NONE', #19408 ) ;
#25021=CARTESIAN_POINT ( 'NONE',  ( 9.884929003653626367, -148.0628878137278832, -27.17402761732495975 ) ) ;
#25023=CARTESIAN_POINT ( 'NONE',  ( 26.11404676487256893, 1.130420376098718593, -113.2169081140373663 ) ) ;
#25025=CIRCLE ( 'NONE', #15765, 151.1787379149930359 ) ;
#25028=CARTESIAN_POINT ( 'NONE',  ( 19.66333377628703261, 137.6761449113044478, 4.491394265032717215 ) ) ;
#25030=VERTEX_POINT ( 'NONE', #9330 ) ;
#25033=CARTESIAN_POINT ( 'NONE',  ( 30.59138290137909877, -2.701446546447516361, -116.1811451928595318 ) ) ;
#25035=EDGE_LOOP ( 'NONE', ( #11860, #7180, #490, #13378 ) ) ;
#25039=DIRECTION ( 'NONE',  ( 0.000000000000000000, 0.000000000000000000, 1.000000000000000000 ) ) ;
#25040=CARTESIAN_POINT ( 'NONE',  ( 109.1587776205901861, 0.007280006032835106486, -0.0008489206734500846221 ) ) ;
#25042=CARTESIAN_POINT ( 'NONE',  ( 28.37603512858355970, 10.20681926544516216, -114.2774673387025075 ) ) ;
#25044=ORIENTED_EDGE ( 'NONE', *, *, #22907, .F. ) ;
#25045=CARTESIAN_POINT ( 'NONE',  ( 28.37599760073042532, 104.0705811520814024, 48.29934869928204222 ) ) ;
#25047=DIRECTION ( 'NONE',  ( -1.000000000000000000, -0.000000000000000000, -0.000000000000000000 ) ) ;
#25048=ADVANCED_FACE ( 'NONE', ( #22726 ), #8380, .F. ) ;
#25049=FACE_OUTER_BOUND ( 'NONE', #24198, .T. ) ;
#25050=CARTESIAN_POINT ( 'NONE',  ( 1.832998868059890096, 108.1944082009169961, -96.70023740551017966 ) ) ;
#25051=CARTESIAN_POINT ( 'NONE',  ( 21.16825799904932381, 125.4548537968709638, 51.02216409572595524 ) ) ;
#25052=CARTESIAN_POINT ( 'NONE',  ( 26.11404676487259024, -12.95861723607377414, -112.4785329405483338 ) ) ;
#25053=CARTESIAN_POINT ( 'NONE',  ( 32.73300124599737160, -89.94078864464117373, 75.82012867748450446 ) ) ;
#25055=CARTESIAN_POINT ( 'NONE',  ( 2.433796855181233454, -142.6247129145646397, -28.83182736670683610 ) ) ;
#25056=EDGE_CURVE ( 'NONE', #23267, #1161, #15989, .T. ) ;
#25058=ORIENTED_EDGE ( 'NONE', *, *, #23934, .F. ) ;
#25061=FACE_OUTER_BOUND ( 'NONE', #2829, .T. ) ;
#25062=CARTESIAN_POINT ( 'NONE',  ( 1.833206310202348588, 58.34025049825128661, -132.8652722326992546 ) ) ;
#25065=CARTESIAN_POINT ( 'NONE',  ( 1.833485406944057594, 44.33323125130110043, -138.1714136985304151 ) ) ;
#25066=CARTESIAN_POINT ( 'NONE',  ( 1.832998868059858122, -132.7810136645734360, -58.53348008137778180 ) ) ;
#25069=CARTESIAN_POINT ( 'NONE',  ( 6.224689322667630975, -121.2721959030543672, 84.93872395422938837 ) ) ;
#25070=CARTESIAN_POINT ( 'NONE',  ( 30.58324630866341565, -16.55818995381066472, -119.8048187378265794 ) ) ;
#25071=CARTESIAN_POINT ( 'NONE',  ( 10.93730112725932635, 0.000000000000000000, -151.1787379149930359 ) ) ;
#25072=CARTESIAN_POINT ( 'NONE',  ( 109.1592201516379674, -0.007620268632971095163, 0.001934867487021801630 ) ) ;
#25074=VERTEX_POINT ( 'NONE', #9469 ) ;
#25075=CARTESIAN_POINT ( 'NONE',  ( 55.79472521941426777, -49.22042574086461997, 53.57698701322198076 ) ) ;
#25079=EDGE_CURVE ( 'NONE', #24828, #335, #27668, .T. ) ;
#25082=CARTESIAN_POINT ( 'NONE',  ( 25.64700659047694842, -107.4550658295753749, 34.67498789830411710 ) ) ;
#25083=CARTESIAN_POINT ( 'NONE',  ( 1.833838850093465700, 145.1097630783160923, -3.453306173377954874E-06 ) ) ;
#25084=EDGE_CURVE ( 'NONE', #3139, #18502, #20778, .T. ) ;
#25087=VERTEX_POINT ( 'NONE', #20392 ) ;
#25088=CARTESIAN_POINT ( 'NONE',  ( 26.11404676487257603, -84.89295829319543429, 74.91683232330944975 ) ) ;
#25089=CARTESIAN_POINT ( 'NONE',  ( 13.84597867724998288, 132.0026437215597355, 64.00674338125878648 ) ) ;
#25090=CARTESIAN_POINT ( 'NONE',  ( 9.884929003653626367, 132.4189379373570432, 71.59798461011378379 ) ) ;
#25091=CARTESIAN_POINT ( 'NONE',  ( 1.832998868059890096, -108.1944082009150634, -96.70023740551232549 ) ) ;
#25093=CARTESIAN_POINT ( 'NONE',  ( 55.49584447822657296, -71.02133150427246733, -14.82242356768008662 ) ) ;
#25094=CARTESIAN_POINT ( 'NONE',  ( 1.894214914920933079, -132.9862534094753528, -58.16536411968072429 ) ) ;
#25095=CARTESIAN_POINT ( 'NONE',  ( 1.832998868059858122, 137.8420662456176160, -45.34898734665906517 ) ) ;
#25096=CARTESIAN_POINT ( 'NONE',  ( 1.833206308920072081, -30.89799439741721798, 141.7818018507502416 ) ) ;
#25098=FACE_OUTER_BOUND ( 'NONE', #18860, .T. ) ;
#25099=CARTESIAN_POINT ( 'NONE',  ( 28.43349137099836810, -109.5743306972602511, -58.58376153369822248 ) ) ;
#25100=( BOUNDED_SURFACE ( )  B_SPLINE_SURFACE ( 3, 1, ( 
 ( #2977, #11752 ),
 ( #665, #806 ),
 ( #4976, #15918 ),
 ( #5122, #13899 ) ),
 .UNSPECIFIED., .F., .F., .F. ) 
 B_SPLINE_SURFACE_WITH_KNOTS ( ( 4, 4 ),
 ( 2, 2 ),
 ( 0.000000000000000000, 1.000000000000000000 ),
 ( 0.000000000000000000, 1.000000000000000000 ),
 .UNSPECIFIED. ) 
 GEOMETRIC_REPRESENTATION_ITEM ( )  RATIONAL_B_SPLINE_SURFACE ( (
 ( 1.000000000000000000, 1.000000000000000000),
 ( 0.6386103224230316178, 0.9954351624131538845),
 ( 0.6386103224230316178, 0.9954351624131538845),
 ( 1.000000000000000000, 1.000000000000000000) ) ) 
 REPRESENTATION_ITEM ( '' )  SURFACE ( )  );
#25101=EDGE_CURVE ( 'NONE', #207, #17966, #5170, .T. ) ;
#25102=CARTESIAN_POINT ( 'NONE',  ( 13.36082413113063083, 41.18148072373809043, -147.2768864064163665 ) ) ;
#25103=CARTESIAN_POINT ( 'NONE',  ( 26.11404676487256893, 1.130420376098718593, -113.2169081140373663 ) ) ;
#25104=FACE_OUTER_BOUND ( 'NONE', #19858, .T. ) ;
#25105=VERTEX_POINT ( 'NONE', #534 ) ;
#25106=DIRECTION ( 'NONE',  ( -1.000000000000000000, -0.000000000000000000, -0.000000000000000000 ) ) ;
#25108=CARTESIAN_POINT ( 'NONE',  ( 25.64681081121879203, 112.9102952884414464, 0.4157506337731812773 ) ) ;
#25110=FACE_OUTER_BOUND ( 'NONE', #10060, .T. ) ;
#25111=EDGE_LOOP ( 'NONE', ( #23990, #7851, #9971, #16190 ) ) ;
#25112=EDGE_CURVE ( 'NONE', #20568, #17620, #4320, .T. ) ;
#25113=B_SPLINE_CURVE_WITH_KNOTS ( 'NONE', 3,
 ( #12137, #1193, #16591, #18746, #27520, #7831, #21251, #10339, #14627, #25860 ),
 .UNSPECIFIED., .F., .F.,
 ( 4, 3, 3, 4 ),
 ( 1.387778780781445676E-17, 0.0002669560319015911202, 0.0005492286108966362495, 0.0008315040496093336220 ),
 .UNSPECIFIED. ) ;
#25118=DIRECTION ( 'NONE',  ( -0.000000000000000000, 1.000000000000000000, 0.000000000000000000 ) ) ;
#25120=CARTESIAN_POINT ( 'NONE',  ( 25.64700659047697684, -66.55152787776188461, 91.21315746821495907 ) ) ;
#25122=FACE_OUTER_BOUND ( 'NONE', #543, .T. ) ;
#25123=CARTESIAN_POINT ( 'NONE',  ( 25.64681081121879203, 75.24277141833491100, 84.18689316040072868 ) ) ;
#25127=CARTESIAN_POINT ( 'NONE',  ( 1.832998868059890096, -97.49378069860723883, -107.4798986104869982 ) ) ;
#25128=VERTEX_POINT ( 'NONE', #4714 ) ;
#25130=CARTESIAN_POINT ( 'NONE',  ( 109.1586900883932856, 0.007002774699553638779, 0.001385221016527484091 ) ) ;
#25131=DIRECTION ( 'NONE',  ( 0.000000000000000000, 0.000000000000000000, 1.000000000000000000 ) ) ;
#25132=CARTESIAN_POINT ( 'NONE',  ( 25.86096068574581253, 76.38617895399458746, -83.34468010038209229 ) ) ;
#25133=EDGE_CURVE ( 'NONE', #14003, #8000, #13489, .T. ) ;
#25135=CARTESIAN_POINT ( 'NONE',  ( 1.833485406944043827, 85.72460230293692973, 117.0814567582547596 ) ) ;
#25136=CARTESIAN_POINT ( 'NONE',  ( 2.108393763691185363, -71.53437599919723766, -126.4628696952926958 ) ) ;
#25141=CARTESIAN_POINT ( 'NONE',  ( 1.833485406944043827, -14.63699153649458040, 144.3694338680884641 ) ) ;
#25143=CARTESIAN_POINT ( 'NONE',  ( 25.64704443564078673, -97.85065179540796976, 56.33997466860367354 ) ) ;
#25145=( BOUNDED_SURFACE ( )  B_SPLINE_SURFACE ( 3, 1, ( 
 ( #6012, #14768 ),
 ( #1944, #12743 ),
 ( #1534, #3839 ),
 ( #7898, #6158 ) ),
 .UNSPECIFIED., .F., .F., .F. ) 
 B_SPLINE_SURFACE_WITH_KNOTS ( ( 4, 4 ),
 ( 2, 2 ),
 ( 0.000000000000000000, 1.000000000000000000 ),
 ( 0.000000000000000000, 1.000000000000000000 ),
 .UNSPECIFIED. ) 
 GEOMETRIC_REPRESENTATION_ITEM ( )  RATIONAL_B_SPLINE_SURFACE ( (
 ( 1.000000000000000000, 1.000000000000000000),
 ( 0.6386103224230316178, 0.9954351624131538845),
 ( 0.6386103224230316178, 0.9954351624131538845),
 ( 1.000000000000000000, 1.000000000000000000) ) ) 
 REPRESENTATION_ITEM ( '' )  SURFACE ( )  );
#25146=EDGE_LOOP ( 'NONE', ( #26644, #14993, #7933, #13871 ) ) ;
#25148=ORIENTED_EDGE ( 'NONE', *, *, #27628, .F. ) ;
#25149=CARTESIAN_POINT ( 'NONE',  ( 25.70243777736189372, -45.26941207740225082, -103.4793210720852983 ) ) ;
#25150=CARTESIAN_POINT ( 'NONE',  ( 6.224689322667630975, -118.2566963816764911, -89.08920297664333532 ) ) ;
#25151=VERTEX_POINT ( 'NONE', #10193 ) ;
#25152=B_SPLINE_CURVE_WITH_KNOTS ( 'NONE', 3,
 ( #25965, #6388, #13417, #13137, #24239, #19616, #28245, #26377, #43, #8683 ),
 .UNSPECIFIED., .F., .F.,
 ( 4, 3, 3, 4 ),
 ( 6.938893903907228378E-18, 0.0002669560319015750198, 0.0005492286108966477421, 0.0008315040496093457651 ),
 .UNSPECIFIED. ) ;
#25154=CARTESIAN_POINT ( 'NONE',  ( 0.000000000000000000, 1.806757805586603712E-14, 143.8872038478949946 ) ) ;
#25155=CARTESIAN_POINT ( 'NONE',  ( 1.833206310202334377, -117.8322271314358716, -84.68961945193576923 ) ) ;
#25156=CARTESIAN_POINT ( 'NONE',  ( 2.433796855181205476, -13.76554153471595043, -144.8571464219890572 ) ) ;
#25160=CARTESIAN_POINT ( 'NONE',  ( 32.73300124599737160, -108.9684813982492244, 44.31599526637918274 ) ) ;
#25161=CARTESIAN_POINT ( 'NONE',  ( 13.36082413113063083, -143.3553710183992962, 53.25066407421756054 ) ) ;
#25162=CARTESIAN_POINT ( 'NONE',  ( 1.834118845439484335, 141.9019470378991343, -30.34413640949558655 ) ) ;
#25164=EDGE_CURVE ( 'NONE', #15699, #8105, #9106, .T. ) ;
#25166=ORIENTED_EDGE ( 'NONE', *, *, #3641, .T. ) ;
#25168=CARTESIAN_POINT ( 'NONE',  ( 16.75465622695673673, 79.80233222761980016, 117.7275519421676506 ) ) ;
#25169=CARTESIAN_POINT ( 'NONE',  ( 6.224689322667647851, -76.23997225729179661, -126.9212313063852662 ) ) ;
#25170=DIRECTION ( 'NONE',  ( -1.000000000000000000, -0.000000000000000000, -0.000000000000000000 ) ) ;
#25171=ADVANCED_FACE ( 'NONE', ( #18527 ), #11296, .F. ) ;
#25172=CARTESIAN_POINT ( 'NONE',  ( 8.186469777910918566, -3.468244369820856932, -149.3111477498017905 ) ) ;
#25173=CARTESIAN_POINT ( 'NONE',  ( 1.833838850093477912, -132.5643663243753281, -59.02145475724777413 ) ) ;
#25175=ORIENTED_EDGE ( 'NONE', *, *, #24634, .T. ) ;
#25176=CARTESIAN_POINT ( 'NONE',  ( 26.11404676487257603, 98.61392875273364211, 55.62948129436280453 ) ) ;
#25177=CARTESIAN_POINT ( 'NONE',  ( 2.063896406836605024, 43.61045647697694250, 138.5688025270880246 ) ) ;
#25180=CARTESIAN_POINT ( 'NONE',  ( 25.64692232868534560, 107.4854307433087257, 34.58055111992081265 ) ) ;
#25182=CARTESIAN_POINT ( 'NONE',  ( 1.832998868059858122, -144.2584710144579390, -15.69902610990523151 ) ) ;
#25184=CARTESIAN_POINT ( 'NONE',  ( 1.832998868059890096, 58.53348008137826497, -132.7810136645732371 ) ) ;
#25185=CARTESIAN_POINT ( 'NONE',  ( 1.833750490713643266, -29.90883416717514010, -141.9939712933759211 ) ) ;
#25186=CARTESIAN_POINT ( 'NONE',  ( 109.1589550718175161, 0.001354998915253774082, -0.007453082872782202176 ) ) ;
#25187=ORIENTED_EDGE ( 'NONE', *, *, #1971, .F. ) ;
#25191=CARTESIAN_POINT ( 'NONE',  ( 109.1587776205901577, -0.003592288931009647752, -0.006388631651928880321 ) ) ;
#25192=EDGE_CURVE ( 'NONE', #7808, #25689, #12864, .T. ) ;
#25193=CARTESIAN_POINT ( 'NONE',  ( 10.93730112725996051, 20.69552240458543224, -149.7554878793147282 ) ) ;
#25195=CARTESIAN_POINT ( 'NONE',  ( 28.37603512858456156, -55.80522682147343261, 100.2461737936628765 ) ) ;
#25196=CARTESIAN_POINT ( 'NONE',  ( 1.833838850855499025, 44.92600961247843827, -137.9800888515318320 ) ) ;
#25197=EDGE_CURVE ( 'NONE', #28149, #26886, #23156, .T. ) ;
#25200=ADVANCED_FACE ( 'NONE', ( #20959 ), #28128, .T. ) ;
#25201=EDGE_LOOP ( 'NONE', ( #276, #27176, #13967, #2147 ) ) ;
#25203=CARTESIAN_POINT ( 'NONE',  ( 28.43349137099834678, -69.71646995966243310, 102.8504004831932832 ) ) ;
#25204=DIRECTION ( 'NONE',  ( 0.000000000000000000, 0.000000000000000000, 1.000000000000000000 ) ) ;
#25205=CARTESIAN_POINT ( 'NONE',  ( 55.49584447822657296, -36.50733923851242935, 62.69727227546388804 ) ) ;
#25206=CARTESIAN_POINT ( 'NONE',  ( 1.832998868059890096, -107.4798986104866572, 97.49378069860762253 ) ) ;
#25208=CARTESIAN_POINT ( 'NONE',  ( 32.73300124599732186, 0.000000000000000000, 0.000000000000000000 ) ) ;
#25209=ORIENTED_EDGE ( 'NONE', *, *, #27996, .T. ) ;
#25211=DIRECTION ( 'NONE',  ( -1.000000000000000000, -0.000000000000000000, -0.000000000000000000 ) ) ;
#25212=CARTESIAN_POINT ( 'NONE',  ( 25.98107933586710772, -10.73978443746659295, -112.6229961579377203 ) ) ;
#25213=B_SPLINE_CURVE_WITH_KNOTS ( 'NONE', 3,
 ( #25846, #6272, #22077, #13016, #6548, #28262, #25982 ),
 .UNSPECIFIED., .F., .F.,
 ( 4, 3, 4 ),
 ( 6.557988972572477070E-16, 0.02816610861753243711, 0.04000277880656291640 ),
 .UNSPECIFIED. ) ;
#25214=CARTESIAN_POINT ( 'NONE',  ( 109.1587776205901577, 0.004965871434389453401, -0.005390665547499381982 ) ) ;
#25215=ORIENTED_EDGE ( 'NONE', *, *, #1473, .F. ) ;
#25216=CARTESIAN_POINT ( 'NONE',  ( 25.98552792386799837, -57.50018541500355695, -97.43552975939674354 ) ) ;
#25219=VECTOR ( 'NONE', #19580, 1000.000000000000114 ) ;
#25220=ORIENTED_EDGE ( 'NONE', *, *, #18998, .T. ) ;
#25224=DIRECTION ( 'NONE',  ( 0.000000000000000000, 0.000000000000000000, 1.000000000000000000 ) ) ;
#25226=B_SPLINE_CURVE_WITH_KNOTS ( 'NONE', 3,
 ( #20465, #891, #9677, #3060, #16293, #25089, #1041 ),
 .UNSPECIFIED., .F., .F.,
 ( 4, 3, 4 ),
 ( 0.000000000000000000, 0.02398743853561325495, 0.04000277880656212537 ),
 .UNSPECIFIED. ) ;
#25228=CARTESIAN_POINT ( 'NONE',  ( 2.430230287190592531, -107.1617224697470903, 98.44218333480735339 ) ) ;
#25229=B_SPLINE_CURVE_WITH_KNOTS ( 'NONE', 3,
 ( #25003, #26976, #20648, #1223, #3388, #16048, #940, #9729, #20936, #18064 ),
 .UNSPECIFIED., .F., .F.,
 ( 4, 3, 3, 4 ),
 ( 1.387778780781445676E-17, 0.0002669560319015871629, 0.0005492286108966491515, 0.0008315040496093398020 ),
 .UNSPECIFIED. ) ;
#25231=( BOUNDED_SURFACE ( )  B_SPLINE_SURFACE ( 3, 1, ( 
 ( #24595, #16358 ),
 ( #13910, #25150 ),
 ( #22278, #11466 ),
 ( #20389, #2539 ) ),
 .UNSPECIFIED., .F., .F., .F. ) 
 B_SPLINE_SURFACE_WITH_KNOTS ( ( 4, 4 ),
 ( 2, 2 ),
 ( 0.000000000000000000, 1.000000000000000000 ),
 ( 0.000000000000000000, 1.000000000000000000 ),
 .UNSPECIFIED. ) 
 GEOMETRIC_REPRESENTATION_ITEM ( )  RATIONAL_B_SPLINE_SURFACE ( (
 ( 1.000000000000000000, 1.000000000000000000),
 ( 0.6386103224230302855, 0.9954351624131538845),
 ( 0.6386103224230302855, 0.9954351624131538845),
 ( 1.000000000000000000, 1.000000000000000000) ) ) 
 REPRESENTATION_ITEM ( '' )  SURFACE ( )  );
#25234=DIRECTION ( 'NONE',  ( -0.5946245182733607137, -0.7870422510449642806, -0.1642747008466272085 ) ) ;
#25236=B_SPLINE_CURVE_WITH_KNOTS ( 'NONE', 3,
 ( #10571, #6937, #2297, #11524, #21500, #588, #9229 ),
 .UNSPECIFIED., .F., .F.,
 ( 4, 3, 4 ),
 ( 4.730677113667733359E-16, 0.02816610861753244058, 0.04000277880656269436 ),
 .UNSPECIFIED. ) ;
#25237=VECTOR ( 'NONE', #14432, 1000.000000000000114 ) ;
#25238=ADVANCED_FACE ( 'NONE', ( #11023 ), #27082, .F. ) ;
#25242=CIRCLE ( 'NONE', #2209, 117.6351876552689504 ) ;
#25243=DIRECTION ( 'NONE',  ( 0.5946245182733607137, 0.7992853357633866729, 0.08697490616139734454 ) ) ;
#25247=CARTESIAN_POINT ( 'NONE',  ( 13.36082413113061307, -106.9547846563642963, 109.3026516754228794 ) ) ;
#25248=CARTESIAN_POINT ( 'NONE',  ( 2.108985857320894386, -107.1123114102935006, 98.16869034643272585 ) ) ;
#25250=DIRECTION ( 'NONE',  ( 0.000000000000000000, 0.000000000000000000, 1.000000000000000000 ) ) ;
#25251=ORIENTED_EDGE ( 'NONE', *, *, #21968, .T. ) ;
#25252=CARTESIAN_POINT ( 'NONE',  ( 2.108985857320888169, -16.46110181986589183, -144.3577886602088256 ) ) ;
#25257=CARTESIAN_POINT ( 'NONE',  ( 28.37599760073042177, -114.7183216384031397, -1.794331790580630637 ) ) ;
#25258=ADVANCED_FACE ( 'NONE', ( #1797 ), #18258, .F. ) ;
#25259=CARTESIAN_POINT ( 'NONE',  ( 2.063896406836605024, -16.52087515463875178, 144.3268707900446657 ) ) ;
#25260=B_SPLINE_CURVE_WITH_KNOTS ( 'NONE', 3,
 ( #17231, #10770, #8598, #15195 ),
 .UNSPECIFIED., .F., .F.,
 ( 4, 4 ),
 ( 0.000000000000000000, 0.01077107196513874682 ),
 .UNSPECIFIED. ) ;
#25262=( BOUNDED_SURFACE ( )  B_SPLINE_SURFACE ( 3, 1, ( 
 ( #28196, #16984 ),
 ( #21584, #4026 ),
 ( #5924, #8092 ),
 ( #12796, #23636 ) ),
 .UNSPECIFIED., .F., .F., .F. ) 
 B_SPLINE_SURFACE_WITH_KNOTS ( ( 4, 4 ),
 ( 2, 2 ),
 ( 0.000000000000000000, 1.000000000000000000 ),
 ( 0.000000000000000000, 1.000000000000000000 ),
 .UNSPECIFIED. ) 
 GEOMETRIC_REPRESENTATION_ITEM ( )  RATIONAL_B_SPLINE_SURFACE ( (
 ( 1.000000000000000000, 1.000000000000000000),
 ( 0.9956975270656955868, 0.8568959468854907557),
 ( 0.9956975270656955868, 0.8568959468854907557),
 ( 1.000000000000000000, 1.000000000000000000) ) ) 
 REPRESENTATION_ITEM ( '' )  SURFACE ( )  );
#25263=DIRECTION ( 'NONE',  ( 1.000000000000000000, 0.000000000000000000, 0.000000000000000000 ) ) ;
#25264=ADVANCED_FACE ( 'NONE', ( #26129 ), #28187, .F. ) ;
#25265=CARTESIAN_POINT ( 'NONE',  ( 6.224689322667647851, 62.55544044765247236, 134.1951906609240837 ) ) ;
#25266=CARTESIAN_POINT ( 'NONE',  ( 32.73300124599735739, -99.90245962373877830, 62.10906484417201767 ) ) ;
#25268=CARTESIAN_POINT ( 'NONE',  ( 1.833838850855462388, -58.94016894581382360, -132.6005571022085689 ) ) ;
#25269=CARTESIAN_POINT ( 'NONE',  ( 1.832998868059890096, 58.53348008137649572, 132.7810136645739760 ) ) ;
#25271=VERTEX_POINT ( 'NONE', #21954 ) ;
#25273=CARTESIAN_POINT ( 'NONE',  ( 10.93730112725990189, -97.44200844886194091, -115.5857507957714461 ) ) ;
#25274=CARTESIAN_POINT ( 'NONE',  ( 1.833838850093464812, 85.29338149487213627, 117.3962623502777092 ) ) ;
#25277=( LENGTH_UNIT ( ) NAMED_UNIT ( * ) SI_UNIT ( .MILLI., .METRE. ) );
#25280=CARTESIAN_POINT ( 'NONE',  ( 109.1589550718175161, -0.001014448720249593950, -0.007507020724820351841 ) ) ;
#25282=CARTESIAN_POINT ( 'NONE',  ( 21.16825799904935934, 133.3214686481432807, 23.82367662027858302 ) ) ;
#25284=CARTESIAN_POINT ( 'NONE',  ( 13.36082413113061307, -150.7747251079863702, 25.56125765253402449 ) ) ;
#25286=ORIENTED_EDGE ( 'NONE', *, *, #7410, .T. ) ;
#25288=ORIENTED_EDGE ( 'NONE', *, *, #2121, .T. ) ;
#25291=EDGE_CURVE ( 'NONE', #5142, #119, #11500, .T. ) ;
#25292=VERTEX_POINT ( 'NONE', #14903 ) ;
#25293=AXIS2_PLACEMENT_3D ( 'NONE', #16466, #22530, #2800 ) ;
#25296=EDGE_CURVE ( 'NONE', #4923, #5291, #11596, .T. ) ;
#25298=CARTESIAN_POINT ( 'NONE',  ( 10.93730112725932635, 149.7554878793145576, 20.69552240458357062 ) ) ;
#25300=ORIENTED_EDGE ( 'NONE', *, *, #17061, .T. ) ;
#25302=CARTESIAN_POINT ( 'NONE',  ( 55.49584447822657296, -72.18163437663935156, -7.317474139116371568 ) ) ;
#25303=CARTESIAN_POINT ( 'NONE',  ( 109.1586900883932856, 0.0001010081143884183533, -0.007137750914552287197 ) ) ;
#25304=CARTESIAN_POINT ( 'NONE',  ( 25.73574536432416338, -102.8730547980546959, -46.68445899255593901 ) ) ;
#25307=ORIENTED_EDGE ( 'NONE', *, *, #18310, .T. ) ;
#25309=CARTESIAN_POINT ( 'NONE',  ( 55.49584447822657296, -29.75369869230911135, -66.16986612640803855 ) ) ;
#25310=CARTESIAN_POINT ( 'NONE',  ( 109.1587776205901577, 0.001605238040359037010, -0.007151389024634743213 ) ) ;
#25312=CARTESIAN_POINT ( 'NONE',  ( 1.894214914920946624, 132.9862534094756938, 58.16536411967987164 ) ) ;
#25315=CARTESIAN_POINT ( 'NONE',  ( 1.833485406944043827, 107.4794113447409529, 97.49333871408727248 ) ) ;
#25316=( BOUNDED_SURFACE ( )  B_SPLINE_SURFACE ( 3, 1, ( 
 ( #1464, #14560 ),
 ( #14842, #27939 ),
 ( #3477, #23654 ),
 ( #27811, #12538 ) ),
 .UNSPECIFIED., .F., .F., .F. ) 
 B_SPLINE_SURFACE_WITH_KNOTS ( ( 4, 4 ),
 ( 2, 2 ),
 ( 0.000000000000000000, 1.000000000000000000 ),
 ( 0.000000000000000000, 1.000000000000000000 ),
 .UNSPECIFIED. ) 
 GEOMETRIC_REPRESENTATION_ITEM ( )  RATIONAL_B_SPLINE_SURFACE ( (
 ( 1.000000000000000000, 1.000000000000000000),
 ( 0.9956975270656954757, 0.8568959468854893125),
 ( 0.9956975270656954757, 0.8568959468854893125),
 ( 1.000000000000000000, 1.000000000000000000) ) ) 
 REPRESENTATION_ITEM ( '' )  SURFACE ( )  );
#25317=DIRECTION ( 'NONE',  ( 1.000000000000000000, 0.000000000000000000, 0.000000000000000000 ) ) ;
#25318=ORIENTED_EDGE ( 'NONE', *, *, #5169, .F. ) ;
#25319=CARTESIAN_POINT ( 'NONE',  ( 5.340103579038253834, -135.6222865281525571, -57.86178752084628485 ) ) ;
#25320=CARTESIAN_POINT ( 'NONE',  ( 26.11404676487257603, 92.25884714080409310, 65.63269960453273200 ) ) ;
#25322=CARTESIAN_POINT ( 'NONE',  ( 1.834118845439484335, 85.43746956710005236, -117.2918069668792498 ) ) ;
#25323=VECTOR ( 'NONE', #25643, 1000.000000000000000 ) ;
#25326=DIRECTION ( 'NONE',  ( 1.000000000000000000, -0.000000000000000000, -0.000000000000000000 ) ) ;
#25328=ORIENTED_EDGE ( 'NONE', *, *, #24976, .F. ) ;
#25330=ADVANCED_FACE ( 'NONE', ( #28276 ), #1491, .T. ) ;
#25331=VECTOR ( 'NONE', #9212, 1000.000000000000000 ) ;
#25334=ORIENTED_EDGE ( 'NONE', *, *, #8489, .T. ) ;
#25335=ADVANCED_FACE ( 'NONE', ( #26836 ), #450, .F. ) ;
#25337=B_SPLINE_CURVE_WITH_KNOTS ( 'NONE', 3,
 ( #4939, #4503, #2337, #476 ),
 .UNSPECIFIED., .F., .F.,
 ( 4, 4 ),
 ( 1.962615573354718958E-17, 0.008383560773332745034 ),
 .UNSPECIFIED. ) ;
#25338=ORIENTED_EDGE ( 'NONE', *, *, #21125, .F. ) ;
#25344=CARTESIAN_POINT ( 'NONE',  ( 6.224689322667647851, -148.0369967195763081, 2.565137105443233700 ) ) ;
#25347=B_SPLINE_CURVE_WITH_KNOTS ( 'NONE', 3,
 ( #6069, #17395, #1719, #10516 ),
 .UNSPECIFIED., .F., .F.,
 ( 4, 4 ),
 ( 2.238801616996865814E-16, 0.008383748772659661841 ),
 .UNSPECIFIED. ) ;
#25349=CARTESIAN_POINT ( 'NONE',  ( 1.833603222531973387, -125.4455769441937605, -72.93978951866115779 ) ) ;
#25350=CARTESIAN_POINT ( 'NONE',  ( 1.833206310202335265, 97.64934828277093004, 107.3376456496884401 ) ) ;
#25351=CARTESIAN_POINT ( 'NONE',  ( 25.81918753295380142, -45.11728622333212968, 103.6306245682013696 ) ) ;
#25352=VECTOR ( 'NONE', #25993, 1000.000000000000000 ) ;
#25353=ORIENTED_EDGE ( 'NONE', *, *, #7450, .F. ) ;
#25354=CARTESIAN_POINT ( 'NONE',  ( 9.884929003653626367, 57.36421526887348676, -139.1775604444698047 ) ) ;
#25355=CARTESIAN_POINT ( 'NONE',  ( 30.59141879584271706, 116.1811685142589141, 2.701465575440082478 ) ) ;
#25356=CARTESIAN_POINT ( 'NONE',  ( 6.224689322667630975, 134.1951906609239131, 62.55544044765293421 ) ) ;
#25357=CARTESIAN_POINT ( 'NONE',  ( 119.2224693531409088, 70.00000000000002842, 19.99999999999995026 ) ) ;
#25358=CARTESIAN_POINT ( 'NONE',  ( 2.433796855181219243, 107.1581411821798895, -98.43889364293755762 ) ) ;
#25359=CARTESIAN_POINT ( 'NONE',  ( 1.833750490713715431, -138.0897889879342131, 44.58740205676281931 ) ) ;
#25360=ORIENTED_EDGE ( 'NONE', *, *, #3144, .T. ) ;
#25361=CARTESIAN_POINT ( 'NONE',  ( 1.833838848569386837, -144.2962335061013732, 15.34509722932487463 ) ) ;
#25362=CARTESIAN_POINT ( 'NONE',  ( 2.433796855181219243, -31.67151202412867761, -142.0211193075559493 ) ) ;
#25363=( BOUNDED_SURFACE ( )  B_SPLINE_SURFACE ( 3, 1, ( 
 ( #868, #4906 ),
 ( #6792, #22627 ),
 ( #11673, #13674 ),
 ( #20587, #15684 ) ),
 .UNSPECIFIED., .F., .F., .F. ) 
 B_SPLINE_SURFACE_WITH_KNOTS ( ( 4, 4 ),
 ( 2, 2 ),
 ( 0.000000000000000000, 1.000000000000000000 ),
 ( 0.000000000000000000, 1.000000000000000000 ),
 .UNSPECIFIED. ) 
 GEOMETRIC_REPRESENTATION_ITEM ( )  RATIONAL_B_SPLINE_SURFACE ( (
 ( 1.000000000000000000, 1.000000000000000000),
 ( 0.9960225298536222738, 0.9999952330161893110),
 ( 0.9960225298536222738, 0.9999952330161893110),
 ( 1.000000000000000000, 1.000000000000000000) ) ) 
 REPRESENTATION_ITEM ( '' )  SURFACE ( )  );
#25364=CARTESIAN_POINT ( 'NONE',  ( 2.433796855181219243, 86.69855925933974561, 116.8607839509059829 ) ) ;
#25367=CARTESIAN_POINT ( 'NONE',  ( 1.833721034905635205, 145.1093571238132540, -0.3559403234842271058 ) ) ;
#25368=VECTOR ( 'NONE', #20275, 1000.000000000000000 ) ;
#25369=CARTESIAN_POINT ( 'NONE',  ( 1.833485406944057594, 125.9346397303435197, 72.09189602597754742 ) ) ;
#25370=ORIENTED_EDGE ( 'NONE', *, *, #10740, .F. ) ;
#25371=AXIS2_PLACEMENT_3D ( 'NONE', #16052, #12031, #22702 ) ;
#25372=ORIENTED_EDGE ( 'NONE', *, *, #19493, .T. ) ;
#25373=EDGE_CURVE ( 'NONE', #27978, #3848, #21140, .T. ) ;
#25375=CIRCLE ( 'NONE', #1006, 151.1787379149930359 ) ;
#25376=ADVANCED_FACE ( 'NONE', ( #4959 ), #9457, .F. ) ;
#25377=CARTESIAN_POINT ( 'NONE',  ( 25.64692872815574631, -110.3764733653606953, -23.79008960806713802 ) ) ;
#25378=CARTESIAN_POINT ( 'NONE',  ( 1.834118845439484335, 0.1779704863090299238, -145.1099497418795750 ) ) ;
#25379=CARTESIAN_POINT ( 'NONE',  ( 2.430230287190592531, -86.70145658344580397, -116.8646894862420993 ) ) ;
#25380=DIRECTION ( 'NONE',  ( -0.5914120900931442160, -0.2415416038593017345, 0.7693434820005526920 ) ) ;
#25381=FACE_OUTER_BOUND ( 'NONE', #24106, .T. ) ;
#25382=ORIENTED_EDGE ( 'NONE', *, *, #25015, .T. ) ;
#25383=CARTESIAN_POINT ( 'NONE',  ( 55.79472521941428198, 35.74479459808936355, -63.36760613016186028 ) ) ;
#25384=CARTESIAN_POINT ( 'NONE',  ( 9.884929003653608603, -109.0134320167725974, -103.8128997986868711 ) ) ;
#25385=EDGE_CURVE ( 'NONE', #21385, #11913, #10496, .T. ) ;
#25387=CARTESIAN_POINT ( 'NONE',  ( 109.1586059443104944, -0.003127959656212910868, 0.006344953511164418483 ) ) ;
#25388=CARTESIAN_POINT ( 'NONE',  ( 25.64660436782551756, -110.3216080362391125, 24.04259444204624430 ) ) ;
#25389=LINE ( 'NONE', #12142, #25237 ) ;
#25390=AXIS2_PLACEMENT_3D ( 'NONE', #8413, #21220, #3653 ) ;
#25391=CARTESIAN_POINT ( 'NONE',  ( 25.64700659047693776, -66.18331466615499892, -91.48068002582091651 ) ) ;
#25393=CARTESIAN_POINT ( 'NONE',  ( 25.64692232868534560, -0.3267662677143608474, -112.9106972861223426 ) ) ;
#25394=DIRECTION ( 'NONE',  ( 0.5914120900931444380, -0.5938529060132660131, -0.5455001977188070894 ) ) ;
#25395=CARTESIAN_POINT ( 'NONE',  ( 25.86096068574584805, 12.80894308910881563, -112.3259320600842557 ) ) ;
#25397=FACE_OUTER_BOUND ( 'NONE', #23900, .T. ) ;
#25399=ORIENTED_EDGE ( 'NONE', *, *, #21254, .T. ) ;
#25401=( BOUNDED_SURFACE ( )  B_SPLINE_SURFACE ( 3, 1, ( 
 ( #12689, #14705 ),
 ( #23514, #6101 ),
 ( #12550, #21612 ),
 ( #28224, #1474 ) ),
 .UNSPECIFIED., .F., .F., .F. ) 
 B_SPLINE_SURFACE_WITH_KNOTS ( ( 4, 4 ),
 ( 2, 2 ),
 ( 0.000000000000000000, 1.000000000000000000 ),
 ( 0.000000000000000000, 1.000000000000000000 ),
 .UNSPECIFIED. ) 
 GEOMETRIC_REPRESENTATION_ITEM ( )  RATIONAL_B_SPLINE_SURFACE ( (
 ( 1.000000000000000000, 1.000000000000000000),
 ( 0.9960225298536222738, 0.9999952330161893110),
 ( 0.9960225298536222738, 0.9999952330161893110),
 ( 1.000000000000000000, 1.000000000000000000) ) ) 
 REPRESENTATION_ITEM ( '' )  SURFACE ( )  );
#25402=B_SPLINE_CURVE_WITH_KNOTS ( 'NONE', 3,
 ( #222, #9438, #13882, #26837, #20503, #20074, #24712 ),
 .UNSPECIFIED., .F., .F.,
 ( 4, 3, 4 ),
 ( 4.909604562510253576E-17, 0.02816610861753246833, 0.04000277880656220864 ),
 .UNSPECIFIED. ) ;
#25406=VERTEX_POINT ( 'NONE', #15593 ) ;
#25407=EDGE_CURVE ( 'NONE', #14659, #13886, #17564, .T. ) ;
#25408=VECTOR ( 'NONE', #14452, 999.9999999999998863 ) ;
#25410=EDGE_CURVE ( 'NONE', #17451, #13981, #21708, .T. ) ;
#25411=CIRCLE ( 'NONE', #17568, 151.1787379149930359 ) ;
#25412=CARTESIAN_POINT ( 'NONE',  ( 1.833485406944057594, -141.8265699653869376, 30.69200235378888308 ) ) ;
#25414=CARTESIAN_POINT ( 'NONE',  ( 2.430230287190572103, 138.8342928068226172, -43.58368230469245930 ) ) ;
#25415=LINE ( 'NONE', #20641, #25408 ) ;
#25417=B_SPLINE_CURVE_WITH_KNOTS ( 'NONE', 3,
 ( #26975, #13888, #22698, #3103 ),
 .UNSPECIFIED., .F., .F.,
 ( 4, 4 ),
 ( 1.450544195894442722E-16, 0.008383748772659595921 ),
 .UNSPECIFIED. ) ;
#25418=CARTESIAN_POINT ( 'NONE',  ( 2.433796855181205476, 28.83182736670536528, 142.6247129145649239 ) ) ;
#25422=ORIENTED_EDGE ( 'NONE', *, *, #5811, .T. ) ;
#25423=ORIENTED_EDGE ( 'NONE', *, *, #1932, .F. ) ;
#25424=CARTESIAN_POINT ( 'NONE',  ( 1.833485406944057594, -125.4007332306550921, 73.01664920992921282 ) ) ;
#25427=CARTESIAN_POINT ( 'NONE',  ( 10.93730112725971004, 10.89264110825002163, 150.7858122213661147 ) ) ;
#25428=FACE_OUTER_BOUND ( 'NONE', #2944, .T. ) ;
#25429=CARTESIAN_POINT ( 'NONE',  ( 2.263178607246638219, 144.7392885066942938, 13.80342482180135022 ) ) ;
#25430=VERTEX_POINT ( 'NONE', #21065 ) ;
#25431=CARTESIAN_POINT ( 'NONE',  ( 109.1586900883932856, 0.0008465529156545867481, -0.007088091345232581594 ) ) ;
#25432=VECTOR ( 'NONE', #7621, 1000.000000000000114 ) ;
#25433=EDGE_CURVE ( 'NONE', #23751, #16681, #14613, .T. ) ;
#25435=CARTESIAN_POINT ( 'NONE',  ( 1.833838850093452821, -15.16809710532158739, 144.3148369740567887 ) ) ;
#25437=CARTESIAN_POINT ( 'NONE',  ( 25.64681081121879203, -97.99105938547964456, 56.09509703373309719 ) ) ;
#25438=EDGE_CURVE ( 'NONE', #8964, #16334, #14247, .T. ) ;
#25440=ORIENTED_EDGE ( 'NONE', *, *, #18954, .T. ) ;
#25442=EDGE_CURVE ( 'NONE', #20568, #27505, #25415, .T. ) ;
#25443=CARTESIAN_POINT ( 'NONE',  ( 1.833206310202323941, -85.89457578512735836, -116.9567751109827611 ) ) ;
#25445=ORIENTED_EDGE ( 'NONE', *, *, #23215, .F. ) ;
#25446=CARTESIAN_POINT ( 'NONE',  ( 109.1586900883932856, 0.006819617742892440312, -0.002109621908824174229 ) ) ;
#25447=CARTESIAN_POINT ( 'NONE',  ( 28.37603512858358812, -114.7183465482399640, 1.794342805482467496 ) ) ;
#25449=CARTESIAN_POINT ( 'NONE',  ( 1.833485406944043827, -73.01664920992880070, -125.4007332306553195 ) ) ;
#25451=CARTESIAN_POINT ( 'NONE',  ( 1.893872463202078027, -59.90695624048775869, 132.2106029832900447 ) ) ;
#25452=VECTOR ( 'NONE', #23869, 1000.000000000000227 ) ;
#25453=CARTESIAN_POINT ( 'NONE',  ( 109.1721716018069657, -0.01488186354166052411, -0.008358834333183878806 ) ) ;
#25455=CARTESIAN_POINT ( 'NONE',  ( 2.433796855181205476, 116.8607839509056561, 86.69855925934011509 ) ) ;
#25456=CARTESIAN_POINT ( 'NONE',  ( 109.1586900883932856, -0.0001010081143976501722, -0.007137750914550312215 ) ) ;
#25460=CARTESIAN_POINT ( 'NONE',  ( 26.28373643307410035, -4.159810388345511534, -127.4927519498666157 ) ) ;
#25461=CARTESIAN_POINT ( 'NONE',  ( 1.833750490713697223, 85.50916867388957598, -117.2391074582364467 ) ) ;
#25464=ORIENTED_EDGE ( 'NONE', *, *, #9380, .T. ) ;
#25465=ORIENTED_EDGE ( 'NONE', *, *, #7740, .T. ) ;
#25466=EDGE_LOOP ( 'NONE', ( #8969, #17762, #883, #4596, #19651, #27285, #18938, #12435, #7725, #9176, #27398, #11973, #18265, #12759, #2346, #27213, #3931, #5126, #10448, #23532, #2210, #3280, #10941, #3828, #15336, #21743, #1502, #7465, #4842, #11569, #10172, #23176, #2851, #9057, #16425, #21675, #4889, #1758, #28367, #2406, #5324, #15498, #9599, #18151, #25752, #7891, #959, #21520, #91, #24310, #3368, #1548, #25933, #25288, #17466, #3386, #12473, #22042, #2910, #18947, #26707, #21840, #6246, #4705, #22990, #25422, #1791, #13758, #7161, #26637, #21554, #10473, #15219, #6332, #26587, #26265, #13739, #21833, #8245, #17858, #15909, #12612, #11968, #8513, #20314, #17272, #740, #22696, #2241, #3219, #20133, #1596, #28272, #2814, #146, #18038, #16966, #14036, #13531, #8566, #3192, #21909, #23167, #10245, #2171, #25879, #14693, #6261, #16554, #19084, #5763, #24802, #11629, #22145, #27826, #1253, #24647, #14442, #15950, #839, #27859, #8452, #15650, #17756, #21330, #17168, #27828, #7909, #1761, #12148, #24515, #14691, #776, #639, #27898, #7239, #19218, #4111, #9514, #424, #5467, #9747, #67, #26347, #12798, #11356, #22945, #1148, #20895, #19626, #17125, #5149, #19126, #25251, #5334, #19313, #7529, #16022, #689, #15383, #18472, #14586, #19630, #6754, #5308, #12150, #17674, #10980, #5171, #16575, #12544, #11655, #22643, #5377, #22345, #9301, #3698, #4134, #21656, #8940, #6590, #21863, #3767, #279 ) ) ;
#25467=DIRECTION ( 'NONE',  ( 0.5914120900931444380, 0.7693434820005550234, -0.2415416038592938797 ) ) ;
#25469=CARTESIAN_POINT ( 'NONE',  ( 8.186469777911021595, 140.9315935720377411, -49.43817851233925609 ) ) ;
#25472=ORIENTED_EDGE ( 'NONE', *, *, #9074, .T. ) ;
#25473=CARTESIAN_POINT ( 'NONE',  ( 1.893872463202021184, 71.74819926215178612, 126.1771883101040146 ) ) ;
#25477=CARTESIAN_POINT ( 'NONE',  ( 16.75465622695654844, -25.01894884133755070, -140.0080030360330170 ) ) ;
#25478=CARTESIAN_POINT ( 'NONE',  ( 9.884929003653626367, 141.8132360130364589, -50.49804566711977571 ) ) ;
#25479=DIRECTION ( 'NONE',  ( -1.000000000000000000, -0.000000000000000000, -0.000000000000000000 ) ) ;
#25480=CARTESIAN_POINT ( 'NONE',  ( 25.64703792032469565, 107.4308312803558749, 34.74993974076994618 ) ) ;
#25483=EDGE_CURVE ( 'NONE', #24182, #11790, #28310, .T. ) ;
#25484=VERTEX_POINT ( 'NONE', #9717 ) ;
#25486=CARTESIAN_POINT ( 'NONE',  ( 13.36082413113063083, -41.18148072373715962, 147.2768864064166507 ) ) ;
#25488=CARTESIAN_POINT ( 'NONE',  ( 13.36082413113063083, 119.8836995922739419, -94.94363694443931934 ) ) ;
#25489=EDGE_CURVE ( 'NONE', #20246, #13959, #2949, .T. ) ;
#25490=ORIENTED_EDGE ( 'NONE', *, *, #25925, .F. ) ;
#25492=B_SPLINE_CURVE_WITH_KNOTS ( 'NONE', 3,
 ( #3531, #9888, #22995, #5556, #5412, #27567, #25143, #16204, #2979, #25437 ),
 .UNSPECIFIED., .F., .F.,
 ( 4, 3, 3, 4 ),
 ( 1.387778780781445676E-17, 0.0002669560319015820129, 0.0005492286108966361411, 0.0008315040496093414283 ),
 .UNSPECIFIED. ) ;
#25494=CARTESIAN_POINT ( 'NONE',  ( 26.11404676487259024, 76.59696442953192275, 83.38016054979810576 ) ) ;
#25495=VECTOR ( 'NONE', #12452, 1000.000000000000000 ) ;
#25496=CARTESIAN_POINT ( 'NONE',  ( 25.64699802086726166, -23.24292564406113470, 110.4930320910559942 ) ) ;
#25497=CARTESIAN_POINT ( 'NONE',  ( 32.73300124599740002, -110.6325518752271080, -39.98094346392423404 ) ) ;
#25498=CARTESIAN_POINT ( 'NONE',  ( 1.833809397773845440, 141.9016658667396200, 30.34407330672235048 ) ) ;
#25501=CARTESIAN_POINT ( 'NONE',  ( 25.64692872815576408, 112.3258062264003740, -11.48248630407163340 ) ) ;
#25502=CARTESIAN_POINT ( 'NONE',  ( 2.433796855181205476, -16.65276281464661423, 144.5536872373191102 ) ) ;
#25503=ORIENTED_EDGE ( 'NONE', *, *, #7740, .F. ) ;
#25504=VERTEX_POINT ( 'NONE', #5389 ) ;
#25505=CARTESIAN_POINT ( 'NONE',  ( 1.833809397773848993, -30.34407330672281589, 141.9016658667395632 ) ) ;
#25508=LINE ( 'NONE', #3461, #10974 ) ;
#25513=CARTESIAN_POINT ( 'NONE',  ( 5.340103556456385014, 57.86178752079319310, 135.6222865117683511 ) ) ;
#25514=CARTESIAN_POINT ( 'NONE',  ( 109.1721716018069515, -0.001583175916617694974, -0.01699510305643761945 ) ) ;
#25517=CARTESIAN_POINT ( 'NONE',  ( 2.108393763691166267, 46.11438684123344700, -137.7805780486501988 ) ) ;
#25518=CARTESIAN_POINT ( 'NONE',  ( 25.73574536432416693, 65.74844932374649886, 91.86645484851332810 ) ) ;
#25520=CARTESIAN_POINT ( 'NONE',  ( 25.65782528836482257, 22.91156770660802522, 110.5695798068304185 ) ) ;
#25522=ORIENTED_EDGE ( 'NONE', *, *, #4933, .F. ) ;
#25523=EDGE_LOOP ( 'NONE', ( #25044, #24194, #23922, #20628 ) ) ;
#25525=CARTESIAN_POINT ( 'NONE',  ( 25.64681081121879203, -107.5125461021405044, 34.49579773461748999 ) ) ;
#25527=DIRECTION ( 'NONE',  ( 0.5946245182733607137, 0.1642747008466135250, 0.7870422510449672782 ) ) ;
#25528=( BOUNDED_SURFACE ( )  B_SPLINE_SURFACE ( 3, 1, ( 
 ( #13647, #18387 ),
 ( #24759, #24621 ),
 ( #20263, #27170 ),
 ( #26740, #698 ) ),
 .UNSPECIFIED., .F., .F., .F. ) 
 B_SPLINE_SURFACE_WITH_KNOTS ( ( 4, 4 ),
 ( 2, 2 ),
 ( 0.000000000000000000, 1.000000000000000000 ),
 ( 0.000000000000000000, 1.000000000000000000 ),
 .UNSPECIFIED. ) 
 GEOMETRIC_REPRESENTATION_ITEM ( )  RATIONAL_B_SPLINE_SURFACE ( (
 ( 1.000000000000000000, 1.000000000000000000),
 ( 0.9956975270656954757, 0.8568959468854893125),
 ( 0.9956975270656954757, 0.8568959468854893125),
 ( 1.000000000000000000, 1.000000000000000000) ) ) 
 REPRESENTATION_ITEM ( '' )  SURFACE ( )  );
#25529=CARTESIAN_POINT ( 'NONE',  ( 30.58324630866346538, 77.95273942827475366, -92.47020419020104498 ) ) ;
#25530=CARTESIAN_POINT ( 'NONE',  ( 10.93730112725932635, 0.000000000000000000, 0.000000000000000000 ) ) ;
#25532=EDGE_CURVE ( 'NONE', #20029, #6423, #436, .T. ) ;
#25533=CARTESIAN_POINT ( 'NONE',  ( 32.73300124599732186, 0.000000000000000000, 0.000000000000000000 ) ) ;
#25535=CARTESIAN_POINT ( 'NONE',  ( 25.64708010899965629, -11.74803558238360957, 112.2984447178532719 ) ) ;
#25540=CARTESIAN_POINT ( 'NONE',  ( 109.1624594426973118, 0.006066618937910909712, -0.01476644236456991707 ) ) ;
#25543=CARTESIAN_POINT ( 'NONE',  ( 32.73300124599740002, 103.7392577722183660, -55.46353551261898218 ) ) ;
#25544=ORIENTED_EDGE ( 'NONE', *, *, #25584, .F. ) ;
#25548=CARTESIAN_POINT ( 'NONE',  ( 109.1624594426973118, -0.01216903288310969451, -0.01033277910989000709 ) ) ;
#25550=ORIENTED_EDGE ( 'NONE', *, *, #12383, .T. ) ;
#25551=ORIENTED_EDGE ( 'NONE', *, *, #4289, .F. ) ;
#25556=CARTESIAN_POINT ( 'NONE',  ( 25.98107933586723917, 35.99661810151007302, -107.2544904356368534 ) ) ;
#25557=CARTESIAN_POINT ( 'NONE',  ( 10.93730112726006354, 148.8212007290666747, -26.59437931460595905 ) ) ;
#25558=CARTESIAN_POINT ( 'NONE',  ( 1.833485406944043827, 138.1714136985314383, -44.33323125129781772 ) ) ;
#25559=CARTESIAN_POINT ( 'NONE',  ( 25.64708010899966339, 56.50300922386594493, 97.75667227735105769 ) ) ;
#25563=( BOUNDED_SURFACE ( )  B_SPLINE_SURFACE ( 3, 1, ( 
 ( #4794, #38 ),
 ( #4360, #8681 ),
 ( #24099, #8833 ),
 ( #15282, #15870 ) ),
 .UNSPECIFIED., .F., .F., .F. ) 
 B_SPLINE_SURFACE_WITH_KNOTS ( ( 4, 4 ),
 ( 2, 2 ),
 ( 0.000000000000000000, 1.000000000000000000 ),
 ( 0.000000000000000000, 1.000000000000000000 ),
 .UNSPECIFIED. ) 
 GEOMETRIC_REPRESENTATION_ITEM ( )  RATIONAL_B_SPLINE_SURFACE ( (
 ( 1.000000000000000000, 1.000000000000000000),
 ( 0.9956975270656955868, 0.8568959468854907557),
 ( 0.9956975270656955868, 0.8568959468854907557),
 ( 1.000000000000000000, 1.000000000000000000) ) ) 
 REPRESENTATION_ITEM ( '' )  SURFACE ( )  );
#25564=ORIENTED_EDGE ( 'NONE', *, *, #27827, .F. ) ;
#25565=CARTESIAN_POINT ( 'NONE',  ( 2.430230287190581429, 1.451610819319768764, -145.5073573687466535 ) ) ;
#25567=LINE ( 'NONE', #19208, #5936 ) ;
#25568=LINE ( 'NONE', #5704, #17501 ) ;
#25569=CARTESIAN_POINT ( 'NONE',  ( 10.93730112725990011, -115.5857507957697976, -97.44200844886394464 ) ) ;
#25570=FACE_OUTER_BOUND ( 'NONE', #670, .T. ) ;
#25575=CARTESIAN_POINT ( 'NONE',  ( 109.1592201516379674, 0.007856029051022768092, -0.0003082430542016078114 ) ) ;
#25577=ORIENTED_EDGE ( 'NONE', *, *, #27973, .T. ) ;
#25578=EDGE_LOOP ( 'NONE', ( #12249, #2040, #26299, #16271 ) ) ;
#25579=CARTESIAN_POINT ( 'NONE',  ( 1.833838850855463054, 97.03125735562237253, 107.8971100408353720 ) ) ;
#25580=ORIENTED_EDGE ( 'NONE', *, *, #852, .F. ) ;
#25581=CARTESIAN_POINT ( 'NONE',  ( 109.1586059443104944, 0.007068659269321313221, -0.0002768082440289001381 ) ) ;
#25582=CARTESIAN_POINT ( 'NONE',  ( 109.1586900883932856, -0.007088091345232585064, -0.0008465529156545589925 ) ) ;
#25584=EDGE_CURVE ( 'NONE', #13097, #12529, #15532, .T. ) ;
#25585=DIRECTION ( 'NONE',  ( 0.000000000000000000, 0.000000000000000000, 1.000000000000000000 ) ) ;
#25586=B_SPLINE_CURVE_WITH_KNOTS ( 'NONE', 3,
 ( #16064, #3117, #24865, #5130, #9596, #18356 ),
 .UNSPECIFIED., .F., .F.,
 ( 4, 2, 4 ),
 ( 1.390486644391990834E-17, 0.0006311571484586074154, 0.001262314296917200953 ),
 .UNSPECIFIED. ) ;
#25587=CARTESIAN_POINT ( 'NONE',  ( 32.73300124599734318, 105.8473486001051072, 51.32617430724947383 ) ) ;
#25588=DIRECTION ( 'NONE',  ( 0.000000000000000000, 0.000000000000000000, 1.000000000000000000 ) ) ;
#25589=CARTESIAN_POINT ( 'NONE',  ( 19.66333377628667023, 129.5498775999591317, 46.81583828063135400 ) ) ;
#25590=EDGE_CURVE ( 'NONE', #19162, #26024, #18369, .T. ) ;
#25591=B_SPLINE_CURVE_WITH_KNOTS ( 'NONE', 3,
 ( #12274, #12403, #3073, #16303, #21190, #1475, #8115, #9841, #10284, #27526 ),
 .UNSPECIFIED., .F., .F.,
 ( 4, 3, 3, 4 ),
 ( 0.000000000000000000, 0.0002669560319015562089, 0.0005492286108966316959, 0.0008315040496093448977 ),
 .UNSPECIFIED. ) ;
#25594=CARTESIAN_POINT ( 'NONE',  ( 32.73300124599734318, 89.94078864464067635, 75.82012867748514395 ) ) ;
#25597=EDGE_CURVE ( 'NONE', #2611, #2245, #6720, .T. ) ;
#25598=ORIENTED_EDGE ( 'NONE', *, *, #9667, .T. ) ;
#25599=ORIENTED_EDGE ( 'NONE', *, *, #780, .T. ) ;
#25603=CARTESIAN_POINT ( 'NONE',  ( 32.73300124599732186, 0.000000000000000000, 0.000000000000000000 ) ) ;
#25604=CARTESIAN_POINT ( 'NONE',  ( 2.433796855181233454, -1.451562450948615135, -145.5024947199069913 ) ) ;
#25605=CARTESIAN_POINT ( 'NONE',  ( 10.93730112725990367, -125.1380233598473950, -84.82621002473567273 ) ) ;
#25608=CARTESIAN_POINT ( 'NONE',  ( 2.433796855181233454, -16.65276281464466024, -144.5536872373193660 ) ) ;
#25609=EDGE_CURVE ( 'NONE', #3978, #17856, #538, .T. ) ;
#25610=ORIENTED_EDGE ( 'NONE', *, *, #22802, .T. ) ;
#25611=DIRECTION ( 'NONE',  ( -1.000000000000000000, -0.000000000000000000, -0.000000000000000000 ) ) ;
#25613=CARTESIAN_POINT ( 'NONE',  ( 25.73574536432416338, -67.05280231777561539, 90.91878692682003305 ) ) ;
#25614=CARTESIAN_POINT ( 'NONE',  ( 10.93730112725978287, -140.0398180619114896, 56.95489579269701608 ) ) ;
#25618=CARTESIAN_POINT ( 'NONE',  ( 26.11404676487257603, -84.89295829319442532, -74.91683232331061504 ) ) ;
#25619=VERTEX_POINT ( 'NONE', #27445 ) ;
#25623=ORIENTED_EDGE ( 'NONE', *, *, #19778, .F. ) ;
#25624=CARTESIAN_POINT ( 'NONE',  ( 119.2224693531408803, 0.000000000000000000, -19.99999999999998934 ) ) ;
#25625=ORIENTED_EDGE ( 'NONE', *, *, #4323, .T. ) ;
#25626=CARTESIAN_POINT ( 'NONE',  ( 55.49584447822657296, 7.849835876629293274, -72.12568090333334681 ) ) ;
#25627=CARTESIAN_POINT ( 'NONE',  ( 109.1592201516379674, -0.001127733110579631293, 0.007780772729118876421 ) ) ;
#25630=CARTESIAN_POINT ( 'NONE',  ( 30.58324630866343341, 57.02364853894626862, -106.6567942264190663 ) ) ;
#25631=CARTESIAN_POINT ( 'NONE',  ( 25.81918753295379432, 74.93271318951838111, -84.61657260023565641 ) ) ;
#25633=B_SPLINE_CURVE_WITH_KNOTS ( 'NONE', 3,
 ( #12082, #20857, #1139, #18695, #8064, #3571 ),
 .UNSPECIFIED., .F., .F.,
 ( 4, 2, 4 ),
 ( 3.469446951953614189E-18, 0.0006311636237756678520, 0.001262327247551332235 ),
 .UNSPECIFIED. ) ;
#25634=CARTESIAN_POINT ( 'NONE',  ( 1.833750490713671244, -59.26520711749956405, 132.4555075118566378 ) ) ;
#25635=DIRECTION ( 'NONE',  ( -1.000000000000000000, -0.000000000000000000, -0.000000000000000000 ) ) ;
#25637=ORIENTED_EDGE ( 'NONE', *, *, #22408, .T. ) ;
#25639=ORIENTED_EDGE ( 'NONE', *, *, #23569, .T. ) ;
#25640=CARTESIAN_POINT ( 'NONE',  ( 30.59138290137873284, 88.14703743378230172, 75.73279410806755152 ) ) ;
#25641=CARTESIAN_POINT ( 'NONE',  ( 26.28373643307408614, -71.57300207276453818, 105.5888781856748011 ) ) ;
#25642=CARTESIAN_POINT ( 'NONE',  ( 32.73300124599732186, 0.000000000000000000, 0.000000000000000000 ) ) ;
#25643=DIRECTION ( 'NONE',  ( -0.7071067811865485719, 4.906538933386790339E-16, 0.7071067811865465735 ) ) ;
#25645=CARTESIAN_POINT ( 'NONE',  ( 32.73300124599738581, -114.2056417606545864, -28.19767303745721065 ) ) ;
#25648=CARTESIAN_POINT ( 'NONE',  ( 26.11404676487259024, -12.95861723607377414, -112.4785329405483338 ) ) ;
#25650=CARTESIAN_POINT ( 'NONE',  ( 28.37603512858454735, -75.42810021528147502, 86.45299531409429505 ) ) ;
#25652=CARTESIAN_POINT ( 'NONE',  ( 26.11404676487259024, -57.58742681967517285, 97.48350837663589630 ) ) ;
#25653=CARTESIAN_POINT ( 'NONE',  ( 32.73300124599736449, -115.8010721414085253, 20.69176323058589162 ) ) ;
#25655=CARTESIAN_POINT ( 'NONE',  ( 1.832998868059890096, 45.34898734666050046, 137.8420662456171897 ) ) ;
#25657=CARTESIAN_POINT ( 'NONE',  ( 25.64708228042122329, -11.76327187353738246, -112.2968511928420554 ) ) ;
#25661=ORIENTED_EDGE ( 'NONE', *, *, #2121, .F. ) ;
#25662=ORIENTED_EDGE ( 'NONE', *, *, #9207, .F. ) ;
#25663=( BOUNDED_SURFACE ( )  B_SPLINE_SURFACE ( 3, 1, ( 
 ( #18603, #7536 ),
 ( #13987, #7109 ),
 ( #27374, #20608 ),
 ( #16442, #25228 ) ),
 .UNSPECIFIED., .F., .F., .F. ) 
 B_SPLINE_SURFACE_WITH_KNOTS ( ( 4, 4 ),
 ( 2, 2 ),
 ( 0.000000000000000000, 1.000000000000000000 ),
 ( 0.000000000000000000, 1.000000000000000000 ),
 .UNSPECIFIED. ) 
 GEOMETRIC_REPRESENTATION_ITEM ( )  RATIONAL_B_SPLINE_SURFACE ( (
 ( 1.000000000000000000, 1.000000000000000000),
 ( 0.6386103224230316178, 0.9954351624131538845),
 ( 0.6386103224230316178, 0.9954351624131538845),
 ( 1.000000000000000000, 1.000000000000000000) ) ) 
 REPRESENTATION_ITEM ( '' )  SURFACE ( )  );
#25666=CARTESIAN_POINT ( 'NONE',  ( 1.833603222531972277, 30.60504697399407092, -141.8454679205784146 ) ) ;
#25667=EDGE_CURVE ( 'NONE', #7268, #9431, #3247, .T. ) ;
#25669=ORIENTED_EDGE ( 'NONE', *, *, #27802, .T. ) ;
#25670=EDGE_CURVE ( 'NONE', #23219, #11589, #16515, .T. ) ;
#25671=FACE_OUTER_BOUND ( 'NONE', #977, .T. ) ;
#25672=CARTESIAN_POINT ( 'NONE',  ( 1.832998868059890096, 132.3466930259793912, 59.50898020732553562 ) ) ;
#25674=B_SPLINE_CURVE_WITH_KNOTS ( 'NONE', 3,
 ( #25006, #11747, #7288, #22988, #13892, #660 ),
 .UNSPECIFIED., .F., .F.,
 ( 4, 2, 4 ),
 ( 1.301042606982605321E-18, 0.0006311636237756746825, 0.001262327247551348064 ),
 .UNSPECIFIED. ) ;
#25675=B_SPLINE_CURVE_WITH_KNOTS ( 'NONE', 3,
 ( #26427, #23744, #6726, #22116 ),
 .UNSPECIFIED., .F., .F.,
 ( 4, 4 ),
 ( 2.081668171172168513E-17, 0.008383748772659474491 ),
 .UNSPECIFIED. ) ;
#25677=CARTESIAN_POINT ( 'NONE',  ( 2.263178113027038307, -138.7064940342181387, 43.59477710889679258 ) ) ;
#25679=CARTESIAN_POINT ( 'NONE',  ( 109.1592201516379674, -0.003661068210032719476, 0.006957642258155058955 ) ) ;
#25682=CARTESIAN_POINT ( 'NONE',  ( 2.430230287190589422, 133.5180086894991121, 57.85706160874191539 ) ) ;
#25683=CARTESIAN_POINT ( 'NONE',  ( 109.1592201516379674, -0.006957642258146943919, 0.003661068210037270957 ) ) ;
#25684=CARTESIAN_POINT ( 'NONE',  ( 25.64670758986457599, 12.29747533046116104, -112.2393466678476699 ) ) ;
#25686=VERTEX_POINT ( 'NONE', #8046 ) ;
#25687=CARTESIAN_POINT ( 'NONE',  ( 1.834118845439484335, -141.9019470378989638, 30.34413640949651736 ) ) ;
#25688=CARTESIAN_POINT ( 'NONE',  ( 109.1587776205901861, -0.005880209827414154510, 0.004375189885423086227 ) ) ;
#25689=VERTEX_POINT ( 'NONE', #27876 ) ;
#25690=ORIENTED_EDGE ( 'NONE', *, *, #18333, .T. ) ;
#25694=EDGE_CURVE ( 'NONE', #19089, #11885, #27583, .T. ) ;
#25695=LINE ( 'NONE', #21217, #1524 ) ;
#25698=CARTESIAN_POINT ( 'NONE',  ( 109.1586059443104944, 0.003930911098393215057, 0.005881369279875419721 ) ) ;
#25700=CARTESIAN_POINT ( 'NONE',  ( 55.49584447822657296, -29.26468316696729488, -66.38758986585143873 ) ) ;
#25701=ORIENTED_EDGE ( 'NONE', *, *, #24787, .T. ) ;
#25703=CARTESIAN_POINT ( 'NONE',  ( 25.64703792032473828, -107.4308312803555339, -34.74993974077065673 ) ) ;
#25706=CARTESIAN_POINT ( 'NONE',  ( 25.64681081121879203, 91.59071981940661544, -66.03065707438841514 ) ) ;
#25707=ORIENTED_EDGE ( 'NONE', *, *, #25112, .T. ) ;
#25710=CARTESIAN_POINT ( 'NONE',  ( 8.186469777910813761, -118.7566730872907499, 90.56875928602684667 ) ) ;
#25711=VERTEX_POINT ( 'NONE', #1391 ) ;
#25713=ORIENTED_EDGE ( 'NONE', *, *, #13205, .F. ) ;
#25714=LINE ( 'NONE', #27722, #25495 ) ;
#25715=ORIENTED_EDGE ( 'NONE', *, *, #9044, .T. ) ;
#25717=CARTESIAN_POINT ( 'NONE',  ( 109.1592201516379674, -0.003476928926125439582, 0.007051465909551701133 ) ) ;
#25718=EDGE_CURVE ( 'NONE', #20262, #14585, #10807, .T. ) ;
#25719=EDGE_CURVE ( 'NONE', #13141, #3154, #2895, .T. ) ;
#25720=EDGE_LOOP ( 'NONE', ( #13902, #17650, #25423, #6295 ) ) ;
#25722=CARTESIAN_POINT ( 'NONE',  ( 55.79472521941428198, 42.17269936297718402, -59.28412330436260191 ) ) ;
#25723=CARTESIAN_POINT ( 'NONE',  ( 10.93730112725972425, -79.81734490845995822, 128.3908183996588264 ) ) ;
#25724=CARTESIAN_POINT ( 'NONE',  ( 10.93730112726005999, 136.0306644680993600, -65.95960219662998725 ) ) ;
#25728=DIRECTION ( 'NONE',  ( -1.000000000000000000, -0.000000000000000000, -0.000000000000000000 ) ) ;
#25729=DIRECTION ( 'NONE',  ( 0.5946245182733607137, 0.6521823330503020433, -0.4701913299128754331 ) ) ;
#25732=ORIENTED_EDGE ( 'NONE', *, *, #10839, .F. ) ;
#25734=CARTESIAN_POINT ( 'NONE',  ( 109.1586900883932856, -0.0006456433529162976378, -0.007109207791181751390 ) ) ;
#25735=DIRECTION ( 'NONE',  ( 0.000000000000000000, 0.000000000000000000, 1.000000000000000000 ) ) ;
#25737=CARTESIAN_POINT ( 'NONE',  ( 2.063896406836609909, -126.4736179849642923, -71.46753739786147719 ) ) ;
#25738=ORIENTED_EDGE ( 'NONE', *, *, #17788, .T. ) ;
#25742=DIRECTION ( 'NONE',  ( -0.5914120900931443270, -0.3206367055789489662, 0.7398809652417994709 ) ) ;
#25744=CARTESIAN_POINT ( 'NONE',  ( 25.64681081121879203, 75.24277141833491100, 84.18689316040072868 ) ) ;
#25745=FACE_OUTER_BOUND ( 'NONE', #20813, .T. ) ;
#25746=CARTESIAN_POINT ( 'NONE',  ( 8.186469829614448912, 113.2805153378652250, -97.33125097511772594 ) ) ;
#25749=ADVANCED_FACE ( 'NONE', ( #1668 ), #14226, .F. ) ;
#25750=CARTESIAN_POINT ( 'NONE',  ( 13.36082413113061307, -152.7944199136426846, -6.345145185219647210 ) ) ;
#25751=EDGE_CURVE ( 'NONE', #13659, #8222, #8073, .T. ) ;
#25752=ORIENTED_EDGE ( 'NONE', *, *, #13443, .T. ) ;
#25756=EDGE_CURVE ( 'NONE', #19, #5056, #15041, .T. ) ;
#25757=CARTESIAN_POINT ( 'NONE',  ( 28.37599760073042887, -91.75439000741646112, -68.88138253892495300 ) ) ;
#25759=CARTESIAN_POINT ( 'NONE',  ( 13.36082413113063083, -67.94366799842725868, -137.0038452127807034 ) ) ;
#25760=ADVANCED_FACE ( 'NONE', ( #2365 ), #20114, .F. ) ;
#25764=CARTESIAN_POINT ( 'NONE',  ( 5.340103556456395673, 43.36842540065497786, 140.9275371673309110 ) ) ;
#25766=CARTESIAN_POINT ( 'NONE',  ( 25.64708228042121618, 112.2968511928421123, -11.76327187353699344 ) ) ;
#25767=CARTESIAN_POINT ( 'NONE',  ( 25.64704443564076541, 35.01840413910274208, -107.3436266109709862 ) ) ;
#25769=CONICAL_SURFACE ( 'NONE', #23536, 117.6351876552689504, 0.9945805576725580410 ) ;
#25771=DIRECTION ( 'NONE',  ( -1.000000000000000000, -0.000000000000000000, -0.000000000000000000 ) ) ;
#25777=CARTESIAN_POINT ( 'NONE',  ( 2.433796855181233454, 46.34326152018744693, 137.9325382748286870 ) ) ;
#25778=CARTESIAN_POINT ( 'NONE',  ( 10.93730112725985926, -150.7858122213662853, 10.89264110824944609 ) ) ;
#25780=CARTESIAN_POINT ( 'NONE',  ( 25.64681081121879203, -97.57530875170564855, -56.81519825470856944 ) ) ;
#25781=CARTESIAN_POINT ( 'NONE',  ( 30.58324630866349736, -52.76949945162314748, -108.8243914523534812 ) ) ;
#25786=CARTESIAN_POINT ( 'NONE',  ( 25.64692872815576408, -46.21877827526630966, 103.0182448446672367 ) ) ;
#25791=VERTEX_POINT ( 'NONE', #11735 ) ;
#25794=CARTESIAN_POINT ( 'NONE',  ( 25.73574536432414206, -107.6875787074509105, 34.14219540448098655 ) ) ;
#25795=VECTOR ( 'NONE', #4555, 1000.000000000000000 ) ;
#25797=CARTESIAN_POINT ( 'NONE',  ( 109.1778270068192853, -0.007323887274071854900, -0.005755170886745502971 ) ) ;
#25799=CARTESIAN_POINT ( 'NONE',  ( 2.063896406836605024, -43.61045647697596905, -138.5688025270883088 ) ) ;
#25800=CARTESIAN_POINT ( 'NONE',  ( 32.73300124599732186, 0.000000000000000000, 0.000000000000000000 ) ) ;
#25804=CARTESIAN_POINT ( 'NONE',  ( 8.186469829614019034, 127.5731248499976402, 77.65916164626368356 ) ) ;
#25805=CARTESIAN_POINT ( 'NONE',  ( 9.884929003653626367, 85.04731144912678076, -124.2095058357569144 ) ) ;
#25808=CARTESIAN_POINT ( 'NONE',  ( 32.73300124599732186, 0.000000000000000000, 0.000000000000000000 ) ) ;
#25809=DIRECTION ( 'NONE',  ( 1.000000000000000000, -0.000000000000000000, -0.000000000000000000 ) ) ;
#25811=CARTESIAN_POINT ( 'NONE',  ( 16.05277956358200342, -141.0713346807233677, -25.20902801311519781 ) ) ;
#25812=ORIENTED_EDGE ( 'NONE', *, *, #4246, .T. ) ;
#25814=VERTEX_POINT ( 'NONE', #14454 ) ;
#25816=DIRECTION ( 'NONE',  ( 0.5946245182733607137, 0.5357871896547409252, 0.5994612328333236428 ) ) ;
#25817=ORIENTED_EDGE ( 'NONE', *, *, #18889, .F. ) ;
#25822=EDGE_CURVE ( 'NONE', #7920, #23443, #1508, .T. ) ;
#25824=CARTESIAN_POINT ( 'NONE',  ( 25.64670758986458310, -83.57526425215448285, -75.92149922855281829 ) ) ;
#25825=VECTOR ( 'NONE', #27125, 1000.000000000000000 ) ;
#25827=AXIS2_PLACEMENT_3D ( 'NONE', #1027, #25211, #24932 ) ;
#25829=CARTESIAN_POINT ( 'NONE',  ( 30.59141879584292312, -84.53180090073624342, -79.74795589902120696 ) ) ;
#25830=CARTESIAN_POINT ( 'NONE',  ( 26.11404676487259024, 45.01677474591551942, -103.8885755249565079 ) ) ;
#25832=CARTESIAN_POINT ( 'NONE',  ( 25.87036335909427009, 102.8789780196095478, -46.88819766600006034 ) ) ;
#25833=CARTESIAN_POINT ( 'NONE',  ( 25.69398547355839924, 112.9401428107247369, -0.7422864227369042611 ) ) ;
#25834=ORIENTED_EDGE ( 'NONE', *, *, #7236, .F. ) ;
#25835=ORIENTED_EDGE ( 'NONE', *, *, #3227, .T. ) ;
#25836=CARTESIAN_POINT ( 'NONE',  ( 25.64703792032469920, 112.9111140735909373, -0.1487959541345440784 ) ) ;
#25840=CARTESIAN_POINT ( 'NONE',  ( 2.433796855181233454, -109.1007109081219539, -96.28145139437795308 ) ) ;
#25843=ORIENTED_EDGE ( 'NONE', *, *, #13326, .T. ) ;
#25844=CARTESIAN_POINT ( 'NONE',  ( 25.64681081121879203, 91.59071981940661544, -66.03065707438841514 ) ) ;
#25845=CARTESIAN_POINT ( 'NONE',  ( 2.433796855181205476, -144.5536872373190818, -16.65276281464712582 ) ) ;
#25846=CARTESIAN_POINT ( 'NONE',  ( 10.93730112725990367, -104.7670965581004054, -108.9902118373752842 ) ) ;
#25849=ADVANCED_FACE ( 'NONE', ( #24382 ), #787, .F. ) ;
#25851=AXIS2_PLACEMENT_3D ( 'NONE', #16748, #9686, #22950 ) ;
#25853=VECTOR ( 'NONE', #15534, 1000.000000000000000 ) ;
#25855=CARTESIAN_POINT ( 'NONE',  ( 1.893872463202057155, -14.22435552397911351, -144.4512189534318622 ) ) ;
#25860=CARTESIAN_POINT ( 'NONE',  ( 25.64681081121879203, 83.63051021305903987, 75.86069728269016821 ) ) ;
#25861=CARTESIAN_POINT ( 'NONE',  ( 25.64681081121879203, 56.09509703373343115, 97.99105938547943140 ) ) ;
#25862=CARTESIAN_POINT ( 'NONE',  ( 2.063896406836605024, -132.1577797566301911, -60.31174178979941303 ) ) ;
#25866=DIRECTION ( 'NONE',  ( 0.000000000000000000, 0.000000000000000000, 1.000000000000000000 ) ) ;
#25867=CIRCLE ( 'NONE', #27695, 117.6351876552689504 ) ;
#25869=ORIENTED_EDGE ( 'NONE', *, *, #17505, .F. ) ;
#25871=DIRECTION ( 'NONE',  ( 0.000000000000000000, 1.000000000000000000, 3.469446951953603342E-16 ) ) ;
#25873=FACE_OUTER_BOUND ( 'NONE', #11118, .T. ) ;
#25874=CARTESIAN_POINT ( 'NONE',  ( 8.186469777910586387, 102.4860666868860761, 108.6390983781759729 ) ) ;
#25877=DIRECTION ( 'NONE',  ( 0.5946245182733608248, 0.3994439555666180475, 0.6977579871484577145 ) ) ;
#25878=ADVANCED_FACE ( 'NONE', ( #26810 ), #5598, .F. ) ;
#25879=ORIENTED_EDGE ( 'NONE', *, *, #13577, .T. ) ;
#25880=CARTESIAN_POINT ( 'NONE',  ( 25.64700659047698039, -112.3162501909139905, 11.57609179463922899 ) ) ;
#25881=CARTESIAN_POINT ( 'NONE',  ( 109.1586900883932856, -0.007137750914552287197, -0.0001010081143883916684 ) ) ;
#25882=ADVANCED_FACE ( 'NONE', ( #20043 ), #23581, .T. ) ;
#25883=CARTESIAN_POINT ( 'NONE',  ( 1.833485406944043827, 45.34878176254417070, -137.8414413349080974 ) ) ;
#25884=CARTESIAN_POINT ( 'NONE',  ( 25.98107933586709350, -110.8834224379717597, 22.45325949158445411 ) ) ;
#25885=CARTESIAN_POINT ( 'NONE',  ( 25.81918753295378011, -55.70247894228241137, 98.34688456803380063 ) ) ;
#25888=CARTESIAN_POINT ( 'NONE',  ( 6.224689322667630975, 28.26953958630619823, 145.3353551538642137 ) ) ;
#25889=VECTOR ( 'NONE', #23939, 999.9999999999998863 ) ;
#25891=CARTESIAN_POINT ( 'NONE',  ( 26.28373643307400087, 114.7784771129682895, -55.65614982951183265 ) ) ;
#25893=ORIENTED_EDGE ( 'NONE', *, *, #6076, .T. ) ;
#25895=AXIS2_PLACEMENT_3D ( 'NONE', #26357, #24216, #994 ) ;
#25897=B_SPLINE_CURVE_WITH_KNOTS ( 'NONE', 3,
 ( #6795, #7087, #4616, #7227 ),
 .UNSPECIFIED., .F., .F.,
 ( 4, 4 ),
 ( 6.315918300066952003E-16, 0.008383748772660097257 ),
 .UNSPECIFIED. ) ;
#25898=CARTESIAN_POINT ( 'NONE',  ( 25.64681081121880624, 102.9795863647034935, -46.30456157731225630 ) ) ;
#25899=DIRECTION ( 'NONE',  ( -1.000000000000000000, -0.000000000000000000, -0.000000000000000000 ) ) ;
#25901=B_SPLINE_CURVE_WITH_KNOTS ( 'NONE', 3,
 ( #6240, #3787, #23382, #23807, #27823, #8530, #16757 ),
 .UNSPECIFIED., .F., .F.,
 ( 4, 3, 4 ),
 ( 0.000000000000000000, 0.02398743853561357761, 0.04000277880656222251 ),
 .UNSPECIFIED. ) ;
#25902=CARTESIAN_POINT ( 'NONE',  ( 55.79472521941428198, 63.36760613016223687, 35.74479459808869564 ) ) ;
#25903=CARTESIAN_POINT ( 'NONE',  ( 28.37599760073043242, -108.5491283158099520, -37.15642189426513653 ) ) ;
#25904=CARTESIAN_POINT ( 'NONE',  ( 30.58324630866338012, 21.27395054437408461, -119.0579156359856512 ) ) ;
#25906=VECTOR ( 'NONE', #1727, 1000.000000000000114 ) ;
#25908=CARTESIAN_POINT ( 'NONE',  ( 25.64660436782567032, -46.45435812945166987, -102.9120797476510774 ) ) ;
#25911=ADVANCED_FACE ( 'NONE', ( #15721 ), #12394, .F. ) ;
#25916=CARTESIAN_POINT ( 'NONE',  ( 119.2224693531408803, -69.99999999999998579, 40.00000000000003553 ) ) ;
#25921=CARTESIAN_POINT ( 'NONE',  ( 109.1587776205901577, -0.006729130500857921811, 0.002904816147418899739 ) ) ;
#25922=CARTESIAN_POINT ( 'NONE',  ( 28.43349137099840718, -54.21282462801698188, -111.8014342888391184 ) ) ;
#25925=EDGE_CURVE ( 'NONE', #22173, #27786, #18317, .T. ) ;
#25927=EDGE_CURVE ( 'NONE', #23545, #10869, #14564, .T. ) ;
#25928=VERTEX_POINT ( 'NONE', #761 ) ;
#25929=CARTESIAN_POINT ( 'NONE',  ( 25.64700659047696263, -112.2686754657454316, -12.02873506870284537 ) ) ;
#25930=CARTESIAN_POINT ( 'NONE',  ( 94.22246935314088034, -151.1871800109700246, -6.938893903907228378E-15 ) ) ;
#25931=ORIENTED_EDGE ( 'NONE', *, *, #25442, .F. ) ;
#25933=ORIENTED_EDGE ( 'NONE', *, *, #3005, .T. ) ;
#25934=CARTESIAN_POINT ( 'NONE',  ( 109.1592201516379674, -0.001331853079201447297, 0.007748443302134876837 ) ) ;
#25935=CARTESIAN_POINT ( 'NONE',  ( 2.430230287190572103, 137.9371479820462696, 46.34481016236872364 ) ) ;
#25936=CARTESIAN_POINT ( 'NONE',  ( 25.64681081121879203, -97.99105938547884875, -56.09509703373446854 ) ) ;
#25937=CARTESIAN_POINT ( 'NONE',  ( 109.1592201516379674, -0.004194960840980736620, 0.006649399203953376171 ) ) ;
#25938=ORIENTED_EDGE ( 'NONE', *, *, #19841, .T. ) ;
#25940=EDGE_CURVE ( 'NONE', #7024, #26408, #6670, .T. ) ;
#25942=CARTESIAN_POINT ( 'NONE',  ( 109.1624594426973260, 0.01531968460305923631, -0.004489871836309145513 ) ) ;
#25943=EDGE_CURVE ( 'NONE', #8211, #4083, #16593, .T. ) ;
#25948=CARTESIAN_POINT ( 'NONE',  ( 1.833603222531972499, -141.8454679205784998, -30.60504697399356999 ) ) ;
#25952=EDGE_CURVE ( 'NONE', #16681, #25814, #3797, .T. ) ;
#25954=VERTEX_POINT ( 'NONE', #9989 ) ;
#25956=CARTESIAN_POINT ( 'NONE',  ( 28.37644542392847313, -34.54617949428011769, -119.4444529625693008 ) ) ;
#25958=EDGE_LOOP ( 'NONE', ( #22619, #11766, #13505, #18586 ) ) ;
#25962=CARTESIAN_POINT ( 'NONE',  ( 28.37603512858445498, 75.42810021528217135, -86.45299531409385452 ) ) ;
#25963=CARTESIAN_POINT ( 'NONE',  ( 32.73300124599738581, 84.80615050150476009, -81.52272205837115848 ) ) ;
#25965=CARTESIAN_POINT ( 'NONE',  ( 25.64681081121879203, -110.3564950173083474, 23.88203588908045916 ) ) ;
#25967=CARTESIAN_POINT ( 'NONE',  ( 2.433796855181205476, -57.85512797797802165, -133.5135467655523769 ) ) ;
#25968=CARTESIAN_POINT ( 'NONE',  ( 109.1586900883932856, 0.006130969560687363727, -0.003656351050331872743 ) ) ;
#25969=EDGE_CURVE ( 'NONE', #24442, #14145, #25591, .T. ) ;
#25970=ORIENTED_EDGE ( 'NONE', *, *, #13482, .T. ) ;
#25971=VERTEX_POINT ( 'NONE', #7836 ) ;
#25972=CARTESIAN_POINT ( 'NONE',  ( 25.64681081121879203, 112.9102952884414464, -0.4157506337731811663 ) ) ;
#25974=ADVANCED_FACE ( 'NONE', ( #25098 ), #21215, .F. ) ;
#25976=CARTESIAN_POINT ( 'NONE',  ( 25.81918753295379432, 10.88546493099006618, -112.5005889664127494 ) ) ;
#25977=CARTESIAN_POINT ( 'NONE',  ( 1.833485406944043827, 137.8414413349092058, -45.34878176254091642 ) ) ;
#25980=CARTESIAN_POINT ( 'NONE',  ( 25.64692872815574987, 97.94438212068907035, -56.17679456083698142 ) ) ;
#25982=CARTESIAN_POINT ( 'NONE',  ( 32.73300124599740002, -81.52272205837138586, -84.80615050150450429 ) ) ;
#25984=VERTEX_POINT ( 'NONE', #5663 ) ;
#25988=VERTEX_POINT ( 'NONE', #18611 ) ;
#25989=B_SPLINE_CURVE_WITH_KNOTS ( 'NONE', 3,
 ( #17376, #20067, #2506, #26684 ),
 .UNSPECIFIED., .F., .F.,
 ( 4, 4 ),
 ( 0.000000000000000000, 0.01077107196513875376 ),
 .UNSPECIFIED. ) ;
#25991=ORIENTED_EDGE ( 'NONE', *, *, #14506, .F. ) ;
#25992=CARTESIAN_POINT ( 'NONE',  ( 109.1589550718174877, -0.002126635388725514868, -0.007270618150629025271 ) ) ;
#25993=DIRECTION ( 'NONE',  ( -1.000000000000000000, -0.000000000000000000, -0.000000000000000000 ) ) ;
#25994=CARTESIAN_POINT ( 'NONE',  ( 25.64660436782556374, -110.5628080555244708, -22.90783756890965961 ) ) ;
#25995=CARTESIAN_POINT ( 'NONE',  ( 1.833485406944057594, 138.1714136985308699, 44.33323125129973619 ) ) ;
#25997=CARTESIAN_POINT ( 'NONE',  ( 25.64670758986457955, -112.2393466678476983, -12.29747533046081998 ) ) ;
#25998=EDGE_CURVE ( 'NONE', #17616, #8222, #27381, .T. ) ;
#26000=CARTESIAN_POINT ( 'NONE',  ( 1.833838850093516770, 0.1779693352087572122, 145.1097630783160923 ) ) ;
#26005=EDGE_LOOP ( 'NONE', ( #6982, #14424, #21483, #5647 ) ) ;
#26006=CARTESIAN_POINT ( 'NONE',  ( 109.1589550718175161, -0.006445391216541674316, 0.003980125429509196594 ) ) ;
#26007=CARTESIAN_POINT ( 'NONE',  ( 1.833750490713686787, -72.78591676344051109, 125.5350013574267649 ) ) ;
#26009=ADVANCED_FACE ( 'NONE', ( #20907 ), #26749, .T. ) ;
#26011=DIRECTION ( 'NONE',  ( 0.000000000000000000, 0.000000000000000000, -1.000000000000000000 ) ) ;
#26012=CARTESIAN_POINT ( 'NONE',  ( 2.433796855181205476, 84.34988187690927930, 118.5671979538059730 ) ) ;
#26014=VERTEX_POINT ( 'NONE', #22699 ) ;
#26015=CARTESIAN_POINT ( 'NONE',  ( 32.73300124599736449, -117.3295799645430435, 8.473903470905730373 ) ) ;
#26016=( BOUNDED_SURFACE ( )  B_SPLINE_SURFACE ( 3, 1, ( 
 ( #17739, #28383 ),
 ( #11272, #11131 ),
 ( #6531, #19903 ),
 ( #188, #8977 ) ),
 .UNSPECIFIED., .F., .F., .F. ) 
 B_SPLINE_SURFACE_WITH_KNOTS ( ( 4, 4 ),
 ( 2, 2 ),
 ( 0.000000000000000000, 1.000000000000000000 ),
 ( 0.000000000000000000, 1.000000000000000000 ),
 .UNSPECIFIED. ) 
 GEOMETRIC_REPRESENTATION_ITEM ( )  RATIONAL_B_SPLINE_SURFACE ( (
 ( 1.000000000000000000, 1.000000000000000000),
 ( 0.6386103224230316178, 0.9954351624131538845),
 ( 0.6386103224230316178, 0.9954351624131538845),
 ( 1.000000000000000000, 1.000000000000000000) ) ) 
 REPRESENTATION_ITEM ( '' )  SURFACE ( )  );
#26018=CARTESIAN_POINT ( 'NONE',  ( 25.73574536432414561, -91.86645484851345600, 65.74844932374622886 ) ) ;
#26019=CARTESIAN_POINT ( 'NONE',  ( 26.11404676487257603, -90.92995828888153653, -67.46175819463459788 ) ) ;
#26023=B_SPLINE_CURVE_WITH_KNOTS ( 'NONE', 3,
 ( #8910, #12928, #21720, #13076 ),
 .UNSPECIFIED., .F., .F.,
 ( 4, 4 ),
 ( 0.000000000000000000, 0.01077107196513875723 ),
 .UNSPECIFIED. ) ;
#26024=VERTEX_POINT ( 'NONE', #9444 ) ;
#26025=FACE_OUTER_BOUND ( 'NONE', #8631, .T. ) ;
#26026=ORIENTED_EDGE ( 'NONE', *, *, #22788, .F. ) ;
#26029=CARTESIAN_POINT ( 'NONE',  ( -90.83090735639699176, 0.000000000000000000, -37.50000000000001421 ) ) ;
#26030=CARTESIAN_POINT ( 'NONE',  ( 109.1586059443104944, -0.001921075557418409560, 0.006808232911146182807 ) ) ;
#26031=EDGE_CURVE ( 'NONE', #3338, #7920, #5279, .T. ) ;
#26032=CARTESIAN_POINT ( 'NONE',  ( 8.186469777910859946, -145.3272523831805074, 34.43598809570094943 ) ) ;
#26033=CARTESIAN_POINT ( 'NONE',  ( 119.2224693531408803, 70.00000000000004263, 39.99999999999999289 ) ) ;
#26036=EDGE_CURVE ( 'NONE', #1993, #14040, #2967, .T. ) ;
#26037=DIRECTION ( 'NONE',  ( -1.000000000000000000, -0.000000000000000000, -0.000000000000000000 ) ) ;
#26039=CARTESIAN_POINT ( 'NONE',  ( 10.93730112725996229, -20.69552240458240888, -149.7554878793151545 ) ) ;
#26040=CARTESIAN_POINT ( 'NONE',  ( 25.64692232868534205, 34.58055111992187136, -107.4854307433083704 ) ) ;
#26044=CARTESIAN_POINT ( 'NONE',  ( 25.64708228042119842, 103.1335618347711574, 45.96113332231374926 ) ) ;
#26045=B_SPLINE_CURVE_WITH_KNOTS ( 'NONE', 3,
 ( #21674, #10600, #1946, #26132, #19643, #10467, #6422 ),
 .UNSPECIFIED., .F., .F.,
 ( 4, 3, 4 ),
 ( 0.000000000000000000, 0.02398743853561336251, 0.04000277880656219476 ),
 .UNSPECIFIED. ) ;
#26047=CARTESIAN_POINT ( 'NONE',  ( 109.1586059443104944, 0.004524147648825563653, -0.005438258427231146795 ) ) ;
#26049=FACE_OUTER_BOUND ( 'NONE', #18931, .T. ) ;
#26050=CARTESIAN_POINT ( 'NONE',  ( 28.43349137099831481, -46.80919715692979111, 115.0977416143055621 ) ) ;
#26051=ORIENTED_EDGE ( 'NONE', *, *, #385, .F. ) ;
#26052=CARTESIAN_POINT ( 'NONE',  ( 28.37603512858359522, 1.794342805482873171, 114.7183465482399640 ) ) ;
#26053=CARTESIAN_POINT ( 'NONE',  ( 10.93730112725992676, -65.95960219663038515, -136.0306644680990473 ) ) ;
#26054=CARTESIAN_POINT ( 'NONE',  ( 1.833721034905662295, 117.1867194831490480, -85.58110185769974976 ) ) ;
#26056=ORIENTED_EDGE ( 'NONE', *, *, #2684, .F. ) ;
#26057=CARTESIAN_POINT ( 'NONE',  ( 25.64708010899965274, -112.2984447178532577, -11.74803558238400036 ) ) ;
#26058=LINE ( 'NONE', #23360, #1926 ) ;
#26063=EDGE_CURVE ( 'NONE', #5582, #19356, #3246, .T. ) ;
#26064=CARTESIAN_POINT ( 'NONE',  ( 2.063896406836609909, 96.20114399516543813, -108.8509294491455108 ) ) ;
#26065=EDGE_CURVE ( 'NONE', #21162, #3526, #18011, .T. ) ;
#26066=CARTESIAN_POINT ( 'NONE',  ( 28.37603512858451182, 65.97809844506251409, -93.86378016273907576 ) ) ;
#26070=VERTEX_POINT ( 'NONE', #4968 ) ;
#26071=CARTESIAN_POINT ( 'NONE',  ( 55.79472521941426777, 43.35047097963528273, -58.42842213658284578 ) ) ;
#26073=B_SPLINE_CURVE_WITH_KNOTS ( 'NONE', 3,
 ( #12271, #9838, #14125, #9542, #22801, #1192, #27377, #3347 ),
 .UNSPECIFIED., .F., .F.,
 ( 4, 2, 2, 4 ),
 ( 0.000000000000000000, 0.0002429588503611127296, 0.0004859177007222254593, 0.0009718354014444932024 ),
 .UNSPECIFIED. ) ;
#26074=CARTESIAN_POINT ( 'NONE',  ( 55.49584447822657296, 36.04376091928543246, 62.96491934286007108 ) ) ;
#26075=DIRECTION ( 'NONE',  ( 0.5946245182733607137, -0.5955128528260776877, -0.5401723099040898202 ) ) ;
#26076=CARTESIAN_POINT ( 'NONE',  ( 1.833838848569427027, 96.96512505224374934, -107.9566558236566749 ) ) ;
#26077=CARTESIAN_POINT ( 'NONE',  ( 1.833750490713672132, -141.8829662951650903, -30.43107162406015576 ) ) ;
#26078=CARTESIAN_POINT ( 'NONE',  ( 10.93730112725972070, -4.928439153521261495, 151.0983828010090804 ) ) ;
#26079=LINE ( 'NONE', #21341, #25889 ) ;
#26081=ORIENTED_EDGE ( 'NONE', *, *, #4351, .T. ) ;
#26082=VERTEX_POINT ( 'NONE', #5401 ) ;
#26083=CARTESIAN_POINT ( 'NONE',  ( 1.834118845439484335, 15.34511559672872671, -144.2964192726480519 ) ) ;
#26087=ORIENTED_EDGE ( 'NONE', *, *, #193, .F. ) ;
#26089=EDGE_CURVE ( 'NONE', #4782, #16696, #22842, .T. ) ;
#26090=ADVANCED_BREP_SHAPE_REPRESENTATION ( '', ( #8673, #27263 ), #16248 ) ;
#26093=EDGE_CURVE ( 'NONE', #25791, #17323, #22099, .T. ) ;
#26095=CARTESIAN_POINT ( 'NONE',  ( 109.1721716018069515, 0.01157047143378738159, -0.01254847260354039276 ) ) ;
#26096=EDGE_CURVE ( 'NONE', #14998, #7877, #25229, .T. ) ;
#26097=CARTESIAN_POINT ( 'NONE',  ( 55.79472521941428198, -69.41463258328498398, -21.78881894124774732 ) ) ;
#26098=CARTESIAN_POINT ( 'NONE',  ( 8.186469777910478030, 149.3111477498015631, -3.468244369822261142 ) ) ;
#26101=CARTESIAN_POINT ( 'NONE',  ( 25.64660436782576625, 102.9120797476511626, -46.45435812945127196 ) ) ;
#26102=CARTESIAN_POINT ( 'NONE',  ( 28.37644542392849800, -65.64862111872122341, 105.5967537682339668 ) ) ;
#26106=CARTESIAN_POINT ( 'NONE',  ( 25.64681081121879203, 91.59071981940572016, 66.03065707438965148 ) ) ;
#26108=B_SPLINE_CURVE_WITH_KNOTS ( 'NONE', 3,
 ( #8865, #23991, #19224, #6010, #6563, #4244 ),
 .UNSPECIFIED., .F., .F.,
 ( 4, 2, 4 ),
 ( 0.000000000000000000, 0.0006311636237756768509, 0.001262327247551353702 ),
 .UNSPECIFIED. ) ;
#26110=CARTESIAN_POINT ( 'NONE',  ( 109.1624594426973118, 0.002129375066974254459, 0.01582142368019177209 ) ) ;
#26112=ORIENTED_EDGE ( 'NONE', *, *, #4099, .T. ) ;
#26114=DIRECTION ( 'NONE',  ( -0.5946245182733608248, 0.7870422510449656128, 0.1642747008466218794 ) ) ;
#26115=CARTESIAN_POINT ( 'NONE',  ( 1.833485406944043827, -108.1939177044932592, 96.69979900902130510 ) ) ;
#26116=VERTEX_POINT ( 'NONE', #7152 ) ;
#26120=EDGE_LOOP ( 'NONE', ( #19191, #3887, #13802, #4853 ) ) ;
#26124=EDGE_LOOP ( 'NONE', ( #23423, #507 ) ) ;
#26125=EDGE_CURVE ( 'NONE', #3474, #12622, #27246, .T. ) ;
#26126=CARTESIAN_POINT ( 'NONE',  ( 24.01988960052053201, 127.2243989116375076, 31.41104197353366345 ) ) ;
#26127=CARTESIAN_POINT ( 'NONE',  ( 2.433796855181205476, 142.6247129145651797, -28.83182736670396196 ) ) ;
#26129=FACE_OUTER_BOUND ( 'NONE', #19357, .T. ) ;
#26132=CARTESIAN_POINT ( 'NONE',  ( 19.66333377628716050, -9.924285918885514590, -137.3914191246404357 ) ) ;
#26133=( BOUNDED_SURFACE ( )  B_SPLINE_SURFACE ( 3, 1, ( 
 ( #24159, #17372 ),
 ( #28173, #4419 ),
 ( #24441, #21705 ),
 ( #2244, #28308 ) ),
 .UNSPECIFIED., .F., .F., .F. ) 
 B_SPLINE_SURFACE_WITH_KNOTS ( ( 4, 4 ),
 ( 2, 2 ),
 ( 0.000000000000000000, 1.000000000000000000 ),
 ( 0.000000000000000000, 1.000000000000000000 ),
 .UNSPECIFIED. ) 
 GEOMETRIC_REPRESENTATION_ITEM ( )  RATIONAL_B_SPLINE_SURFACE ( (
 ( 1.000000000000000000, 1.000000000000000000),
 ( 0.9956975270656954757, 0.8568959468854893125),
 ( 0.9956975270656954757, 0.8568959468854893125),
 ( 1.000000000000000000, 1.000000000000000000) ) ) 
 REPRESENTATION_ITEM ( '' )  SURFACE ( )  );
#26134=CARTESIAN_POINT ( 'NONE',  ( 1.833721034905647418, 125.8463597577927118, 72.24642519953816588 ) ) ;
#26135=CARTESIAN_POINT ( 'NONE',  ( 1.831572820252008738, -14.18623102066671038, -144.4165162501764428 ) ) ;
#26137=CARTESIAN_POINT ( 'NONE',  ( 25.81918753295380142, -112.3053965977762374, 12.74259626488116126 ) ) ;
#26138=ORIENTED_EDGE ( 'NONE', *, *, #23226, .T. ) ;
#26140=CARTESIAN_POINT ( 'NONE',  ( 32.73300124599734318, 113.0038235389602477, 32.68291970228275289 ) ) ;
#26141=CARTESIAN_POINT ( 'NONE',  ( 2.108985857320944124, 118.2933707022557570, 84.36123201973842356 ) ) ;
#26142=CARTESIAN_POINT ( 'NONE',  ( 26.11404676487257603, 84.89295829319495112, 74.91683232331003239 ) ) ;
#26143=CARTESIAN_POINT ( 'NONE',  ( 8.186469829614438254, 102.4860667297611769, -108.6390983847740301 ) ) ;
#26146=CARTESIAN_POINT ( 'NONE',  ( 2.433796855181205476, -137.9325382748282038, -46.34326152018883249 ) ) ;
#26148=ORIENTED_EDGE ( 'NONE', *, *, #18065, .F. ) ;
#26150=CARTESIAN_POINT ( 'NONE',  ( 2.063896406836605024, 31.51663808384751775, -141.8093313989357682 ) ) ;
#26152=CARTESIAN_POINT ( 'NONE',  ( 55.49584447822657296, 72.18163437663939419, 7.317474139115872411 ) ) ;
#26153=CARTESIAN_POINT ( 'NONE',  ( 1.833206308920094285, -45.54896581797555655, 137.7753864329223745 ) ) ;
#26154=VERTEX_POINT ( 'NONE', #21646 ) ;
#26155=CARTESIAN_POINT ( 'NONE',  ( 2.063896406836605024, 28.88716984836320023, 142.3682421260908484 ) ) ;
#26156=CARTESIAN_POINT ( 'NONE',  ( 1.833838850093465700, 15.16809710532252886, -144.3148369740566181 ) ) ;
#26157=EDGE_CURVE ( 'NONE', #2848, #9399, #14460, .T. ) ;
#26159=CARTESIAN_POINT ( 'NONE',  ( 25.64660436782546427, 112.2303901742709797, -12.37913844082926573 ) ) ;
#26160=ADVANCED_FACE ( 'NONE', ( #4085 ), #1554, .F. ) ;
#26161=LINE ( 'NONE', #11047, #7401 ) ;
#26162=DIRECTION ( 'NONE',  ( 1.000000000000000000, 0.000000000000000000, 0.000000000000000000 ) ) ;
#26165=FACE_OUTER_BOUND ( 'NONE', #12716, .T. ) ;
#26167=CARTESIAN_POINT ( 'NONE',  ( 25.73574536432416693, 46.68445899255630849, -102.8730547980545538 ) ) ;
#26168=CARTESIAN_POINT ( 'NONE',  ( 2.433796855181233454, -138.8296532063085351, -43.58222566461785163 ) ) ;
#26169=CARTESIAN_POINT ( 'NONE',  ( 10.93730112725943471, 119.3442956573271516, 92.80059208661684522 ) ) ;
#26171=CARTESIAN_POINT ( 'NONE',  ( 25.87036335909426654, 110.7910326764402953, 22.53739730344084080 ) ) ;
#26173=CARTESIAN_POINT ( 'NONE',  ( 13.36082413113061307, -6.345145185219113415, 152.7944199136427130 ) ) ;
#26174=CARTESIAN_POINT ( 'NONE',  ( 109.1592201516379674, 0.001127733110588118211, 0.007780772729122761334 ) ) ;
#26175=VERTEX_POINT ( 'NONE', #12718 ) ;
#26176=( BOUNDED_SURFACE ( )  B_SPLINE_SURFACE ( 3, 1, ( 
 ( #20143, #430 ),
 ( #17973, #24641 ),
 ( #4894, #22617 ),
 ( #11661, #26904 ) ),
 .UNSPECIFIED., .F., .F., .F. ) 
 B_SPLINE_SURFACE_WITH_KNOTS ( ( 4, 4 ),
 ( 2, 2 ),
 ( 0.000000000000000000, 1.000000000000000000 ),
 ( 0.000000000000000000, 1.000000000000000000 ),
 .UNSPECIFIED. ) 
 GEOMETRIC_REPRESENTATION_ITEM ( )  RATIONAL_B_SPLINE_SURFACE ( (
 ( 1.000000000000000000, 1.000000000000000000),
 ( 0.9956975270656954757, 0.8568959468854893125),
 ( 0.9956975270656954757, 0.8568959468854893125),
 ( 1.000000000000000000, 1.000000000000000000) ) ) 
 REPRESENTATION_ITEM ( '' )  SURFACE ( )  );
#26177=ORIENTED_EDGE ( 'NONE', *, *, #19438, .T. ) ;
#26179=CARTESIAN_POINT ( 'NONE',  ( 26.28373643307404706, -114.7784771129677637, 55.65614982951248635 ) ) ;
#26180=CARTESIAN_POINT ( 'NONE',  ( 109.1586900883932856, -0.006819617742893414360, -0.002109621908814778967 ) ) ;
#26181=CARTESIAN_POINT ( 'NONE',  ( 2.433796855181205476, -142.0211193075553524, -31.67151202413115385 ) ) ;
#26182=CARTESIAN_POINT ( 'NONE',  ( 30.58324630866342986, -41.10517620771124570, -113.7441547345751616 ) ) ;
#26183=DIRECTION ( 'NONE',  ( -0.5914120900931443270, -0.5938529060132696769, 0.5455001977188030926 ) ) ;
#26186=CARTESIAN_POINT ( 'NONE',  ( 25.86096068574579476, -33.98552076022123458, -107.8247115223745283 ) ) ;
#26187=CARTESIAN_POINT ( 'NONE',  ( 2.430230287190572103, 57.85706160874143933, 133.5180086894993110 ) ) ;
#26188=CARTESIAN_POINT ( 'NONE',  ( 1.833809397773872307, 117.5007887865419320, -85.14934054436353961 ) ) ;
#26190=CARTESIAN_POINT ( 'NONE',  ( 9.884929003653608603, -78.87917189085001723, 128.2151425008039212 ) ) ;
#26193=CARTESIAN_POINT ( 'NONE',  ( 1.894214914920961057, -45.75988301372547085, -137.7482714433628530 ) ) ;
#26194=CARTESIAN_POINT ( 'NONE',  ( 1.833838850093440387, -117.3962664098817754, -85.29337590730665397 ) ) ;
#26195=VERTEX_POINT ( 'NONE', #21073 ) ;
#26196=EDGE_CURVE ( 'NONE', #18732, #12739, #15930, .T. ) ;
#26197=ORIENTED_EDGE ( 'NONE', *, *, #5315, .T. ) ;
#26199=CARTESIAN_POINT ( 'NONE',  ( 30.58324630866342630, -33.60235057864056074, 116.1819705588612095 ) ) ;
#26202=AXIS2_PLACEMENT_3D ( 'NONE', #4182, #6353, #8942 ) ;
#26203=CARTESIAN_POINT ( 'NONE',  ( 109.1592201516379674, -0.006957642258146943919, 0.003661068210037270957 ) ) ;
#26204=ORIENTED_EDGE ( 'NONE', *, *, #11938, .T. ) ;
#26206=B_SPLINE_CURVE_WITH_KNOTS ( 'NONE', 3,
 ( #28288, #17219, #28152, #26141, #6297, #14779 ),
 .UNSPECIFIED., .F., .F.,
 ( 4, 2, 4 ),
 ( 1.388456241783856658E-17, 0.0006311571484586121859, 0.001262314296917210711 ),
 .UNSPECIFIED. ) ;
#26208=CARTESIAN_POINT ( 'NONE',  ( 1.832998868059858122, -144.3700883710216090, -14.63705790014155816 ) ) ;
#26209=CARTESIAN_POINT ( 'NONE',  ( 26.11404676487257603, 113.2169081140373947, 1.130420376097532653 ) ) ;
#26210=CARTESIAN_POINT ( 'NONE',  ( 6.224689322667630975, -84.93872395422891941, -121.2721959030546657 ) ) ;
#26211=CARTESIAN_POINT ( 'NONE',  ( 119.2224693531408803, -69.99999999999998579, 40.00000000000003553 ) ) ;
#26213=( BOUNDED_SURFACE ( )  B_SPLINE_SURFACE ( 3, 1, ( 
 ( #23924, #24201 ),
 ( #24337, #26064 ),
 ( #4044, #19300 ),
 ( #17555, #2017 ) ),
 .UNSPECIFIED., .F., .F., .F. ) 
 B_SPLINE_SURFACE_WITH_KNOTS ( ( 4, 4 ),
 ( 2, 2 ),
 ( 0.000000000000000000, 1.000000000000000000 ),
 ( 0.000000000000000000, 1.000000000000000000 ),
 .UNSPECIFIED. ) 
 GEOMETRIC_REPRESENTATION_ITEM ( )  RATIONAL_B_SPLINE_SURFACE ( (
 ( 1.000000000000000000, 1.000000000000000000),
 ( 0.9956975270656954757, 0.8568959468854893125),
 ( 0.9956975270656954757, 0.8568959468854893125),
 ( 1.000000000000000000, 1.000000000000000000) ) ) 
 REPRESENTATION_ITEM ( '' )  SURFACE ( )  );
#26214=EDGE_CURVE ( 'NONE', #12942, #7524, #17660, .T. ) ;
#26216=EDGE_CURVE ( 'NONE', #26384, #12090, #4952, .T. ) ;
#26217=ORIENTED_EDGE ( 'NONE', *, *, #5174, .F. ) ;
#26219=CIRCLE ( 'NONE', #18408, 117.6351876552689504 ) ;
#26220=CARTESIAN_POINT ( 'NONE',  ( 25.64681081121880624, 35.28660243342550729, 107.2555980796242494 ) ) ;
#26221=VERTEX_POINT ( 'NONE', #13568 ) ;
#26222=CONICAL_SURFACE ( 'NONE', #21177, 117.6351876552689504, 0.9945805576725580410 ) ;
#26223=VERTEX_POINT ( 'NONE', #17603 ) ;
#26226=B_SPLINE_CURVE_WITH_KNOTS ( 'NONE', 3,
 ( #7567, #9166, #15483, #6874 ),
 .UNSPECIFIED., .F., .F.,
 ( 4, 4 ),
 ( 6.938893903907227607E-18, 0.008383560773332725952 ),
 .UNSPECIFIED. ) ;
#26228=DIRECTION ( 'NONE',  ( -0.5914120900931443270, 0.3206367055789539067, -0.7398809652417974725 ) ) ;
#26229=CARTESIAN_POINT ( 'NONE',  ( 2.433796855181233454, -144.8571464219888298, -13.76554153471842312 ) ) ;
#26234=VECTOR ( 'NONE', #4768, 1000.000000000000227 ) ;
#26239=ORIENTED_EDGE ( 'NONE', *, *, #1749, .F. ) ;
#26240=EDGE_LOOP ( 'NONE', ( #27066, #3554, #16795, #16811 ) ) ;
#26241=ADVANCED_FACE ( 'NONE', ( #4655 ), #9288, .F. ) ;
#26247=CARTESIAN_POINT ( 'NONE',  ( 1.832998868059858122, -72.09222286251171852, 125.9352106559981621 ) ) ;
#26248=VERTEX_POINT ( 'NONE', #196 ) ;
#26250=( BOUNDED_SURFACE ( )  B_SPLINE_SURFACE ( 3, 1, ( 
 ( #5958, #21616 ),
 ( #1620, #1894 ),
 ( #14710, #10696 ),
 ( #28229, #23524 ) ),
 .UNSPECIFIED., .F., .F., .F. ) 
 B_SPLINE_SURFACE_WITH_KNOTS ( ( 4, 4 ),
 ( 2, 2 ),
 ( 0.000000000000000000, 1.000000000000000000 ),
 ( 0.000000000000000000, 1.000000000000000000 ),
 .UNSPECIFIED. ) 
 GEOMETRIC_REPRESENTATION_ITEM ( )  RATIONAL_B_SPLINE_SURFACE ( (
 ( 1.000000000000000000, 1.000000000000000000),
 ( 0.9956975270656954757, 0.8568959468854893125),
 ( 0.9956975270656954757, 0.8568959468854893125),
 ( 1.000000000000000000, 1.000000000000000000) ) ) 
 REPRESENTATION_ITEM ( '' )  SURFACE ( )  );
#26251=EDGE_CURVE ( 'NONE', #24022, #18945, #13422, .T. ) ;
#26253=CARTESIAN_POINT ( 'NONE',  ( 55.79472521941428198, 72.75035398477136539, -0.7279028900796159496 ) ) ;
#26254=ORIENTED_EDGE ( 'NONE', *, *, #13068, .F. ) ;
#26255=ORIENTED_EDGE ( 'NONE', *, *, #8240, .T. ) ;
#26257=EDGE_CURVE ( 'NONE', #26024, #7427, #10125, .T. ) ;
#26258=ORIENTED_EDGE ( 'NONE', *, *, #26901, .T. ) ;
#26261=CIRCLE ( 'NONE', #5120, 151.1787379149930359 ) ;
#26262=VECTOR ( 'NONE', #5419, 1000.000000000000000 ) ;
#26265=ORIENTED_EDGE ( 'NONE', *, *, #25084, .T. ) ;
#26266=CARTESIAN_POINT ( 'NONE',  ( 9.884929003653626367, -124.2095058357571702, -85.04731144912641128 ) ) ;
#26267=CARTESIAN_POINT ( 'NONE',  ( 10.93730112725972781, -92.80059208661754155, 119.3442956573269100 ) ) ;
#26268=CARTESIAN_POINT ( 'NONE',  ( 109.1624594426973118, 0.01551217196237750923, -0.003771499231554137181 ) ) ;
#26269=LINE ( 'NONE', #26547, #7418 ) ;
#26270=CARTESIAN_POINT ( 'NONE',  ( 55.79472521941428198, 69.41463258328512609, 21.78881894124727836 ) ) ;
#26271=CARTESIAN_POINT ( 'NONE',  ( 25.64681081121879203, 103.3177883989779531, 45.54494737132259274 ) ) ;
#26272=CARTESIAN_POINT ( 'NONE',  ( 1.893872463202013856, -117.9862474593102633, 84.54426271294393302 ) ) ;
#26274=EDGE_CURVE ( 'NONE', #25406, #16728, #24521, .T. ) ;
#26276=B_SPLINE_CURVE_WITH_KNOTS ( 'NONE', 3,
 ( #1297, #9815, #14678, #23482, #10098, #27638 ),
 .UNSPECIFIED., .F., .F.,
 ( 4, 2, 4 ),
 ( 0.000000000000000000, 0.0006311636237756806456, 0.001262327247551361291 ),
 .UNSPECIFIED. ) ;
#26277=ORIENTED_EDGE ( 'NONE', *, *, #455, .T. ) ;
#26278=CARTESIAN_POINT ( 'NONE',  ( 25.81918753295378011, 83.36706424720549080, -76.32043280377732231 ) ) ;
#26280=CARTESIAN_POINT ( 'NONE',  ( 2.063896406836609909, -86.47093297168922277, -116.7302989755746268 ) ) ;
#26281=EDGE_CURVE ( 'NONE', #26365, #5798, #15258, .T. ) ;
#26284=CARTESIAN_POINT ( 'NONE',  ( 1.833206308920068972, 84.68961866583003939, 117.8322276971139075 ) ) ;
#26285=CARTESIAN_POINT ( 'NONE',  ( 28.37599760073042887, 111.8383885143455387, 25.60640155549204877 ) ) ;
#26286=ORIENTED_EDGE ( 'NONE', *, *, #10196, .T. ) ;
#26287=CARTESIAN_POINT ( 'NONE',  ( 25.64708010899963142, -34.94352788466213866, -107.3680906278375886 ) ) ;
#26291=DIRECTION ( 'NONE',  ( -0.5946245182733607137, 0.7999021332774024495, 0.08110646981859331861 ) ) ;
#26293=ORIENTED_EDGE ( 'NONE', *, *, #672, .F. ) ;
#26294=CARTESIAN_POINT ( 'NONE',  ( 9.884929003653608603, -139.1775604444707710, 57.36421526887111355 ) ) ;
#26296=CARTESIAN_POINT ( 'NONE',  ( 2.430230287190572103, -96.28466919684024106, -109.1043569252024241 ) ) ;
#26298=CARTESIAN_POINT ( 'NONE',  ( 26.04756280548352620, 65.62256188141849123, -92.21166514879033116 ) ) ;
#26299=ORIENTED_EDGE ( 'NONE', *, *, #18252, .T. ) ;
#26301=AXIS2_PLACEMENT_3D ( 'NONE', #21818, #12878, #3970 ) ;
#26305=CARTESIAN_POINT ( 'NONE',  ( 30.59141879584313983, -9.457572341075664468, -115.8270959620730736 ) ) ;
#26306=CARTESIAN_POINT ( 'NONE',  ( 8.186469829613956861, 148.1306754360699074, 19.05650981809850819 ) ) ;
#26307=CARTESIAN_POINT ( 'NONE',  ( 32.73300124599737870, 20.69176323058787759, -115.8010721414081132 ) ) ;
#26308=CARTESIAN_POINT ( 'NONE',  ( 32.73300124599732186, 0.000000000000000000, 0.000000000000000000 ) ) ;
#26309=CARTESIAN_POINT ( 'NONE',  ( 32.73300124599741423, -97.37344512919810313, -66.00340565729437969 ) ) ;
#26310=CARTESIAN_POINT ( 'NONE',  ( 28.37599760073042532, 68.88138253892522300, -91.75439000741624795 ) ) ;
#26312=LINE ( 'NONE', #6889, #23334 ) ;
#26313=EDGE_LOOP ( 'NONE', ( #24118, #9623, #1175, #15697 ) ) ;
#26315=CARTESIAN_POINT ( 'NONE',  ( 25.64681081121879203, 103.3177883989779531, 45.54494737132259274 ) ) ;
#26318=CARTESIAN_POINT ( 'NONE',  ( 1.831572820252009626, 144.4165162501763007, 14.18623102066816166 ) ) ;
#26319=CARTESIAN_POINT ( 'NONE',  ( 109.1624594426973260, -0.0004639210235576873820, 0.01595733256931099880 ) ) ;
#26320=CARTESIAN_POINT ( 'NONE',  ( 24.22246935314087324, 90.00000000000005684, 39.99999999999999289 ) ) ;
#26321=CARTESIAN_POINT ( 'NONE',  ( 109.1589550718175161, -0.006257602293702388060, -0.004269295012381895196 ) ) ;
#26325=CARTESIAN_POINT ( 'NONE',  ( 25.64681081121880624, 23.88203588908233499, -110.3564950173079353 ) ) ;
#26326=CARTESIAN_POINT ( 'NONE',  ( 109.1592201516379674, 0.0003082430542015802727, 0.007856029051022768092 ) ) ;
#26329=CARTESIAN_POINT ( 'NONE',  ( 109.1778270068192853, -0.009220257877180833977, 0.001322180554001369359 ) ) ;
#26333=CARTESIAN_POINT ( 'NONE',  ( 25.64681081121879203, 110.3564950173081769, 23.88203588908119457 ) ) ;
#26335=ORIENTED_EDGE ( 'NONE', *, *, #26901, .F. ) ;
#26338=FACE_OUTER_BOUND ( 'NONE', #26541, .T. ) ;
#26339=AXIS2_PLACEMENT_3D ( 'NONE', #15150, #25611, #23973 ) ;
#26344=VECTOR ( 'NONE', #791, 1000.000000000000000 ) ;
#26345=AXIS2_PLACEMENT_3D ( 'NONE', #27495, #1169, #27202 ) ;
#26347=ORIENTED_EDGE ( 'NONE', *, *, #22704, .T. ) ;
#26349=CARTESIAN_POINT ( 'NONE',  ( 1.833838848569445679, 141.9017642089168589, -30.34409872482092752 ) ) ;
#26350=CARTESIAN_POINT ( 'NONE',  ( 1.833838848569444790, -45.01064392477834986, -137.9525894882061721 ) ) ;
#26351=EDGE_CURVE ( 'NONE', #23299, #13256, #22512, .T. ) ;
#26356=CARTESIAN_POINT ( 'NONE',  ( 1.832998868059890096, -73.01698022778442976, 125.4013017422228558 ) ) ;
#26357=CARTESIAN_POINT ( 'NONE',  ( 119.2224693531408803, -90.00000000000005684, 39.99999999999997158 ) ) ;
#26359=CARTESIAN_POINT ( 'NONE',  ( 32.73300124599735028, -8.473903470906931190, 117.3295799645429156 ) ) ;
#26360=EDGE_LOOP ( 'NONE', ( #23560, #20025, #6429, #7754 ) ) ;
#26361=ORIENTED_EDGE ( 'NONE', *, *, #21511, .T. ) ;
#26362=CARTESIAN_POINT ( 'NONE',  ( 1.833485406944043827, -125.9346397303440455, 72.09189602597663793 ) ) ;
#26363=CARTESIAN_POINT ( 'NONE',  ( 24.01988960052069899, -36.40943914739808918, -125.8850824254502641 ) ) ;
#26364=ORIENTED_EDGE ( 'NONE', *, *, #26031, .T. ) ;
#26365=VERTEX_POINT ( 'NONE', #2778 ) ;
#26366=ORIENTED_EDGE ( 'NONE', *, *, #5810, .F. ) ;
#26369=CARTESIAN_POINT ( 'NONE',  ( 109.1586900883932856, 0.006130969560687363727, -0.003656351050331872743 ) ) ;
#26370=CARTESIAN_POINT ( 'NONE',  ( 25.70243777736191149, 11.07690056740865714, 112.4037002646848009 ) ) ;
#26375=CARTESIAN_POINT ( 'NONE',  ( 25.64704443564076541, 66.25951665433285598, 91.42548471394218268 ) ) ;
#26377=CARTESIAN_POINT ( 'NONE',  ( 25.64700659047693421, -110.4909389345861115, 23.25292178500328077 ) ) ;
#26378=EDGE_CURVE ( 'NONE', #11237, #7653, #19036, .T. ) ;
#26379=( BOUNDED_SURFACE ( )  B_SPLINE_SURFACE ( 3, 1, ( 
 ( #9434, #5098 ),
 ( #26967, #16033 ),
 ( #13878, #2954 ),
 ( #11727, #9007 ) ),
 .UNSPECIFIED., .F., .F., .F. ) 
 B_SPLINE_SURFACE_WITH_KNOTS ( ( 4, 4 ),
 ( 2, 2 ),
 ( 0.000000000000000000, 1.000000000000000000 ),
 ( 0.000000000000000000, 1.000000000000000000 ),
 .UNSPECIFIED. ) 
 GEOMETRIC_REPRESENTATION_ITEM ( )  RATIONAL_B_SPLINE_SURFACE ( (
 ( 1.000000000000000000, 1.000000000000000000),
 ( 0.9960225298536222738, 0.9999952330161893110),
 ( 0.9960225298536222738, 0.9999952330161893110),
 ( 1.000000000000000000, 1.000000000000000000) ) ) 
 REPRESENTATION_ITEM ( '' )  SURFACE ( )  );
#26381=CARTESIAN_POINT ( 'NONE',  ( 25.98552792386800903, 113.1317367103340246, -1.078856412011222288 ) ) ;
#26382=CARTESIAN_POINT ( 'NONE',  ( 26.11404676487259024, 103.8885755249575453, -45.01677474591305383 ) ) ;
#26384=VERTEX_POINT ( 'NONE', #12206 ) ;
#26385=CARTESIAN_POINT ( 'NONE',  ( 1.832998868059858122, 108.1944082009170245, -96.70023740551016544 ) ) ;
#26386=CARTESIAN_POINT ( 'NONE',  ( 13.36082413113063083, -152.6206443696327995, -9.660980093456263518 ) ) ;
#26387=CARTESIAN_POINT ( 'NONE',  ( 26.11404676487257603, -22.43340081644687345, -110.9778746459749499 ) ) ;
#26391=CARTESIAN_POINT ( 'NONE',  ( 25.65782528836479059, 0.5778133093793608177, -112.9169519833626794 ) ) ;
#26392=CARTESIAN_POINT ( 'NONE',  ( 21.16825799904904315, -87.29264348877902080, 103.5479404090032745 ) ) ;
#26395=CARTESIAN_POINT ( 'NONE',  ( 25.64708228042122329, 97.80372460135754409, -56.42152786924399521 ) ) ;
#26400=EDGE_LOOP ( 'NONE', ( #17529, #24585, #24922, #25328 ) ) ;
#26401=CARTESIAN_POINT ( 'NONE',  ( 2.433796855181233454, -126.7346379669250780, -71.49415740225209959 ) ) ;
#26403=CARTESIAN_POINT ( 'NONE',  ( 109.1721716018069515, 0.01550977894511844715, 0.007126480965768039466 ) ) ;
#26405=B_SPLINE_CURVE_WITH_KNOTS ( 'NONE', 3,
 ( #24941, #7674, #11831, #884, #9670, #8637, #14966 ),
 .UNSPECIFIED., .F., .F.,
 ( 4, 3, 4 ),
 ( 5.724587470723463412E-16, 0.02816610861753240935, 0.04000277880656283314 ),
 .UNSPECIFIED. ) ;
#26407=EDGE_CURVE ( 'NONE', #771, #15935, #7709, .T. ) ;
#26408=VERTEX_POINT ( 'NONE', #20550 ) ;
#26409=ADVANCED_FACE ( 'NONE', ( #27591 ), #11582, .F. ) ;
#26411=EDGE_CURVE ( 'NONE', #20545, #24427, #22823, .T. ) ;
#26412=CARTESIAN_POINT ( 'NONE',  ( 25.69398547355840634, -110.6264597420658049, -22.75551036952039041 ) ) ;
#26413=CARTESIAN_POINT ( 'NONE',  ( 2.263178607246658647, 144.4462811785179213, -16.59120332982995549 ) ) ;
#26415=DIRECTION ( 'NONE',  ( 1.000000000000000000, -0.000000000000000000, -0.000000000000000000 ) ) ;
#26419=EDGE_LOOP ( 'NONE', ( #19709, #6046, #28371, #19465 ) ) ;
#26420=DIRECTION ( 'NONE',  ( 0.000000000000000000, 0.000000000000000000, 1.000000000000000000 ) ) ;
#26423=CARTESIAN_POINT ( 'NONE',  ( 24.01988960052057465, 121.3896480498357704, -49.36855864442009079 ) ) ;
#26426=CARTESIAN_POINT ( 'NONE',  ( 1.893872463202055156, -107.2274879309820932, -97.83022426232074054 ) ) ;
#26427=CARTESIAN_POINT ( 'NONE',  ( 32.73300124599731475, 117.5726003567930036, -3.836798148479248827 ) ) ;
#26428=CARTESIAN_POINT ( 'NONE',  ( 25.65782528836480836, -91.69136324939144345, 65.90345832277442639 ) ) ;
#26429=FACE_OUTER_BOUND ( 'NONE', #20274, .T. ) ;
#26433=ORIENTED_EDGE ( 'NONE', *, *, #3462, .T. ) ;
#26434=CARTESIAN_POINT ( 'NONE',  ( 26.11404676487257603, 97.48350837663606683, 57.58742681967482469 ) ) ;
#26435=ADVANCED_FACE ( 'NONE', ( #22738 ), #12512, .F. ) ;
#26436=CARTESIAN_POINT ( 'NONE',  ( 2.433796855181233454, 109.1007109081226076, 96.28145139437721411 ) ) ;
#26438=ORIENTED_EDGE ( 'NONE', *, *, #8244, .T. ) ;
#26440=CARTESIAN_POINT ( 'NONE',  ( 26.11404676487257603, 47.08215554553657256, -102.9690087468796662 ) ) ;
#26442=CARTESIAN_POINT ( 'NONE',  ( 28.43349137099832191, 21.85613782299149221, -122.3147591366314373 ) ) ;
#26444=ORIENTED_EDGE ( 'NONE', *, *, #9123, .F. ) ;
#26445=FACE_OUTER_BOUND ( 'NONE', #6961, .T. ) ;
#26446=EDGE_CURVE ( 'NONE', #9428, #24314, #21741, .T. ) ;
#26448=CARTESIAN_POINT ( 'NONE',  ( 26.11404676487259024, -47.08215554553450488, -102.9690087468806325 ) ) ;
#26450=ORIENTED_EDGE ( 'NONE', *, *, #16694, .F. ) ;
#26451=ORIENTED_EDGE ( 'NONE', *, *, #778, .F. ) ;
#26456=CARTESIAN_POINT ( 'NONE',  ( 25.64681081121879203, 75.24277141833491100, 84.18689316040072868 ) ) ;
#26457=CARTESIAN_POINT ( 'NONE',  ( 109.1586900883932856, -0.001582822706032874097, -0.006960773163852184385 ) ) ;
#26458=CARTESIAN_POINT ( 'NONE',  ( 1.833809397773803251, 72.70895493223548556, -125.5796696653631273 ) ) ;
#26459=CARTESIAN_POINT ( 'NONE',  ( 19.66333377628745893, -114.0223162644903567, 77.29039328249557173 ) ) ;
#26460=ORIENTED_EDGE ( 'NONE', *, *, #5525, .F. ) ;
#26463=CARTESIAN_POINT ( 'NONE',  ( 25.64707127832796019, 1.378041109049876443E-14, 112.9112343549835487 ) ) ;
#26465=( BOUNDED_SURFACE ( )  B_SPLINE_SURFACE ( 3, 1, ( 
 ( #4569, #7315 ),
 ( #11624, #7462 ),
 ( #20541, #22578 ),
 ( #13342, #4861 ) ),
 .UNSPECIFIED., .F., .F., .F. ) 
 B_SPLINE_SURFACE_WITH_KNOTS ( ( 4, 4 ),
 ( 2, 2 ),
 ( 0.000000000000000000, 1.000000000000000000 ),
 ( 0.000000000000000000, 1.000000000000000000 ),
 .UNSPECIFIED. ) 
 GEOMETRIC_REPRESENTATION_ITEM ( )  RATIONAL_B_SPLINE_SURFACE ( (
 ( 1.000000000000000000, 1.000000000000000000),
 ( 0.6386103224230302855, 0.9954351624131538845),
 ( 0.6386103224230302855, 0.9954351624131538845),
 ( 1.000000000000000000, 1.000000000000000000) ) ) 
 REPRESENTATION_ITEM ( '' )  SURFACE ( )  );
#26466=CARTESIAN_POINT ( 'NONE',  ( 25.64681081121880624, -75.24277141833435678, -84.18689316040122606 ) ) ;
#26468=CARTESIAN_POINT ( 'NONE',  ( 28.37599760073042887, 48.29934869928308672, -104.0705811520809192 ) ) ;
#26471=ORIENTED_EDGE ( 'NONE', *, *, #18461, .F. ) ;
#26472=( BOUNDED_SURFACE ( )  B_SPLINE_SURFACE ( 3, 1, ( 
 ( #14518, #25488 ),
 ( #10626, #7932 ),
 ( #5762, #23324 ),
 ( #5898, #17097 ) ),
 .UNSPECIFIED., .F., .F., .F. ) 
 B_SPLINE_SURFACE_WITH_KNOTS ( ( 4, 4 ),
 ( 2, 2 ),
 ( 0.000000000000000000, 1.000000000000000000 ),
 ( 0.000000000000000000, 1.000000000000000000 ),
 .UNSPECIFIED. ) 
 GEOMETRIC_REPRESENTATION_ITEM ( )  RATIONAL_B_SPLINE_SURFACE ( (
 ( 1.000000000000000000, 1.000000000000000000),
 ( 0.6386103224230316178, 0.9954351624131538845),
 ( 0.6386103224230316178, 0.9954351624131538845),
 ( 1.000000000000000000, 1.000000000000000000) ) ) 
 REPRESENTATION_ITEM ( '' )  SURFACE ( )  );
#26473=ORIENTED_EDGE ( 'NONE', *, *, #14324, .T. ) ;
#26474=ORIENTED_EDGE ( 'NONE', *, *, #17781, .T. ) ;
#26475=EDGE_CURVE ( 'NONE', #18704, #28095, #21754, .T. ) ;
#26477=CARTESIAN_POINT ( 'NONE',  ( 109.1586059443104944, 0.005983234375914148369, -0.003774052605966652253 ) ) ;
#26478=EDGE_CURVE ( 'NONE', #1807, #23985, #28144, .T. ) ;
#26479=ORIENTED_EDGE ( 'NONE', *, *, #17339, .F. ) ;
#26482=ORIENTED_EDGE ( 'NONE', *, *, #20403, .T. ) ;
#26484=ORIENTED_EDGE ( 'NONE', *, *, #21224, .F. ) ;
#26485=CARTESIAN_POINT ( 'NONE',  ( 1.893872463202055156, 31.10971550360780213, -141.7768406633801135 ) ) ;
#26486=CARTESIAN_POINT ( 'NONE',  ( 1.833721034905619218, -45.17977675814218230, -137.8972080590636722 ) ) ;
#26489=CARTESIAN_POINT ( 'NONE',  ( 109.1592201516379674, 0.004194960840990064228, 0.006649399203953477652 ) ) ;
#26491=CARTESIAN_POINT ( 'NONE',  ( 32.73300124599737160, -89.94078864464117373, 75.82012867748450446 ) ) ;
#26493=CARTESIAN_POINT ( 'NONE',  ( 1.833809397773859873, 14.99109763364144854, 144.3333383260367384 ) ) ;
#26496=CARTESIAN_POINT ( 'NONE',  ( 26.04756280548353686, -1.110889087301714317, -113.1727782765314174 ) ) ;
#26503=VERTEX_POINT ( 'NONE', #18821 ) ;
#26504=( BOUNDED_SURFACE ( )  B_SPLINE_SURFACE ( 3, 1, ( 
 ( #4267, #28432 ),
 ( #24282, #13316 ),
 ( #8885, #6585 ),
 ( #11314, #17646 ) ),
 .UNSPECIFIED., .F., .F., .F. ) 
 B_SPLINE_SURFACE_WITH_KNOTS ( ( 4, 4 ),
 ( 2, 2 ),
 ( 0.000000000000000000, 1.000000000000000000 ),
 ( 0.000000000000000000, 1.000000000000000000 ),
 .UNSPECIFIED. ) 
 GEOMETRIC_REPRESENTATION_ITEM ( )  RATIONAL_B_SPLINE_SURFACE ( (
 ( 1.000000000000000000, 1.000000000000000000),
 ( 0.9956975270656955868, 0.8568959468854907557),
 ( 0.9956975270656955868, 0.8568959468854907557),
 ( 1.000000000000000000, 1.000000000000000000) ) ) 
 REPRESENTATION_ITEM ( '' )  SURFACE ( )  );
#26506=ADVANCED_FACE ( 'NONE', ( #1544 ), #27223, .T. ) ;
#26507=DIRECTION ( 'NONE',  ( 1.000000000000000000, 0.000000000000000000, 0.000000000000000000 ) ) ;
#26508=B_SPLINE_CURVE_WITH_KNOTS ( 'NONE', 3,
 ( #12819, #8386, #21757, #3916, #21606, #25529, #1881 ),
 .UNSPECIFIED., .F., .F.,
 ( 4, 3, 4 ),
 ( 6.214185311943901542E-16, 0.02816610861753243017, 0.04000277880656280538 ),
 .UNSPECIFIED. ) ;
#26509=ADVANCED_FACE ( 'NONE', ( #5880 ), #2584, .F. ) ;
#26511=ADVANCED_FACE ( 'NONE', ( #16821 ), #1824, .F. ) ;
#26520=ORIENTED_EDGE ( 'NONE', *, *, #25407, .F. ) ;
#26522=CARTESIAN_POINT ( 'NONE',  ( 25.64708228042118776, 91.32398912287028736, 66.39944550735300766 ) ) ;
#26527=CARTESIAN_POINT ( 'NONE',  ( 32.73300124599734318, 97.37344512919861472, 66.00340565729376863 ) ) ;
#26532=CARTESIAN_POINT ( 'NONE',  ( 2.433796855181233454, -84.34988187691011774, 118.5671979538053904 ) ) ;
#26534=VERTEX_POINT ( 'NONE', #19522 ) ;
#26535=ORIENTED_EDGE ( 'NONE', *, *, #8244, .F. ) ;
#26538=EDGE_CURVE ( 'NONE', #24633, #12673, #23592, .T. ) ;
#26540=CARTESIAN_POINT ( 'NONE',  ( 109.1587776205901861, 0.006388631651935892941, 0.003592288931003373258 ) ) ;
#26541=EDGE_LOOP ( 'NONE', ( #3551, #12984, #9509, #22137 ) ) ;
#26546=CARTESIAN_POINT ( 'NONE',  ( 1.832998868059890096, 137.8420662456176160, -45.34898734665905096 ) ) ;
#26547=CARTESIAN_POINT ( 'NONE',  ( 55.79472521941426777, -37.00555938668304634, 62.63970324008249690 ) ) ;
#26548=CARTESIAN_POINT ( 'NONE',  ( 1.834118845439484335, 107.7186227765454731, 97.22976650547458632 ) ) ;
#26550=CARTESIAN_POINT ( 'NONE',  ( 25.73574536432414916, -0.8061344836377023482, 112.9674920590232574 ) ) ;
#26551=CARTESIAN_POINT ( 'NONE',  ( 25.64692872815577829, -56.73392579406778680, 97.62272225320926111 ) ) ;
#26556=CARTESIAN_POINT ( 'NONE',  ( 26.11404676487257603, -108.0249973236469572, 33.91085499298339556 ) ) ;
#26557=B_SPLINE_CURVE_WITH_KNOTS ( 'NONE', 3,
 ( #5554, #19214, #16640, #27565, #5410, #7881, #3398 ),
 .UNSPECIFIED., .F., .F.,
 ( 4, 3, 4 ),
 ( 0.000000000000000000, 0.02398743853561371292, 0.04000277880656220864 ),
 .UNSPECIFIED. ) ;
#26558=CARTESIAN_POINT ( 'NONE',  ( 1.833485406944057594, -125.4007332306550921, 73.01664920992921282 ) ) ;
#26559=ORIENTED_EDGE ( 'NONE', *, *, #1434, .F. ) ;
#26562=CARTESIAN_POINT ( 'NONE',  ( 25.64708228042119487, 112.2886173090159616, 11.84161204513297605 ) ) ;
#26563=CARTESIAN_POINT ( 'NONE',  ( 1.833485406944043827, -45.34878176254329674, 137.8414413349084100 ) ) ;
#26564=VERTEX_POINT ( 'NONE', #8313 ) ;
#26567=EDGE_CURVE ( 'NONE', #25087, #18715, #1811, .T. ) ;
#26568=CARTESIAN_POINT ( 'NONE',  ( 109.1624594426973260, 0.01551217196236919470, 0.003771499231549628635 ) ) ;
#26572=DIRECTION ( 'NONE',  ( -0.5914120900931443270, 0.1598001217819472741, -0.7903769105750327872 ) ) ;
#26573=PLANE ( 'NONE',  #9675 ) ;
#26574=ORIENTED_EDGE ( 'NONE', *, *, #7103, .T. ) ;
#26575=DIRECTION ( 'NONE',  ( -1.000000000000000000, -0.000000000000000000, -0.000000000000000000 ) ) ;
#26576=CARTESIAN_POINT ( 'NONE',  ( 55.79472521941426777, -6.880567342319213964, -72.42790650415581410 ) ) ;
#26577=CARTESIAN_POINT ( 'NONE',  ( 25.64699802086723324, -34.66526531169716208, 107.4581924007664071 ) ) ;
#26578=LINE ( 'NONE', #11054, #18150 ) ;
#26580=CARTESIAN_POINT ( 'NONE',  ( 1.832998868059890096, -58.53348008137737679, 132.7810136645736350 ) ) ;
#26581=EDGE_LOOP ( 'NONE', ( #12837, #8999, #28189, #5085 ) ) ;
#26582=CARTESIAN_POINT ( 'NONE',  ( 109.1624594426973260, -0.008380433676406151208, 0.01358749486988127669 ) ) ;
#26583=FACE_OUTER_BOUND ( 'NONE', #5020, .T. ) ;
#26585=VECTOR ( 'NONE', #23345, 1000.000000000000000 ) ;
#26586=CARTESIAN_POINT ( 'NONE',  ( 109.1778270068192853, 0.009031542838326012818, -0.002278716897417647214 ) ) ;
#26587=ORIENTED_EDGE ( 'NONE', *, *, #21382, .T. ) ;
#26588=B_SPLINE_CURVE_WITH_KNOTS ( 'NONE', 3,
 ( #15093, #28466, #8771, #23911 ),
 .UNSPECIFIED., .F., .F.,
 ( 4, 4 ),
 ( 1.173473438232358829E-16, 0.008383748772659590717 ),
 .UNSPECIFIED. ) ;
#26589=VERTEX_POINT ( 'NONE', #3851 ) ;
#26591=CARTESIAN_POINT ( 'NONE',  ( 2.430230287190581429, -133.5180086894995100, 57.85706160874099169 ) ) ;
#26592=CARTESIAN_POINT ( 'NONE',  ( 26.11404676487259024, -33.91085499298451822, 108.0249973236466445 ) ) ;
#26595=CARTESIAN_POINT ( 'NONE',  ( 26.11404676487257603, -103.8885755249572469, 45.01677474591374306 ) ) ;
#26596=CARTESIAN_POINT ( 'NONE',  ( 25.81918753295379432, 46.82320532096518662, 102.8711004511195028 ) ) ;
#26597=ORIENTED_EDGE ( 'NONE', *, *, #2247, .F. ) ;
#26598=CARTESIAN_POINT ( 'NONE',  ( 1.833206308920069860, 132.2594750499825977, 59.70089323729781938 ) ) ;
#26602=FACE_OUTER_BOUND ( 'NONE', #23436, .T. ) ;
#26603=EDGE_CURVE ( 'NONE', #26024, #24227, #17220, .T. ) ;
#26604=FACE_OUTER_BOUND ( 'NONE', #24605, .T. ) ;
#26605=CARTESIAN_POINT ( 'NONE',  ( 1.834118845439484335, 72.70910183320567910, 125.5799175751972143 ) ) ;
#26606=VERTEX_POINT ( 'NONE', #12477 ) ;
#26608=EDGE_CURVE ( 'NONE', #26730, #604, #20351, .T. ) ;
#26609=CARTESIAN_POINT ( 'NONE',  ( 1.833485406944057594, -117.7091014914944225, -84.86072343962690923 ) ) ;
#26612=ORIENTED_EDGE ( 'NONE', *, *, #2594, .T. ) ;
#26613=ORIENTED_EDGE ( 'NONE', *, *, #24753, .F. ) ;
#26615=CARTESIAN_POINT ( 'NONE',  ( 25.64700659047694487, -23.25292178500283669, -110.4909389345861825 ) ) ;
#26617=ORIENTED_EDGE ( 'NONE', *, *, #18954, .F. ) ;
#26618=DIRECTION ( 'NONE',  ( -0.5946245182733608248, -0.7332888028688948623, 0.3297108033645193004 ) ) ;
#26622=EDGE_LOOP ( 'NONE', ( #24700, #16333, #15475, #12185 ) ) ;
#26624=CARTESIAN_POINT ( 'NONE',  ( 2.263178113027063176, 13.80342493153510652, 144.7392881653024403 ) ) ;
#26625=CARTESIAN_POINT ( 'NONE',  ( 109.1587776205901577, 0.007280006032833117625, 0.0008489206734409118381 ) ) ;
#26626=CARTESIAN_POINT ( 'NONE',  ( 2.433796855181233454, 74.00833731765563073, 125.2830755159756677 ) ) ;
#26627=CARTESIAN_POINT ( 'NONE',  ( 109.1589550718174877, -0.001014448720240690048, 0.007507020724817400209 ) ) ;
#26628=CARTESIAN_POINT ( 'NONE',  ( 13.36082413113061307, -84.67697637120325282, -127.3428651193256940 ) ) ;
#26635=CARTESIAN_POINT ( 'NONE',  ( 1.832998868059890096, 96.70023740551124547, 108.1944082009160581 ) ) ;
#26637=ORIENTED_EDGE ( 'NONE', *, *, #28444, .T. ) ;
#26639=CARTESIAN_POINT ( 'NONE',  ( 26.11404676487257603, -22.43340081644687345, -110.9778746459749499 ) ) ;
#26640=EDGE_CURVE ( 'NONE', #19484, #21175, #19374, .T. ) ;
#26641=CARTESIAN_POINT ( 'NONE',  ( 25.64681081121879203, 107.2555980796245905, -35.28660243342437752 ) ) ;
#26642=VERTEX_POINT ( 'NONE', #26142 ) ;
#26644=ORIENTED_EDGE ( 'NONE', *, *, #14796, .F. ) ;
#26645=CARTESIAN_POINT ( 'NONE',  ( 109.1587776205901577, -0.002185517590245302823, -0.006995903587858420293 ) ) ;
#26646=CARTESIAN_POINT ( 'NONE',  ( 109.1592201516379674, -0.002720803050370518023, -0.007376275279032888654 ) ) ;
#26647=AXIS2_PLACEMENT_3D ( 'NONE', #25624, #28305, #1828 ) ;
#26648=CARTESIAN_POINT ( 'NONE',  ( 32.73300124599739291, -103.7392577722171865, -55.46353551262117776 ) ) ;
#26649=CARTESIAN_POINT ( 'NONE',  ( 26.11404676487259024, -97.48350837663652158, 57.58742681967414256 ) ) ;
#26653=CARTESIAN_POINT ( 'NONE',  ( 26.11404676487259024, -90.92995828888244603, 67.46175819463337575 ) ) ;
#26654=CARTESIAN_POINT ( 'NONE',  ( 10.93730112725983439, -148.8212007290663621, 26.59437931460704263 ) ) ;
#26655=CARTESIAN_POINT ( 'NONE',  ( 1.832998868059890096, -29.64765804470170352, 142.0492247521721936 ) ) ;
#26656=CARTESIAN_POINT ( 'NONE',  ( 19.66333377628734169, -72.72773398758253904, 116.9853418557801916 ) ) ;
#26657=CIRCLE ( 'NONE', #20229, 117.6351876552689504 ) ;
#26659=CARTESIAN_POINT ( 'NONE',  ( 2.430230287190592531, -144.8619874886005903, -13.76600171652791715 ) ) ;
#26661=CIRCLE ( 'NONE', #14239, 80.00000000000000000 ) ;
#26662=CARTESIAN_POINT ( 'NONE',  ( 1.833750490713712322, -144.2866297127912389, -15.43355859895807214 ) ) ;
#26666=CARTESIAN_POINT ( 'NONE',  ( 28.43349137099832191, -116.8557575815931528, 42.22940898499174978 ) ) ;
#26669=( BOUNDED_SURFACE ( )  B_SPLINE_SURFACE ( 3, 1, ( 
 ( #22348, #2610 ),
 ( #11391, #4921 ),
 ( #13686, #22493 ),
 ( #11532, #10923 ) ),
 .UNSPECIFIED., .F., .F., .F. ) 
 B_SPLINE_SURFACE_WITH_KNOTS ( ( 4, 4 ),
 ( 2, 2 ),
 ( 0.000000000000000000, 1.000000000000000000 ),
 ( 0.000000000000000000, 1.000000000000000000 ),
 .UNSPECIFIED. ) 
 GEOMETRIC_REPRESENTATION_ITEM ( )  RATIONAL_B_SPLINE_SURFACE ( (
 ( 1.000000000000000000, 1.000000000000000000),
 ( 0.9960225298536222738, 0.9999952330161893110),
 ( 0.9960225298536222738, 0.9999952330161893110),
 ( 1.000000000000000000, 1.000000000000000000) ) ) 
 REPRESENTATION_ITEM ( '' )  SURFACE ( )  );
#26670=AXIS2_PLACEMENT_3D ( 'NONE', #3199, #11978, #26793 ) ;
#26671=ORIENTED_EDGE ( 'NONE', *, *, #6226, .F. ) ;
#26674=CARTESIAN_POINT ( 'NONE',  ( 2.108393763691184031, 1.280847988473803101, -145.2872457912033042 ) ) ;
#26675=ORIENTED_EDGE ( 'NONE', *, *, #10589, .F. ) ;
#26678=ORIENTED_EDGE ( 'NONE', *, *, #23656, .F. ) ;
#26683=VECTOR ( 'NONE', #7117, 1000.000000000000000 ) ;
#26684=CARTESIAN_POINT ( 'NONE',  ( 2.433796855181205476, -84.34988187690851191, -118.5671979538065273 ) ) ;
#26685=B_SPLINE_CURVE_WITH_KNOTS ( 'NONE', 3,
 ( #15433, #24541, #4804, #22372, #15879, #9547, #7838, #25391, #5668, #9689 ),
 .UNSPECIFIED., .F., .F.,
 ( 4, 3, 3, 4 ),
 ( 0.000000000000000000, 0.0002669560319015579978, 0.0005492286108966487179, 0.0008315040496093540050 ),
 .UNSPECIFIED. ) ;
#26688=CARTESIAN_POINT ( 'NONE',  ( 16.75465622695633172, 117.7275519421690149, -79.80233222761897594 ) ) ;
#26689=DIRECTION ( 'NONE',  ( -1.000000000000000000, -0.000000000000000000, -0.000000000000000000 ) ) ;
#26690=EDGE_CURVE ( 'NONE', #11148, #28132, #20754, .T. ) ;
#26691=CARTESIAN_POINT ( 'NONE',  ( 25.73574536432414206, -110.3312765349291737, -24.27578079247274090 ) ) ;
#26692=CARTESIAN_POINT ( 'NONE',  ( 109.1721716018069515, 0.01616973485710005917, 0.005466227998627309036 ) ) ;
#26698=CARTESIAN_POINT ( 'NONE',  ( 1.833206310202334155, 0.7447039688725679563, 145.1075835704899362 ) ) ;
#26699=CARTESIAN_POINT ( 'NONE',  ( 26.11404676487257603, 90.92995828888292920, -67.46175819463273626 ) ) ;
#26700=VERTEX_POINT ( 'NONE', #7009 ) ;
#26701=CARTESIAN_POINT ( 'NONE',  ( 109.1592201516379674, -0.003661068210032719476, 0.006957642258155058955 ) ) ;
#26702=CIRCLE ( 'NONE', #6510, 151.1787379149930359 ) ;
#26703=CARTESIAN_POINT ( 'NONE',  ( 26.28373643307405061, -118.1623717393431718, -48.05579805965654572 ) ) ;
#26705=VERTEX_POINT ( 'NONE', #2370 ) ;
#26706=CARTESIAN_POINT ( 'NONE',  ( 28.43349137099835744, 69.71646995966310101, -102.8504004831928853 ) ) ;
#26707=ORIENTED_EDGE ( 'NONE', *, *, #19535, .F. ) ;
#26710=( BOUNDED_SURFACE ( )  B_SPLINE_SURFACE ( 3, 1, ( 
 ( #7106, #24674 ),
 ( #26792, #22796 ),
 ( #27216, #9830 ),
 ( #4789, #2762 ) ),
 .UNSPECIFIED., .F., .F., .F. ) 
 B_SPLINE_SURFACE_WITH_KNOTS ( ( 4, 4 ),
 ( 2, 2 ),
 ( 0.000000000000000000, 1.000000000000000000 ),
 ( 0.000000000000000000, 1.000000000000000000 ),
 .UNSPECIFIED. ) 
 GEOMETRIC_REPRESENTATION_ITEM ( )  RATIONAL_B_SPLINE_SURFACE ( (
 ( 1.000000000000000000, 1.000000000000000000),
 ( 0.9956975270656954757, 0.8568959468854893125),
 ( 0.9956975270656954757, 0.8568959468854893125),
 ( 1.000000000000000000, 1.000000000000000000) ) ) 
 REPRESENTATION_ITEM ( '' )  SURFACE ( )  );
#26711=ORIENTED_EDGE ( 'NONE', *, *, #24344, .F. ) ;
#26712=CARTESIAN_POINT ( 'NONE',  ( 8.186469829614409832, 34.43598812953313626, -145.3272524103319085 ) ) ;
#26715=ORIENTED_EDGE ( 'NONE', *, *, #12002, .F. ) ;
#26716=CARTESIAN_POINT ( 'NONE',  ( 10.93730112725992676, -65.95960219663038515, -136.0306644680990473 ) ) ;
#26717=CARTESIAN_POINT ( 'NONE',  ( 25.64699802086724034, 107.3112355540545764, -35.11755197949727147 ) ) ;
#26721=ORIENTED_EDGE ( 'NONE', *, *, #26378, .T. ) ;
#26724=CARTESIAN_POINT ( 'NONE',  ( 25.98552792386799126, 33.93357582585639420, -107.9280603639523548 ) ) ;
#26725=CARTESIAN_POINT ( 'NONE',  ( 2.430230287190572103, 60.50928654924933880, -132.3371620660944643 ) ) ;
#26727=VECTOR ( 'NONE', #10852, 1000.000000000000000 ) ;
#26728=EDGE_CURVE ( 'NONE', #26995, #19237, #15273, .T. ) ;
#26729=VERTEX_POINT ( 'NONE', #22645 ) ;
#26730=VERTEX_POINT ( 'NONE', #13984 ) ;
#26731=LINE ( 'NONE', #22438, #8330 ) ;
#26732=CARTESIAN_POINT ( 'NONE',  ( 1.833485406944043827, -44.33323125129830089, -138.1714136985312962 ) ) ;
#26738=CARTESIAN_POINT ( 'NONE',  ( 25.64681081121879203, -91.10197563707900770, -66.70335573067958990 ) ) ;
#26739=ORIENTED_EDGE ( 'NONE', *, *, #14796, .T. ) ;
#26740=CARTESIAN_POINT ( 'NONE',  ( 109.1586900883932856, 0.006561743627145262027, 0.002810909342002427570 ) ) ;
#26742=CARTESIAN_POINT ( 'NONE',  ( 1.833206308920094729, -58.34024961171146373, -132.8652726225758158 ) ) ;
#26743=CARTESIAN_POINT ( 'NONE',  ( 109.1778270068192853, 0.009220257877180842651, -0.001322180554001304307 ) ) ;
#26744=VERTEX_POINT ( 'NONE', #3195 ) ;
#26745=CARTESIAN_POINT ( 'NONE',  ( 109.1778270068192853, 0.007152128381194052670, -0.005967275455169908024 ) ) ;
#26747=CARTESIAN_POINT ( 'NONE',  ( 32.73300124599738581, 8.473903470907664826, -117.3295799645428588 ) ) ;
#26748=ORIENTED_EDGE ( 'NONE', *, *, #3803, .F. ) ;
#26749=CONICAL_SURFACE ( 'NONE', #11127, 117.6351876552689504, 0.9945805576725580410 ) ;
#26751=VERTEX_POINT ( 'NONE', #24672 ) ;
#26752=CIRCLE ( 'NONE', #28131, 117.6351876552689504 ) ;
#26753=( BOUNDED_SURFACE ( )  B_SPLINE_SURFACE ( 3, 1, ( 
 ( #12722, #8989 ),
 ( #15151, #23974 ),
 ( #15437, #11002 ),
 ( #17607, #26247 ) ),
 .UNSPECIFIED., .F., .F., .F. ) 
 B_SPLINE_SURFACE_WITH_KNOTS ( ( 4, 4 ),
 ( 2, 2 ),
 ( 0.000000000000000000, 1.000000000000000000 ),
 ( 0.000000000000000000, 1.000000000000000000 ),
 .UNSPECIFIED. ) 
 GEOMETRIC_REPRESENTATION_ITEM ( )  RATIONAL_B_SPLINE_SURFACE ( (
 ( 1.000000000000000000, 1.000000000000000000),
 ( 0.9956975270656954757, 0.8568959468854893125),
 ( 0.9956975270656954757, 0.8568959468854893125),
 ( 1.000000000000000000, 1.000000000000000000) ) ) 
 REPRESENTATION_ITEM ( '' )  SURFACE ( )  );
#26756=FACE_OUTER_BOUND ( 'NONE', #8257, .T. ) ;
#26757=CARTESIAN_POINT ( 'NONE',  ( 25.69398547355842410, 57.11291030433652338, 97.43788956976163718 ) ) ;
#26759=CARTESIAN_POINT ( 'NONE',  ( 119.2224693531408803, -69.99999999999998579, 40.00000000000003553 ) ) ;
#26760=ORIENTED_EDGE ( 'NONE', *, *, #18252, .F. ) ;
#26761=CARTESIAN_POINT ( 'NONE',  ( 8.186469829614290816, -143.0750865143070598, 42.84118568057157006 ) ) ;
#26762=CARTESIAN_POINT ( 'NONE',  ( 25.87036335909425588, 45.07965203035060142, -103.6841944152901505 ) ) ;
#26765=ADVANCED_FACE ( 'NONE', ( #26931 ), #915, .F. ) ;
#26766=DIRECTION ( 'NONE',  ( -0.5914120900931443270, 0.09226095020377932110, 0.8010740644654240628 ) ) ;
#26768=CARTESIAN_POINT ( 'NONE',  ( 1.833838850093465700, 141.9387658801234977, -30.17001957361848241 ) ) ;
#26769=CARTESIAN_POINT ( 'NONE',  ( 25.64700659047697329, -45.71714758798305667, -103.2418925369177316 ) ) ;
#26771=CARTESIAN_POINT ( 'NONE',  ( 10.93730112725992853, -56.95489579269655422, -140.0398180619117738 ) ) ;
#26773=VECTOR ( 'NONE', #15006, 1000.000000000000114 ) ;
#26774=EDGE_CURVE ( 'NONE', #25292, #4874, #2173, .T. ) ;
#26777=AXIS2_PLACEMENT_3D ( 'NONE', #12976, #25809, #19597 ) ;
#26778=CARTESIAN_POINT ( 'NONE',  ( 8.186469829614395621, 19.05650981810018862, -148.1306754360699927 ) ) ;
#26780=CARTESIAN_POINT ( 'NONE',  ( 25.64681081121879203, 56.81519825470756047, 97.57530875170624540 ) ) ;
#26785=CARTESIAN_POINT ( 'NONE',  ( 10.93730112725969938, 71.28103789254939215, 133.3192575531800799 ) ) ;
#26789=EDGE_LOOP ( 'NONE', ( #17430, #15202, #12567, #8197 ) ) ;
#26791=CIRCLE ( 'NONE', #7531, 151.1787379149930359 ) ;
#26792=CARTESIAN_POINT ( 'NONE',  ( 109.1589550718174877, -0.007553890059312251028, 0.0005685167901298121941 ) ) ;
#26793=DIRECTION ( 'NONE',  ( 0.000000000000000000, 0.000000000000000000, 1.000000000000000000 ) ) ;
#26795=ADVANCED_FACE ( 'NONE', ( #23951 ), #5534, .F. ) ;
#26796=EDGE_CURVE ( 'NONE', #6523, #12888, #1947, .T. ) ;
#26799=B_SPLINE_CURVE_WITH_KNOTS ( 'NONE', 3,
 ( #23525, #25811, #3788, #6628, #1621, #7993, #5671 ),
 .UNSPECIFIED., .F., .F.,
 ( 4, 3, 4 ),
 ( 6.019590444871180375E-16, 0.02816610861753244058, 0.04000277880656280538 ),
 .UNSPECIFIED. ) ;
#26800=CARTESIAN_POINT ( 'NONE',  ( 26.11404676487257603, -74.91683232330916553, -84.89295829319569009 ) ) ;
#26801=CARTESIAN_POINT ( 'NONE',  ( 2.430230287190581429, -142.6294793592099666, 28.83279105684380639 ) ) ;
#26802=EDGE_CURVE ( 'NONE', #12561, #20253, #16639, .T. ) ;
#26805=CARTESIAN_POINT ( 'NONE',  ( 21.16825799904903960, 4.416019842158419806, 135.3612955721067408 ) ) ;
#26806=CARTESIAN_POINT ( 'NONE',  ( 1.831572820252009626, -117.9752562883661255, -84.49389457294256545 ) ) ;
#26810=FACE_OUTER_BOUND ( 'NONE', #19539, .T. ) ;
#26812=ORIENTED_EDGE ( 'NONE', *, *, #716, .T. ) ;
#26816=CARTESIAN_POINT ( 'NONE',  ( 1.834118845439484335, -125.5799175751964754, -72.70910183320698650 ) ) ;
#26821=VERTEX_POINT ( 'NONE', #22202 ) ;
#26827=CARTESIAN_POINT ( 'NONE',  ( 1.833721034905664959, -97.36162733017636128, -107.5990973104333079 ) ) ;
#26828=VERTEX_POINT ( 'NONE', #22688 ) ;
#26829=CARTESIAN_POINT ( 'NONE',  ( 2.063896406836605024, 60.31174178979986777, -132.1577797566299921 ) ) ;
#26830=CIRCLE ( 'NONE', #13977, 151.1787379149930359 ) ;
#26832=CARTESIAN_POINT ( 'NONE',  ( 2.108393763691180478, 125.1820217068196115, 73.75286979200500070 ) ) ;
#26833=CARTESIAN_POINT ( 'NONE',  ( 10.93730112726006354, 145.2260730187408626, -42.00474393596100953 ) ) ;
#26836=FACE_OUTER_BOUND ( 'NONE', #8209, .T. ) ;
#26837=CARTESIAN_POINT ( 'NONE',  ( 26.28373643307434548, 67.34887744616764849, 108.3320567927989231 ) ) ;
#26838=FACE_OUTER_BOUND ( 'NONE', #19637, .T. ) ;
#26841=ORIENTED_EDGE ( 'NONE', *, *, #7138, .F. ) ;
#26844=CARTESIAN_POINT ( 'NONE',  ( 25.64670758986458310, -84.24158725144673099, 75.18147256662025768 ) ) ;
#26845=CARTESIAN_POINT ( 'NONE',  ( 10.93730112726005821, 140.0398180619120865, -56.95489579269602842 ) ) ;
#26846=CARTESIAN_POINT ( 'NONE',  ( 2.433796855181219243, 86.69855925933974561, 116.8607839509059829 ) ) ;
#26847=ORIENTED_EDGE ( 'NONE', *, *, #17307, .F. ) ;
#26848=CARTESIAN_POINT ( 'NONE',  ( 10.93730112725932813, 151.0983828010088246, -4.928439153520510985 ) ) ;
#26849=CARTESIAN_POINT ( 'NONE',  ( 30.58324630866340854, -112.0331114996531454, -45.56259622822469879 ) ) ;
#26850=CARTESIAN_POINT ( 'NONE',  ( 16.05277956358233027, 87.96830019103632026, 113.1291064380262270 ) ) ;
#26851=EDGE_LOOP ( 'NONE', ( #19159, #14599, #8761, #5090 ) ) ;
#26852=CARTESIAN_POINT ( 'NONE',  ( 109.1586900883932856, -0.005715190711481754789, 0.004277182003227202392 ) ) ;
#26853=ORIENTED_EDGE ( 'NONE', *, *, #25079, .F. ) ;
#26854=CARTESIAN_POINT ( 'NONE',  ( 26.11404676487257603, -112.7148551500681037, 10.71016160607530310 ) ) ;
#26855=CARTESIAN_POINT ( 'NONE',  ( 24.01988960052061373, 9.440825210283430025, 130.7041393974934635 ) ) ;
#26856=ORIENTED_EDGE ( 'NONE', *, *, #22231, .F. ) ;
#26857=CARTESIAN_POINT ( 'NONE',  ( 13.36082413113063083, -150.7747251079860291, -25.56125765253606730 ) ) ;
#26860=B_SPLINE_CURVE_WITH_KNOTS ( 'NONE', 3,
 ( #6609, #6464, #21860, #17385, #10647, #21719, #2256 ),
 .UNSPECIFIED., .F., .F.,
 ( 4, 3, 4 ),
 ( 2.619375006920453907E-17, 0.02816610861753245793, 0.04000277880656212537 ),
 .UNSPECIFIED. ) ;
#26862=ADVANCED_FACE ( 'NONE', ( #18634 ), #27215, .F. ) ;
#26864=CARTESIAN_POINT ( 'NONE',  ( 25.64681081121880624, 103.3177883989785499, -45.54494737132120008 ) ) ;
#26866=ADVANCED_FACE ( 'NONE', ( #27107 ), #24291, .F. ) ;
#26867=CARTESIAN_POINT ( 'NONE',  ( 25.64704443564076541, -35.01840413910206706, 107.3436266109712420 ) ) ;
#26868=CARTESIAN_POINT ( 'NONE',  ( 24.01988960052062794, -130.9749633972836591, -4.273195451970020819 ) ) ;
#26870=LINE ( 'NONE', #15934, #8345 ) ;
#26871=EDGE_CURVE ( 'NONE', #4178, #27450, #27945, .T. ) ;
#26872=ORIENTED_EDGE ( 'NONE', *, *, #16880, .T. ) ;
#26873=CARTESIAN_POINT ( 'NONE',  ( 16.75465622695642764, -62.05388459345985552, 127.9746229614485458 ) ) ;
#26878=ORIENTED_EDGE ( 'NONE', *, *, #8812, .F. ) ;
#26879=LINE ( 'NONE', #20255, #17509 ) ;
#26880=FACE_OUTER_BOUND ( 'NONE', #6349, .T. ) ;
#26882=CARTESIAN_POINT ( 'NONE',  ( 28.37644542392848734, 42.25924161794038270, -116.9383271603240360 ) ) ;
#26886=VERTEX_POINT ( 'NONE', #8269 ) ;
#26887=CARTESIAN_POINT ( 'NONE',  ( 16.75465622695658041, -133.7599617830022964, -48.33695624543456404 ) ) ;
#26888=CARTESIAN_POINT ( 'NONE',  ( 2.433796855181205476, -98.43889364293931976, 107.1581411821782268 ) ) ;
#26889=CARTESIAN_POINT ( 'NONE',  ( 1.832998868059858122, 145.1092030902949830, -0.5339089137753102454 ) ) ;
#26891=CARTESIAN_POINT ( 'NONE',  ( 9.884929003653608603, 91.84919534722101275, -119.2676479132364733 ) ) ;
#26892=ORIENTED_EDGE ( 'NONE', *, *, #26924, .F. ) ;
#26893=CARTESIAN_POINT ( 'NONE',  ( 55.79472521941426777, -72.27573336313946584, -8.328398066092509211 ) ) ;
#26896=CARTESIAN_POINT ( 'NONE',  ( 1.833485406944043827, -108.1939177044932592, 96.69979900902130510 ) ) ;
#26897=ORIENTED_EDGE ( 'NONE', *, *, #28325, .T. ) ;
#26898=ORIENTED_EDGE ( 'NONE', *, *, #6361, .F. ) ;
#26899=EDGE_CURVE ( 'NONE', #22237, #7969, #17281, .T. ) ;
#26900=ORIENTED_EDGE ( 'NONE', *, *, #648, .F. ) ;
#26901=EDGE_CURVE ( 'NONE', #5673, #6096, #12844, .T. ) ;
#26902=FACE_OUTER_BOUND ( 'NONE', #4243, .T. ) ;
#26903=CARTESIAN_POINT ( 'NONE',  ( 109.1589550718175161, -0.007008495014555500037, -0.002874971999837398241 ) ) ;
#26904=CARTESIAN_POINT ( 'NONE',  ( 1.832998868059858122, -108.1944082009150776, -96.70023740551231128 ) ) ;
#26906=ORIENTED_EDGE ( 'NONE', *, *, #17863, .T. ) ;
#26907=CARTESIAN_POINT ( 'NONE',  ( 2.263178607246673746, 13.80342482180279262, -144.7392885066941517 ) ) ;
#26908=CARTESIAN_POINT ( 'NONE',  ( 25.64681081121879203, 45.54494737132363724, -103.3177883989774841 ) ) ;
#26909=CARTESIAN_POINT ( 'NONE',  ( 10.93730112725932635, 0.000000000000000000, 0.000000000000000000 ) ) ;
#26910=EDGE_LOOP ( 'NONE', ( #9067, #18626, #5887, #3791 ) ) ;
#26911=EDGE_LOOP ( 'NONE', ( #17889, #5345, #19660, #4259 ) ) ;
#26914=CARTESIAN_POINT ( 'NONE',  ( 2.263178113027050298, -145.3892419963350733, -1.401567040889715621 ) ) ;
#26915=CARTESIAN_POINT ( 'NONE',  ( 13.84597867724980880, 25.80666409311568188, 144.4146018799363560 ) ) ;
#26916=LINE ( 'NONE', #24500, #26234 ) ;
#26917=DIRECTION ( 'NONE',  ( -1.000000000000000000, -0.000000000000000000, -0.000000000000000000 ) ) ;
#26922=CARTESIAN_POINT ( 'NONE',  ( 25.81918753295380142, -107.7789657594972255, -34.03777907512026246 ) ) ;
#26924=EDGE_CURVE ( 'NONE', #10427, #13097, #6122, .T. ) ;
#26925=EDGE_LOOP ( 'NONE', ( #21887, #25187, #15414, #21343 ) ) ;
#26929=EDGE_CURVE ( 'NONE', #8439, #23751, #17032, .T. ) ;
#26930=ORIENTED_EDGE ( 'NONE', *, *, #16250, .T. ) ;
#26931=FACE_OUTER_BOUND ( 'NONE', #2702, .T. ) ;
#26936=UNCERTAINTY_MEASURE_WITH_UNIT (LENGTH_MEASURE( 1.000000000000000082E-05 ), #22572, 'distance_accuracy_value', 'NONE');
#26938=CARTESIAN_POINT ( 'NONE',  ( 32.73300124599739291, -108.9684813982485707, -44.31599526638064646 ) ) ;
#26939=CARTESIAN_POINT ( 'NONE',  ( 25.98552792386799837, -74.89816102339773352, 84.79516057869859935 ) ) ;
#26940=LINE ( 'NONE', #26071, #5147 ) ;
#26941=B_SPLINE_CURVE_WITH_KNOTS ( 'NONE', 3,
 ( #11516, #20293, #24072, #4758, #13529, #4900 ),
 .UNSPECIFIED., .F., .F.,
 ( 4, 2, 4 ),
 ( 2.168404344971008868E-18, 0.0006311636237756730562, 0.001262327247551343727 ),
 .UNSPECIFIED. ) ;
#26942=CARTESIAN_POINT ( 'NONE',  ( 2.108985857320901935, 60.26444811757399833, 132.2056553747747785 ) ) ;
#26944=CARTESIAN_POINT ( 'NONE',  ( 8.186469829613955085, 145.3272524103320222, 34.43598812953141675 ) ) ;
#26949=CARTESIAN_POINT ( 'NONE',  ( 25.64670758986457955, -22.98827151089207632, -110.5460908981864776 ) ) ;
#26952=VERTEX_POINT ( 'NONE', #8138 ) ;
#26953=CARTESIAN_POINT ( 'NONE',  ( 1.833750490713697223, -14.90257883162655084, -144.3424379351781681 ) ) ;
#26956=CARTESIAN_POINT ( 'NONE',  ( 1.833206310202330602, -84.68961945193537133, 117.8322271314361558 ) ) ;
#26957=CARTESIAN_POINT ( 'NONE',  ( 25.64681081121879203, -12.21581276189883170, 112.2483031020013016 ) ) ;
#26958=VERTEX_POINT ( 'NONE', #12710 ) ;
#26959=EDGE_CURVE ( 'NONE', #22124, #16228, #13517, .T. ) ;
#26960=ORIENTED_EDGE ( 'NONE', *, *, #26036, .T. ) ;
#26961=ORIENTED_EDGE ( 'NONE', *, *, #10630, .T. ) ;
#26962=ADVANCED_FACE ( 'NONE', ( #14875 ), #1660, .F. ) ;
#26963=ORIENTED_EDGE ( 'NONE', *, *, #24011, .T. ) ;
#26967=CARTESIAN_POINT ( 'NONE',  ( 109.1586059443104944, 0.006637156007970154009, -0.002447596125914190766 ) ) ;
#26968=CARTESIAN_POINT ( 'NONE',  ( 28.37644542392835234, 102.9230687709019634, -69.76573497038990013 ) ) ;
#26970=B_SPLINE_CURVE_WITH_KNOTS ( 'NONE', 3,
 ( #52, #13858, #11417, #15728 ),
 .UNSPECIFIED., .F., .F.,
 ( 4, 4 ),
 ( 3.405187508996590202E-16, 0.01077107486149765994 ),
 .UNSPECIFIED. ) ;
#26974=ORIENTED_EDGE ( 'NONE', *, *, #18448, .T. ) ;
#26975=CARTESIAN_POINT ( 'NONE',  ( 32.73300124599734318, 16.10546300444822165, 116.5274707358856290 ) ) ;
#26976=CARTESIAN_POINT ( 'NONE',  ( 25.64692232868534560, 66.10288322707316411, -91.53874134430731146 ) ) ;
#26977=CARTESIAN_POINT ( 'NONE',  ( 25.64670758986457955, 56.88615781331626664, -97.53391148296614688 ) ) ;
#26978=CARTESIAN_POINT ( 'NONE',  ( 2.108985857320881507, 1.281428372375777114, 145.2876352664463013 ) ) ;
#26981=LINE ( 'NONE', #22849, #6090 ) ;
#26982=CARTESIAN_POINT ( 'NONE',  ( 25.86096068574578055, 110.7864907291861130, -22.52859312382080503 ) ) ;
#26983=LINE ( 'NONE', #20379, #11171 ) ;
#26989=B_SPLINE_CURVE_WITH_KNOTS ( 'NONE', 3,
 ( #16601, #9993, #14277, #5368 ),
 .UNSPECIFIED., .F., .F.,
 ( 4, 4 ),
 ( 0.000000000000000000, 0.008383560773332717278 ),
 .UNSPECIFIED. ) ;
#26990=B_SPLINE_CURVE_WITH_KNOTS ( 'NONE', 3,
 ( #28014, #1957, #19379, #8182, #8314, #28154, #8457 ),
 .UNSPECIFIED., .F., .F.,
 ( 4, 3, 4 ),
 ( 7.341549781884751001E-16, 0.02816610861753246139, 0.04000277880656284007 ),
 .UNSPECIFIED. ) ;
#26991=FACE_OUTER_BOUND ( 'NONE', #24643, .T. ) ;
#26992=EDGE_CURVE ( 'NONE', #6704, #14115, #10309, .T. ) ;
#26993=CARTESIAN_POINT ( 'NONE',  ( 19.66333377628711077, 9.924285918886457836, 137.3914191246404357 ) ) ;
#26995=VERTEX_POINT ( 'NONE', #1636 ) ;
#26996=CARTESIAN_POINT ( 'NONE',  ( 5.340103579038215642, -71.72120379026111436, 128.8311297206839470 ) ) ;
#26999=CARTESIAN_POINT ( 'NONE',  ( 16.05277956358197144, -109.5668455727254695, -92.36732600443316699 ) ) ;
#27000=CARTESIAN_POINT ( 'NONE',  ( 25.64692232868533139, 107.2834780834840274, -35.20209749635197483 ) ) ;
#27001=CARTESIAN_POINT ( 'NONE',  ( 25.81918753295377655, -113.0221398901143033, 0.9336804662323209270 ) ) ;
#27002=EDGE_LOOP ( 'NONE', ( #10572, #19244, #26474, #9856 ) ) ;
#27003=CARTESIAN_POINT ( 'NONE',  ( 25.64707127832796019, 0.04959866882966159490, 112.9112343549835487 ) ) ;
#27006=ORIENTED_EDGE ( 'NONE', *, *, #11400, .T. ) ;
#27007=ORIENTED_EDGE ( 'NONE', *, *, #28290, .F. ) ;
#27008=VERTEX_POINT ( 'NONE', #10435 ) ;
#27009=CARTESIAN_POINT ( 'NONE',  ( 25.70243777736192570, -90.94412140945908618, -66.98101477609100129 ) ) ;
#27013=CARTESIAN_POINT ( 'NONE',  ( 25.64708228042119131, -83.93578330383134301, 75.52311986517997866 ) ) ;
#27014=CARTESIAN_POINT ( 'NONE',  ( 25.64703792032472762, 45.78915563622703644, -103.2099561461819661 ) ) ;
#27019=CARTESIAN_POINT ( 'NONE',  ( 1.833721034905635872, -145.1093571238132540, 0.3559403234832136942 ) ) ;
#27021=CARTESIAN_POINT ( 'NONE',  ( 1.834118845439484335, -72.40084790867418008, 125.7578880615042749 ) ) ;
#27022=CARTESIAN_POINT ( 'NONE',  ( 8.186469829614386740, -27.65107825763847416, -146.7694295239428186 ) ) ;
#27023=EDGE_CURVE ( 'NONE', #25151, #26744, #23839, .T. ) ;
#27025=DIRECTION ( 'NONE',  ( 0.5914120900931444380, 0.8010740644654229525, 0.09226095020378749512 ) ) ;
#27030=ADVANCED_FACE ( 'NONE', ( #28381 ), #25563, .F. ) ;
#27031=ORIENTED_EDGE ( 'NONE', *, *, #5803, .F. ) ;
#27034=CARTESIAN_POINT ( 'NONE',  ( 109.1778270068192853, -0.0006237116683870695330, 0.009293669915260193218 ) ) ;
#27035=CARTESIAN_POINT ( 'NONE',  ( 10.93730112725932635, 0.000000000000000000, 0.000000000000000000 ) ) ;
#27036=CARTESIAN_POINT ( 'NONE',  ( 13.84597867724968268, -82.31427113894703496, -121.4327876424623440 ) ) ;
#27037=CARTESIAN_POINT ( 'NONE',  ( 26.11404676487259024, 97.48350837663691948, -57.58742681967348176 ) ) ;
#27038=ORIENTED_EDGE ( 'NONE', *, *, #3216, .F. ) ;
#27040=CARTESIAN_POINT ( 'NONE',  ( 25.69398547355839213, 45.25878216557570966, -103.4778695380284148 ) ) ;
#27049=CARTESIAN_POINT ( 'NONE',  ( 109.1587776205901861, 0.006729130500864210183, 0.002904816147411993371 ) ) ;
#27050=( BOUNDED_SURFACE ( )  B_SPLINE_SURFACE ( 3, 1, ( 
 ( #27236, #25102 ),
 ( #5367, #10418 ),
 ( #3924, #6367 ),
 ( #8396, #15118 ) ),
 .UNSPECIFIED., .F., .F., .F. ) 
 B_SPLINE_SURFACE_WITH_KNOTS ( ( 4, 4 ),
 ( 2, 2 ),
 ( 0.000000000000000000, 1.000000000000000000 ),
 ( 0.000000000000000000, 1.000000000000000000 ),
 .UNSPECIFIED. ) 
 GEOMETRIC_REPRESENTATION_ITEM ( )  RATIONAL_B_SPLINE_SURFACE ( (
 ( 1.000000000000000000, 1.000000000000000000),
 ( 0.6386103224230316178, 0.9954351624131538845),
 ( 0.6386103224230316178, 0.9954351624131538845),
 ( 1.000000000000000000, 1.000000000000000000) ) ) 
 REPRESENTATION_ITEM ( '' )  SURFACE ( )  );
#27051=ADVANCED_FACE ( 'NONE', ( #17443 ), #2393, .T. ) ;
#27052=CARTESIAN_POINT ( 'NONE',  ( 2.433796855181219243, -125.2830755159749003, -74.00833731765692391 ) ) ;
#27053=CARTESIAN_POINT ( 'NONE',  ( 109.1721716018069515, -0.01673651515802106193, 0.003350975118860912826 ) ) ;
#27055=CARTESIAN_POINT ( 'NONE',  ( 10.93730112725999248, 42.00474393596446987, -145.2260730187398110 ) ) ;
#27056=CARTESIAN_POINT ( 'NONE',  ( 2.263178113027036531, 16.59120315151768921, -144.4462808674008443 ) ) ;
#27057=B_SPLINE_CURVE_WITH_KNOTS ( 'NONE', 3,
 ( #19575, #28340, #26193, #6489, #3609, #12387 ),
 .UNSPECIFIED., .F., .F.,
 ( 4, 2, 4 ),
 ( 2.084489702152424451E-17, 0.0006311571484585999344, 0.001262314296917178835 ),
 .UNSPECIFIED. ) ;
#27060=CARTESIAN_POINT ( 'NONE',  ( 28.37603512858443366, -45.02094145483448528, 105.5302493666425505 ) ) ;
#27063=EDGE_LOOP ( 'NONE', ( #18148, #2640, #17812, #10540 ) ) ;
#27065=CARTESIAN_POINT ( 'NONE',  ( 1.833750490713715209, 145.1094586213657749, 0.2669522761650450771 ) ) ;
#27066=ORIENTED_EDGE ( 'NONE', *, *, #4748, .F. ) ;
#27070=CARTESIAN_POINT ( 'NONE',  ( 2.433796855181233454, 31.67151202412969724, 142.0211193075556935 ) ) ;
#27072=CARTESIAN_POINT ( 'NONE',  ( 1.894214914920967274, -126.1778046718831376, -71.74757687370589565 ) ) ;
#27074=CARTESIAN_POINT ( 'NONE',  ( 26.11404676487257603, -74.91683232331033082, 84.89295829319468112 ) ) ;
#27075=DIRECTION ( 'NONE',  ( -0.5914120900931443270, 0.3962188444547338761, -0.7023121577978085339 ) ) ;
#27076=CARTESIAN_POINT ( 'NONE',  ( 13.36082413113061307, 9.660980093454693218, 152.6206443696329131 ) ) ;
#27081=CARTESIAN_POINT ( 'NONE',  ( 10.93730112725990367, -133.3192575531795399, -71.28103789255078482 ) ) ;
#27082=( BOUNDED_SURFACE ( )  B_SPLINE_SURFACE ( 3, 1, ( 
 ( #28414, #8714 ),
 ( #26268, #21390 ),
 ( #19784, #6566 ),
 ( #8443, #19640 ) ),
 .UNSPECIFIED., .F., .F., .F. ) 
 B_SPLINE_SURFACE_WITH_KNOTS ( ( 4, 4 ),
 ( 2, 2 ),
 ( 0.000000000000000000, 1.000000000000000000 ),
 ( 0.000000000000000000, 1.000000000000000000 ),
 .UNSPECIFIED. ) 
 GEOMETRIC_REPRESENTATION_ITEM ( )  RATIONAL_B_SPLINE_SURFACE ( (
 ( 1.000000000000000000, 1.000000000000000000),
 ( 0.6386103224230302855, 0.9954351624131538845),
 ( 0.6386103224230302855, 0.9954351624131538845),
 ( 1.000000000000000000, 1.000000000000000000) ) ) 
 REPRESENTATION_ITEM ( '' )  SURFACE ( )  );
#27084=CARTESIAN_POINT ( 'NONE',  ( 109.1624594426973260, 0.01570508117119674002, -0.002863932759303885849 ) ) ;
#27085=EDGE_CURVE ( 'NONE', #11589, #12174, #1145, .T. ) ;
#27086=CARTESIAN_POINT ( 'NONE',  ( 25.87036335909426654, 76.38467849957150690, 83.35447252092892256 ) ) ;
#27089=CARTESIAN_POINT ( 'NONE',  ( 25.64703792032472052, 83.80974623566390846, -75.66285916808213585 ) ) ;
#27090=VERTEX_POINT ( 'NONE', #22658 ) ;
#27092=VERTEX_POINT ( 'NONE', #3738 ) ;
#27093=CARTESIAN_POINT ( 'NONE',  ( 109.1589550718175161, -0.006669585340474292433, -0.003591809816099503141 ) ) ;
#27094=DIRECTION ( 'NONE',  ( -0.5914120900931443270, -0.3352908775637108985, -0.7333565075147389090 ) ) ;
#27095=B_SPLINE_CURVE_WITH_KNOTS ( 'NONE', 3,
 ( #13528, #19002, #5913, #10087, #25498, #8204, #16706, #10240, #23198, #23336 ),
 .UNSPECIFIED., .F., .F.,
 ( 4, 3, 3, 4 ),
 ( 3.469446951953614189E-17, 0.0002669559177086070585, 0.0005339118354150947186, 0.001067817517169157744 ),
 .UNSPECIFIED. ) ;
#27097=ORIENTED_EDGE ( 'NONE', *, *, #2391, .T. ) ;
#27099=VERTEX_POINT ( 'NONE', #11842 ) ;
#27100=CARTESIAN_POINT ( 'NONE',  ( 109.1589550718175161, 0.0002241941239325955654, 0.007571935245608775629 ) ) ;
#27101=LINE ( 'NONE', #22826, #9697 ) ;
#27102=B_SPLINE_CURVE_WITH_KNOTS ( 'NONE', 3,
 ( #175, #7098, #6664, #4920, #20, #26362 ),
 .UNSPECIFIED., .F., .F.,
 ( 4, 2, 4 ),
 ( 4.336808689942017736E-18, 0.0006311636237756799951, 0.001262327247551355003 ),
 .UNSPECIFIED. ) ;
#27104=CARTESIAN_POINT ( 'NONE',  ( 1.833838848569428581, 144.2962335061013448, -15.34509722932385145 ) ) ;
#27107=FACE_OUTER_BOUND ( 'NONE', #10080, .T. ) ;
#27108=MECHANICAL_DESIGN_GEOMETRIC_PRESENTATION_REPRESENTATION('',(#10212),#72);
#27109=CARTESIAN_POINT ( 'NONE',  ( 1.833838848569439683, -72.70900949568685689, -125.5797553397076882 ) ) ;
#27111=CARTESIAN_POINT ( 'NONE',  ( 109.1778270068192853, 0.009293669915253098199, -0.0006237116683806388047 ) ) ;
#27112=AXIS2_PLACEMENT_3D ( 'NONE', #15203, #24023, #2106 ) ;
#27113=B_SPLINE_CURVE_WITH_KNOTS ( 'NONE', 3,
 ( #14637, #3849, #12614, #15327, #28424, #17494, #19792, #10608, #6296, #28151 ),
 .UNSPECIFIED., .F., .F.,
 ( 4, 3, 3, 4 ),
 ( 1.387778780781445676E-17, 0.0002669560319015652078, 0.0005492286108966281180, 0.0008315040496093381757 ),
 .UNSPECIFIED. ) ;
#27114=CARTESIAN_POINT ( 'NONE',  ( 1.832998868059890096, 59.50898020732510929, 132.3466930259795618 ) ) ;
#27115=CARTESIAN_POINT ( 'NONE',  ( 109.1586900883932856, 0.007002774699553659596, -0.001385221016536874366 ) ) ;
#27116=CARTESIAN_POINT ( 'NONE',  ( 19.66333377628701484, -95.46107873288957535, 99.30798531455323541 ) ) ;
#27117=EDGE_CURVE ( 'NONE', #8996, #4319, #3590, .T. ) ;
#27119=VERTEX_POINT ( 'NONE', #24814 ) ;
#27124=CARTESIAN_POINT ( 'NONE',  ( 19.66333377628716406, 33.01772659807287624, -133.7337774474995058 ) ) ;
#27125=DIRECTION ( 'NONE',  ( -0.000000000000000000, -0.000000000000000000, 1.000000000000000000 ) ) ;
#27130=CARTESIAN_POINT ( 'NONE',  ( 109.1586900883932856, 0.006757191295056129768, -0.002301750759607921679 ) ) ;
#27132=ORIENTED_EDGE ( 'NONE', *, *, #17764, .T. ) ;
#27133=CARTESIAN_POINT ( 'NONE',  ( 109.1721716018069657, -0.005466227998629111413, -0.01616973485710948913 ) ) ;
#27137=VECTOR ( 'NONE', #11241, 1000.000000000000227 ) ;
#27142=CIRCLE ( 'NONE', #15169, 20.00000000000000000 ) ;
#27147=EDGE_CURVE ( 'NONE', #10856, #11536, #21283, .T. ) ;
#27148=CARTESIAN_POINT ( 'NONE',  ( 109.1586059443104944, -0.005438258427225644252, 0.004524147648833148731 ) ) ;
#27151=EDGE_CURVE ( 'NONE', #17620, #2385, #6647, .T. ) ;
#27152=ORIENTED_EDGE ( 'NONE', *, *, #25998, .F. ) ;
#27153=CARTESIAN_POINT ( 'NONE',  ( 13.84597867724965070, -64.00674338125939755, 132.0026437215599344 ) ) ;
#27155=CARTESIAN_POINT ( 'NONE',  ( 109.1586059443104944, -0.007001002073869792321, 0.001014167950289951176 ) ) ;
#27156=VERTEX_POINT ( 'NONE', #12507 ) ;
#27157=EDGE_CURVE ( 'NONE', #27476, #22024, #23490, .T. ) ;
#27159=VERTEX_POINT ( 'NONE', #3067 ) ;
#27162=CARTESIAN_POINT ( 'NONE',  ( 1.833485406944043827, 108.1939177044938560, -96.69979900902059455 ) ) ;
#27163=CARTESIAN_POINT ( 'NONE',  ( 1.831572820252008738, -141.7320553118904058, -31.13525033585638369 ) ) ;
#27167=CARTESIAN_POINT ( 'NONE',  ( 2.433796855181233454, 96.28145139437833677, -109.1007109081216129 ) ) ;
#27168=DIRECTION ( 'NONE',  ( -1.000000000000000000, -0.000000000000000000, -0.000000000000000000 ) ) ;
#27169=ORIENTED_EDGE ( 'NONE', *, *, #17569, .T. ) ;
#27170=CARTESIAN_POINT ( 'NONE',  ( 1.831572820252009626, -142.1425225354578004, -29.20415387690713516 ) ) ;
#27174=CARTESIAN_POINT ( 'NONE',  ( 109.1589550718175161, 0.0005685167901217448626, -0.007553890059316987690 ) ) ;
#27176=ORIENTED_EDGE ( 'NONE', *, *, #25667, .T. ) ;
#27177=CARTESIAN_POINT ( 'NONE',  ( 109.1586900883932856, 0.007088091345229654248, -0.0008465529156635364033 ) ) ;
#27180=ORIENTED_EDGE ( 'NONE', *, *, #2766, .T. ) ;
#27181=CONICAL_SURFACE ( 'NONE', #18920, 117.6351876552689504, 0.9945805576725580410 ) ;
#27182=CARTESIAN_POINT ( 'NONE',  ( 109.1778270068192853, 0.001322180554001401668, 0.009220257877180830508 ) ) ;
#27183=CARTESIAN_POINT ( 'NONE',  ( 25.64708228042119131, -23.43704872438680553, -110.4520805602538047 ) ) ;
#27184=CARTESIAN_POINT ( 'NONE',  ( 109.1592201516379674, -0.005027640251767255368, -0.006044422199822518590 ) ) ;
#27185=VECTOR ( 'NONE', #12487, 1000.000000000000000 ) ;
#27186=CARTESIAN_POINT ( 'NONE',  ( 1.894214914920957948, 58.16536411968120746, -132.9862534094750686 ) ) ;
#27190=EDGE_CURVE ( 'NONE', #4782, #16046, #28240, .T. ) ;
#27191=CARTESIAN_POINT ( 'NONE',  ( 2.430230287190589422, -16.65331920325641235, -144.5585181921887568 ) ) ;
#27192=CARTESIAN_POINT ( 'NONE',  ( 109.1592201516379674, 0.004368284148529012062, 0.006536841731953418715 ) ) ;
#27195=ORIENTED_EDGE ( 'NONE', *, *, #27395, .T. ) ;
#27198=FACE_OUTER_BOUND ( 'NONE', #6174, .T. ) ;
#27200=LINE ( 'NONE', #25071, #12428 ) ;
#27202=DIRECTION ( 'NONE',  ( 0.000000000000000000, 1.000000000000000000, 3.122502256758243698E-15 ) ) ;
#27205=CARTESIAN_POINT ( 'NONE',  ( 25.73574536432413140, 84.49061642666573846, -74.99093179013885901 ) ) ;
#27207=VECTOR ( 'NONE', #11742, 1000.000000000000114 ) ;
#27208=CARTESIAN_POINT ( 'NONE',  ( 25.64704443564077252, -107.4261196778965228, 34.76451658509497378 ) ) ;
#27209=AXIS2_PLACEMENT_3D ( 'NONE', #7114, #17738, #4795 ) ;
#27210=ORIENTED_EDGE ( 'NONE', *, *, #11966, .F. ) ;
#27211=CARTESIAN_POINT ( 'NONE',  ( 25.64704443564079739, -75.65149037849816693, 83.82001435192599104 ) ) ;
#27212=ORIENTED_EDGE ( 'NONE', *, *, #9371, .F. ) ;
#27213=ORIENTED_EDGE ( 'NONE', *, *, #5493, .T. ) ;
#27215=( BOUNDED_SURFACE ( )  B_SPLINE_SURFACE ( 3, 1, ( 
 ( #7858, #16036 ),
 ( #5101, #20500 ),
 ( #788, #25265 ),
 ( #12161, #20928 ) ),
 .UNSPECIFIED., .F., .F., .F. ) 
 B_SPLINE_SURFACE_WITH_KNOTS ( ( 4, 4 ),
 ( 2, 2 ),
 ( 0.000000000000000000, 1.000000000000000000 ),
 ( 0.000000000000000000, 1.000000000000000000 ),
 .UNSPECIFIED. ) 
 GEOMETRIC_REPRESENTATION_ITEM ( )  RATIONAL_B_SPLINE_SURFACE ( (
 ( 1.000000000000000000, 1.000000000000000000),
 ( 0.6386103224230316178, 0.9954351624131538845),
 ( 0.6386103224230316178, 0.9954351624131538845),
 ( 1.000000000000000000, 1.000000000000000000) ) ) 
 REPRESENTATION_ITEM ( '' )  SURFACE ( )  );
#27216=CARTESIAN_POINT ( 'NONE',  ( 109.1587776205901577, -0.007186028091163443668, 0.001442274045003878562 ) ) ;
#27218=B_SPLINE_CURVE_WITH_KNOTS ( 'NONE', 3,
 ( #21102, #3694, #27741, #25160 ),
 .UNSPECIFIED., .F., .F.,
 ( 4, 4 ),
 ( 0.000000000000000000, 0.008383560773332731156 ),
 .UNSPECIFIED. ) ;
#27219=CARTESIAN_POINT ( 'NONE',  ( 109.1721716018069515, 0.01019541462303036154, -0.01368917435590592639 ) ) ;
#27221=B_SPLINE_CURVE_WITH_KNOTS ( 'NONE', 3,
 ( #4577, #4727, #22147, #13347, #13927, #26732 ),
 .UNSPECIFIED., .F., .F.,
 ( 4, 2, 4 ),
 ( 1.084202172485504434E-17, 0.0006311636237756648162, 0.001262327247551318574 ),
 .UNSPECIFIED. ) ;
#27223=CONICAL_SURFACE ( 'NONE', #27714, 151.1787379149930359, 0.5880026024245678107 ) ;
#27224=( BOUNDED_SURFACE ( )  B_SPLINE_SURFACE ( 3, 1, ( 
 ( #5167, #16103 ),
 ( #27473, #7785 ),
 ( #25186, #27327 ),
 ( #20709, #15963 ) ),
 .UNSPECIFIED., .F., .F., .F. ) 
 B_SPLINE_SURFACE_WITH_KNOTS ( ( 4, 4 ),
 ( 2, 2 ),
 ( 0.000000000000000000, 1.000000000000000000 ),
 ( 0.000000000000000000, 1.000000000000000000 ),
 .UNSPECIFIED. ) 
 GEOMETRIC_REPRESENTATION_ITEM ( )  RATIONAL_B_SPLINE_SURFACE ( (
 ( 1.000000000000000000, 1.000000000000000000),
 ( 0.9956975270656955868, 0.8568959468854907557),
 ( 0.9956975270656955868, 0.8568959468854907557),
 ( 1.000000000000000000, 1.000000000000000000) ) ) 
 REPRESENTATION_ITEM ( '' )  SURFACE ( )  );
#27225=VECTOR ( 'NONE', #19552, 1000.000000000000114 ) ;
#27226=CARTESIAN_POINT ( 'NONE',  ( 10.93730112725932635, 0.000000000000000000, 0.000000000000000000 ) ) ;
#27229=CARTESIAN_POINT ( 'NONE',  ( 109.1587776205901577, -0.007328861771496576576, -8.330235397652469671E-05 ) ) ;
#27230=CARTESIAN_POINT ( 'NONE',  ( 25.64681081121879203, 45.54494737132363724, -103.3177883989774841 ) ) ;
#27231=CARTESIAN_POINT ( 'NONE',  ( 26.11404676487259024, -24.64483677384768967, -110.5078194225163912 ) ) ;
#27235=CARTESIAN_POINT ( 'NONE',  ( 25.69398547355840279, -83.43419615433049330, 76.12333255527484255 ) ) ;
#27236=CARTESIAN_POINT ( 'NONE',  ( 109.1778270068192853, -0.005186985107080890889, -0.007736698406806078593 ) ) ;
#27237=FACE_OUTER_BOUND ( 'NONE', #14971, .T. ) ;
#27238=CARTESIAN_POINT ( 'NONE',  ( 32.73300124599738581, -28.19767303745521758, -114.2056417606550696 ) ) ;
#27241=ORIENTED_EDGE ( 'NONE', *, *, #28290, .T. ) ;
#27242=CARTESIAN_POINT ( 'NONE',  ( 2.063896406836609909, 141.8093313989364788, -31.51663808384418530 ) ) ;
#27243=CARTESIAN_POINT ( 'NONE',  ( 9.884929003653608603, -65.04493172071570939, 135.7578851563883973 ) ) ;
#27246=B_SPLINE_CURVE_WITH_KNOTS ( 'NONE', 3,
 ( #27709, #12853, #19075, #21228, #7872, #1506 ),
 .UNSPECIFIED., .F., .F.,
 ( 4, 2, 4 ),
 ( 7.806255641895631925E-18, 0.0006311636237756803203, 0.001262327247551352834 ),
 .UNSPECIFIED. ) ;
#27248=ORIENTED_EDGE ( 'NONE', *, *, #26603, .T. ) ;
#27250=ORIENTED_EDGE ( 'NONE', *, *, #23793, .T. ) ;
#27252=EDGE_CURVE ( 'NONE', #22237, #24705, #23609, .T. ) ;
#27253=LINE ( 'NONE', #103, #25795 ) ;
#27254=ADVANCED_FACE ( 'NONE', ( #2117 ), #22450, .F. ) ;
#27255=CARTESIAN_POINT ( 'NONE',  ( 109.1592201516379674, -0.003476928926134757649, -0.007051465909552751508 ) ) ;
#27258=( BOUNDED_SURFACE ( )  B_SPLINE_SURFACE ( 3, 1, ( 
 ( #26489, #13535 ),
 ( #15402, #10829 ),
 ( #19455, #8525 ),
 ( #19591, #6505 ) ),
 .UNSPECIFIED., .F., .F., .F. ) 
 B_SPLINE_SURFACE_WITH_KNOTS ( ( 4, 4 ),
 ( 2, 2 ),
 ( 0.000000000000000000, 1.000000000000000000 ),
 ( 0.000000000000000000, 1.000000000000000000 ),
 .UNSPECIFIED. ) 
 GEOMETRIC_REPRESENTATION_ITEM ( )  RATIONAL_B_SPLINE_SURFACE ( (
 ( 1.000000000000000000, 1.000000000000000000),
 ( 0.6386103224230302855, 0.9954351624131538845),
 ( 0.6386103224230302855, 0.9954351624131538845),
 ( 1.000000000000000000, 1.000000000000000000) ) ) 
 REPRESENTATION_ITEM ( '' )  SURFACE ( )  );
#27260=CARTESIAN_POINT ( 'NONE',  ( 1.894214914920982151, 71.74757687370632198, -126.1778046718828534 ) ) ;
#27261=CARTESIAN_POINT ( 'NONE',  ( 1.831572820252008738, 86.09108691067926600, -116.8148281295960516 ) ) ;
#27262=CARTESIAN_POINT ( 'NONE',  ( 109.1589550718175161, 0.005233222325307164934, 0.005477029346534945282 ) ) ;
#27263=AXIS2_PLACEMENT_3D ( 'NONE', #6878, #24598, #15623 ) ;
#27266=DIRECTION ( 'NONE',  ( -0.5914120900931442160, 0.7333565075147400192, -0.3352908775637083449 ) ) ;
#27267=DIRECTION ( 'NONE',  ( -0.7071067811865485719, 0.000000000000000000, -0.7071067811865465735 ) ) ;
#27268=VECTOR ( 'NONE', #3850, 1000.000000000000114 ) ;
#27270=EDGE_LOOP ( 'NONE', ( #885, #26675, #6549, #7885 ) ) ;
#27272=CARTESIAN_POINT ( 'NONE',  ( 2.433796855181205476, 60.50726454508082952, -132.3327394885224919 ) ) ;
#27273=CARTESIAN_POINT ( 'NONE',  ( 25.64700659047693776, -91.48068002582068914, 66.18331466615532577 ) ) ;
#27274=CARTESIAN_POINT ( 'NONE',  ( 5.340103579038172121, -28.39990973304568911, 144.6887562507423297 ) ) ;
#27279=CARTESIAN_POINT ( 'NONE',  ( 1.833485406944057594, -0.5339064996874559599, -145.1085452359073429 ) ) ;
#27280=CARTESIAN_POINT ( 'NONE',  ( 32.73300124599735028, 72.21147546950551543, 92.86301839380053025 ) ) ;
#27283=CARTESIAN_POINT ( 'NONE',  ( 1.894214914920955728, 116.8658096527534411, -86.08679174687961222 ) ) ;
#27285=ORIENTED_EDGE ( 'NONE', *, *, #9436, .T. ) ;
#27287=ADVANCED_FACE ( 'NONE', ( #8757 ), #5897, .F. ) ;
#27288=EDGE_CURVE ( 'NONE', #23571, #24705, #3899, .T. ) ;
#27289=ORIENTED_EDGE ( 'NONE', *, *, #19249, .F. ) ;
#27291=ORIENTED_EDGE ( 'NONE', *, *, #18829, .T. ) ;
#27296=CARTESIAN_POINT ( 'NONE',  ( 119.2224693531408803, 70.00000000000004263, 39.99999999999999289 ) ) ;
#27297=FACE_OUTER_BOUND ( 'NONE', #4188, .T. ) ;
#27300=CARTESIAN_POINT ( 'NONE',  ( 109.1721716018069657, 0.01665253177026229658, -0.003746085893652622081 ) ) ;
#27302=CARTESIAN_POINT ( 'NONE',  ( 109.1586900883932856, -0.007137750914550312215, 0.0001010081143975802818 ) ) ;
#27305=ORIENTED_EDGE ( 'NONE', *, *, #24157, .T. ) ;
#27307=CARTESIAN_POINT ( 'NONE',  ( 109.1586059443104944, 0.006856640434645982184, 0.001740416220250496498 ) ) ;
#27308=CARTESIAN_POINT ( 'NONE',  ( 28.37644542392834524, 98.15613422114097375, 76.32685750075042108 ) ) ;
#27309=CARTESIAN_POINT ( 'NONE',  ( 24.22246935314087324, -69.99999999999998579, 40.00000000000003553 ) ) ;
#27310=CARTESIAN_POINT ( 'NONE',  ( 13.84597867724981946, 55.26821062125554107, 135.8932891738218132 ) ) ;
#27311=CARTESIAN_POINT ( 'NONE',  ( 1.832998868059858122, -125.9352106559978921, -72.09222286251214484 ) ) ;
#27313=( BOUNDED_SURFACE ( )  B_SPLINE_SURFACE ( 3, 1, ( 
 ( #14152, #2803 ),
 ( #22827, #24986 ),
 ( #23115, #1075 ),
 ( #13877, #27404 ) ),
 .UNSPECIFIED., .F., .F., .F. ) 
 B_SPLINE_SURFACE_WITH_KNOTS ( ( 4, 4 ),
 ( 2, 2 ),
 ( 0.000000000000000000, 1.000000000000000000 ),
 ( 0.000000000000000000, 1.000000000000000000 ),
 .UNSPECIFIED. ) 
 GEOMETRIC_REPRESENTATION_ITEM ( )  RATIONAL_B_SPLINE_SURFACE ( (
 ( 1.000000000000000000, 1.000000000000000000),
 ( 0.9956975270656955868, 0.8568959468854907557),
 ( 0.9956975270656955868, 0.8568959468854907557),
 ( 1.000000000000000000, 1.000000000000000000) ) ) 
 REPRESENTATION_ITEM ( '' )  SURFACE ( )  );
#27314=CARTESIAN_POINT ( 'NONE',  ( 10.93730112725936721, 145.2260730187397542, 42.00474393596321931 ) ) ;
#27315=ORIENTED_EDGE ( 'NONE', *, *, #16181, .F. ) ;
#27316=CARTESIAN_POINT ( 'NONE',  ( 109.1778270068192853, 0.002278716897421752870, -0.009031542838317233382 ) ) ;
#27318=CARTESIAN_POINT ( 'NONE',  ( 25.65782528836481902, 110.3293115225706629, 24.04194111108905574 ) ) ;
#27319=CARTESIAN_POINT ( 'NONE',  ( 109.1592201516379674, -0.007566779963318568183, 0.002134489919774338555 ) ) ;
#27322=LINE ( 'NONE', #10771, #1316 ) ;
#27324=CARTESIAN_POINT ( 'NONE',  ( 1.833206310202349698, 29.44113265021129067, -142.0914673790817346 ) ) ;
#27325=EDGE_CURVE ( 'NONE', #21943, #17335, #26860, .T. ) ;
#27326=CARTESIAN_POINT ( 'NONE',  ( 28.37644542392842695, -95.06674036596263022, 80.14194118792678978 ) ) ;
#27327=CARTESIAN_POINT ( 'NONE',  ( 2.063896406836605024, -86.47093297169081438, 116.7302989755734330 ) ) ;
#27330=VERTEX_POINT ( 'NONE', #8909 ) ;
#27332=ADVANCED_FACE ( 'NONE', ( #19551 ), #26465, .F. ) ;
#27335=ADVANCED_FACE ( 'NONE', ( #26583 ), #18392, .F. ) ;
#27337=DIRECTION ( 'NONE',  ( -1.000000000000000000, -0.000000000000000000, -0.000000000000000000 ) ) ;
#27338=CARTESIAN_POINT ( 'NONE',  ( 25.81918753295378721, 97.41320410180168210, -57.31966094783101795 ) ) ;
#27339=ORIENTED_EDGE ( 'NONE', *, *, #8674, .F. ) ;
#27340=CARTESIAN_POINT ( 'NONE',  ( 25.70243777736191149, 66.98101477609128551, -90.94412140945890144 ) ) ;
#27341=CARTESIAN_POINT ( 'NONE',  ( 25.64700659047696973, -103.2418925369176605, 45.71714758798341904 ) ) ;
#27343=CARTESIAN_POINT ( 'NONE',  ( 1.832998868059858122, 72.09222286251258538, -125.9352106559976363 ) ) ;
#27346=CARTESIAN_POINT ( 'NONE',  ( 109.1592201516379674, 0.002913740842103182058, -0.007302213399787563404 ) ) ;
#27348=CARTESIAN_POINT ( 'NONE',  ( 2.108985857320926804, 84.36123201973967412, -118.2933707022550323 ) ) ;
#27349=CARTESIAN_POINT ( 'NONE',  ( -90.83090735639699176, 4.592425496802575156E-15, 37.50000000000001421 ) ) ;
#27350=CARTESIAN_POINT ( 'NONE',  ( 109.1586900883932856, 0.004277182003220951316, -0.005715190711488736183 ) ) ;
#27355=CARTESIAN_POINT ( 'NONE',  ( 109.1592201516379674, 0.007620268632971107306, -0.001934867487021749589 ) ) ;
#27358=CARTESIAN_POINT ( 'NONE',  ( 25.64670758986459731, -75.92149922855251987, 83.57526425215473864 ) ) ;
#27359=CARTESIAN_POINT ( 'NONE',  ( 25.64706233108857347, 0.08898442854020095771, -112.9112020921832453 ) ) ;
#27360=ORIENTED_EDGE ( 'NONE', *, *, #23458, .T. ) ;
#27364=VERTEX_POINT ( 'NONE', #257 ) ;
#27366=B_SPLINE_CURVE_WITH_KNOTS ( 'NONE', 3,
 ( #21199, #10289, #19046, #8122, #7550, #16307, #20577, #3030 ),
 .UNSPECIFIED., .F., .F.,
 ( 4, 2, 2, 4 ),
 ( 1.734723475976807094E-18, 0.0002429588503611230296, 0.0004859177007222443244, 0.0009718354014444825772 ),
 .UNSPECIFIED. ) ;
#27367=B_SPLINE_CURVE_WITH_KNOTS ( 'NONE', 3,
 ( #21074, #20649, #12302, #25004 ),
 .UNSPECIFIED., .F., .F.,
 ( 4, 4 ),
 ( 2.754785121498913159E-16, 0.01077107486149849434 ),
 .UNSPECIFIED. ) ;
#27368=ORIENTED_EDGE ( 'NONE', *, *, #25927, .T. ) ;
#27369=ORIENTED_EDGE ( 'NONE', *, *, #24094, .T. ) ;
#27372=CARTESIAN_POINT ( 'NONE',  ( 10.93730112725932635, 0.000000000000000000, 0.000000000000000000 ) ) ;
#27374=CARTESIAN_POINT ( 'NONE',  ( 109.1624594426973260, 0.01358749486988130618, 0.008380433676406104371 ) ) ;
#27375=CARTESIAN_POINT ( 'NONE',  ( 1.834118845439484335, -107.7186227765447910, -97.22976650547533950 ) ) ;
#27377=CARTESIAN_POINT ( 'NONE',  ( 25.98107933586720009, 107.9289867379274312, -33.92073193606466930 ) ) ;
#27378=FACE_OUTER_BOUND ( 'NONE', #27765, .T. ) ;
#27381=LINE ( 'NONE', #7692, #13411 ) ;
#27384=CARTESIAN_POINT ( 'NONE',  ( 25.64681081121880624, -23.06870491922396837, 110.5293738517607665 ) ) ;
#27385=CARTESIAN_POINT ( 'NONE',  ( 9.884929003653608603, -149.2134106160914939, -19.90991253123399574 ) ) ;
#27386=CARTESIAN_POINT ( 'NONE',  ( 28.37603512858451182, -58.91311972676474795, -98.45183098818044698 ) ) ;
#27387=CARTESIAN_POINT ( 'NONE',  ( 1.894214914920950177, -107.2270864706596711, 97.83100278581372322 ) ) ;
#27388=ORIENTED_EDGE ( 'NONE', *, *, #24439, .F. ) ;
#27392=( BOUNDED_SURFACE ( )  B_SPLINE_SURFACE ( 3, 1, ( 
 ( #4078, #5977 ),
 ( #12848, #12712 ),
 ( #25698, #15138 ),
 ( #23964, #14734 ) ),
 .UNSPECIFIED., .F., .F., .F. ) 
 B_SPLINE_SURFACE_WITH_KNOTS ( ( 4, 4 ),
 ( 2, 2 ),
 ( 0.000000000000000000, 1.000000000000000000 ),
 ( 0.000000000000000000, 1.000000000000000000 ),
 .UNSPECIFIED. ) 
 GEOMETRIC_REPRESENTATION_ITEM ( )  RATIONAL_B_SPLINE_SURFACE ( (
 ( 1.000000000000000000, 1.000000000000000000),
 ( 0.9960225298536222738, 0.9999952330161893110),
 ( 0.9960225298536222738, 0.9999952330161893110),
 ( 1.000000000000000000, 1.000000000000000000) ) ) 
 REPRESENTATION_ITEM ( '' )  SURFACE ( )  );
#27395=EDGE_CURVE ( 'NONE', #6221, #4343, #15170, .T. ) ;
#27396=B_SPLINE_CURVE_WITH_KNOTS ( 'NONE', 3,
 ( #21573, #19415, #8486, #26039 ),
 .UNSPECIFIED., .F., .F.,
 ( 4, 4 ),
 ( 3.207224699059970292E-16, 0.01077107486149834342 ),
 .UNSPECIFIED. ) ;
#27397=EDGE_LOOP ( 'NONE', ( #26760, #27038, #12417, #17612 ) ) ;
#27398=ORIENTED_EDGE ( 'NONE', *, *, #385, .T. ) ;
#27399=EDGE_CURVE ( 'NONE', #17616, #23498, #8039, .T. ) ;
#27400=EDGE_CURVE ( 'NONE', #4630, #23252, #9032, .T. ) ;
#27401=( BOUNDED_SURFACE ( )  B_SPLINE_SURFACE ( 3, 1, ( 
 ( #14930, #23750 ),
 ( #3996, #19394 ),
 ( #17235, #6311 ),
 ( #15059, #23884 ) ),
 .UNSPECIFIED., .F., .F., .F. ) 
 B_SPLINE_SURFACE_WITH_KNOTS ( ( 4, 4 ),
 ( 2, 2 ),
 ( 0.000000000000000000, 1.000000000000000000 ),
 ( 0.000000000000000000, 1.000000000000000000 ),
 .UNSPECIFIED. ) 
 GEOMETRIC_REPRESENTATION_ITEM ( )  RATIONAL_B_SPLINE_SURFACE ( (
 ( 1.000000000000000000, 1.000000000000000000),
 ( 0.9956975270656954757, 0.8568959468854893125),
 ( 0.9956975270656954757, 0.8568959468854893125),
 ( 1.000000000000000000, 1.000000000000000000) ) ) 
 REPRESENTATION_ITEM ( '' )  SURFACE ( )  );
#27402=CARTESIAN_POINT ( 'NONE',  ( 55.49584447822657296, 29.26468316696772831, 66.38758986585125399 ) ) ;
#27404=CARTESIAN_POINT ( 'NONE',  ( 2.430230287190581429, -84.35270093935177727, -118.5711603495689985 ) ) ;
#27409=CARTESIAN_POINT ( 'NONE',  ( 6.224689322667647851, 100.9623537450651725, 108.2965163446077810 ) ) ;
#27411=CARTESIAN_POINT ( 'NONE',  ( 2.430230287190572103, 142.0258656395021717, 31.67257033707552338 ) ) ;
#27412=CARTESIAN_POINT ( 'NONE',  ( 2.263178113027036087, 57.85473702513869654, 133.3897502891096281 ) ) ;
#27417=CARTESIAN_POINT ( 'NONE',  ( 25.73574536432418469, 57.18187897120932206, -97.42965068311163179 ) ) ;
#27421=EDGE_CURVE ( 'NONE', #22385, #8288, #14830, .T. ) ;
#27422=ORIENTED_EDGE ( 'NONE', *, *, #22750, .T. ) ;
#27423=CARTESIAN_POINT ( 'NONE',  ( 25.64704443564079739, 91.42548471394280796, -66.25951665433191806 ) ) ;
#27424=CARTESIAN_POINT ( 'NONE',  ( 25.98552792386801613, -35.98568266743438926, -107.2612904323493410 ) ) ;
#27427=B_SPLINE_CURVE_WITH_KNOTS ( 'NONE', 3,
 ( #16102, #3302, #2873, #20863 ),
 .UNSPECIFIED., .F., .F.,
 ( 4, 4 ),
 ( 6.938893903907228378E-18, 0.008383560773332719013 ),
 .UNSPECIFIED. ) ;
#27428=EDGE_CURVE ( 'NONE', #24861, #9521, #20032, .T. ) ;
#27429=CARTESIAN_POINT ( 'NONE',  ( 109.1589550718175161, 0.007553890059316984221, 0.0005685167901217716424 ) ) ;
#27430=VERTEX_POINT ( 'NONE', #4995 ) ;
#27431=VERTEX_POINT ( 'NONE', #13772 ) ;
#27432=CARTESIAN_POINT ( 'NONE',  ( 1.834118845439484335, -44.67218053242300613, -138.0627591860434507 ) ) ;
#27434=ORIENTED_EDGE ( 'NONE', *, *, #23918, .T. ) ;
#27435=CARTESIAN_POINT ( 'NONE',  ( 25.64681081121879203, 112.3352186517030731, 11.38886654529711961 ) ) ;
#27438=ADVANCED_FACE ( 'NONE', ( #18672 ), #6639, .F. ) ;
#27439=CARTESIAN_POINT ( 'NONE',  ( 30.59141879584323220, 114.2039975081485750, -21.51299111589929325 ) ) ;
#27441=CARTESIAN_POINT ( 'NONE',  ( 26.11404676487257603, -47.08215554553588333, 102.9690087468800073 ) ) ;
#27445=CARTESIAN_POINT ( 'NONE',  ( 2.433796855181219243, 144.5536872373194228, -16.65276281464415575 ) ) ;
#27446=FACE_OUTER_BOUND ( 'NONE', #16463, .T. ) ;
#27449=ORIENTED_EDGE ( 'NONE', *, *, #13566, .T. ) ;
#27450=VERTEX_POINT ( 'NONE', #971 ) ;
#27459=CARTESIAN_POINT ( 'NONE',  ( 30.58324630866342986, -120.8793175557614603, 3.944468862007250110 ) ) ;
#27464=CARTESIAN_POINT ( 'NONE',  ( 109.1587776205901577, -0.006995903587858441977, 0.002185517590245231699 ) ) ;
#27466=CARTESIAN_POINT ( 'NONE',  ( 55.49584447822657296, 68.91748907713588324, 22.67407039687264714 ) ) ;
#27472=CARTESIAN_POINT ( 'NONE',  ( 1.833485406944043827, -29.64752363041439764, -142.0485807715649003 ) ) ;
#27473=CARTESIAN_POINT ( 'NONE',  ( 109.1587776205901861, 0.002185517590237683917, -0.006995903587863981817 ) ) ;
#27476=VERTEX_POINT ( 'NONE', #12328 ) ;
#27477=CARTESIAN_POINT ( 'NONE',  ( 32.73300124599735739, -72.21147546950616913, 92.86301839379999024 ) ) ;
#27478=CARTESIAN_POINT ( 'NONE',  ( 2.430230287190592531, -60.50928654924668137, -132.3371620660956864 ) ) ;
#27480=CARTESIAN_POINT ( 'NONE',  ( 1.832998868059890096, 144.3700883710219216, -14.63705790013863250 ) ) ;
#27481=CARTESIAN_POINT ( 'NONE',  ( 1.833485406944057594, 125.4007332306555895, -73.01664920992834595 ) ) ;
#27482=CARTESIAN_POINT ( 'NONE',  ( 16.75465622695671897, 140.8868039942614985, 19.47041796022283577 ) ) ;
#27484=( BOUNDED_SURFACE ( )  B_SPLINE_SURFACE ( 3, 1, ( 
 ( #23228, #17146 ),
 ( #14562, #23368 ),
 ( #21033, #27940 ),
 ( #17001, #27812 ) ),
 .UNSPECIFIED., .F., .F., .F. ) 
 B_SPLINE_SURFACE_WITH_KNOTS ( ( 4, 4 ),
 ( 2, 2 ),
 ( 0.000000000000000000, 1.000000000000000000 ),
 ( 0.000000000000000000, 1.000000000000000000 ),
 .UNSPECIFIED. ) 
 GEOMETRIC_REPRESENTATION_ITEM ( )  RATIONAL_B_SPLINE_SURFACE ( (
 ( 1.000000000000000000, 1.000000000000000000),
 ( 0.9956975270656955868, 0.8568959468854907557),
 ( 0.9956975270656955868, 0.8568959468854907557),
 ( 1.000000000000000000, 1.000000000000000000) ) ) 
 REPRESENTATION_ITEM ( '' )  SURFACE ( )  );
#27485=CARTESIAN_POINT ( 'NONE',  ( 1.833485406944043827, -117.0814567582538501, -85.72460230293812344 ) ) ;
#27487=EDGE_CURVE ( 'NONE', #13900, #1601, #27218, .T. ) ;
#27492=CARTESIAN_POINT ( 'NONE',  ( 32.73300124599738581, -16.10546300444743650, -116.5274707358856858 ) ) ;
#27495=CARTESIAN_POINT ( 'NONE',  ( 119.2224693531408803, -90.00000000000005684, 39.99999999999997158 ) ) ;
#27496=B_SPLINE_CURVE_WITH_KNOTS ( 'NONE', 3,
 ( #9419, #22958, #27387, #25248, #1060, #20485 ),
 .UNSPECIFIED., .F., .F.,
 ( 4, 2, 4 ),
 ( 1.388456241783856658E-17, 0.0006311571484586047049, 0.001262314296917195532 ),
 .UNSPECIFIED. ) ;
#27497=ORIENTED_EDGE ( 'NONE', *, *, #3742, .F. ) ;
#27499=CARTESIAN_POINT ( 'NONE',  ( 32.73300124599732186, 0.000000000000000000, 0.000000000000000000 ) ) ;
#27502=CARTESIAN_POINT ( 'NONE',  ( 55.79472521941428198, 62.63970324008313639, -37.00555938668194500 ) ) ;
#27503=CARTESIAN_POINT ( 'NONE',  ( 25.64692872815577473, 0.3216598674799600599, -112.9107203549055498 ) ) ;
#27504=EDGE_CURVE ( 'NONE', #7370, #1405, #24129, .T. ) ;
#27505=VERTEX_POINT ( 'NONE', #27582 ) ;
#27506=CARTESIAN_POINT ( 'NONE',  ( 1.834118845439484335, -132.4921483272724174, -59.18411796427184157 ) ) ;
#27507=CARTESIAN_POINT ( 'NONE',  ( 2.430230287190589422, -28.83279105684524879, 142.6294793592097108 ) ) ;
#27508=ORIENTED_EDGE ( 'NONE', *, *, #25969, .T. ) ;
#27514=DIRECTION ( 'NONE',  ( -1.000000000000000000, 0.000000000000000000, 0.000000000000000000 ) ) ;
#27516=( BOUNDED_SURFACE ( )  B_SPLINE_SURFACE ( 3, 1, ( 
 ( #4587, #6908 ),
 ( #2567, #20561 ),
 ( #27174, #2716 ),
 ( #24326, #701 ) ),
 .UNSPECIFIED., .F., .F., .F. ) 
 B_SPLINE_SURFACE_WITH_KNOTS ( ( 4, 4 ),
 ( 2, 2 ),
 ( 0.000000000000000000, 1.000000000000000000 ),
 ( 0.000000000000000000, 1.000000000000000000 ),
 .UNSPECIFIED. ) 
 GEOMETRIC_REPRESENTATION_ITEM ( )  RATIONAL_B_SPLINE_SURFACE ( (
 ( 1.000000000000000000, 1.000000000000000000),
 ( 0.9956975270656955868, 0.8568959468854907557),
 ( 0.9956975270656955868, 0.8568959468854907557),
 ( 1.000000000000000000, 1.000000000000000000) ) ) 
 REPRESENTATION_ITEM ( '' )  SURFACE ( )  );
#27518=EDGE_CURVE ( 'NONE', #15104, #4903, #773, .T. ) ;
#27520=CARTESIAN_POINT ( 'NONE',  ( 25.64708010899963142, 83.94602815988672262, 75.51173009720550056 ) ) ;
#27521=EDGE_CURVE ( 'NONE', #13492, #3933, #2135, .T. ) ;
#27522=B_SPLINE_CURVE_WITH_KNOTS ( 'NONE', 3,
 ( #8556, #3666, #21233, #10577, #27984, #12857 ),
 .UNSPECIFIED., .F., .F.,
 ( 4, 2, 4 ),
 ( 1.965608005753612659E-17, 0.0006311571484586013438, 0.001262314296917182955 ),
 .UNSPECIFIED. ) ;
#27526=CARTESIAN_POINT ( 'NONE',  ( 25.64681081121880624, -75.24277141833435678, -84.18689316040122606 ) ) ;
#27530=CARTESIAN_POINT ( 'NONE',  ( 2.430230287190592531, -13.76600171652741267, 144.8619874886005903 ) ) ;
#27532=CARTESIAN_POINT ( 'NONE',  ( 25.64703792032467433, -0.1487959541333613023, -112.9111140735909657 ) ) ;
#27533=CARTESIAN_POINT ( 'NONE',  ( 30.59138290137890337, -60.43009393261900897, -99.26509990456075627 ) ) ;
#27535=ORIENTED_EDGE ( 'NONE', *, *, #19954, .F. ) ;
#27536=LINE ( 'NONE', #7845, #9289 ) ;
#27537=ORIENTED_EDGE ( 'NONE', *, *, #13331, .F. ) ;
#27539=CARTESIAN_POINT ( 'NONE',  ( 25.64681081121879203, -112.9102952884414464, -0.4157506337739698132 ) ) ;
#27541=ORIENTED_EDGE ( 'NONE', *, *, #25385, .T. ) ;
#27542=ORIENTED_EDGE ( 'NONE', *, *, #12228, .T. ) ;
#27545=CARTESIAN_POINT ( 'NONE',  ( 26.11404676487259024, 108.0249973236467582, 33.91085499298413453 ) ) ;
#27546=B_SPLINE_CURVE_WITH_KNOTS ( 'NONE', 3,
 ( #2018, #15832, #7072, #4753, #6922, #26757, #2882, #5317 ),
 .UNSPECIFIED., .F., .F.,
 ( 4, 2, 2, 4 ),
 ( 3.469446951953614189E-18, 0.0002429592666046712307, 0.0004859185332093389920, 0.0009718370664186921871 ),
 .UNSPECIFIED. ) ;
#27547=CARTESIAN_POINT ( 'NONE',  ( 1.834118845439484335, 125.5799175751979959, -72.70910183320437170 ) ) ;
#27548=EDGE_CURVE ( 'NONE', #704, #28334, #7306, .T. ) ;
#27553=EDGE_LOOP ( 'NONE', ( #18361, #26444, #21795, #13550 ) ) ;
#27554=ORIENTED_EDGE ( 'NONE', *, *, #25719, .F. ) ;
#27556=CARTESIAN_POINT ( 'NONE',  ( 1.834118845439484335, -29.99597360112969469, -141.9759513273467917 ) ) ;
#27557=CARTESIAN_POINT ( 'NONE',  ( 2.430230287190589422, 126.7388733285345097, 71.49654683843553471 ) ) ;
#27558=EDGE_CURVE ( 'NONE', #5199, #10838, #1667, .T. ) ;
#27559=CARTESIAN_POINT ( 'NONE',  ( 1.833603222531958288, -85.65285110156219162, 117.1340888386546766 ) ) ;
#27560=CARTESIAN_POINT ( 'NONE',  ( 10.93730112725972425, -79.81734490845995822, 128.3908183996588264 ) ) ;
#27562=ORIENTED_EDGE ( 'NONE', *, *, #23041, .F. ) ;
#27563=CARTESIAN_POINT ( 'NONE',  ( 2.433796855181233454, 137.9325382748291418, -46.34326152018600453 ) ) ;
#27565=CARTESIAN_POINT ( 'NONE',  ( 19.66333377628704682, -133.7337774474999037, -33.01772659807248544 ) ) ;
#27567=CARTESIAN_POINT ( 'NONE',  ( 25.64708228042121263, -97.80372460135714618, 56.42152786924468444 ) ) ;
#27569=( BOUNDED_SURFACE ( )  B_SPLINE_SURFACE ( 3, 1, ( 
 ( #7488, #2875 ),
 ( #7339, #23189 ),
 ( #7642, #3445 ),
 ( #11654, #8071 ) ),
 .UNSPECIFIED., .F., .F., .F. ) 
 B_SPLINE_SURFACE_WITH_KNOTS ( ( 4, 4 ),
 ( 2, 2 ),
 ( 0.000000000000000000, 1.000000000000000000 ),
 ( 0.000000000000000000, 1.000000000000000000 ),
 .UNSPECIFIED. ) 
 GEOMETRIC_REPRESENTATION_ITEM ( )  RATIONAL_B_SPLINE_SURFACE ( (
 ( 1.000000000000000000, 1.000000000000000000),
 ( 0.6386103224230316178, 0.9954351624131538845),
 ( 0.6386103224230316178, 0.9954351624131538845),
 ( 1.000000000000000000, 1.000000000000000000) ) ) 
 REPRESENTATION_ITEM ( '' )  SURFACE ( )  );
#27570=ORIENTED_EDGE ( 'NONE', *, *, #15828, .F. ) ;
#27575=VECTOR ( 'NONE', #16998, 1000.000000000000114 ) ;
#27576=CARTESIAN_POINT ( 'NONE',  ( 2.063896406836609909, 57.85593781835596161, -133.2511741302114956 ) ) ;
#27577=CARTESIAN_POINT ( 'NONE',  ( 5.340103579038299131, 133.7487108093472443, -62.06990748397718960 ) ) ;
#27579=EDGE_CURVE ( 'NONE', #13750, #4626, #1425, .T. ) ;
#27580=ORIENTED_EDGE ( 'NONE', *, *, #648, .T. ) ;
#27581=B_SPLINE_CURVE_WITH_KNOTS ( 'NONE', 3,
 ( #17984, #2893, #7511, #22180 ),
 .UNSPECIFIED., .F., .F.,
 ( 4, 4 ),
 ( 3.105545673626859933E-16, 0.01077107486149804332 ),
 .UNSPECIFIED. ) ;
#27582=CARTESIAN_POINT ( 'NONE',  ( 1.833485406944057594, -44.33323125130021225, 138.1714136985306993 ) ) ;
#27583=LINE ( 'NONE', #16813, #16197 ) ;
#27584=CARTESIAN_POINT ( 'NONE',  ( 109.1778270068192853, -0.003210287141656817823, 0.008743876326153495956 ) ) ;
#27586=VERTEX_POINT ( 'NONE', #4255 ) ;
#27587=VERTEX_POINT ( 'NONE', #13037 ) ;
#27590=CARTESIAN_POINT ( 'NONE',  ( 119.2224693531407667, -69.99999999999998579, 20.00000000000007461 ) ) ;
#27591=FACE_OUTER_BOUND ( 'NONE', #6114, .T. ) ;
#27592=CARTESIAN_POINT ( 'NONE',  ( 25.64708228042117000, 11.84161204513409338, -112.2886173090158763 ) ) ;
#27593=CARTESIAN_POINT ( 'NONE',  ( 24.01988960052058886, 49.36855864442128450, 121.3896480498351877 ) ) ;
#27596=CARTESIAN_POINT ( 'NONE',  ( 25.64692232868535626, 45.62640214192403931, -103.2819624397963452 ) ) ;
#27597=ORIENTED_EDGE ( 'NONE', *, *, #23720, .T. ) ;
#27600=DIRECTION ( 'NONE',  ( -0.5914120900931444380, 0.7870418015781071031, -0.1754905759872768534 ) ) ;
#27601=CARTESIAN_POINT ( 'NONE',  ( 2.063896406836609909, 116.7302989755749252, -86.47093297168882486 ) ) ;
#27603=CARTESIAN_POINT ( 'NONE',  ( 26.11404676487257603, 74.91683232330973397, 84.89295829319517850 ) ) ;
#27605=CARTESIAN_POINT ( 'NONE',  ( 6.224689322667647851, -136.2818611715186989, -57.86870174583563653 ) ) ;
#27609=( BOUNDED_SURFACE ( )  B_SPLINE_SURFACE ( 3, 1, ( 
 ( #7330, #18690 ),
 ( #9925, #20559 ),
 ( #22596, #25177 ),
 ( #5446, #11487 ) ),
 .UNSPECIFIED., .F., .F., .F. ) 
 B_SPLINE_SURFACE_WITH_KNOTS ( ( 4, 4 ),
 ( 2, 2 ),
 ( 0.000000000000000000, 1.000000000000000000 ),
 ( 0.000000000000000000, 1.000000000000000000 ),
 .UNSPECIFIED. ) 
 GEOMETRIC_REPRESENTATION_ITEM ( )  RATIONAL_B_SPLINE_SURFACE ( (
 ( 1.000000000000000000, 1.000000000000000000),
 ( 0.9956975270656955868, 0.8568959468854907557),
 ( 0.9956975270656955868, 0.8568959468854907557),
 ( 1.000000000000000000, 1.000000000000000000) ) ) 
 REPRESENTATION_ITEM ( '' )  SURFACE ( )  );
#27610=VECTOR ( 'NONE', #14149, 1000.000000000000114 ) ;
#27611=CARTESIAN_POINT ( 'NONE',  ( 10.93730112725977932, -115.5857507957709913, 97.44200844886238144 ) ) ;
#27613=ORIENTED_EDGE ( 'NONE', *, *, #20990, .F. ) ;
#27615=EDGE_CURVE ( 'NONE', #7588, #22495, #22205, .T. ) ;
#27616=EDGE_LOOP ( 'NONE', ( #4321, #16141, #19287, #7565 ) ) ;
#27617=LINE ( 'NONE', #25626, #7062 ) ;
#27618=CARTESIAN_POINT ( 'NONE',  ( 26.11404676487257603, 12.95861723607603544, -112.4785329405480780 ) ) ;
#27619=EDGE_CURVE ( 'NONE', #8211, #18556, #18608, .T. ) ;
#27622=VECTOR ( 'NONE', #8844, 1000.000000000000114 ) ;
#27624=CARTESIAN_POINT ( 'NONE',  ( 25.64681081121880624, -23.06870491922396837, 110.5293738517607665 ) ) ;
#27626=FACE_OUTER_BOUND ( 'NONE', #3470, .T. ) ;
#27627=VECTOR ( 'NONE', #17710, 1000.000000000000000 ) ;
#27628=EDGE_CURVE ( 'NONE', #27099, #14753, #12109, .T. ) ;
#27629=CARTESIAN_POINT ( 'NONE',  ( 1.833603222531969834, -59.42758433816056396, 132.3826570575581059 ) ) ;
#27630=CARTESIAN_POINT ( 'NONE',  ( 25.64704443564079028, 112.3065506427463305, -11.66968230815798258 ) ) ;
#27631=CARTESIAN_POINT ( 'NONE',  ( 55.79472521941426777, 28.92526238350474088, 66.75682020267539940 ) ) ;
#27632=VERTEX_POINT ( 'NONE', #15040 ) ;
#27633=CIRCLE ( 'NONE', #3266, 117.6351876552689504 ) ;
#27634=ORIENTED_EDGE ( 'NONE', *, *, #11182, .F. ) ;
#27636=CARTESIAN_POINT ( 'NONE',  ( 109.1778270068192853, -0.009177562596833058889, -0.001591747944966620271 ) ) ;
#27637=DIRECTION ( 'NONE',  ( 0.000000000000000000, 0.000000000000000000, -1.000000000000000000 ) ) ;
#27638=CARTESIAN_POINT ( 'NONE',  ( 1.833485406944043827, 144.2578170162062747, 15.69895494453433393 ) ) ;
#27639=CARTESIAN_POINT ( 'NONE',  ( 2.108985857320911705, 107.1123114102940690, -98.16869034643197267 ) ) ;
#27641=CARTESIAN_POINT ( 'NONE',  ( 2.063896406836609909, 142.3682421260907631, 28.88716984836368695 ) ) ;
#27642=VERTEX_POINT ( 'NONE', #12884 ) ;
#27643=DIRECTION ( 'NONE',  ( -0.5914120900931443270, -0.7398809652417984717, -0.3206367055789513532 ) ) ;
#27645=CARTESIAN_POINT ( 'NONE',  ( 25.70243777736190438, -11.07690056740789331, -112.4037002646849004 ) ) ;
#27647=CARTESIAN_POINT ( 'NONE',  ( 109.1587776205901577, 0.002343968083389357145, -0.006944419901758100769 ) ) ;
#27649=CARTESIAN_POINT ( 'NONE',  ( 1.833809397773875638, 145.1096615951801709, 0.1779672212505475359 ) ) ;
#27651=CARTESIAN_POINT ( 'NONE',  ( 109.1586900883932856, 0.002810909342002405019, -0.006561743627145274170 ) ) ;
#27652=VERTEX_POINT ( 'NONE', #1948 ) ;
#27653=VECTOR ( 'NONE', #5786, 1000.000000000000227 ) ;
#27655=EDGE_LOOP ( 'NONE', ( #13479, #4695, #18445, #27901 ) ) ;
#27656=CONICAL_SURFACE ( 'NONE', #15220, 117.6351876552689504, 0.9945805576725580410 ) ;
#27657=EDGE_CURVE ( 'NONE', #17196, #22112, #27732, .T. ) ;
#27659=CARTESIAN_POINT ( 'NONE',  ( 16.05277956358206026, -34.34928806929325162, -139.1285124304122292 ) ) ;
#27660=CARTESIAN_POINT ( 'NONE',  ( 16.75465622695652357, -136.6258322711653648, 39.51671382433896440 ) ) ;
#27661=ADVANCED_FACE ( 'NONE', ( #11443 ), #6812, .F. ) ;
#27662=CARTESIAN_POINT ( 'NONE',  ( -90.83090735639699176, 0.000000000000000000, 0.000000000000000000 ) ) ;
#27665=B_SPLINE_CURVE_WITH_KNOTS ( 'NONE', 3,
 ( #27752, #22884, #27593, #12340, #3703, #27310, #8054 ),
 .UNSPECIFIED., .F., .F.,
 ( 4, 3, 4 ),
 ( 0.000000000000000000, 0.02398743853561340067, 0.04000277880656211149 ),
 .UNSPECIFIED. ) ;
#27666=DIRECTION ( 'NONE',  ( -1.000000000000000000, -0.000000000000000000, -0.000000000000000000 ) ) ;
#27667=CARTESIAN_POINT ( 'NONE',  ( 32.73300124599735739, -28.19767303745682341, 114.2056417606547285 ) ) ;
#27668=B_SPLINE_CURVE_WITH_KNOTS ( 'NONE', 3,
 ( #22575, #2543, #13627, #24742 ),
 .UNSPECIFIED., .F., .F.,
 ( 4, 4 ),
 ( 3.372266854755940974E-16, 0.01077107486149835383 ),
 .UNSPECIFIED. ) ;
#27669=DIRECTION ( 'NONE',  ( -1.000000000000000000, -0.000000000000000000, -0.000000000000000000 ) ) ;
#27670=CARTESIAN_POINT ( 'NONE',  ( 25.64681081121880624, 102.9795863647034935, -46.30456157731225630 ) ) ;
#27671=CARTESIAN_POINT ( 'NONE',  ( 26.28373643307416785, 43.35364178852768191, 119.9673604189456739 ) ) ;
#27672=CARTESIAN_POINT ( 'NONE',  ( 109.1721716018069657, 0.01019541462303493601, 0.01368917435591437623 ) ) ;
#27673=CIRCLE ( 'NONE', #13876, 151.1787379149930359 ) ;
#27675=CARTESIAN_POINT ( 'NONE',  ( 5.340103556456508471, -146.3832391989195116, -17.70136535450057380 ) ) ;
#27676=FACE_OUTER_BOUND ( 'NONE', #642, .T. ) ;
#27677=CARTESIAN_POINT ( 'NONE',  ( 26.11404676487257603, -57.58742681967381571, -97.48350837663670632 ) ) ;
#27678=CARTESIAN_POINT ( 'NONE',  ( 21.16825799904901828, -106.9139171613931580, 83.13600836828973684 ) ) ;
#27679=CARTESIAN_POINT ( 'NONE',  ( 25.73574536432418114, 12.61003673872037112, -112.2643803187782936 ) ) ;
#27680=ORIENTED_EDGE ( 'NONE', *, *, #17130, .T. ) ;
#27681=CARTESIAN_POINT ( 'NONE',  ( 109.1721716018069515, 0.01699510305643760558, -0.001583175916617861941 ) ) ;
#27683=CARTESIAN_POINT ( 'NONE',  ( 1.831572820252009626, 141.7320553118910027, -31.13525033585354151 ) ) ;
#27684=B_SPLINE_CURVE_WITH_KNOTS ( 'NONE', 3,
 ( #20762, #11847, #14272, #762, #9687, #20618, #16159, #1055 ),
 .UNSPECIFIED., .F., .F.,
 ( 4, 2, 2, 4 ),
 ( 6.938893903907228378E-18, 0.0002429588503611349287, 0.0004859177007222629185, 0.0009718354014444958045 ),
 .UNSPECIFIED. ) ;
#27685=FACE_OUTER_BOUND ( 'NONE', #19574, .T. ) ;
#27686=VERTEX_POINT ( 'NONE', #4962 ) ;
#27687=EDGE_LOOP ( 'NONE', ( #12386, #4572, #25580, #11685 ) ) ;
#27688=ORIENTED_EDGE ( 'NONE', *, *, #24527, .T. ) ;
#27692=B_SPLINE_CURVE_WITH_KNOTS ( 'NONE', 3,
 ( #9629, #22037, #22894, #18394 ),
 .UNSPECIFIED., .F., .F.,
 ( 4, 4 ),
 ( 6.133075535169769447E-16, 0.008383748772660102461 ),
 .UNSPECIFIED. ) ;
#27693=VECTOR ( 'NONE', #24719, 1000.000000000000000 ) ;
#27695=AXIS2_PLACEMENT_3D ( 'NONE', #17167, #6521, #8401 ) ;
#27696=ADVANCED_FACE ( 'NONE', ( #26838 ), #13736, .F. ) ;
#27697=CARTESIAN_POINT ( 'NONE',  ( 1.833838850093440387, -141.9387658801233556, 30.17001957361944520 ) ) ;
#27698=EDGE_CURVE ( 'NONE', #4083, #28198, #20995, .T. ) ;
#27701=CARTESIAN_POINT ( 'NONE',  ( 8.186469777910758694, 63.89871389959457559, 134.9918587298865873 ) ) ;
#27702=CARTESIAN_POINT ( 'NONE',  ( 1.833485406944057594, 72.09189602597886903, -125.9346397303427665 ) ) ;
#27703=B_SPLINE_CURVE_WITH_KNOTS ( 'NONE', 3,
 ( #22255, #2512, #2963, #7278 ),
 .UNSPECIFIED., .F., .F.,
 ( 4, 4 ),
 ( 2.928344767506750777E-16, 0.008383748772659755516 ),
 .UNSPECIFIED. ) ;
#27704=CARTESIAN_POINT ( 'NONE',  ( 55.79472521941428198, 66.16469064668339684, -30.25520714117840626 ) ) ;
#27705=CARTESIAN_POINT ( 'NONE',  ( 25.69398547355838147, -112.3990349503584980, -11.06723946918872237 ) ) ;
#27706=ORIENTED_EDGE ( 'NONE', *, *, #16616, .T. ) ;
#27708=CARTESIAN_POINT ( 'NONE',  ( 109.1587776205901861, 0.002343968083398739830, 0.006944419901758138065 ) ) ;
#27709=CARTESIAN_POINT ( 'NONE',  ( 2.433796855181219243, 133.5135467655526043, -57.85512797797757401 ) ) ;
#27711=CARTESIAN_POINT ( 'NONE',  ( 26.11404676487257603, -36.06104232266378062, -107.3263591096434197 ) ) ;
#27712=CARTESIAN_POINT ( 'NONE',  ( 24.22246935314087324, 90.00000000000005684, 39.99999999999999289 ) ) ;
#27713=CARTESIAN_POINT ( 'NONE',  ( 25.70243777736186530, 90.94412140945959777, 66.98101477609036181 ) ) ;
#27714=AXIS2_PLACEMENT_3D ( 'NONE', #1399, #1676, #28289 ) ;
#27715=ORIENTED_EDGE ( 'NONE', *, *, #16475, .F. ) ;
#27719=CARTESIAN_POINT ( 'NONE',  ( 2.433796855181219243, -116.8607839509062671, 86.69855925933937613 ) ) ;
#27721=ORIENTED_EDGE ( 'NONE', *, *, #25164, .F. ) ;
#27722=CARTESIAN_POINT ( 'NONE',  ( 55.79472521941428198, -42.17269936297680033, 59.28412330436287192 ) ) ;
#27725=EDGE_CURVE ( 'NONE', #24971, #22236, #11724, .T. ) ;
#27726=B_SPLINE_CURVE_WITH_KNOTS ( 'NONE', 3,
 ( #16822, #23173, #25469, #5588 ),
 .UNSPECIFIED., .F., .F.,
 ( 4, 4 ),
 ( 3.770221040707433269E-16, 0.01077107486149843883 ),
 .UNSPECIFIED. ) ;
#27727=DIRECTION ( 'NONE',  ( 1.000000000000000000, -0.000000000000000000, -0.000000000000000000 ) ) ;
#27728=VERTEX_POINT ( 'NONE', #18057 ) ;
#27730=CARTESIAN_POINT ( 'NONE',  ( 32.73300124599732186, 0.000000000000000000, 0.000000000000000000 ) ) ;
#27731=CARTESIAN_POINT ( 'NONE',  ( 109.1586900883932856, -0.002810909342002450555, 0.006561743627145253353 ) ) ;
#27732=CIRCLE ( 'NONE', #23153, 12.50000000000000178 ) ;
#27738=CARTESIAN_POINT ( 'NONE',  ( 13.84597867724990294, 146.6243035057529482, 4.782757490006329881 ) ) ;
#27741=CARTESIAN_POINT ( 'NONE',  ( 30.59141879584285917, -107.2355637993505582, 44.78722686469172487 ) ) ;
#27742=CARTESIAN_POINT ( 'NONE',  ( 30.58324630866353289, 92.47020419020178394, 77.95273942827370206 ) ) ;
#27749=LINE ( 'NONE', #23018, #20354 ) ;
#27750=CARTESIAN_POINT ( 'NONE',  ( 109.1589550718174877, -0.007132058561965932270, -0.002553077953671684542 ) ) ;
#27751=DIRECTION ( 'NONE',  ( 0.000000000000000000, 0.000000000000000000, 1.000000000000000000 ) ) ;
#27752=CARTESIAN_POINT ( 'NONE',  ( 32.73300124599735739, 44.31599526637956643, 108.9684813982490539 ) ) ;
#27758=CARTESIAN_POINT ( 'NONE',  ( 1.833206310202336820, -0.7447039688715555439, -145.1075835704899362 ) ) ;
#27759=CARTESIAN_POINT ( 'NONE',  ( 55.79472521941428198, -28.92526238350520273, 66.75682020267520045 ) ) ;
#27760=CARTESIAN_POINT ( 'NONE',  ( 2.430230287190592531, 137.9371479820468949, -46.34481016236681228 ) ) ;
#27761=CARTESIAN_POINT ( 'NONE',  ( 25.64692872815575697, 107.2850779876534233, 35.19724814977951866 ) ) ;
#27762=DIRECTION ( 'NONE',  ( 0.5914120900931444380, -0.07630783613000820254, -0.8027508043202538079 ) ) ;
#27765=EDGE_LOOP ( 'NONE', ( #15307, #11394, #13297, #11473 ) ) ;
#27766=CARTESIAN_POINT ( 'NONE',  ( 2.430230287190592531, 13.76600171652835947, -144.8619874886005334 ) ) ;
#27768=CARTESIAN_POINT ( 'NONE',  ( 1.834118845439484335, 117.2918069668801024, 85.43746956709887286 ) ) ;
#27771=B_SPLINE_CURVE_WITH_KNOTS ( 'NONE', 3,
 ( #14584, #23250, #5678, #22963 ),
 .UNSPECIFIED., .F., .F.,
 ( 4, 4 ),
 ( 4.496917212498578222E-17, 0.008383748772659509185 ),
 .UNSPECIFIED. ) ;
#27775=EDGE_CURVE ( 'NONE', #6393, #20633, #13883, .T. ) ;
#27776=ADVANCED_FACE ( 'NONE', ( #20504 ), #11763, .F. ) ;
#27778=CARTESIAN_POINT ( 'NONE',  ( 1.833485406944043827, 73.01664920993141550, -125.4007332306537563 ) ) ;
#27780=CARTESIAN_POINT ( 'NONE',  ( 25.64692232868535982, -23.15582834340360918, 110.5112661748244562 ) ) ;
#27781=CARTESIAN_POINT ( 'NONE',  ( 55.49584447822657296, 62.69727227546452752, -36.50733923851132090 ) ) ;
#27782=CARTESIAN_POINT ( 'NONE',  ( 2.433796855181233454, 116.8607839509068498, -86.69855925933855190 ) ) ;
#27783=CARTESIAN_POINT ( 'NONE',  ( 1.833691583653512369, -59.34641645332730064, 132.4191286035304529 ) ) ;
#27784=CARTESIAN_POINT ( 'NONE',  ( 25.87036335909427365, -74.91347493818321368, 84.67915015758833874 ) ) ;
#27785=CARTESIAN_POINT ( 'NONE',  ( 2.263178113027036975, -16.59120315151675129, 144.4462808674009580 ) ) ;
#27786=VERTEX_POINT ( 'NONE', #7864 ) ;
#27788=CARTESIAN_POINT ( 'NONE',  ( 25.65782528836479415, -97.50004228081019164, -56.95887699624839939 ) ) ;
#27789=B_SPLINE_CURVE_WITH_KNOTS ( 'NONE', 3,
 ( #8717, #6160, #28143, #8303, #21956, #2217, #81 ),
 .UNSPECIFIED., .F., .F.,
 ( 4, 3, 4 ),
 ( 0.000000000000000000, 0.02398743853561346312, 0.04000277880656213231 ),
 .UNSPECIFIED. ) ;
#27791=CARTESIAN_POINT ( 'NONE',  ( 2.433796855181205476, -46.34326152018838485, 137.9325382748283744 ) ) ;
#27792=CARTESIAN_POINT ( 'NONE',  ( 32.73300124599735739, -105.8473486001054482, 51.32617430724869223 ) ) ;
#27793=FACE_OUTER_BOUND ( 'NONE', #24297, .T. ) ;
#27794=DIRECTION ( 'NONE',  ( 0.5914120900931444380, 0.7643865440136088374, 0.2567974902965169393 ) ) ;
#27795=DIRECTION ( 'NONE',  ( 0.5914120900931444380, 0.2415416038592911596, 0.7693434820005559116 ) ) ;
#27796=ORIENTED_EDGE ( 'NONE', *, *, #1030, .F. ) ;
#27797=CARTESIAN_POINT ( 'NONE',  ( 1.833721034905636982, -144.2772269874177482, 15.52204855105793158 ) ) ;
#27799=CARTESIAN_POINT ( 'NONE',  ( 5.340103579038177450, 88.52145169228961663, 117.9209211655060443 ) ) ;
#27800=CARTESIAN_POINT ( 'NONE',  ( 2.433796855181219243, -137.9325382748288291, 46.34326152018696376 ) ) ;
#27801=CARTESIAN_POINT ( 'NONE',  ( 109.1592201516379674, -0.007748443302128564178, 0.001331853079208289697 ) ) ;
#27802=EDGE_CURVE ( 'NONE', #12568, #14056, #8012, .T. ) ;
#27804=CARTESIAN_POINT ( 'NONE',  ( 32.73300124599738581, 32.68291970228383292, -113.0038235389598782 ) ) ;
#27805=DIRECTION ( 'NONE',  ( 0.000000000000000000, 0.000000000000000000, 1.000000000000000000 ) ) ;
#27806=ORIENTED_EDGE ( 'NONE', *, *, #26125, .T. ) ;
#27807=EDGE_CURVE ( 'NONE', #14489, #24734, #14471, .T. ) ;
#27810=CARTESIAN_POINT ( 'NONE',  ( 25.65782528836479770, -107.5689571161381366, 34.34372400279215753 ) ) ;
#27811=CARTESIAN_POINT ( 'NONE',  ( 109.1586900883932856, 0.006960773163852190457, -0.001582822706032850245 ) ) ;
#27812=CARTESIAN_POINT ( 'NONE',  ( 2.430230287190581429, -57.85706160874058668, -133.5180086894997089 ) ) ;
#27814=FACE_OUTER_BOUND ( 'NONE', #13586, .T. ) ;
#27817=CARTESIAN_POINT ( 'NONE',  ( 55.49584447822657296, 53.73688382046265843, 48.74506217377899731 ) ) ;
#27818=CARTESIAN_POINT ( 'NONE',  ( 109.1586059443104944, -0.003930911098385119970, 0.005881369279880081791 ) ) ;
#27819=CARTESIAN_POINT ( 'NONE',  ( 25.64700659047694131, -12.02873506870245457, 112.2686754657454600 ) ) ;
#27821=CARTESIAN_POINT ( 'NONE',  ( 16.05277956358234448, 118.6216415718956796, 80.40847413522560316 ) ) ;
#27822=LINE ( 'NONE', #18756, #16828 ) ;
#27823=CARTESIAN_POINT ( 'NONE',  ( 16.75465622695648804, 141.8562168210796415, -10.24707101927895181 ) ) ;
#27826=ORIENTED_EDGE ( 'NONE', *, *, #3755, .F. ) ;
#27827=EDGE_CURVE ( 'NONE', #16498, #2445, #26791, .T. ) ;
#27828=ORIENTED_EDGE ( 'NONE', *, *, #3462, .F. ) ;
#27829=CARTESIAN_POINT ( 'NONE',  ( 1.832998868059890096, 15.69902610990563474, -144.2584710144578821 ) ) ;
#27830=CARTESIAN_POINT ( 'NONE',  ( 2.433796855181219243, -31.67151202412867761, -142.0211193075559493 ) ) ;
#27833=VERTEX_POINT ( 'NONE', #25558 ) ;
#27836=CARTESIAN_POINT ( 'NONE',  ( 2.108393763691174705, -73.75286979200549808, 125.1820217068194410 ) ) ;
#27837=AXIS2_PLACEMENT_3D ( 'NONE', #20913, #9994, #9374 ) ;
#27838=CARTESIAN_POINT ( 'NONE',  ( 32.73300124599737870, -117.5726003567929041, -3.836798148480059734 ) ) ;
#27840=CARTESIAN_POINT ( 'NONE',  ( 2.108985857320948565, 71.53406810961664064, -126.4634971826977505 ) ) ;
#27842=B_SPLINE_CURVE_WITH_KNOTS ( 'NONE', 3,
 ( #26639, #13548, #18000, #8817 ),
 .UNSPECIFIED., .F., .F.,
 ( 4, 4 ),
 ( 0.000000000000000000, 0.008383560773332705135 ),
 .UNSPECIFIED. ) ;
#27847=ORIENTED_EDGE ( 'NONE', *, *, #10379, .T. ) ;
#27849=CARTESIAN_POINT ( 'NONE',  ( 25.64681081121879203, -107.2555980796238657, -35.28660243342658731 ) ) ;
#27852=CARTESIAN_POINT ( 'NONE',  ( 109.1778270068192853, -0.001322180554006250003, 0.009220257877172547203 ) ) ;
#27854=CARTESIAN_POINT ( 'NONE',  ( 25.65782528836479059, 91.01210296572949687, 66.83837989650099587 ) ) ;
#27856=CARTESIAN_POINT ( 'NONE',  ( 10.93730112726005999, 128.3908183996603327, -79.81734490845792607 ) ) ;
#27857=EDGE_CURVE ( 'NONE', #22381, #28052, #3164, .T. ) ;
#27859=ORIENTED_EDGE ( 'NONE', *, *, #25101, .F. ) ;
#27860=CARTESIAN_POINT ( 'NONE',  ( 2.430230287190581429, -125.2872625092157364, -74.01081053031229828 ) ) ;
#27861=ADVANCED_FACE ( 'NONE', ( #16476 ), #17450, .F. ) ;
#27863=( BOUNDED_SURFACE ( )  B_SPLINE_SURFACE ( 3, 1, ( 
 ( #18247, #11216 ),
 ( #6910, #24472 ),
 ( #13511, #26891 ),
 ( #22306, #15818 ) ),
 .UNSPECIFIED., .F., .F., .F. ) 
 B_SPLINE_SURFACE_WITH_KNOTS ( ( 4, 4 ),
 ( 2, 2 ),
 ( 0.000000000000000000, 1.000000000000000000 ),
 ( 0.000000000000000000, 1.000000000000000000 ),
 .UNSPECIFIED. ) 
 GEOMETRIC_REPRESENTATION_ITEM ( )  RATIONAL_B_SPLINE_SURFACE ( (
 ( 1.000000000000000000, 1.000000000000000000),
 ( 0.6386103224230302855, 0.9954351624131538845),
 ( 0.6386103224230302855, 0.9954351624131538845),
 ( 1.000000000000000000, 1.000000000000000000) ) ) 
 REPRESENTATION_ITEM ( '' )  SURFACE ( )  );
#27864=ORIENTED_EDGE ( 'NONE', *, *, #11089, .F. ) ;
#27865=CARTESIAN_POINT ( 'NONE',  ( 9.884929003653626367, -19.90991253123145910, -149.2134106160918066 ) ) ;
#27866=VERTEX_POINT ( 'NONE', #3238 ) ;
#27867=DIRECTION ( 'NONE',  ( 0.000000000000000000, 0.000000000000000000, 1.000000000000000000 ) ) ;
#27870=CARTESIAN_POINT ( 'NONE',  ( 32.73300124599731475, 117.5726003567930036, -3.836798148479248827 ) ) ;
#27872=CARTESIAN_POINT ( 'NONE',  ( 26.11404676487257603, -107.3263591096432776, 36.06104232266415721 ) ) ;
#27873=CARTESIAN_POINT ( 'NONE',  ( 1.833691583653583423, 0.3559373310815163172, -145.1092556475513220 ) ) ;
#27875=CARTESIAN_POINT ( 'NONE',  ( 10.93730112725996051, -4.928439153519255989, -151.0983828010092793 ) ) ;
#27876=CARTESIAN_POINT ( 'NONE',  ( 2.433796855181233454, -118.5671979538051062, -84.34988187691051564 ) ) ;
#27877=CARTESIAN_POINT ( 'NONE',  ( 5.340103579038222747, -146.3832392131352833, 17.70136536264617533 ) ) ;
#27882=CARTESIAN_POINT ( 'NONE',  ( 109.1586059443104944, 0.001198897580738995505, -0.006971743774739763526 ) ) ;
#27883=ADVANCED_FACE ( 'NONE', ( #12020 ), #28470, .F. ) ;
#27885=CARTESIAN_POINT ( 'NONE',  ( 2.433796855181233454, 46.34326152018744693, 137.9325382748286870 ) ) ;
#27887=CARTESIAN_POINT ( 'NONE',  ( 26.28373643307413587, -9.189598927292804476, 127.2291519022771524 ) ) ;
#27890=ORIENTED_EDGE ( 'NONE', *, *, #11022, .F. ) ;
#27891=CARTESIAN_POINT ( 'NONE',  ( 30.59141879584276325, 99.26511058698885392, 60.43012207290984605 ) ) ;
#27892=CARTESIAN_POINT ( 'NONE',  ( 1.833485406944057594, -145.1085452359073429, 0.5339064996879626657 ) ) ;
#27893=CARTESIAN_POINT ( 'NONE',  ( 55.79472521941428198, 71.31192372336674623, 14.41365263906578242 ) ) ;
#27895=DIRECTION ( 'NONE',  ( -1.000000000000000000, -0.000000000000000000, -0.000000000000000000 ) ) ;
#27897=CARTESIAN_POINT ( 'NONE',  ( 1.833485406944057594, 117.7091014914950193, 84.86072343962607079 ) ) ;
#27898=ORIENTED_EDGE ( 'NONE', *, *, #15143, .T. ) ;
#27899=CARTESIAN_POINT ( 'NONE',  ( 109.1624594426973260, -0.01570508117119675737, 0.002863932759303782632 ) ) ;
#27900=CARTESIAN_POINT ( 'NONE',  ( 1.894214914920935744, -137.7482714433626541, 45.75988301372592559 ) ) ;
#27901=ORIENTED_EDGE ( 'NONE', *, *, #11628, .F. ) ;
#27902=DIRECTION ( 'NONE',  ( -1.000000000000000000, -0.000000000000000000, -0.000000000000000000 ) ) ;
#27903=VERTEX_POINT ( 'NONE', #21363 ) ;
#27907=CARTESIAN_POINT ( 'NONE',  ( 1.834118845439484335, 144.3336252355298939, -14.99112450600100921 ) ) ;
#27908=CARTESIAN_POINT ( 'NONE',  ( 109.1586059443104944, -0.001014167950290020132, -0.007001002073869782780 ) ) ;
#27909=CARTESIAN_POINT ( 'NONE',  ( 10.93730112726003156, 119.3442956573285443, -92.80059208661575099 ) ) ;
#27915=B_SPLINE_CURVE_WITH_KNOTS ( 'NONE', 3,
 ( #4045, #12817, #26066, #8646 ),
 .UNSPECIFIED., .F., .F.,
 ( 4, 4 ),
 ( 5.279490611805676199E-16, 0.008383748772660024398 ),
 .UNSPECIFIED. ) ;
#27916=CARTESIAN_POINT ( 'NONE',  ( 1.832998868059890096, -15.69902610990276948, -144.2584710144581948 ) ) ;
#27917=CARTESIAN_POINT ( 'NONE',  ( 26.11404676487257603, 113.2169081140373947, 1.130420376097532653 ) ) ;
#27918=EDGE_CURVE ( 'NONE', #1343, #28093, #10373, .T. ) ;
#27922=CARTESIAN_POINT ( 'NONE',  ( -40.00000000000000000, 0.000000000000000000, 0.000000000000000000 ) ) ;
#27924=ORIENTED_EDGE ( 'NONE', *, *, #8363, .F. ) ;
#27925=LINE ( 'NONE', #8223, #1755 ) ;
#27927=DIRECTION ( 'NONE',  ( 0.5914120900931445490, 0.8063295922669343474, 0.008020494143004668411 ) ) ;
#27928=ADVANCED_FACE ( 'NONE', ( #6126 ), #27392, .F. ) ;
#27929=ADVANCED_FACE ( 'NONE', ( #14879 ), #16388, .F. ) ;
#27930=DIRECTION ( 'NONE',  ( 0.000000000000000000, -0.000000000000000000, -1.000000000000000000 ) ) ;
#27932=CARTESIAN_POINT ( 'NONE',  ( 2.433796855181205476, -144.5536872373190818, -16.65276281464712582 ) ) ;
#27933=CARTESIAN_POINT ( 'NONE',  ( 25.64681081121879203, -97.57530875170644435, 56.81519825470720519 ) ) ;
#27935=ORIENTED_EDGE ( 'NONE', *, *, #10421, .F. ) ;
#27939=CARTESIAN_POINT ( 'NONE',  ( 2.063896406836609909, -132.1577797566310153, 60.31174178979762246 ) ) ;
#27940=CARTESIAN_POINT ( 'NONE',  ( 2.063896406836605024, -57.85593781835329708, -133.2511741302126325 ) ) ;
#27941=ADVANCED_FACE ( 'NONE', ( #8415 ), #13941, .T. ) ;
#27944=DIRECTION ( 'NONE',  ( 0.000000000000000000, 0.000000000000000000, -1.000000000000000000 ) ) ;
#27945=B_SPLINE_CURVE_WITH_KNOTS ( 'NONE', 3,
 ( #23822, #19332, #25829, #21218 ),
 .UNSPECIFIED., .F., .F.,
 ( 4, 4 ),
 ( 0.000000000000000000, 0.008383560773332724217 ),
 .UNSPECIFIED. ) ;
#27947=CARTESIAN_POINT ( 'NONE',  ( 6.224689322667647851, 2.565137105443750620, 148.0369967195762797 ) ) ;
#27948=CARTESIAN_POINT ( 'NONE',  ( 26.11404676487259024, 107.3263591096435476, -36.06104232266339693 ) ) ;
#27952=CARTESIAN_POINT ( 'NONE',  ( 109.1624594426973260, -0.01503296564240493884, -0.005372302061310853770 ) ) ;
#27953=CARTESIAN_POINT ( 'NONE',  ( 2.430230287190581429, 74.01081053031275303, -125.2872625092154522 ) ) ;
#27955=CARTESIAN_POINT ( 'NONE',  ( 5.340103579038286696, 126.5279493327095821, -75.71042924122917839 ) ) ;
#27957=CARTESIAN_POINT ( 'NONE',  ( 32.73300124599739291, -20.69176323058542621, -115.8010721414085538 ) ) ;
#27959=CONICAL_SURFACE ( 'NONE', #2657, 117.6351876552689504, 0.9945805576725580410 ) ;
#27960=VERTEX_POINT ( 'NONE', #22218 ) ;
#27961=CARTESIAN_POINT ( 'NONE',  ( 5.340103579038161463, 75.71042924123044315, 126.5279493327087152 ) ) ;
#27964=ORIENTED_EDGE ( 'NONE', *, *, #7823, .T. ) ;
#27966=CARTESIAN_POINT ( 'NONE',  ( 2.433796855181233454, 43.58222566461826375, -138.8296532063083646 ) ) ;
#27968=CARTESIAN_POINT ( 'NONE',  ( 1.833485406944043827, -142.0485807715647297, 29.64752363041495542 ) ) ;
#27969=AXIS2_PLACEMENT_3D ( 'NONE', #10222, #25479, #23029 ) ;
#27970=EDGE_CURVE ( 'NONE', #3161, #22601, #15850, .T. ) ;
#27971=CONICAL_SURFACE ( 'NONE', #15547, 117.6351876552689504, 0.9945805576725580410 ) ;
#27972=CARTESIAN_POINT ( 'NONE',  ( 55.79472521941428198, -72.75035398477136539, 0.7279028900791078005 ) ) ;
#27973=EDGE_CURVE ( 'NONE', #25128, #5199, #9335, .T. ) ;
#27974=CARTESIAN_POINT ( 'NONE',  ( 13.36082413113061307, 147.2768864064173329, -41.18148072373461588 ) ) ;
#27975=CARTESIAN_POINT ( 'NONE',  ( 5.340103556456581302, 144.6887562347053517, -28.39990973639923055 ) ) ;
#27978=VERTEX_POINT ( 'NONE', #18021 ) ;
#27979=ORIENTED_EDGE ( 'NONE', *, *, #17979, .F. ) ;
#27980=CARTESIAN_POINT ( 'NONE',  ( 1.833485406944043827, 144.3694338680886915, -14.63699153649211127 ) ) ;
#27981=CARTESIAN_POINT ( 'NONE',  ( 24.01988960052044675, 36.40943914739906972, 125.8850824254503777 ) ) ;
#27982=CARTESIAN_POINT ( 'NONE',  ( 26.11404676487259024, 22.43340081644921113, -110.9778746459744667 ) ) ;
#27984=CARTESIAN_POINT ( 'NONE',  ( 2.263178607246701279, 96.24282447295591680, -108.9830946142703567 ) ) ;
#27986=ORIENTED_EDGE ( 'NONE', *, *, #25694, .T. ) ;
#27987=CARTESIAN_POINT ( 'NONE',  ( 25.64700659047697684, 91.48068002582108704, -66.18331466615464365 ) ) ;
#27988=CARTESIAN_POINT ( 'NONE',  ( 19.66333377628684431, 95.46107873289045642, -99.30798531455279488 ) ) ;
#27990=ORIENTED_EDGE ( 'NONE', *, *, #11157, .F. ) ;
#27994=ORIENTED_EDGE ( 'NONE', *, *, #17599, .F. ) ;
#27995=CARTESIAN_POINT ( 'NONE',  ( 21.16825799904898631, 106.9139171613937833, -83.13600836828904050 ) ) ;
#27996=EDGE_CURVE ( 'NONE', #21108, #23498, #2329, .T. ) ;
#28002=CARTESIAN_POINT ( 'NONE',  ( 10.93730112725943471, 133.3192575531795683, 71.28103789254991796 ) ) ;
#28004=DIRECTION ( 'NONE',  ( -1.000000000000000000, -0.000000000000000000, -0.000000000000000000 ) ) ;
#28005=EDGE_CURVE ( 'NONE', #7362, #28115, #2797, .T. ) ;
#28007=DIRECTION ( 'NONE',  ( 0.000000000000000000, 0.000000000000000000, 1.000000000000000000 ) ) ;
#28008=CARTESIAN_POINT ( 'NONE',  ( 94.22246935314088034, 70.00000000000002842, -6.938893903907228378E-15 ) ) ;
#28013=CARTESIAN_POINT ( 'NONE',  ( 109.1587776205901577, -0.007151389024634725866, -0.001605238040359110302 ) ) ;
#28014=CARTESIAN_POINT ( 'NONE',  ( 10.93730112725971715, 20.69552240458328995, 149.7554878793148703 ) ) ;
#28015=CARTESIAN_POINT ( 'NONE',  ( 25.87036335909428075, -76.38467849957089584, -83.35447252092937731 ) ) ;
#28016=CARTESIAN_POINT ( 'NONE',  ( 26.11404676487259024, -90.92995828888244603, 67.46175819463337575 ) ) ;
#28018=LINE ( 'NONE', #1815, #6511 ) ;
#28019=FACE_OUTER_BOUND ( 'NONE', #9031, .T. ) ;
#28024=CARTESIAN_POINT ( 'NONE',  ( 109.1586900883932856, -0.007002774699553647453, -0.001385221016527435301 ) ) ;
#28025=CARTESIAN_POINT ( 'NONE',  ( 1.832998868059858122, -125.9352106559989153, 72.09222286251038270 ) ) ;
#28027=VERTEX_POINT ( 'NONE', #19752 ) ;
#28028=CARTESIAN_POINT ( 'NONE',  ( 2.433796855181219243, -137.9325382748288291, 46.34326152018696376 ) ) ;
#28029=ORIENTED_EDGE ( 'NONE', *, *, #19278, .F. ) ;
#28031=ORIENTED_EDGE ( 'NONE', *, *, #22128, .T. ) ;
#28034=EDGE_CURVE ( 'NONE', #8194, #23751, #13444, .T. ) ;
#28037=B_SPLINE_CURVE_WITH_KNOTS ( 'NONE', 3,
 ( #19045, #27821, #8121, #19184, #12692, #21478, #19311 ),
 .UNSPECIFIED., .F., .F.,
 ( 4, 3, 4 ),
 ( 8.673617379884035472E-18, 0.02816610861753243711, 0.04000277880656209761 ),
 .UNSPECIFIED. ) ;
#28039=CARTESIAN_POINT ( 'NONE',  ( 10.93730112725983439, -146.7718404940644916, 36.23586118136483236 ) ) ;
#28040=EDGE_CURVE ( 'NONE', #21976, #8964, #19611, .T. ) ;
#28041=CARTESIAN_POINT ( 'NONE',  ( 10.93730112725943471, 133.3192575531795683, 71.28103789254991796 ) ) ;
#28042=CARTESIAN_POINT ( 'NONE',  ( 109.1586059443104944, -0.001921075557427598824, -0.006808232911144234713 ) ) ;
#28044=LINE ( 'NONE', #8906, #1889 ) ;
#28045=CARTESIAN_POINT ( 'NONE',  ( 1.833485406944057594, -58.53321471326971448, 132.7804117027886548 ) ) ;
#28047=CARTESIAN_POINT ( 'NONE',  ( 109.1592201516379674, -0.007780772729122749191, 0.001127733110588196924 ) ) ;
#28048=CARTESIAN_POINT ( 'NONE',  ( 109.1778270068192853, -0.007323887274081492156, 0.005755170886745393684 ) ) ;
#28049=CARTESIAN_POINT ( 'NONE',  ( 25.64708010899963853, 34.83947233573820768, -107.4019003251853235 ) ) ;
#28050=ORIENTED_EDGE ( 'NONE', *, *, #7030, .F. ) ;
#28051=VECTOR ( 'NONE', #21762, 1000.000000000000114 ) ;
#28052=VERTEX_POINT ( 'NONE', #22949 ) ;
#28054=LINE ( 'NONE', #14953, #17149 ) ;
#28056=CIRCLE ( 'NONE', #2289, 151.1787379149930359 ) ;
#28059=FACE_OUTER_BOUND ( 'NONE', #19498, .T. ) ;
#28060=CARTESIAN_POINT ( 'NONE',  ( 21.16825799904898986, -51.02216409572659472, 125.4548537968712623 ) ) ;
#28061=ORIENTED_EDGE ( 'NONE', *, *, #7365, .T. ) ;
#28064=AXIS2_PLACEMENT_3D ( 'NONE', #22906, #7498, #4893 ) ;
#28065=CARTESIAN_POINT ( 'NONE',  ( 28.37599760073043242, -58.91309773266217320, 98.45181492308101667 ) ) ;
#28066=EDGE_LOOP ( 'NONE', ( #27537, #1264, #27497, #23456 ) ) ;
#28068=CARTESIAN_POINT ( 'NONE',  ( 25.64692232868534560, -12.12735788170734708, -112.2580042965358444 ) ) ;
#28069=ORIENTED_EDGE ( 'NONE', *, *, #28164, .T. ) ;
#28070=( BOUNDED_SURFACE ( )  B_SPLINE_SURFACE ( 3, 1, ( 
 ( #5766, #9944 ),
 ( #3310, #14664 ),
 ( #10234, #14524 ),
 ( #14223, #23467 ) ),
 .UNSPECIFIED., .F., .F., .F. ) 
 B_SPLINE_SURFACE_WITH_KNOTS ( ( 4, 4 ),
 ( 2, 2 ),
 ( 0.000000000000000000, 1.000000000000000000 ),
 ( 0.000000000000000000, 1.000000000000000000 ),
 .UNSPECIFIED. ) 
 GEOMETRIC_REPRESENTATION_ITEM ( )  RATIONAL_B_SPLINE_SURFACE ( (
 ( 1.000000000000000000, 1.000000000000000000),
 ( 0.9956975270656954757, 0.8568959468854893125),
 ( 0.9956975270656954757, 0.8568959468854893125),
 ( 1.000000000000000000, 1.000000000000000000) ) ) 
 REPRESENTATION_ITEM ( '' )  SURFACE ( )  );
#28071=ORIENTED_EDGE ( 'NONE', *, *, #23921, .T. ) ;
#28072=ORIENTED_EDGE ( 'NONE', *, *, #16617, .T. ) ;
#28074=B_SPLINE_CURVE_WITH_KNOTS ( 'NONE', 3,
 ( #19167, #27659, #8107, #5653, #5802, #14559, #6091 ),
 .UNSPECIFIED., .F., .F.,
 ( 4, 3, 4 ),
 ( 4.776383977182116463E-16, 0.02816610861753245099, 0.04000277880656272905 ),
 .UNSPECIFIED. ) ;
#28077=CONICAL_SURFACE ( 'NONE', #15654, 117.6351876552689504, 0.9945805576725580410 ) ;
#28080=CARTESIAN_POINT ( 'NONE',  ( 13.36082413113063083, -94.94363694443971724, -119.8836995922736151 ) ) ;
#28082=CARTESIAN_POINT ( 'NONE',  ( 5.340103579038189885, -43.36842539899472371, 140.9275371836309887 ) ) ;
#28084=CARTESIAN_POINT ( 'NONE',  ( 2.430230287190592531, 98.44218333480770866, 107.1617224697467634 ) ) ;
#28085=LINE ( 'NONE', #27817, #17608 ) ;
#28087=CARTESIAN_POINT ( 'NONE',  ( 6.224689322667630975, 129.4863684118297442, -71.79702446228166934 ) ) ;
#28089=CONICAL_SURFACE ( 'NONE', #21638, 117.6351876552689504, 0.9945805576725580410 ) ;
#28091=B_SPLINE_CURVE_WITH_KNOTS ( 'NONE', 3,
 ( #23023, #14203, #7192, #9485, #16527, #27013, #9621, #18104, #2858, #11637 ),
 .UNSPECIFIED., .F., .F.,
 ( 4, 3, 3, 4 ),
 ( 0.000000000000000000, 0.0002669560319015905239, 0.0005492286108966571746, 0.0008315040496093635460 ),
 .UNSPECIFIED. ) ;
#28092=FACE_OUTER_BOUND ( 'NONE', #7185, .T. ) ;
#28093=VERTEX_POINT ( 'NONE', #27670 ) ;
#28095=VERTEX_POINT ( 'NONE', #24957 ) ;
#28096=CARTESIAN_POINT ( 'NONE',  ( 25.64681081121880624, -23.88203588908001507, -110.3564950173084185 ) ) ;
#28097=CARTESIAN_POINT ( 'NONE',  ( 1.833485406944043827, 117.0814567582544612, 85.72460230293732764 ) ) ;
#28099=ORIENTED_EDGE ( 'NONE', *, *, #24378, .F. ) ;
#28100=ORIENTED_EDGE ( 'NONE', *, *, #17130, .F. ) ;
#28102=EDGE_CURVE ( 'NONE', #3978, #7877, #5662, .T. ) ;
#28104=CARTESIAN_POINT ( 'NONE',  ( 94.22246935314088034, -69.99999999999998579, 12.49999999999999467 ) ) ;
#28105=EDGE_CURVE ( 'NONE', #2445, #25504, #23370, .T. ) ;
#28110=APPLICATION_CONTEXT ( 'automotive_design' ) ;
#28113=CARTESIAN_POINT ( 'NONE',  ( 2.430230287190592531, -132.3371620660954875, 60.50928654924707928 ) ) ;
#28114=DIRECTION ( 'NONE',  ( -0.5914120900931443270, -0.7903769105750333424, -0.1598001217819445263 ) ) ;
#28115=VERTEX_POINT ( 'NONE', #9685 ) ;
#28116=EDGE_LOOP ( 'NONE', ( #6063, #20634, #14752, #25661 ) ) ;
#28118=CARTESIAN_POINT ( 'NONE',  ( 25.64681081121880624, -56.81519825470823548, 97.57530875170583329 ) ) ;
#28122=ORIENTED_EDGE ( 'NONE', *, *, #28349, .F. ) ;
#28123=CARTESIAN_POINT ( 'NONE',  ( 2.433796855181219243, 144.5536872373194228, -16.65276281464415575 ) ) ;
#28127=EDGE_LOOP ( 'NONE', ( #10766, #17636, #568, #6987 ) ) ;
#28128=CONICAL_SURFACE ( 'NONE', #7962, 117.6351876552689504, 0.9945805576725580410 ) ;
#28129=EDGE_CURVE ( 'NONE', #309, #10148, #14770, .T. ) ;
#28130=ORIENTED_EDGE ( 'NONE', *, *, #12677, .F. ) ;
#28131=AXIS2_PLACEMENT_3D ( 'NONE', #28223, #8657, #4468 ) ;
#28132=VERTEX_POINT ( 'NONE', #7545 ) ;
#28133=B_SPLINE_CURVE_WITH_KNOTS ( 'NONE', 3,
 ( #3637, #23386, #22962, #1340 ),
 .UNSPECIFIED., .F., .F.,
 ( 4, 4 ),
 ( 1.386477127738322940E-16, 0.008383748772659576839 ),
 .UNSPECIFIED. ) ;
#28135=EDGE_CURVE ( 'NONE', #14412, #23015, #10007, .T. ) ;
#28136=CARTESIAN_POINT ( 'NONE',  ( 2.108985857320888169, -86.43462668039059338, -116.7869613039528929 ) ) ;
#28139=CARTESIAN_POINT ( 'NONE',  ( 28.37644542392837010, 120.7150203538609645, 29.80435743553996275 ) ) ;
#28140=CARTESIAN_POINT ( 'NONE',  ( 109.1624594426973118, -0.01551217196237748668, 0.003771499231554245168 ) ) ;
#28142=CARTESIAN_POINT ( 'NONE',  ( 2.433796855181219243, 144.5536872373194228, -16.65276281464415575 ) ) ;
#28143=CARTESIAN_POINT ( 'NONE',  ( 24.01988960052062438, -4.273195451969565184, 130.9749633972837159 ) ) ;
#28144=CIRCLE ( 'NONE', #7029, 117.6351876552689504 ) ;
#28146=DIRECTION ( 'NONE',  ( 0.000000000000000000, 0.000000000000000000, 1.000000000000000000 ) ) ;
#28147=CARTESIAN_POINT ( 'NONE',  ( 2.263178113027034755, -118.4461880110609115, 84.32376073259185034 ) ) ;
#28149=VERTEX_POINT ( 'NONE', #5506 ) ;
#28151=CARTESIAN_POINT ( 'NONE',  ( 25.64681081121879203, 56.81519825470891760, -97.57530875170544959 ) ) ;
#28152=CARTESIAN_POINT ( 'NONE',  ( 1.894214914920984372, 117.9869255019031868, 84.54370816135612188 ) ) ;
#28154=CARTESIAN_POINT ( 'NONE',  ( 30.58324630866335880, 16.55818995381147829, 119.8048187378265652 ) ) ;
#28156=CARTESIAN_POINT ( 'NONE',  ( 25.87036335909427720, -90.88222105969110487, 67.25332031939115041 ) ) ;
#28157=CARTESIAN_POINT ( 'NONE',  ( 1.833485406944043827, -97.49333871408762775, 107.4794113447406119 ) ) ;
#28159=CARTESIAN_POINT ( 'NONE',  ( 10.93730112725994275, -26.59437931460641025, -148.8212007290665042 ) ) ;
#28161=DIRECTION ( 'NONE',  ( -1.000000000000000000, -0.000000000000000000, -0.000000000000000000 ) ) ;
#28163=EDGE_LOOP ( 'NONE', ( #17653, #3385, #6736, #14616 ) ) ;
#28164=EDGE_CURVE ( 'NONE', #16763, #21239, #10665, .T. ) ;
#28166=VECTOR ( 'NONE', #18399, 999.9999999999998863 ) ;
#28167=FACE_OUTER_BOUND ( 'NONE', #26005, .T. ) ;
#28168=VECTOR ( 'NONE', #11734, 1000.000000000000000 ) ;
#28170=CARTESIAN_POINT ( 'NONE',  ( 2.263178607246715490, -28.85718361841014712, 142.5035407554793210 ) ) ;
#28171=VECTOR ( 'NONE', #24461, 1000.000000000000114 ) ;
#28172=CARTESIAN_POINT ( 'NONE',  ( 109.1721716018069657, 0.01467989464939309721, -0.008708654716139472077 ) ) ;
#28173=CARTESIAN_POINT ( 'NONE',  ( 109.1589550718174877, 0.002126635388725465863, 0.007270618150629040016 ) ) ;
#28174=CARTESIAN_POINT ( 'NONE',  ( 25.64708228042119842, 97.76433875577640720, 56.48974615488955919 ) ) ;
#28175=B_SPLINE_CURVE_WITH_KNOTS ( 'NONE', 3,
 ( #3582, #1424, #10232, #27477 ),
 .UNSPECIFIED., .F., .F.,
 ( 4, 4 ),
 ( 0.000000000000000000, 0.008383560773332722482 ),
 .UNSPECIFIED. ) ;
#28176=CARTESIAN_POINT ( 'NONE',  ( 1.833485406944043827, 125.4007332306545379, 73.01664920993009389 ) ) ;
#28177=CARTESIAN_POINT ( 'NONE',  ( 25.64681081121879203, 56.09509703373481670, -97.99105938547863559 ) ) ;
#28180=LINE ( 'NONE', #15213, #8327 ) ;
#28181=CARTESIAN_POINT ( 'NONE',  ( 1.833750490713712322, -132.6726660571947889, 58.77746103890230955 ) ) ;
#28182=LINE ( 'NONE', #24168, #24014 ) ;
#28186=VERTEX_POINT ( 'NONE', #19040 ) ;
#28187=( BOUNDED_SURFACE ( )  B_SPLINE_SURFACE ( 3, 1, ( 
 ( #8868, #79 ),
 ( #4393, #24268 ),
 ( #15171, #17207 ),
 ( #13165, #2076 ) ),
 .UNSPECIFIED., .F., .F., .F. ) 
 B_SPLINE_SURFACE_WITH_KNOTS ( ( 4, 4 ),
 ( 2, 2 ),
 ( 0.000000000000000000, 1.000000000000000000 ),
 ( 0.000000000000000000, 1.000000000000000000 ),
 .UNSPECIFIED. ) 
 GEOMETRIC_REPRESENTATION_ITEM ( )  RATIONAL_B_SPLINE_SURFACE ( (
 ( 1.000000000000000000, 1.000000000000000000),
 ( 0.9956975270656954757, 0.8568959468854893125),
 ( 0.9956975270656954757, 0.8568959468854893125),
 ( 1.000000000000000000, 1.000000000000000000) ) ) 
 REPRESENTATION_ITEM ( '' )  SURFACE ( )  );
#28189=ORIENTED_EDGE ( 'NONE', *, *, #4888, .F. ) ;
#28190=CARTESIAN_POINT ( 'NONE',  ( 26.11404676487257603, -97.48350837663569735, -57.58742681967552102 ) ) ;
#28193=CARTESIAN_POINT ( 'NONE',  ( 109.1592201516379674, 0.007302213399779926284, -0.002913740842108661615 ) ) ;
#28196=CARTESIAN_POINT ( 'NONE',  ( 109.1586900883932856, -0.005833932871487544462, 0.004113747441000897322 ) ) ;
#28197=CARTESIAN_POINT ( 'NONE',  ( 1.832998868059858122, -0.5339089137737902391, -145.1092030902949830 ) ) ;
#28198=VERTEX_POINT ( 'NONE', #8526 ) ;
#28200=CARTESIAN_POINT ( 'NONE',  ( 1.833485406944043827, -145.1085452359073145, -0.5339064996899981486 ) ) ;
#28201=VECTOR ( 'NONE', #2711, 1000.000000000000000 ) ;
#28202=CARTESIAN_POINT ( 'NONE',  ( 25.64704443564080805, 23.60610532597107181, -110.4160069635930626 ) ) ;
#28203=EDGE_CURVE ( 'NONE', #13865, #11082, #23635, .T. ) ;
#28204=EDGE_CURVE ( 'NONE', #17409, #19804, #18055, .T. ) ;
#28206=B_SPLINE_CURVE_WITH_KNOTS ( 'NONE', 3,
 ( #19124, #8469, #23747, #15055, #25885, #14795, #12763, #15196 ),
 .UNSPECIFIED., .F., .F.,
 ( 4, 2, 2, 4 ),
 ( 6.938893903907228378E-18, 0.0002429592666046707157, 0.0004859185332093344926, 0.0009718370664186905608 ),
 .UNSPECIFIED. ) ;
#28207=ORIENTED_EDGE ( 'NONE', *, *, #5392, .F. ) ;
#28209=ADVANCED_FACE ( 'NONE', ( #5812 ), #25401, .F. ) ;
#28212=EDGE_CURVE ( 'NONE', #8318, #24769, #28085, .T. ) ;
#28217=CARTESIAN_POINT ( 'NONE',  ( 2.430230287190592531, -1.451610819316726975, -145.5073573687467103 ) ) ;
#28220=CARTESIAN_POINT ( 'NONE',  ( 26.11404676487257603, 92.25884714080498838, -65.63269960453146723 ) ) ;
#28223=CARTESIAN_POINT ( 'NONE',  ( 32.73300124599732186, 0.000000000000000000, 0.000000000000000000 ) ) ;
#28224=CARTESIAN_POINT ( 'NONE',  ( 109.1586900883932856, -0.007109207791181747921, 0.0006456433529163218155 ) ) ;
#28229=CARTESIAN_POINT ( 'NONE',  ( 109.1586900883932856, -0.002301750759607945531, -0.006757191295056121962 ) ) ;
#28230=( BOUNDED_SURFACE ( )  B_SPLINE_SURFACE ( 3, 1, ( 
 ( #22022, #25935 ),
 ( #19583, #6354 ),
 ( #13232, #24066 ),
 ( #13105, #2284 ) ),
 .UNSPECIFIED., .F., .F., .F. ) 
 B_SPLINE_SURFACE_WITH_KNOTS ( ( 4, 4 ),
 ( 2, 2 ),
 ( 0.000000000000000000, 1.000000000000000000 ),
 ( 0.000000000000000000, 1.000000000000000000 ),
 .UNSPECIFIED. ) 
 GEOMETRIC_REPRESENTATION_ITEM ( )  RATIONAL_B_SPLINE_SURFACE ( (
 ( 1.000000000000000000, 1.000000000000000000),
 ( 0.6386103224230302855, 0.9954351624131538845),
 ( 0.6386103224230302855, 0.9954351624131538845),
 ( 1.000000000000000000, 1.000000000000000000) ) ) 
 REPRESENTATION_ITEM ( '' )  SURFACE ( )  );
#28231=CARTESIAN_POINT ( 'NONE',  ( 9.884929003653608603, -146.3148513795964334, -35.39789245780480087 ) ) ;
#28232=EDGE_LOOP ( 'NONE', ( #4252, #16604, #18282, #15449 ) ) ;
#28236=CARTESIAN_POINT ( 'NONE',  ( 25.81918753295377300, 35.81374485821615394, 107.2019194967336801 ) ) ;
#28237=ORIENTED_EDGE ( 'NONE', *, *, #2285, .F. ) ;
#28238=EDGE_LOOP ( 'NONE', ( #15092, #23233, #21997, #4350 ) ) ;
#28239=ORIENTED_EDGE ( 'NONE', *, *, #2134, .T. ) ;
#28240=B_SPLINE_CURVE_WITH_KNOTS ( 'NONE', 3,
 ( #10089, #19142, #617, #12369, #16975, #25766, #27630, #21149, #25501, #8083 ),
 .UNSPECIFIED., .F., .F.,
 ( 4, 3, 3, 4 ),
 ( 6.938893903907228378E-18, 0.0002669560319015735019, 0.0005492286108966399358, 0.0008315040496093465240 ),
 .UNSPECIFIED. ) ;
#28243=CARTESIAN_POINT ( 'NONE',  ( 119.2224693531408803, 70.00000000000004263, 19.99999999999997513 ) ) ;
#28245=CARTESIAN_POINT ( 'NONE',  ( 25.64704443564076186, -110.4715096490034654, 23.34498572103285241 ) ) ;
#28249=ORIENTED_EDGE ( 'NONE', *, *, #26157, .F. ) ;
#28250=B_SPLINE_CURVE_WITH_KNOTS ( 'NONE', 3,
 ( #4139, #25757, #2243, #10631 ),
 .UNSPECIFIED., .F., .F.,
 ( 4, 4 ),
 ( 0.000000000000000000, 0.008383560773332725952 ),
 .UNSPECIFIED. ) ;
#28251=CARTESIAN_POINT ( 'NONE',  ( 25.70243777736190793, -57.10783651465036570, 97.44734253939064672 ) ) ;
#28255=CARTESIAN_POINT ( 'NONE',  ( 109.1592201516379674, -0.004368284148525305825, 0.006536841731961986514 ) ) ;
#28259=( BOUNDED_SURFACE ( )  B_SPLINE_SURFACE ( 3, 1, ( 
 ( #22749, #3014 ),
 ( #1555, #1137 ),
 ( #5448, #25322 ),
 ( #3569, #10359 ) ),
 .UNSPECIFIED., .F., .F., .F. ) 
 B_SPLINE_SURFACE_WITH_KNOTS ( ( 4, 4 ),
 ( 2, 2 ),
 ( 0.000000000000000000, 1.000000000000000000 ),
 ( 0.000000000000000000, 1.000000000000000000 ),
 .UNSPECIFIED. ) 
 GEOMETRIC_REPRESENTATION_ITEM ( )  RATIONAL_B_SPLINE_SURFACE ( (
 ( 1.000000000000000000, 1.000000000000000000),
 ( 0.9960225298536222738, 0.9999952330161893110),
 ( 0.9960225298536222738, 0.9999952330161893110),
 ( 1.000000000000000000, 1.000000000000000000) ) ) 
 REPRESENTATION_ITEM ( '' )  SURFACE ( )  );
#28262=CARTESIAN_POINT ( 'NONE',  ( 30.58324630866338723, -83.81536267638887239, -87.19147450740442196 ) ) ;
#28263=VERTEX_POINT ( 'NONE', #22903 ) ;
#28264=ORIENTED_EDGE ( 'NONE', *, *, #13405, .F. ) ;
#28268=ORIENTED_EDGE ( 'NONE', *, *, #27579, .T. ) ;
#28270=ORIENTED_EDGE ( 'NONE', *, *, #19395, .F. ) ;
#28271=CARTESIAN_POINT ( 'NONE',  ( 1.832998868059858122, -138.1720401012269974, 44.33343224355186862 ) ) ;
#28272=ORIENTED_EDGE ( 'NONE', *, *, #9006, .T. ) ;
#28274=ADVANCED_FACE ( 'NONE', ( #1002 ), #28302, .F. ) ;
#28276=FACE_OUTER_BOUND ( 'NONE', #22848, .T. ) ;
#28278=CARTESIAN_POINT ( 'NONE',  ( 109.1721716018069657, 0.001984900887706629938, 0.01695288006057377519 ) ) ;
#28279=CARTESIAN_POINT ( 'NONE',  ( 26.11404676487257603, 45.01677474591409833, 103.8885755249570906 ) ) ;
#28280=EDGE_CURVE ( 'NONE', #22329, #23985, #28175, .T. ) ;
#28281=CARTESIAN_POINT ( 'NONE',  ( 30.59141879584321089, 111.3296561588019387, -33.33270905817467167 ) ) ;
#28282=CARTESIAN_POINT ( 'NONE',  ( 109.1586900883932856, 0.002109621908824146474, 0.006819617742892447251 ) ) ;
#28284=CARTESIAN_POINT ( 'NONE',  ( 26.11404676487259024, 55.62948129436384193, -98.61392875273304526 ) ) ;
#28285=ORIENTED_EDGE ( 'NONE', *, *, #27807, .F. ) ;
#28288=CARTESIAN_POINT ( 'NONE',  ( 1.833485406944057594, 117.7091014914950193, 84.86072343962607079 ) ) ;
#28289=DIRECTION ( 'NONE',  ( 0.000000000000000000, 0.000000000000000000, -1.000000000000000000 ) ) ;
#28290=EDGE_CURVE ( 'NONE', #11098, #12613, #27617, .T. ) ;
#28293=CARTESIAN_POINT ( 'NONE',  ( 1.833485406944071361, 29.64752363041738548, -142.0485807715643034 ) ) ;
#28295=CARTESIAN_POINT ( 'NONE',  ( 2.263178113027034755, -107.1074314657337396, -98.32595894905942657 ) ) ;
#28296=CARTESIAN_POINT ( 'NONE',  ( 1.831572820252008738, 31.13525033585688462, -141.7320553118902922 ) ) ;
#28297=DIRECTION ( 'NONE',  ( 0.000000000000000000, 0.000000000000000000, -1.000000000000000000 ) ) ;
#28302=( BOUNDED_SURFACE ( )  B_SPLINE_SURFACE ( 3, 1, ( 
 ( #3448, #18706 ),
 ( #18405, #23330 ),
 ( #23193, #16701 ),
 ( #27182, #7647 ) ),
 .UNSPECIFIED., .F., .F., .F. ) 
 B_SPLINE_SURFACE_WITH_KNOTS ( ( 4, 4 ),
 ( 2, 2 ),
 ( 0.000000000000000000, 1.000000000000000000 ),
 ( 0.000000000000000000, 1.000000000000000000 ),
 .UNSPECIFIED. ) 
 GEOMETRIC_REPRESENTATION_ITEM ( )  RATIONAL_B_SPLINE_SURFACE ( (
 ( 1.000000000000000000, 1.000000000000000000),
 ( 0.6386103224230302855, 0.9954351624131538845),
 ( 0.6386103224230302855, 0.9954351624131538845),
 ( 1.000000000000000000, 1.000000000000000000) ) ) 
 REPRESENTATION_ITEM ( '' )  SURFACE ( )  );
#28304=ORIENTED_EDGE ( 'NONE', *, *, #96, .T. ) ;
#28305=DIRECTION ( 'NONE',  ( 0.7071067811865465735, 0.000000000000000000, -0.7071067811865485719 ) ) ;
#28308=CARTESIAN_POINT ( 'NONE',  ( 1.832998868059858122, -97.49378069860723883, -107.4798986104869982 ) ) ;
#28310=B_SPLINE_CURVE_WITH_KNOTS ( 'NONE', 3,
 ( #5690, #927, #14302, #3235, #12162, #5535, #25556, #12016 ),
 .UNSPECIFIED., .F., .F.,
 ( 4, 2, 2, 4 ),
 ( 0.000000000000000000, 0.0002429588503611233006, 0.0004859177007222466012, 0.0009718354014444932024 ),
 .UNSPECIFIED. ) ;
#28311=CARTESIAN_POINT ( 'NONE',  ( 25.64703792032469210, 97.85829113439956473, 56.32669596053470684 ) ) ;
#28316=CARTESIAN_POINT ( 'NONE',  ( 1.833206310202324385, -138.2356391007179752, -44.13245377365773692 ) ) ;
#28317=FACE_BOUND ( 'NONE', #7435, .T. ) ;
#28320=CARTESIAN_POINT ( 'NONE',  ( 6.224689322667647851, -100.9623537450644335, -108.2965163446084631 ) ) ;
#28322=CARTESIAN_POINT ( 'NONE',  ( 26.11404676487259024, -67.46175819463304890, -90.92995828888270182 ) ) ;
#28323=CARTESIAN_POINT ( 'NONE',  ( 109.1624594426973118, 0.01216903288310962859, 0.01033277910989008688 ) ) ;
#28325=EDGE_CURVE ( 'NONE', #17556, #11003, #2423, .T. ) ;
#28326=VERTEX_POINT ( 'NONE', #26029 ) ;
#28329=CARTESIAN_POINT ( 'NONE',  ( 109.1586059443104944, 0.003774052605959034648, -0.005983234375919689943 ) ) ;
#28330=CARTESIAN_POINT ( 'NONE',  ( 109.1587776205901577, -0.0006832286435102948811, -0.007297420966928593392 ) ) ;
#28334=VERTEX_POINT ( 'NONE', #6050 ) ;
#28335=CARTESIAN_POINT ( 'NONE',  ( 32.73300124599735739, 3.836798148478847370, 117.5726003567930178 ) ) ;
#28336=CARTESIAN_POINT ( 'NONE',  ( 109.1592201516379674, -0.006536841731962029015, -0.004368284148525239038 ) ) ;
#28337=CARTESIAN_POINT ( 'NONE',  ( 25.64692232868537758, 23.15582834340436946, -110.5112661748242857 ) ) ;
#28338=FACE_OUTER_BOUND ( 'NONE', #17055, .T. ) ;
#28339=ORIENTED_EDGE ( 'NONE', *, *, #9945, .F. ) ;
#28340=CARTESIAN_POINT ( 'NONE',  ( 1.833206310202334821, -45.54896489827059014, -137.7753867363982181 ) ) ;
#28342=ORIENTED_EDGE ( 'NONE', *, *, #12510, .T. ) ;
#28343=ORIENTED_EDGE ( 'NONE', *, *, #14912, .T. ) ;
#28344=B_SPLINE_CURVE_WITH_KNOTS ( 'NONE', 3,
 ( #18928, #14597, #8013, #16777, #25559, #5837, #932, #28359, #1886, #9085 ),
 .UNSPECIFIED., .F., .F.,
 ( 4, 3, 3, 4 ),
 ( 0.000000000000000000, 0.0002669560319015731767, 0.0005492286108966727871, 0.0008315040496093689670 ),
 .UNSPECIFIED. ) ;
#28346=CARTESIAN_POINT ( 'NONE',  ( 109.1721716018069515, -0.006757465437533647160, -0.01567407524361267776 ) ) ;
#28349=EDGE_CURVE ( 'NONE', #5993, #24848, #19570, .T. ) ;
#28352=B_SPLINE_CURVE_WITH_KNOTS ( 'NONE', 3,
 ( #27982, #1919, #23971, #19076, #23832, #13008, #28391, #17042 ),
 .UNSPECIFIED., .F., .F.,
 ( 4, 2, 2, 4 ),
 ( 7.757919228897728493E-18, 0.0002429592666046677342, 0.0004859185332093277163, 0.0009718370664186610705 ),
 .UNSPECIFIED. ) ;
#28353=CARTESIAN_POINT ( 'NONE',  ( 28.37603512858355614, 112.5845402829049249, 22.09615328858486905 ) ) ;
#28354=ORIENTED_EDGE ( 'NONE', *, *, #13482, .F. ) ;
#28355=EDGE_CURVE ( 'NONE', #26070, #23363, #20939, .T. ) ;
#28358=LINE ( 'NONE', #15537, #28051 ) ;
#28359=CARTESIAN_POINT ( 'NONE',  ( 25.64700659047695197, 56.25842064176090673, 97.89757946487027596 ) ) ;
#28363=CARTESIAN_POINT ( 'NONE',  ( 109.1586900883932856, 0.001385221016536850079, 0.007002774699553664800 ) ) ;
#28366=EDGE_LOOP ( 'NONE', ( #6373, #15123, #24084, #1623 ) ) ;
#28367=ORIENTED_EDGE ( 'NONE', *, *, #16429, .T. ) ;
#28368=CARTESIAN_POINT ( 'NONE',  ( 8.186469777910739154, 77.65916160569911142, 127.5731248346290414 ) ) ;
#28369=CARTESIAN_POINT ( 'NONE',  ( 1.833485406944043827, -138.1714136985311256, 44.33323125129879116 ) ) ;
#28370=ORIENTED_EDGE ( 'NONE', *, *, #17307, .T. ) ;
#28371=ORIENTED_EDGE ( 'NONE', *, *, #9559, .T. ) ;
#28372=ORIENTED_EDGE ( 'NONE', *, *, #6076, .F. ) ;
#28374=CARTESIAN_POINT ( 'NONE',  ( 2.430230287190589422, -138.8342928068217077, -43.58368230469532278 ) ) ;
#28377=CARTESIAN_POINT ( 'NONE',  ( 6.224689322667647851, 121.2721959030538130, 84.93872395423015575 ) ) ;
#28380=EDGE_CURVE ( 'NONE', #16927, #13485, #14420, .T. ) ;
#28381=FACE_OUTER_BOUND ( 'NONE', #10093, .T. ) ;
#28382=CARTESIAN_POINT ( 'NONE',  ( 94.22246935314088034, -151.1871800109700246, -12.50000000000000888 ) ) ;
#28383=CARTESIAN_POINT ( 'NONE',  ( 13.36082413113063083, -151.2941478187909468, 22.28175172543511096 ) ) ;
#28384=( BOUNDED_SURFACE ( )  B_SPLINE_SURFACE ( 3, 1, ( 
 ( #24677, #6676 ),
 ( #184, #2322 ),
 ( #24529, #13697 ),
 ( #11268, #4490 ) ),
 .UNSPECIFIED., .F., .F., .F. ) 
 B_SPLINE_SURFACE_WITH_KNOTS ( ( 4, 4 ),
 ( 2, 2 ),
 ( 0.000000000000000000, 1.000000000000000000 ),
 ( 0.000000000000000000, 1.000000000000000000 ),
 .UNSPECIFIED. ) 
 GEOMETRIC_REPRESENTATION_ITEM ( )  RATIONAL_B_SPLINE_SURFACE ( (
 ( 1.000000000000000000, 1.000000000000000000),
 ( 0.9956975270656954757, 0.8568959468854893125),
 ( 0.9956975270656954757, 0.8568959468854893125),
 ( 1.000000000000000000, 1.000000000000000000) ) ) 
 REPRESENTATION_ITEM ( '' )  SURFACE ( )  );
#28386=LINE ( 'NONE', #13139, #6005 ) ;
#28387=PLANE ( 'NONE',  #22463 ) ;
#28388=EDGE_LOOP ( 'NONE', ( #15082, #23646, #19321, #8512 ) ) ;
#28389=ORIENTED_EDGE ( 'NONE', *, *, #3223, .F. ) ;
#28391=CARTESIAN_POINT ( 'NONE',  ( 25.64660436782557440, 22.90783756891005396, -110.5628080555243713 ) ) ;
#28392=B_SPLINE_CURVE_WITH_KNOTS ( 'NONE', 3,
 ( #26957, #24973, #636, #18036, #3084, #9557, #6837, #15581 ),
 .UNSPECIFIED., .F., .F.,
 ( 4, 2, 2, 4 ),
 ( 1.734723475976807094E-18, 0.0002429588503611205359, 0.0004859177007222393371, 0.0009718354014444821436 ),
 .UNSPECIFIED. ) ;
#28395=LINE ( 'NONE', #4228, #22466 ) ;
#28398=CARTESIAN_POINT ( 'NONE',  ( 16.75465622695635659, 98.56308464785224999, -102.5353941815395160 ) ) ;
#28400=ORIENTED_EDGE ( 'NONE', *, *, #8839, .F. ) ;
#28401=ORIENTED_EDGE ( 'NONE', *, *, #23260, .T. ) ;
#28403=VERTEX_POINT ( 'NONE', #17375 ) ;
#28404=CARTESIAN_POINT ( 'NONE',  ( 1.831572820252009626, 117.9752562883666940, 84.49389457294174122 ) ) ;
#28405=ORIENTED_EDGE ( 'NONE', *, *, #18952, .T. ) ;
#28407=CARTESIAN_POINT ( 'NONE',  ( 26.04756280548353686, 67.42001818240466093, 90.90573670389261451 ) ) ;
#28409=B_SPLINE_CURVE_WITH_KNOTS ( 'NONE', 3,
 ( #21421, #10494, #12909, #17369, #28170, #19133 ),
 .UNSPECIFIED., .F., .F.,
 ( 4, 2, 4 ),
 ( 3.476216610979977084E-18, 0.0006311571484586040543, 0.001262314296917204422 ),
 .UNSPECIFIED. ) ;
#28411=CARTESIAN_POINT ( 'NONE',  ( 13.36082413113061307, -22.28175172543663507, 151.2941478187906910 ) ) ;
#28412=CARTESIAN_POINT ( 'NONE',  ( 2.433796855181219243, 31.67151202413165478, -142.0211193075552956 ) ) ;
#28414=CARTESIAN_POINT ( 'NONE',  ( 109.1592201516379674, 0.006957642258155071965, 0.003661068210032695190 ) ) ;
#28415=CARTESIAN_POINT ( 'NONE',  ( 1.833485406944043827, 144.2578170162065021, -15.69895494453236395 ) ) ;
#28416=CARTESIAN_POINT ( 'NONE',  ( 30.59141879584289825, -113.0806649571964755, -26.79785525806519786 ) ) ;
#28418=CARTESIAN_POINT ( 'NONE',  ( 1.833809397773856542, 125.5796696653637952, 72.70895493223410710 ) ) ;
#28420=CARTESIAN_POINT ( 'NONE',  ( 1.833206308920055205, -117.8322276971141491, 84.68961866582966991 ) ) ;
#28421=CARTESIAN_POINT ( 'NONE',  ( 25.69398547355841700, -112.2438548322123353, 12.54367966928010425 ) ) ;
#28423=ORIENTED_EDGE ( 'NONE', *, *, #7236, .T. ) ;
#28424=CARTESIAN_POINT ( 'NONE',  ( 25.64708010899962787, 56.40825696968397551, -97.81137751680941506 ) ) ;
#28426=CARTESIAN_POINT ( 'NONE',  ( 1.833485406944057594, -72.09189602597798796, 125.9346397303433065 ) ) ;
#28429=CARTESIAN_POINT ( 'NONE',  ( 25.86096068574580897, 97.40497849554891729, 57.38862431273619791 ) ) ;
#28430=CARTESIAN_POINT ( 'NONE',  ( 1.833838850093517214, 1.355257560975019971E-17, -145.1097630783160923 ) ) ;
#28431=ORIENTED_EDGE ( 'NONE', *, *, #21484, .T. ) ;
#28432=CARTESIAN_POINT ( 'NONE',  ( 1.832998868059858122, 58.53348008137646019, 132.7810136645740045 ) ) ;
#28434=CARTESIAN_POINT ( 'NONE',  ( 2.433796855181205476, 109.1007109081238724, -96.28145139437575040 ) ) ;
#28437=CARTESIAN_POINT ( 'NONE',  ( 1.833485406944043827, 15.69895494453577101, -144.2578170162061326 ) ) ;
#28438=CARTESIAN_POINT ( 'NONE',  ( 10.93730112725932635, 0.000000000000000000, 0.000000000000000000 ) ) ;
#28441=CARTESIAN_POINT ( 'NONE',  ( 25.64692232868534560, -112.9106972861223426, 0.3267662677147551431 ) ) ;
#28444=EDGE_CURVE ( 'NONE', #28093, #25271, #7247, .T. ) ;
#28445=EDGE_LOOP ( 'NONE', ( #17169, #9607, #1448, #20223 ) ) ;
#28448=CARTESIAN_POINT ( 'NONE',  ( 55.79472521941428198, 54.55111121764083748, 48.13855120843901858 ) ) ;
#28449=CARTESIAN_POINT ( 'NONE',  ( 1.833485406944057594, -138.1714136985305572, -44.33323125130066700 ) ) ;
#28450=CARTESIAN_POINT ( 'NONE',  ( 28.37644542392847313, -89.64009552702840722, -86.16884085958031392 ) ) ;
#28451=CARTESIAN_POINT ( 'NONE',  ( 13.36082413113063083, -148.1362653801005251, 37.97423473099245683 ) ) ;
#28452=CARTESIAN_POINT ( 'NONE',  ( 2.430230287190589422, 46.34481016236826179, 137.9371479820464117 ) ) ;
#28453=CARTESIAN_POINT ( 'NONE',  ( 109.1721716018069657, -0.01127028715940094246, 0.01281875973824537183 ) ) ;
#28454=CARTESIAN_POINT ( 'NONE',  ( 2.430230287190572103, -1.451610819318766232, 145.5073573687466819 ) ) ;
#28456=VERTEX_POINT ( 'NONE', #4558 ) ;
#28461=CARTESIAN_POINT ( 'NONE',  ( 119.2224693531408803, -69.99999999999998579, -20.00000000000000355 ) ) ;
#28463=LINE ( 'NONE', #7193, #28201 ) ;
#28466=CARTESIAN_POINT ( 'NONE',  ( 30.59138290137877902, 38.47117663195945880, 109.6600423140541523 ) ) ;
#28468=CARTESIAN_POINT ( 'NONE',  ( 1.833485406944043827, 117.7091014914961420, -84.86072343962446496 ) ) ;
#28470=( BOUNDED_SURFACE ( )  B_SPLINE_SURFACE ( 3, 1, ( 
 ( #18639, #27411 ),
 ( #7721, #15009 ),
 ( #10716, #19203 ),
 ( #21498, #2051 ) ),
 .UNSPECIFIED., .F., .F., .F. ) 
 B_SPLINE_SURFACE_WITH_KNOTS ( ( 4, 4 ),
 ( 2, 2 ),
 ( 0.000000000000000000, 1.000000000000000000 ),
 ( 0.000000000000000000, 1.000000000000000000 ),
 .UNSPECIFIED. ) 
 GEOMETRIC_REPRESENTATION_ITEM ( )  RATIONAL_B_SPLINE_SURFACE ( (
 ( 1.000000000000000000, 1.000000000000000000),
 ( 0.6386103224230302855, 0.9954351624131538845),
 ( 0.6386103224230302855, 0.9954351624131538845),
 ( 1.000000000000000000, 1.000000000000000000) ) ) 
 REPRESENTATION_ITEM ( '' )  SURFACE ( )  );
#28471=CARTESIAN_POINT ( 'NONE',  ( 25.65782528836481191, 12.37768345530126091, -112.2379831684171307 ) ) ;
#28472=CARTESIAN_POINT ( 'NONE',  ( 109.1624594426973260, -0.001206615835671285284, -0.01591840958352308891 ) ) ;
#28473=ORIENTED_EDGE ( 'NONE', *, *, #11019, .F. ) ;
#28474=CARTESIAN_POINT ( 'NONE',  ( 28.43349137099829349, 8.951033805646366304, -123.9292945876798200 ) ) ;
#28475=CARTESIAN_POINT ( 'NONE',  ( 1.833750490713712322, -117.2391074582366883, -85.50916867388922071 ) ) ;
#28476=ORIENTED_EDGE ( 'NONE', *, *, #23918, .F. ) ;
#28477=( BOUNDED_SURFACE ( )  B_SPLINE_SURFACE ( 3, 1, ( 
 ( #7125, #18171 ),
 ( #478, #18030 ),
 ( #11713, #3211 ),
 ( #22667, #5227 ) ),
 .UNSPECIFIED., .F., .F., .F. ) 
 B_SPLINE_SURFACE_WITH_KNOTS ( ( 4, 4 ),
 ( 2, 2 ),
 ( 0.000000000000000000, 1.000000000000000000 ),
 ( 0.000000000000000000, 1.000000000000000000 ),
 .UNSPECIFIED. ) 
 GEOMETRIC_REPRESENTATION_ITEM ( )  RATIONAL_B_SPLINE_SURFACE ( (
 ( 1.000000000000000000, 1.000000000000000000),
 ( 0.6386103224230302855, 0.9954351624131538845),
 ( 0.6386103224230302855, 0.9954351624131538845),
 ( 1.000000000000000000, 1.000000000000000000) ) ) 
 REPRESENTATION_ITEM ( '' )  SURFACE ( )  );
#28479=ADVANCED_FACE ( 'NONE', ( #13330 ), #152, .F. ) ;
#28480=VERTEX_POINT ( 'NONE', #20100 ) ;
#28481=CARTESIAN_POINT ( 'NONE',  ( 2.433796855181233454, 142.6247129145648387, 28.83182736670586266 ) ) ;
#28494=COLOUR_RGB('Light Blue',0.38,0.62,0.78);
#28495=FILL_AREA_STYLE_COLOUR('',#28494);
#28496=FILL_AREA_STYLE('',(#28495));
#28497=SURFACE_STYLE_FILL_AREA(#28496);
#28498=SURFACE_SIDE_STYLE('',(#28497));
#28499=SURFACE_STYLE_USAGE(.BOTH.,#28498);
#28500=PRESENTATION_STYLE_ASSIGNMENT((#28499));
ENDSEC;
END-ISO-10303-21;
